ISO-10303-21;
HEADER;
/* Generated by software containing ST-Developer
 * from STEP Tools, Inc. (www.steptools.com) 
 */

FILE_DESCRIPTION(
/* description */ (
'Independent keyed-quill tailstock, native coupled50mm slider andM16x2
 feed screw, conical dead center, bronze sleeves/thrust washers, cross
-pinned handwheel and bolted guide key. Custom center taper; no standa
rd taper compatibility, machine-bed compatibility or load rating assig
ned.'),
/* implementation_level */ '2;1');

FILE_NAME(
/* name */ 'Socket head cap screw M8x20.step',
/* time_stamp */ '2026-11-14T07:17:36-08:00',
/* author */ (''),
/* organization */ (''),
/* preprocessor_version */ 'ST-DEVELOPER v20.2',
/* originating_system */ 'Autodesk Translation Framework v15.17.0.0',
/* authorisation */ '');

FILE_SCHEMA (('AUTOMOTIVE_DESIGN { 1 0 10303 214 3 1 1 }'));
ENDSEC;

DATA;
#10=MECHANICAL_DESIGN_GEOMETRIC_PRESENTATION_REPRESENTATION('',(#167),#289387);
#114=CONICAL_SURFACE('',#17748,3.5,0.785398163397448);
#115=CONICAL_SURFACE('',#17774,3.5,0.785398163397448);
#133=SHAPE_REPRESENTATION_RELATIONSHIP('SRR','None',#289468,#150);
#150=ADVANCED_BREP_SHAPE_REPRESENTATION('',(#184),#289384);
#167=STYLED_ITEM('',(#289553),#184);
#184=MANIFOLD_SOLID_BREP('Body1',#16855);
#267=FACE_BOUND('',#1739,.T.);
#268=FACE_BOUND('',#1742,.T.);
#297=B_SPLINE_SURFACE_WITH_KNOTS('',3,3,((#259610,#259611,#259612,#259613,
#259614,#259615,#259616,#259617,#259618,#259619,#259620,#259621,#259622,
#259623,#259624,#259625,#259626,#259627,#259628,#259629,#259630,#259631,
#259632,#259633,#259634,#259635,#259636,#259637,#259638,#259639,#259640,
#259641,#259642,#259643,#259644,#259645,#259646,#259647,#259648,#259649,
#259650,#259651,#259652,#259653,#259654,#259655,#259656,#259657,#259658,
#259659,#259660,#259661,#259662,#259663,#259664,#259665,#259666,#259667,
#259668,#259669,#259670,#259671,#259672,#259673,#259674,#259675,#259676,
#259677,#259678,#259679,#259680,#259681,#259682,#259683,#259684,#259685,
#259686,#259687,#259688,#259689,#259690,#259691,#259692,#259693,#259694,
#259695,#259696,#259697,#259698,#259699,#259700,#259701,#259702,#259703,
#259704,#259705,#259706,#259707,#259708,#259709,#259710,#259711,#259712),
(#259713,#259714,#259715,#259716,#259717,#259718,#259719,#259720,#259721,
#259722,#259723,#259724,#259725,#259726,#259727,#259728,#259729,#259730,
#259731,#259732,#259733,#259734,#259735,#259736,#259737,#259738,#259739,
#259740,#259741,#259742,#259743,#259744,#259745,#259746,#259747,#259748,
#259749,#259750,#259751,#259752,#259753,#259754,#259755,#259756,#259757,
#259758,#259759,#259760,#259761,#259762,#259763,#259764,#259765,#259766,
#259767,#259768,#259769,#259770,#259771,#259772,#259773,#259774,#259775,
#259776,#259777,#259778,#259779,#259780,#259781,#259782,#259783,#259784,
#259785,#259786,#259787,#259788,#259789,#259790,#259791,#259792,#259793,
#259794,#259795,#259796,#259797,#259798,#259799,#259800,#259801,#259802,
#259803,#259804,#259805,#259806,#259807,#259808,#259809,#259810,#259811,
#259812,#259813,#259814,#259815),(#259816,#259817,#259818,#259819,#259820,
#259821,#259822,#259823,#259824,#259825,#259826,#259827,#259828,#259829,
#259830,#259831,#259832,#259833,#259834,#259835,#259836,#259837,#259838,
#259839,#259840,#259841,#259842,#259843,#259844,#259845,#259846,#259847,
#259848,#259849,#259850,#259851,#259852,#259853,#259854,#259855,#259856,
#259857,#259858,#259859,#259860,#259861,#259862,#259863,#259864,#259865,
#259866,#259867,#259868,#259869,#259870,#259871,#259872,#259873,#259874,
#259875,#259876,#259877,#259878,#259879,#259880,#259881,#259882,#259883,
#259884,#259885,#259886,#259887,#259888,#259889,#259890,#259891,#259892,
#259893,#259894,#259895,#259896,#259897,#259898,#259899,#259900,#259901,
#259902,#259903,#259904,#259905,#259906,#259907,#259908,#259909,#259910,
#259911,#259912,#259913,#259914,#259915,#259916,#259917,#259918),(#259919,
#259920,#259921,#259922,#259923,#259924,#259925,#259926,#259927,#259928,
#259929,#259930,#259931,#259932,#259933,#259934,#259935,#259936,#259937,
#259938,#259939,#259940,#259941,#259942,#259943,#259944,#259945,#259946,
#259947,#259948,#259949,#259950,#259951,#259952,#259953,#259954,#259955,
#259956,#259957,#259958,#259959,#259960,#259961,#259962,#259963,#259964,
#259965,#259966,#259967,#259968,#259969,#259970,#259971,#259972,#259973,
#259974,#259975,#259976,#259977,#259978,#259979,#259980,#259981,#259982,
#259983,#259984,#259985,#259986,#259987,#259988,#259989,#259990,#259991,
#259992,#259993,#259994,#259995,#259996,#259997,#259998,#259999,#260000,
#260001,#260002,#260003,#260004,#260005,#260006,#260007,#260008,#260009,
#260010,#260011,#260012,#260013,#260014,#260015,#260016,#260017,#260018,
#260019,#260020,#260021)),.UNSPECIFIED.,.F.,.F.,.F.,(4,4),(4,1,1,1,1,1,
1,1,1,1,1,1,1,1,1,1,1,1,1,1,1,1,1,1,1,1,1,1,1,1,1,1,1,1,1,1,1,1,1,1,1,1,
1,1,1,1,1,1,1,1,1,1,1,1,1,1,1,1,1,1,1,1,1,1,1,1,1,1,1,1,1,1,1,1,1,1,1,1,
1,1,1,1,1,1,1,1,1,1,1,1,1,1,1,1,1,1,1,1,1,1,4),(-0.000373081420709297,0.0826691585557874),
(11.61455969934,12.609327240686,13.6034402536173,14.5975532665487,15.59166627948,
16.5857792924113,17.5798923053427,18.574005318274,19.5681183312054,20.5622313441367,
21.556344357068,22.5504573699994,23.5445703829307,24.5386833958621,25.5327964087934,
26.5269094217247,27.5210224346561,28.5151354475874,29.5092484605188,30.5033614734501,
31.4974744863814,32.4915874993128,33.4857005122441,34.4798135251755,35.4739265381068,
36.4680395510381,37.4621525639695,38.4562655769008,39.4503785898322,40.4444916027635,
41.4386046156948,42.4327176286262,43.4268306415575,44.4209436544889,45.4150566674202,
46.4091696803515,47.4032826932829,48.3973957062142,49.3915087191456,50.3856217320769,
51.3797347450082,52.3738477579396,53.3679607708709,54.3620737838023,55.3561867967336,
56.3502998096649,57.3444128225963,58.3385258355276,59.332638848459,60.3267518613903,
61.3208648743217,62.314977887253,63.3090909001843,64.3032039131157,65.297316926047,
66.2914299389783,67.2855429519097,68.279655964841,69.2737689777724,70.2678819907037,
71.2619950036351,72.2561080165664,73.2502210294977,74.2443340424291,75.2384470553604,
76.2325600682917,77.2266730812231,78.2207860941544,79.2148991070858,80.2090121200171,
81.2031251329484,82.1972381458798,83.1913511588111,84.1854641717425,85.1795771846738,
86.1736901976051,87.1678032105365,88.1619162234678,89.1560292363992,90.1501422493305,
91.1442552622619,92.1383682751932,93.1324812881245,94.1265943010559,95.1207073139872,
96.1148203269185,97.1089333398499,98.1030463527812,99.0971593657126,100.091272378644,
101.085385391575,102.079498404507,103.073611417438,104.067724430369,105.061837443301,
106.055950456232,107.050063469163,108.044176482095,109.038289495026,110.032402507957,
111.027172073706),.UNSPECIFIED.);
#298=B_SPLINE_SURFACE_WITH_KNOTS('',3,3,((#260116,#260117,#260118,#260119,
#260120,#260121,#260122,#260123,#260124,#260125,#260126,#260127,#260128,
#260129,#260130,#260131,#260132,#260133,#260134,#260135,#260136,#260137,
#260138,#260139,#260140,#260141,#260142,#260143,#260144,#260145,#260146,
#260147,#260148,#260149,#260150,#260151,#260152,#260153,#260154,#260155,
#260156,#260157,#260158,#260159,#260160,#260161,#260162,#260163,#260164,
#260165,#260166,#260167,#260168,#260169,#260170,#260171,#260172,#260173,
#260174,#260175,#260176,#260177,#260178,#260179,#260180,#260181,#260182,
#260183,#260184,#260185,#260186,#260187,#260188,#260189,#260190,#260191,
#260192,#260193,#260194,#260195,#260196,#260197,#260198,#260199,#260200,
#260201,#260202,#260203,#260204,#260205,#260206,#260207,#260208,#260209,
#260210,#260211,#260212,#260213,#260214,#260215,#260216,#260217,#260218,
#260219,#260220),(#260221,#260222,#260223,#260224,#260225,#260226,#260227,
#260228,#260229,#260230,#260231,#260232,#260233,#260234,#260235,#260236,
#260237,#260238,#260239,#260240,#260241,#260242,#260243,#260244,#260245,
#260246,#260247,#260248,#260249,#260250,#260251,#260252,#260253,#260254,
#260255,#260256,#260257,#260258,#260259,#260260,#260261,#260262,#260263,
#260264,#260265,#260266,#260267,#260268,#260269,#260270,#260271,#260272,
#260273,#260274,#260275,#260276,#260277,#260278,#260279,#260280,#260281,
#260282,#260283,#260284,#260285,#260286,#260287,#260288,#260289,#260290,
#260291,#260292,#260293,#260294,#260295,#260296,#260297,#260298,#260299,
#260300,#260301,#260302,#260303,#260304,#260305,#260306,#260307,#260308,
#260309,#260310,#260311,#260312,#260313,#260314,#260315,#260316,#260317,
#260318,#260319,#260320,#260321,#260322,#260323,#260324,#260325),(#260326,
#260327,#260328,#260329,#260330,#260331,#260332,#260333,#260334,#260335,
#260336,#260337,#260338,#260339,#260340,#260341,#260342,#260343,#260344,
#260345,#260346,#260347,#260348,#260349,#260350,#260351,#260352,#260353,
#260354,#260355,#260356,#260357,#260358,#260359,#260360,#260361,#260362,
#260363,#260364,#260365,#260366,#260367,#260368,#260369,#260370,#260371,
#260372,#260373,#260374,#260375,#260376,#260377,#260378,#260379,#260380,
#260381,#260382,#260383,#260384,#260385,#260386,#260387,#260388,#260389,
#260390,#260391,#260392,#260393,#260394,#260395,#260396,#260397,#260398,
#260399,#260400,#260401,#260402,#260403,#260404,#260405,#260406,#260407,
#260408,#260409,#260410,#260411,#260412,#260413,#260414,#260415,#260416,
#260417,#260418,#260419,#260420,#260421,#260422,#260423,#260424,#260425,
#260426,#260427,#260428,#260429,#260430),(#260431,#260432,#260433,#260434,
#260435,#260436,#260437,#260438,#260439,#260440,#260441,#260442,#260443,
#260444,#260445,#260446,#260447,#260448,#260449,#260450,#260451,#260452,
#260453,#260454,#260455,#260456,#260457,#260458,#260459,#260460,#260461,
#260462,#260463,#260464,#260465,#260466,#260467,#260468,#260469,#260470,
#260471,#260472,#260473,#260474,#260475,#260476,#260477,#260478,#260479,
#260480,#260481,#260482,#260483,#260484,#260485,#260486,#260487,#260488,
#260489,#260490,#260491,#260492,#260493,#260494,#260495,#260496,#260497,
#260498,#260499,#260500,#260501,#260502,#260503,#260504,#260505,#260506,
#260507,#260508,#260509,#260510,#260511,#260512,#260513,#260514,#260515,
#260516,#260517,#260518,#260519,#260520,#260521,#260522,#260523,#260524,
#260525,#260526,#260527,#260528,#260529,#260530,#260531,#260532,#260533,
#260534,#260535)),.UNSPECIFIED.,.F.,.F.,.F.,(4,4),(4,1,1,1,1,1,1,1,1,1,
1,1,1,1,1,1,1,1,1,1,1,1,1,1,1,1,1,1,1,1,1,1,1,1,1,1,1,1,1,1,1,1,1,1,1,1,
1,1,1,1,1,1,1,1,1,1,1,1,1,1,1,1,1,1,1,1,1,1,1,1,1,1,1,1,1,1,1,1,1,1,1,1,
1,1,1,1,1,1,1,1,1,1,1,1,1,1,1,1,1,1,1,1,4),(-0.000656555906784362,0.0823778368201467),
(8.31473274985795,9.3095612095702,10.3043896692825,11.2992181289947,12.294046588707,
13.2888750484192,14.2837035081315,15.2785319678437,16.273360427556,17.2681888872682,
18.2630173469805,19.2578458066927,20.252674266405,21.2475027261172,22.2423311858295,
23.2371596455417,24.231988105254,25.2268165649662,26.2216450246785,27.2164734843908,
28.211301944103,29.2061304038153,30.2009588635275,31.1957873232398,32.190615782952,
33.1854442426643,34.1802727023765,35.1751011620888,36.169929621801,37.1647580815133,
38.1595865412255,39.1544150009378,40.14924346065,41.1440719203623,42.1389003800745,
43.1337288397868,44.1285572994991,45.1233857592113,46.1182142189236,47.1130426786358,
48.1078711383481,49.1026995980603,50.0975280577726,51.0923565174848,52.0871849771971,
53.0820134369093,54.0768418966216,55.0716703563338,56.0664988160461,57.0613272757583,
58.0561557354706,59.0509841951828,60.0458126548951,61.0406411146073,62.0354695743196,
63.0302980340319,64.0251264937441,65.0199549534563,66.0147834131686,67.0096118728809,
68.0044403325931,68.9992687923054,69.9940972520176,70.9889257117299,71.9837541714421,
72.9785826311544,73.9734110908666,74.9682395505789,75.9630680102911,76.9578964700034,
77.9527249297156,78.9475533894279,79.9423818491401,80.9372103088524,81.9320387685647,
82.9268672282769,83.9216956879892,84.9165241477014,85.9113526074137,86.9061810671259,
87.9010095268382,88.8958379865504,89.8906664462627,90.8854949059749,91.8803233656872,
92.8751518253994,93.8699802851117,94.8648087448239,95.8596372045362,96.8544656642484,
97.8492941239607,98.8441225836729,99.8389510433852,100.833779503097,101.82860796281,
102.823436422522,103.818264882234,104.813093341946,105.807921801659,106.802750261371,
107.797578721083,108.792407180795,109.787892196415),.UNSPECIFIED.);
#393=PLANE('',#17775);
#394=PLANE('',#17776);
#395=PLANE('',#17777);
#396=PLANE('',#17778);
#397=PLANE('',#17779);
#398=PLANE('',#17780);
#399=PLANE('',#17781);
#400=PLANE('',#17782);
#401=PLANE('',#17786);
#402=PLANE('',#17787);
#979=FACE_OUTER_BOUND('',#1709,.T.);
#980=FACE_OUTER_BOUND('',#1710,.T.);
#981=FACE_OUTER_BOUND('',#1711,.T.);
#982=FACE_OUTER_BOUND('',#1712,.T.);
#983=FACE_OUTER_BOUND('',#1713,.T.);
#984=FACE_OUTER_BOUND('',#1714,.T.);
#985=FACE_OUTER_BOUND('',#1715,.T.);
#986=FACE_OUTER_BOUND('',#1716,.T.);
#987=FACE_OUTER_BOUND('',#1717,.T.);
#988=FACE_OUTER_BOUND('',#1718,.T.);
#989=FACE_OUTER_BOUND('',#1719,.T.);
#990=FACE_OUTER_BOUND('',#1720,.T.);
#991=FACE_OUTER_BOUND('',#1721,.T.);
#992=FACE_OUTER_BOUND('',#1722,.T.);
#993=FACE_OUTER_BOUND('',#1723,.T.);
#994=FACE_OUTER_BOUND('',#1724,.T.);
#995=FACE_OUTER_BOUND('',#1725,.T.);
#996=FACE_OUTER_BOUND('',#1726,.T.);
#997=FACE_OUTER_BOUND('',#1727,.T.);
#998=FACE_OUTER_BOUND('',#1728,.T.);
#999=FACE_OUTER_BOUND('',#1729,.T.);
#1000=FACE_OUTER_BOUND('',#1730,.T.);
#1001=FACE_OUTER_BOUND('',#1731,.T.);
#1002=FACE_OUTER_BOUND('',#1732,.T.);
#1003=FACE_OUTER_BOUND('',#1733,.T.);
#1004=FACE_OUTER_BOUND('',#1734,.T.);
#1005=FACE_OUTER_BOUND('',#1735,.T.);
#1006=FACE_OUTER_BOUND('',#1736,.T.);
#1007=FACE_OUTER_BOUND('',#1737,.T.);
#1008=FACE_OUTER_BOUND('',#1738,.T.);
#1009=FACE_OUTER_BOUND('',#1740,.T.);
#1010=FACE_OUTER_BOUND('',#1741,.T.);
#1011=FACE_OUTER_BOUND('',#1743,.T.);
#1709=EDGE_LOOP('',(#14845,#14846,#14847,#14848,#14849,#14850,#14851,#14852,
#14853));
#1710=EDGE_LOOP('',(#14854,#14855,#14856,#14857));
#1711=EDGE_LOOP('',(#14858,#14859,#14860,#14861));
#1712=EDGE_LOOP('',(#14862,#14863,#14864,#14865,#14866));
#1713=EDGE_LOOP('',(#14867,#14868,#14869,#14870,#14871));
#1714=EDGE_LOOP('',(#14872,#14873,#14874,#14875,#14876));
#1715=EDGE_LOOP('',(#14877,#14878,#14879,#14880,#14881));
#1716=EDGE_LOOP('',(#14882,#14883,#14884,#14885,#14886,#14887));
#1717=EDGE_LOOP('',(#14888,#14889,#14890,#14891));
#1718=EDGE_LOOP('',(#14892,#14893,#14894,#14895));
#1719=EDGE_LOOP('',(#14896,#14897,#14898,#14899,#14900,#14901));
#1720=EDGE_LOOP('',(#14902,#14903,#14904,#14905,#14906));
#1721=EDGE_LOOP('',(#14907,#14908,#14909,#14910,#14911));
#1722=EDGE_LOOP('',(#14912,#14913,#14914,#14915,#14916));
#1723=EDGE_LOOP('',(#14917,#14918,#14919,#14920,#14921));
#1724=EDGE_LOOP('',(#14922,#14923,#14924,#14925));
#1725=EDGE_LOOP('',(#14926,#14927,#14928,#14929,#14930));
#1726=EDGE_LOOP('',(#14931,#14932,#14933,#14934,#14935,#14936,#14937,#14938,
#14939,#14940,#14941,#14942,#14943,#14944,#14945,#14946,#14947,#14948,#14949,
#14950,#14951,#14952,#14953,#14954,#14955,#14956,#14957,#14958,#14959,#14960,
#14961,#14962,#14963,#14964,#14965,#14966));
#1727=EDGE_LOOP('',(#14967,#14968,#14969));
#1728=EDGE_LOOP('',(#14970,#14971,#14972));
#1729=EDGE_LOOP('',(#14973,#14974,#14975,#14976,#14977,#14978,#14979,#14980,
#14981,#14982,#14983,#14984,#14985,#14986,#14987,#14988,#14989,#14990,#14991,
#14992,#14993,#14994,#14995,#14996,#14997,#14998,#14999,#15000,#15001,#15002,
#15003,#15004,#15005,#15006,#15007,#15008,#15009,#15010,#15011,#15012,#15013,
#15014));
#1730=EDGE_LOOP('',(#15015,#15016,#15017,#15018,#15019,#15020,#15021,#15022,
#15023,#15024,#15025,#15026,#15027,#15028,#15029,#15030,#15031,#15032,#15033,
#15034,#15035,#15036,#15037,#15038,#15039,#15040,#15041,#15042,#15043,#15044,
#15045,#15046,#15047,#15048,#15049,#15050,#15051,#15052,#15053,#15054,#15055));
#1731=EDGE_LOOP('',(#15056,#15057,#15058,#15059));
#1732=EDGE_LOOP('',(#15060,#15061,#15062,#15063));
#1733=EDGE_LOOP('',(#15064,#15065,#15066,#15067));
#1734=EDGE_LOOP('',(#15068,#15069,#15070,#15071));
#1735=EDGE_LOOP('',(#15072,#15073,#15074,#15075));
#1736=EDGE_LOOP('',(#15076,#15077,#15078,#15079));
#1737=EDGE_LOOP('',(#15080,#15081,#15082,#15083,#15084,#15085));
#1738=EDGE_LOOP('',(#15086));
#1739=EDGE_LOOP('',(#15087,#15088,#15089,#15090));
#1740=EDGE_LOOP('',(#15091,#15092,#15093,#15094));
#1741=EDGE_LOOP('',(#15095));
#1742=EDGE_LOOP('',(#15096,#15097,#15098,#15099,#15100,#15101));
#1743=EDGE_LOOP('',(#15102));
#1963=CIRCLE('',#17749,3.933);
#1964=CIRCLE('',#17750,3.22275);
#1965=CIRCLE('',#17751,3.);
#1966=CIRCLE('',#17752,3.22275);
#1967=CIRCLE('',#17754,3.22275);
#1968=CIRCLE('',#17771,3.933);
#1969=CIRCLE('',#17772,3.933);
#1970=CIRCLE('',#17783,6.5);
#1971=CIRCLE('',#17785,6.5);
#3646=B_SPLINE_CURVE_WITH_KNOTS('',3,(#247356,#247357,#247358,#247359,#247360,
#247361,#247362,#247363,#247364,#247365,#247366,#247367,#247368,#247369,
#247370,#247371,#247372,#247373,#247374,#247375,#247376,#247377,#247378,
#247379,#247380,#247381,#247382,#247383,#247384,#247385,#247386,#247387,
#247388,#247389,#247390,#247391,#247392,#247393,#247394,#247395,#247396,
#247397,#247398,#247399,#247400,#247401,#247402,#247403,#247404,#247405,
#247406,#247407,#247408,#247409,#247410,#247411,#247412,#247413,#247414,
#247415,#247416,#247417,#247418,#247419,#247420,#247421,#247422,#247423,
#247424,#247425,#247426,#247427,#247428,#247429,#247430,#247431,#247432,
#247433,#247434,#247435,#247436,#247437,#247438,#247439,#247440,#247441,
#247442,#247443,#247444,#247445,#247446,#247447,#247448,#247449,#247450,
#247451,#247452,#247453,#247454,#247455,#247456,#247457,#247458,#247459,
#247460,#247461,#247462,#247463,#247464,#247465,#247466,#247467,#247468,
#247469,#247470,#247471,#247472,#247473,#247474,#247475,#247476,#247477,
#247478,#247479,#247480,#247481,#247482,#247483,#247484,#247485,#247486,
#247487,#247488,#247489,#247490,#247491,#247492,#247493,#247494,#247495,
#247496,#247497,#247498,#247499,#247500,#247501,#247502,#247503,#247504,
#247505,#247506,#247507,#247508,#247509,#247510,#247511,#247512,#247513,
#247514,#247515,#247516,#247517,#247518,#247519,#247520,#247521,#247522,
#247523,#247524,#247525,#247526,#247527,#247528,#247529,#247530,#247531,
#247532,#247533,#247534,#247535,#247536,#247537,#247538,#247539,#247540,
#247541,#247542,#247543,#247544,#247545,#247546,#247547,#247548,#247549,
#247550,#247551,#247552,#247553,#247554,#247555,#247556,#247557,#247558,
#247559,#247560,#247561,#247562,#247563,#247564,#247565,#247566,#247567,
#247568,#247569,#247570,#247571,#247572,#247573,#247574,#247575,#247576,
#247577,#247578,#247579,#247580,#247581,#247582,#247583,#247584,#247585,
#247586,#247587,#247588,#247589,#247590,#247591,#247592,#247593,#247594,
#247595,#247596,#247597,#247598,#247599,#247600,#247601,#247602,#247603,
#247604,#247605,#247606,#247607,#247608,#247609,#247610,#247611,#247612,
#247613,#247614,#247615,#247616,#247617,#247618,#247619,#247620,#247621,
#247622,#247623,#247624,#247625,#247626,#247627,#247628,#247629),
 .UNSPECIFIED.,.F.,.F.,(4,3,3,3,3,3,3,3,3,3,3,3,3,3,3,3,3,3,3,3,3,3,3,3,
3,3,3,3,3,3,3,3,3,3,3,3,3,3,3,3,3,3,3,3,3,3,3,3,3,3,3,3,3,3,3,3,3,3,3,3,
3,3,3,3,3,3,3,3,3,3,3,3,3,3,3,3,3,3,3,3,3,3,3,3,3,3,3,3,3,3,3,4),(-2.02747957522558,
-1.99824474635933,-1.99629697858914,-1.96434886453735,-1.94771240967622,
-1.93464992018109,-1.92899254917003,-1.8963788881421,-1.86351124585845,
-1.84194255873285,-1.83673933906724,-1.80209590099024,-1.76903471505845,
-1.73643586541624,-1.71730072608774,-1.70954969143332,-1.70500834289113,
-1.69816558675924,-1.66796497076637,-1.66624311511707,-1.63347199808372,
-1.59881224827677,-1.58364860773623,-1.57740361260911,-1.57281360985668,
-1.53925479883535,-1.50531500590784,-1.47148480017328,-1.45673015640375,
-1.44483082316201,-1.44007092151362,-1.40580982079488,-1.37203186923789,
-1.35619399962815,-1.32417162930309,-1.32246375520252,-1.31137143543089,
-1.30408331014913,-1.27083606559476,-1.23645358594825,-1.20182786580053,
-1.17685917371408,-1.17113655759577,-1.16634083510167,-1.13153658048666,
-1.09665147006904,-1.06221352047721,-1.0321459247931,-1.02687330274833,
-1.00207832910898,-0.970106886116407,-0.968154570621599,-0.933428976642505,
-0.89821340097426,-0.889062877044913,-0.883889592269312,-0.848660796107921,
-0.81299245745828,-0.777358669907495,-0.759631620008249,-0.746573372525805,
-0.741724080509391,-0.705701740199829,-0.670225247749574,-0.635542270713525,
-0.611878481403642,-0.600013081478758,-0.594932488268286,-0.560071350862289,
-0.524344779833904,-0.48796845368674,-0.459087602195323,-0.453607297630247,
-0.448569183216579,-0.412045530179206,-0.375288304735632,-0.339100257750381,
-0.318555603751638,-0.303972630746695,-0.298673006997446,-0.261788714920118,
-0.256921641755406,-0.223059098039412,-0.220857509819622,-0.184147769510166,
-0.161129298321395,-0.154473005979913,-0.149382466658041,-0.11203684999353,
-0.0747139011585263,-0.0373569505792632,0.),.UNSPECIFIED.);
#3647=B_SPLINE_CURVE_WITH_KNOTS('',3,(#247637,#247638,#247639,#247640,#247641,
#247642,#247643,#247644,#247645,#247646,#247647,#247648,#247649,#247650,
#247651,#247652,#247653,#247654,#247655,#247656,#247657,#247658,#247659,
#247660,#247661,#247662,#247663,#247664,#247665,#247666,#247667,#247668,
#247669,#247670,#247671,#247672,#247673,#247674,#247675,#247676,#247677,
#247678,#247679,#247680,#247681,#247682,#247683,#247684,#247685),
 .UNSPECIFIED.,.F.,.F.,(4,3,3,3,3,3,3,3,3,3,3,3,3,3,3,3,4),(-0.379502319520468,
-0.350579328605622,-0.315279094551637,-0.279996782838352,-0.268904605244671,
-0.264656187206077,-0.230575220092214,-0.196553534542628,-0.163007386746561,
-0.142631463403241,-0.131301183629302,-0.126714514936786,-0.0943066959694338,
-0.0623519123392507,-0.0311759561696254,-0.00354365828344034,-6.47742434437623E-14),
 .UNSPECIFIED.);
#3648=B_SPLINE_CURVE_WITH_KNOTS('',3,(#247691,#247692,#247693,#247694,#247695,
#247696,#247697,#247698,#247699,#247700,#247701,#247702,#247703,#247704,
#247705,#247706,#247707,#247708,#247709,#247710,#247711,#247712,#247713,
#247714,#247715,#247716,#247717,#247718,#247719,#247720,#247721,#247722,
#247723,#247724,#247725,#247726,#247727,#247728,#247729,#247730,#247731,
#247732,#247733,#247734,#247735,#247736,#247737,#247738,#247739,#247740,
#247741,#247742,#247743,#247744,#247745,#247746,#247747,#247748,#247749,
#247750,#247751,#247752,#247753,#247754,#247755,#247756,#247757,#247758,
#247759,#247760,#247761,#247762,#247763,#247764,#247765,#247766,#247767,
#247768,#247769,#247770,#247771,#247772,#247773,#247774,#247775,#247776,
#247777,#247778,#247779,#247780,#247781,#247782,#247783,#247784,#247785,
#247786,#247787,#247788,#247789,#247790,#247791,#247792,#247793,#247794,
#247795,#247796,#247797,#247798,#247799,#247800,#247801,#247802,#247803,
#247804,#247805,#247806,#247807,#247808,#247809,#247810,#247811,#247812,
#247813,#247814,#247815,#247816,#247817,#247818,#247819,#247820,#247821,
#247822,#247823,#247824,#247825,#247826,#247827,#247828,#247829,#247830,
#247831,#247832,#247833,#247834,#247835,#247836,#247837,#247838,#247839,
#247840,#247841,#247842,#247843,#247844,#247845,#247846,#247847,#247848,
#247849,#247850,#247851,#247852,#247853,#247854,#247855,#247856,#247857,
#247858,#247859,#247860,#247861,#247862,#247863,#247864,#247865,#247866,
#247867,#247868),.UNSPECIFIED.,.F.,.F.,(4,3,3,3,3,3,3,3,3,3,3,3,3,3,3,3,
3,3,3,3,3,3,3,3,3,3,3,3,3,3,3,3,3,3,3,3,3,3,3,3,3,3,3,3,3,3,3,3,3,3,3,3,
3,3,3,3,3,3,3,4),(10.3763203563934,10.4685630468881,10.5606871195005,10.6530034956873,
10.7449811286153,10.8369328546413,10.9288843331454,11.0214677821077,11.1135450142217,
11.2063815716082,11.2992181289947,11.3925071972562,11.4856743835116,11.5787469958742,
11.671756411856,11.7647335460437,11.8577029439718,11.9506891380896,12.0437754407899,
12.136915160519,12.2302071912169,12.294046588707,12.3870547316618,12.4799363079774,
12.5727190398393,12.6654333606845,12.7581122928936,12.8507807367849,12.943463577407,
13.0362446719034,13.1290776878867,13.2220637037164,13.2888750484192,13.382032516625,
13.4750651584355,13.5680004849872,13.6608690716508,13.7537032475578,13.8465277306185,
13.9393672240905,14.0323049649879,14.125294863567,14.2184365482503,14.2837035081315,
14.3768524935008,14.4698769118861,14.5628042846802,14.6556653589909,14.7484922973377,
14.8413098275675,14.9341426631096,15.0270742465684,15.1200582578556,15.2131945567684,
15.2785319678437,15.3799288349245,15.480948245519,15.5817221848362,15.6821411676171,
15.7079632676789),.UNSPECIFIED.);
#3649=B_SPLINE_CURVE_WITH_KNOTS('',3,(#247871,#247872,#247873,#247874,#247875,
#247876,#247877,#247878,#247879,#247880,#247881,#247882,#247883,#247884,
#247885,#247886,#247887,#247888,#247889,#247890,#247891,#247892,#247893,
#247894,#247895,#247896,#247897,#247898,#247899,#247900,#247901,#247902,
#247903,#247904,#247905,#247906,#247907,#247908,#247909,#247910,#247911,
#247912,#247913,#247914,#247915,#247916,#247917,#247918,#247919,#247920,
#247921,#247922,#247923,#247924,#247925,#247926,#247927,#247928,#247929,
#247930,#247931,#247932,#247933,#247934,#247935,#247936,#247937,#247938,
#247939,#247940,#247941,#247942,#247943,#247944,#247945,#247946,#247947,
#247948,#247949,#247950,#247951,#247952,#247953,#247954,#247955,#247956,
#247957,#247958,#247959,#247960,#247961,#247962,#247963,#247964,#247965,
#247966,#247967,#247968,#247969,#247970,#247971,#247972,#247973,#247974,
#247975,#247976,#247977,#247978,#247979,#247980,#247981,#247982,#247983,
#247984,#247985,#247986,#247987,#247988,#247989,#247990,#247991,#247992,
#247993,#247994,#247995,#247996,#247997,#247998,#247999,#248000,#248001,
#248002,#248003,#248004,#248005,#248006),.UNSPECIFIED.,.F.,.F.,(4,3,3,3,
3,3,3,3,3,3,3,3,3,3,3,3,3,3,3,3,3,3,3,3,3,3,3,3,3,3,3,3,3,3,3,3,3,3,3,3,
3,3,3,3,3,4),(11.6152142277546,11.7105094858962,11.8057504942051,11.9009592767727,
11.9961843748489,12.0914240174434,12.1866982082662,12.2820269791461,12.3774952630653,
12.4730416608485,12.5687527374881,12.609327240686,12.7015323089428,12.7935998055635,
12.8855584723409,12.9774367511178,13.069272429844,13.1610912608687,13.2529189756459,
13.3448411934394,13.436811901971,13.5289383207552,13.6034402536173,13.6967164976112,
13.7898681174578,13.8829224520209,13.975909532746,14.0688618527508,14.1618039767653,
14.2547604544307,14.347813236206,14.4409173688033,14.5341703263431,14.5975532665487,
14.6908501826115,14.784025381243,14.8771061578232,14.9701238940431,15.0631094575167,
15.1560873828664,15.2490821917039,15.3421770033991,15.4353252969455,15.5286254390666,
15.59166627948,15.7079632679489),.UNSPECIFIED.);
#3650=B_SPLINE_CURVE_WITH_KNOTS('',3,(#248011,#248012,#248013,#248014,#248015,
#248016,#248017,#248018,#248019,#248020,#248021,#248022,#248023,#248024,
#248025,#248026,#248027,#248028,#248029,#248030,#248031,#248032,#248033,
#248034,#248035,#248036,#248037,#248038,#248039,#248040,#248041,#248042,
#248043,#248044,#248045,#248046,#248047,#248048,#248049,#248050,#248051,
#248052,#248053,#248054,#248055,#248056,#248057,#248058,#248059,#248060,
#248061,#248062,#248063,#248064,#248065,#248066,#248067,#248068,#248069,
#248070,#248071,#248072,#248073,#248074,#248075,#248076,#248077,#248078,
#248079,#248080,#248081,#248082,#248083,#248084,#248085,#248086,#248087,
#248088,#248089,#248090,#248091,#248092,#248093,#248094,#248095,#248096,
#248097,#248098,#248099,#248100,#248101,#248102,#248103,#248104,#248105,
#248106,#248107,#248108,#248109,#248110,#248111,#248112,#248113,#248114,
#248115,#248116,#248117,#248118,#248119,#248120,#248121,#248122,#248123,
#248124,#248125,#248126,#248127,#248128,#248129,#248130,#248131,#248132,
#248133,#248134,#248135,#248136,#248137,#248138,#248139,#248140,#248141,
#248142,#248143,#248144,#248145,#248146,#248147,#248148,#248149,#248150,
#248151,#248152,#248153,#248154,#248155,#248156,#248157,#248158,#248159,
#248160,#248161,#248162,#248163,#248164,#248165,#248166,#248167,#248168,
#248169,#248170,#248171,#248172,#248173,#248174,#248175,#248176,#248177,
#248178,#248179,#248180,#248181,#248182,#248183,#248184,#248185,#248186,
#248187,#248188,#248189,#248190,#248191,#248192,#248193,#248194,#248195,
#248196,#248197,#248198,#248199,#248200,#248201,#248202,#248203,#248204,
#248205,#248206,#248207,#248208,#248209,#248210,#248211,#248212,#248213,
#248214,#248215,#248216,#248217,#248218,#248219,#248220,#248221,#248222),
 .UNSPECIFIED.,.F.,.F.,(4,2,2,2,2,2,2,2,2,2,2,2,2,2,2,2,2,2,2,2,2,2,2,2,
2,2,2,2,2,2,2,2,2,2,2,2,2,2,2,2,2,2,2,2,2,2,2,2,2,2,2,2,2,2,2,2,2,2,2,2,
2,2,2,2,2,2,2,2,2,2,2,2,2,2,2,2,2,2,2,2,2,2,2,2,2,2,2,2,2,2,2,2,2,2,2,2,
2,2,2,2,2,2,2,2,2,4),(-2.03067141131433,-1.97483616077069,-1.96126379034493,
-1.9545729520835,-1.94924404260476,-1.94319645392332,-1.93277625310953,
-1.87740289985723,-1.82305026185814,-1.80032478632167,-1.7945208337889,
-1.79115358029843,-1.78812090026516,-1.78392753539794,-1.77381178780753,
-1.75897702158424,-1.7089001526612,-1.64844411523202,-1.63800185762131,
-1.63188981306857,-1.62656806293351,-1.61996968429409,-1.60687468288044,
-1.55774436938992,-1.5062960375289,-1.4794697209714,-1.47346806347462,-1.47002274413215,
-1.46701074783559,-1.46296765821994,-1.45374385803148,-1.44064312057713,
-1.40093987702096,-1.33175045168366,-1.31859465808437,-1.3118969602576,
-1.30656687157817,-1.30052251491307,-1.29011952281498,-1.2353637336783,
-1.18209964995384,-1.15782795374053,-1.15191601322357,-1.14852504088423,
-1.14549976297345,-1.14135560017372,-1.13153664036763,-1.11728774956787,
-1.07097628306266,-1.0108018768231,-0.997222669837635,-0.990530695708932,
-0.985201911922215,-0.979155583314236,-0.968740455130169,-0.913538364394459,
-0.85948627542512,-0.836326513585347,-0.830491039560349,-0.827117003020576,
-0.824086653374452,-0.819908246120698,-0.809883740708039,-0.79523042661246,
-0.74635779995978,-0.689476235577065,-0.675858091793467,-0.669157890249812,
-0.663827486230811,-0.657784576464042,-0.647388695842203,-0.592870630599238,
-0.540029374168084,-0.515159180350477,-0.509209357314793,-0.505809712305229,
-0.502784523415308,-0.498652144176125,-0.488915986734228,-0.474831487736167,
-0.429531130530253,-0.368212505709077,-0.354584366405084,-0.347880538645923,
-0.342547713937049,-0.336502488409553,-0.326103555440953,-0.313437790281824,
-0.286206819983695,-0.246066940785503,-0.22982085334851,-0.19472010318304,
-0.188368341713729,-0.184843822290316,-0.181847158005165,-0.177933589784178,
-0.169418797408968,-0.132209288608843,-0.0626984163688823,-0.0379054806914244,
-0.0292672891627416,-0.0236050312665482,-0.0185480379602508,-0.0132366222581118,
-0.00734349179396152,-0.000945049796771579),.UNSPECIFIED.);
#3651=B_SPLINE_CURVE_WITH_KNOTS('',3,(#248223,#248224,#248225,#248226,#248227,
#248228,#248229,#248230,#248231,#248232,#248233,#248234,#248235,#248236,
#248237,#248238,#248239,#248240,#248241,#248242,#248243,#248244,#248245,
#248246,#248247,#248248,#248249,#248250,#248251,#248252,#248253,#248254,
#248255,#248256,#248257,#248258,#248259,#248260,#248261,#248262,#248263,
#248264,#248265,#248266,#248267,#248268,#248269,#248270,#248271,#248272,
#248273,#248274,#248275,#248276,#248277,#248278,#248279,#248280,#248281,
#248282,#248283,#248284,#248285,#248286,#248287,#248288,#248289,#248290,
#248291,#248292,#248293,#248294,#248295,#248296,#248297,#248298,#248299,
#248300,#248301,#248302,#248303,#248304,#248305,#248306,#248307,#248308,
#248309,#248310,#248311,#248312,#248313,#248314,#248315,#248316,#248317,
#248318,#248319,#248320,#248321,#248322,#248323,#248324,#248325,#248326,
#248327,#248328,#248329,#248330,#248331,#248332,#248333,#248334,#248335,
#248336,#248337,#248338,#248339,#248340,#248341,#248342,#248343,#248344,
#248345,#248346,#248347,#248348,#248349,#248350,#248351,#248352,#248353,
#248354,#248355,#248356,#248357,#248358,#248359,#248360,#248361,#248362,
#248363,#248364,#248365,#248366,#248367,#248368,#248369,#248370,#248371,
#248372,#248373,#248374,#248375,#248376,#248377,#248378,#248379,#248380,
#248381,#248382,#248383,#248384,#248385,#248386,#248387,#248388,#248389,
#248390,#248391,#248392,#248393,#248394,#248395,#248396,#248397,#248398,
#248399,#248400,#248401,#248402,#248403,#248404,#248405,#248406,#248407,
#248408,#248409,#248410,#248411,#248412,#248413,#248414,#248415,#248416,
#248417,#248418,#248419,#248420,#248421,#248422,#248423,#248424,#248425,
#248426),.UNSPECIFIED.,.F.,.F.,(4,2,2,2,2,2,2,2,2,2,2,2,2,2,2,2,2,2,2,2,
2,2,2,2,2,2,2,2,2,2,2,2,2,2,2,2,2,2,2,2,2,2,2,2,2,2,2,2,2,2,2,2,2,2,2,2,
2,2,2,2,2,2,2,2,2,2,2,2,2,2,2,2,2,2,2,2,2,2,2,2,2,2,2,2,2,2,2,2,2,2,2,2,
2,2,2,2,2,2,2,2,2,4),(-4.06024336860817,-4.01103093763988,-3.96064562767585,
-3.94732081492831,-3.94061788480259,-3.935264494322,-3.92907883301094,-3.91855996553229,
-3.86473609846212,-3.82694857062176,-3.79988403095017,-3.78944272167838,
-3.78183318208697,-3.77815115892528,-3.77510947605076,-3.77150688488609,
-3.765014522366,-3.72747951411371,-3.64463736684358,-3.6274606957388,-3.62002097883177,
-3.61448358951176,-3.60857175650951,-3.59922385331445,-3.56936521439295,
-3.50038098158607,-3.47725865926583,-3.46333140306374,-3.45851718481015,
-3.45530992008311,-3.45242578797797,-3.44760990687348,-3.4346648612484,
-3.37315107853622,-3.32275563082252,-3.30657769464003,-3.29931747220349,
-3.29381689393851,-3.28785179805557,-3.27821603365067,-3.2460953895588,
-3.18377392033821,-3.14533094013184,-3.13889302885373,-3.13534271705904,
-3.13226981654794,-3.12824642799737,-3.11917154938555,-3.0675409065031,
-3.01860421874562,-2.99912151847835,-2.98455694764226,-2.9775926015785,
-2.97213596036157,-2.9660351025152,-2.95574364731131,-2.91315560025828,
-2.84809684012526,-2.83129167150733,-2.82016906103291,-2.81576275529667,
-2.81264460943735,-2.80924806003364,-2.8035231533907,-2.78254715361318,
-2.72720686048132,-2.67621104046059,-2.6627715404695,-2.65601592257644,
-2.65062146082266,-2.64438840593758,-2.63378554905489,-2.57707604629983,
-2.53584161241735,-2.51354582093467,-2.49996531294343,-2.4952061534296,
-2.49201814165426,-2.4887349503665,-2.48352632456309,-2.46758367680557,
-2.44867351299677,-2.39110641406612,-2.36332328365804,-2.3444113612538,
-2.33670506103856,-2.33113408528844,-2.32533441689205,-2.31646820370616,
-2.2909478684611,-2.2241291642873,-2.18578324295766,-2.17707113585314,-2.17306808095327,
-2.1700026845052,-2.16639021933042,-2.15984851911487,-2.12011471493321,
-2.07743418681169,-2.04509749541676,-2.0308601546849,-2.03077061808298),
 .UNSPECIFIED.);
#3652=B_SPLINE_CURVE_WITH_KNOTS('',3,(#248432,#248433,#248434,#248435),
 .UNSPECIFIED.,.F.,.F.,(4,4),(-0.0010441278808804,-0.000941427881473156),
 .UNSPECIFIED.);
#3653=B_SPLINE_CURVE_WITH_KNOTS('',3,(#248436,#248437,#248438,#248439,#248440,
#248441,#248442,#248443,#248444,#248445,#248446,#248447,#248448,#248449,
#248450,#248451,#248452,#248453,#248454,#248455,#248456,#248457,#248458,
#248459,#248460,#248461,#248462,#248463,#248464,#248465,#248466,#248467,
#248468,#248469,#248470,#248471,#248472,#248473,#248474,#248475,#248476,
#248477,#248478,#248479,#248480,#248481,#248482,#248483,#248484,#248485,
#248486,#248487,#248488,#248489,#248490,#248491,#248492,#248493,#248494,
#248495,#248496,#248497,#248498,#248499,#248500,#248501,#248502,#248503,
#248504,#248505,#248506,#248507,#248508,#248509,#248510,#248511,#248512,
#248513,#248514,#248515,#248516,#248517,#248518,#248519,#248520,#248521,
#248522,#248523,#248524,#248525,#248526,#248527,#248528,#248529,#248530,
#248531,#248532,#248533,#248534,#248535,#248536,#248537,#248538,#248539,
#248540,#248541,#248542,#248543,#248544,#248545,#248546,#248547,#248548,
#248549,#248550,#248551,#248552,#248553,#248554,#248555,#248556,#248557,
#248558,#248559,#248560,#248561,#248562,#248563,#248564,#248565,#248566,
#248567,#248568,#248569,#248570,#248571,#248572,#248573,#248574,#248575,
#248576,#248577,#248578,#248579,#248580,#248581,#248582,#248583,#248584,
#248585,#248586,#248587,#248588,#248589,#248590,#248591,#248592,#248593,
#248594,#248595,#248596,#248597,#248598,#248599,#248600,#248601,#248602,
#248603,#248604,#248605,#248606,#248607,#248608,#248609,#248610,#248611,
#248612,#248613,#248614,#248615,#248616,#248617,#248618,#248619,#248620,
#248621,#248622,#248623,#248624,#248625,#248626,#248627,#248628,#248629,
#248630,#248631,#248632,#248633,#248634,#248635,#248636,#248637,#248638,
#248639,#248640,#248641,#248642,#248643,#248644,#248645),.UNSPECIFIED.,
 .F.,.F.,(4,2,2,2,2,2,2,2,2,2,2,2,2,2,2,2,2,2,2,2,2,2,2,2,2,2,2,2,2,2,2,
2,2,2,2,2,2,2,2,2,2,2,2,2,2,2,2,2,2,2,2,2,2,2,2,2,2,2,2,2,2,2,2,2,2,2,2,
2,2,2,2,2,2,2,2,2,2,2,2,2,2,2,2,2,2,2,2,2,2,2,2,2,2,2,2,2,2,2,2,2,2,2,2,
2,4),(-4.06000788164972,-4.0490529277794,-4.0449969392343,-4.04198931254412,
-4.0391085131236,-4.03576120822483,-4.03004756816254,-4.00845705239628,
-3.95057220832007,-3.89738773129655,-3.88703658997922,-3.88100414033653,
-3.87567366802917,-3.868960948112,-3.85527264034345,-3.79734136389309,-3.74937474976475,
-3.73486201898847,-3.72490988315929,-3.72074368142778,-3.71771539811846,
-3.71433589767344,-3.70847476776611,-3.68494175028851,-3.62034744739797,
-3.57544766813393,-3.56544034148988,-3.5594818588834,-3.55413894643412,
-3.54730386680118,-3.53625234529564,-3.45604119929961,-3.40827534981182,
-3.40173300907305,-3.39820709497625,-3.3952093357214,-3.3913604164974,-3.38327876583815,
-3.31743613076699,-3.26404475569927,-3.24787839060404,-3.24071613607295,
-3.23532956044951,-3.22952866484843,-3.22025402320601,-3.18994975342525,
-3.12705909501232,-3.09004799435543,-3.08155205725997,-3.07763990307568,
-3.07464231721219,-3.0711151154941,-3.06474859461741,-3.02868648049119,
-3.01330103703042,-2.97267755409784,-2.94587933930806,-2.92751860680357,
-2.91999723969625,-2.91455162275291,-2.90887749047995,-2.90019837081972,
-2.87529825664998,-2.80771639459657,-2.77883145846871,-2.76799276510915,
-2.76000176277614,-2.75618425865536,-2.7534802590545,-2.75000509641622,
-2.74387094394008,-2.71442112058098,-2.66487400011064,-2.61207544008875,
-2.60173630994273,-2.59570607247023,-2.59037469025189,-2.58365698577204,
-2.57040160050305,-2.50348730762648,-2.46213296590742,-2.44872968238932,
-2.43934809470799,-2.43527796176851,-2.43226283502322,-2.42883322124811,
-2.42290025906192,-2.39717684288309,-2.34498340605783,-2.29082024311193,
-2.28043698799768,-2.27439725905009,-2.26906717127117,-2.26236404223516,
-2.2487280651821,-2.19013852699169,-2.14261465343102,-2.12110801857514,
-2.11561513428152,-2.11231610431234,-2.10929091289068,-2.10563518934698,
-2.09632790046346,-2.03095948049066,-2.03067141131433),.UNSPECIFIED.);
#3654=B_SPLINE_CURVE_WITH_KNOTS('',3,(#248646,#248647,#248648,#248649,#248650,
#248651,#248652,#248653,#248654,#248655,#248656,#248657,#248658,#248659,
#248660,#248661,#248662,#248663,#248664,#248665,#248666,#248667,#248668,
#248669,#248670,#248671,#248672,#248673,#248674,#248675,#248676,#248677,
#248678,#248679,#248680,#248681,#248682,#248683,#248684,#248685,#248686,
#248687,#248688,#248689,#248690,#248691,#248692,#248693,#248694,#248695,
#248696,#248697,#248698,#248699,#248700,#248701,#248702,#248703,#248704,
#248705,#248706,#248707,#248708,#248709,#248710,#248711,#248712,#248713,
#248714,#248715,#248716,#248717,#248718,#248719,#248720,#248721,#248722,
#248723,#248724,#248725,#248726,#248727,#248728,#248729,#248730,#248731,
#248732,#248733,#248734,#248735,#248736,#248737,#248738,#248739,#248740,
#248741,#248742,#248743,#248744,#248745,#248746,#248747,#248748,#248749,
#248750,#248751,#248752,#248753,#248754,#248755,#248756,#248757,#248758,
#248759,#248760,#248761,#248762,#248763,#248764,#248765,#248766,#248767,
#248768,#248769,#248770,#248771,#248772,#248773,#248774,#248775,#248776,
#248777,#248778,#248779,#248780,#248781,#248782,#248783,#248784,#248785,
#248786,#248787,#248788,#248789,#248790,#248791,#248792,#248793,#248794,
#248795,#248796,#248797,#248798,#248799,#248800,#248801,#248802,#248803,
#248804,#248805,#248806,#248807,#248808,#248809,#248810,#248811,#248812,
#248813,#248814,#248815,#248816,#248817,#248818,#248819,#248820,#248821,
#248822,#248823,#248824,#248825,#248826,#248827,#248828,#248829,#248830,
#248831,#248832,#248833,#248834,#248835,#248836,#248837,#248838,#248839,
#248840,#248841,#248842,#248843,#248844,#248845,#248846,#248847,#248848,
#248849,#248850,#248851,#248852,#248853,#248854,#248855,#248856,#248857,
#248858,#248859),.UNSPECIFIED.,.F.,.F.,(4,2,2,2,2,2,2,2,2,2,2,2,2,2,2,2,
2,2,2,2,2,2,2,2,2,2,2,2,2,2,2,2,2,2,2,2,2,2,2,2,2,2,2,2,2,2,2,2,2,2,2,2,
2,2,2,2,2,2,2,2,2,2,2,2,2,2,2,2,2,2,2,2,2,2,2,2,2,2,2,2,2,2,2,2,2,2,2,2,
2,2,2,2,2,2,2,2,2,2,2,2,2,2,2,2,2,2,4),(-2.03077061808298,-2.02055497819448,
-2.01386303777659,-2.00842532828469,-2.00213243245978,-1.99095608667018,
-1.92975997225102,-1.86395954660106,-1.8557293319733,-1.85181618094681,
-1.84875688259027,-1.84507566739787,-1.83801827904976,-1.82884566161254,
-1.80676468105038,-1.76530813189062,-1.70846287298297,-1.6978618494301,
-1.69163023327029,-1.68623730939664,-1.67948405694965,-1.66605114574467,
-1.6150922529632,-1.55982087497854,-1.53870033584592,-1.53296254066424,
-1.52956302728876,-1.52644289827209,-1.5220375466739,-1.5109407677984,-1.49419603380479,
-1.429686933506,-1.38662833180775,-1.37630269963784,-1.37019030724985,-1.36472854712188,
-1.35776465823026,-1.34322688969505,-1.32379474589797,-1.2687596457538,
-1.26052245996461,-1.21922338157848,-1.21265567901223,-1.20903697087285,
-1.20597159627351,-1.20197542502426,-1.19330310569111,-1.15534308323836,
-1.08958527540451,-1.06290592868058,-1.05391148214489,-1.04808444815133,
-1.04252802674135,-1.0349076162412,-1.016549384954,-0.989897764633018,-0.949224549136618,
-0.934233302568002,-0.897957045876173,-0.891496759073359,-0.887902004265296,
-0.884862730251556,-0.880849158009556,-0.872082002163689,-0.833214053748261,
-0.764905908432308,-0.741089653023172,-0.73244112623066,-0.727261538535745,
-0.721736249545464,-0.714304276331715,-0.697109032219287,-0.614187985446788,
-0.576830332333955,-0.570341550970263,-0.566740208648143,-0.563672321912328,
-0.559650370391542,-0.550838273879347,-0.511537765051561,-0.442001568670601,
-0.41949531311763,-0.411030856338562,-0.405885055828772,-0.400337725289012,
-0.392772447364188,-0.374762442562489,-0.348811754576788,-0.306785831119333,
-0.291464462354942,-0.255653646910567,-0.249205092313655,-0.245612831395585,
-0.242573027726789,-0.238555302358582,-0.230278547225392,-0.221678285298059,
-0.196433013886694,-0.143637614041602,-0.102019751448381,-0.0917804785727679,
-0.0856864194060444,-0.0802207649475341,-0.0732238710232165,-0.0656228449603274,
-0.0464796131870714,-0.00122941941383501),.UNSPECIFIED.);
#3655=B_SPLINE_CURVE_WITH_KNOTS('',3,(#248864,#248865,#248866,#248867,#248868,
#248869,#248870,#248871,#248872,#248873,#248874,#248875,#248876,#248877,
#248878,#248879,#248880,#248881,#248882,#248883,#248884,#248885,#248886,
#248887,#248888,#248889,#248890,#248891,#248892,#248893,#248894,#248895,
#248896,#248897,#248898,#248899,#248900,#248901,#248902,#248903,#248904,
#248905,#248906,#248907,#248908,#248909,#248910,#248911,#248912,#248913,
#248914,#248915,#248916,#248917,#248918,#248919,#248920,#248921,#248922,
#248923,#248924,#248925,#248926,#248927,#248928,#248929,#248930,#248931,
#248932,#248933,#248934,#248935,#248936,#248937,#248938,#248939,#248940,
#248941,#248942,#248943,#248944,#248945,#248946,#248947,#248948,#248949,
#248950,#248951,#248952,#248953,#248954,#248955,#248956,#248957,#248958,
#248959,#248960,#248961,#248962,#248963,#248964,#248965,#248966,#248967,
#248968,#248969,#248970,#248971,#248972,#248973,#248974,#248975,#248976,
#248977,#248978,#248979,#248980,#248981,#248982,#248983,#248984,#248985,
#248986,#248987,#248988,#248989,#248990,#248991,#248992,#248993,#248994,
#248995,#248996,#248997,#248998,#248999,#249000,#249001,#249002,#249003,
#249004,#249005,#249006,#249007,#249008,#249009,#249010,#249011,#249012,
#249013,#249014,#249015,#249016,#249017,#249018,#249019,#249020,#249021,
#249022,#249023,#249024,#249025,#249026,#249027,#249028,#249029,#249030,
#249031,#249032,#249033,#249034,#249035,#249036,#249037,#249038,#249039,
#249040,#249041,#249042,#249043,#249044,#249045,#249046,#249047,#249048,
#249049,#249050,#249051,#249052,#249053,#249054,#249055,#249056,#249057,
#249058,#249059,#249060,#249061,#249062,#249063,#249064,#249065,#249066,
#249067,#249068,#249069,#249070,#249071,#249072,#249073,#249074,#249075,
#249076,#249077,#249078,#249079,#249080,#249081,#249082,#249083,#249084,
#249085,#249086,#249087,#249088,#249089,#249090,#249091,#249092,#249093,
#249094,#249095,#249096,#249097,#249098,#249099,#249100,#249101,#249102,
#249103,#249104,#249105,#249106,#249107,#249108,#249109,#249110,#249111,
#249112,#249113,#249114,#249115,#249116,#249117,#249118,#249119,#249120,
#249121,#249122,#249123,#249124,#249125,#249126,#249127,#249128,#249129,
#249130,#249131,#249132,#249133),.UNSPECIFIED.,.F.,.F.,(4,2,2,2,2,2,2,2,
2,2,2,2,2,2,2,2,2,2,2,2,2,2,2,2,2,2,2,2,2,2,2,2,2,2,2,2,2,2,2,2,2,2,2,2,
2,2,2,2,2,2,2,2,2,2,2,2,2,2,2,2,2,2,2,2,2,2,2,2,2,2,2,2,2,2,2,2,2,2,2,2,
2,2,2,2,2,2,2,2,2,2,2,2,2,2,2,2,2,2,2,2,2,2,2,2,2,2,2,2,2,2,2,2,2,2,2,2,
2,2,2,2,2,2,2,2,2,2,2,2,2,2,2,2,2,2,4),(-2.03049264206931,-2.03028509209775,
-1.98875219490121,-1.92233554041634,-1.9150056198462,-1.91127243186873,
-1.90822889792823,-1.90496847502886,-1.89964943273837,-1.8802164542492,
-1.8407220076384,-1.77124689806472,-1.75810845416528,-1.75141546601951,
-1.74608716725735,-1.74004275566971,-1.72963437144085,-1.67461500588666,
-1.62087088884263,-1.59730235228608,-1.59143874872317,-1.5880588295639,
-1.58503086613491,-1.580866144922,-1.57092206009866,-1.55642651649832,-1.50855832268436,
-1.45055252814352,-1.43688012976825,-1.43017066320431,-1.42484070775506,
-1.41880664012084,-1.40844716940965,-1.35502090777339,-1.30423856273821,
-1.2764873914327,-1.27043833552235,-1.2669826848018,-1.26427582822313,-1.26043080914499,
-1.25229351986786,-1.20600348109814,-1.12725914149006,-1.11604488040571,
-1.10916252113611,-1.10381437563225,-1.09788246207519,-1.08799762548072,
-1.04539533043727,-0.983611048514379,-0.955209749741391,-0.949128074285096,
-0.945665074020801,-0.94295953996442,-0.939125610181733,-0.931046650042836,
-0.897785034127711,-0.837694352007401,-0.801306047639294,-0.791513762783684,
-0.785601674986457,-0.780248747260584,-0.773328260650355,-0.758526466873553,
-0.738520003470266,-0.679712632760192,-0.634659508142356,-0.628165958685232,
-0.624610692810223,-0.621616521564816,-0.617744008496053,-0.609460659659126,
-0.57439713558441,-0.512475341887416,-0.479530541052491,-0.469994403080385,
-0.464137451718634,-0.458769699658739,-0.451736555519746,-0.436308791976659,
-0.376238255739193,-0.316586119393395,-0.307971054437799,-0.304078960075506,
-0.301188401675312,-0.301123873795849,-0.301064179693311,-0.301008824114215,
-0.300957378105432,-0.300909468102858,-0.300864767136011,-0.300822987675755,
-0.300783875764898,-0.300747206180224,-0.300712778420836,-0.300680413357834,
-0.300649950409566,-0.3006212451624,-0.300594167364014,-0.300568599205255,
-0.300544433843571,-0.30052157413206,-0.300485514880745,-0.300449837416733,
-0.300414525371713,-0.300379562987406,-0.300344935070795,-0.300310626980818,
-0.300276624597331,-0.300242914278798,-0.300209482840455,-0.300176317528037,
-0.30014340600438,-0.300110736314592,-0.300078296869722,-0.300046076425722,
-0.300014064062174,-0.299982249171943,-0.299950621429795,-0.299919170791457,
-0.299887887475917,-0.299856761937967,-0.296027465083763,-0.29153099791895,
-0.283725619066497,-0.266253683265083,-0.193692098516056,-0.158540528277937,
-0.148825311640787,-0.142929767128729,-0.137572628360742,-0.130619378177436,
-0.115637592219247,-0.0953077315725876,-0.0010441278808804),
 .UNSPECIFIED.);
#3656=B_SPLINE_CURVE_WITH_KNOTS('',3,(#249135,#249136,#249137,#249138),
 .UNSPECIFIED.,.F.,.F.,(4,4),(-0.00122941941383501,-0.000938193424354277),
 .UNSPECIFIED.);
#3657=B_SPLINE_CURVE_WITH_KNOTS('',3,(#249139,#249140,#249141,#249142,#249143,
#249144,#249145,#249146,#249147,#249148,#249149,#249150,#249151,#249152,
#249153,#249154,#249155,#249156,#249157,#249158,#249159,#249160,#249161,
#249162,#249163,#249164,#249165,#249166,#249167,#249168,#249169,#249170,
#249171,#249172,#249173,#249174,#249175,#249176,#249177,#249178,#249179,
#249180,#249181,#249182,#249183,#249184,#249185,#249186,#249187,#249188,
#249189,#249190,#249191,#249192,#249193,#249194,#249195,#249196,#249197,
#249198,#249199,#249200,#249201,#249202,#249203,#249204,#249205,#249206,
#249207,#249208,#249209,#249210,#249211,#249212,#249213,#249214,#249215,
#249216,#249217,#249218,#249219,#249220,#249221,#249222,#249223,#249224,
#249225,#249226,#249227,#249228,#249229,#249230,#249231,#249232,#249233,
#249234,#249235,#249236,#249237,#249238,#249239,#249240,#249241,#249242,
#249243,#249244,#249245,#249246,#249247,#249248,#249249,#249250,#249251,
#249252,#249253,#249254,#249255,#249256,#249257,#249258,#249259,#249260,
#249261,#249262,#249263,#249264,#249265,#249266,#249267,#249268,#249269,
#249270,#249271,#249272,#249273,#249274,#249275,#249276,#249277,#249278,
#249279,#249280,#249281,#249282,#249283,#249284,#249285,#249286,#249287,
#249288,#249289,#249290,#249291,#249292,#249293,#249294,#249295,#249296,
#249297,#249298,#249299,#249300,#249301,#249302,#249303,#249304,#249305,
#249306,#249307,#249308,#249309,#249310,#249311,#249312,#249313,#249314,
#249315,#249316,#249317,#249318,#249319,#249320,#249321,#249322,#249323,
#249324,#249325,#249326,#249327,#249328,#249329,#249330,#249331,#249332,
#249333,#249334,#249335,#249336,#249337,#249338,#249339,#249340,#249341,
#249342,#249343,#249344,#249345,#249346,#249347,#249348,#249349,#249350,
#249351,#249352,#249353,#249354,#249355,#249356),.UNSPECIFIED.,.F.,.F.,
(4,2,2,2,2,2,2,2,2,2,2,2,2,2,2,2,2,2,2,2,2,2,2,2,2,2,2,2,2,2,2,2,2,2,2,
2,2,2,2,2,2,2,2,2,2,2,2,2,2,2,2,2,2,2,2,2,2,2,2,2,2,2,2,2,2,2,2,2,2,2,2,
2,2,2,2,2,2,2,2,2,2,2,2,2,2,2,2,2,2,2,2,2,2,2,2,2,2,2,2,2,2,2,2,2,2,2,2,
2,4),(-4.05980598877536,-4.00607694824287,-3.99262316888618,-3.98819389244878,
-3.98419843106118,-3.98113306609582,-3.97751367387623,-3.97094319247696,
-3.92930711700454,-3.88698963756487,-3.84933018664956,-3.83338570315429,
-3.82676395598467,-3.82656688810241,-3.82101619355601,-3.81587539147052,
-3.80743801250747,-3.78511797659816,-3.71506698191493,-3.67594244555395,
-3.6671486089494,-3.66312999380678,-3.66009004847685,-3.6564982027568,-3.65005182179954,
-3.61430656934356,-3.59931918298223,-3.5591584577112,-3.53190815441749,
-3.51325375846902,-3.50558646815111,-3.50002153283071,-3.49489904946328,
-3.48656362695737,-3.4649352795161,-3.3945191928488,-3.35490508492687,-3.34606080179038,
-3.34203287068172,-3.33896432985524,-3.33536678876337,-3.32889544246668,
-3.29220181534951,-3.20904506029438,-3.19156318726119,-3.1840836680527,
-3.17855051860901,-3.17338319225235,-3.16480186199284,-3.14147430196178,
-3.07266462457491,-3.03361265844576,-3.02482625938831,-3.02080898143384,
-3.0177415487464,-3.01413703310056,-3.00763397481958,-2.96969300776106,
-2.95759595440448,-2.91906459686975,-2.89047633493205,-2.87117647121552,
-2.86340987786898,-2.85782732523811,-2.85204364559089,-2.84325756130552,
-2.81841727248823,-2.75099216672519,-2.71242933902449,-2.70369341142794,
-2.69968524333211,-2.69661849251979,-2.69300735707348,-2.68647504482617,
-2.64729114378985,-2.63667200591327,-2.58183473035739,-2.56243895268676,
-2.54792014731511,-2.54095927695921,-2.53549723360981,-2.52938176642631,
-2.5190441890201,-2.47580374196751,-2.41139602287648,-2.39465753334207,
-2.38356424368313,-2.37915907781165,-2.37603874914964,-2.37263882131665,
-2.36689960775753,-2.34576350041702,-2.29052543613442,-2.23958511204373,
-2.22615325606372,-2.21939986273756,-2.21400650838632,-2.20777405399907,
-2.19717080610413,-2.14016681058464,-2.09843380492365,-2.07657693387381,
-2.06318069390806,-2.05844680709546,-2.05526477219033,-2.05197516342719,
-2.04673797527469,-2.03055789688724,-2.03039724048114),.UNSPECIFIED.);
#3658=B_SPLINE_CURVE_WITH_KNOTS('',3,(#249361,#249362,#249363,#249364,#249365,
#249366,#249367,#249368,#249369,#249370,#249371,#249372,#249373,#249374,
#249375,#249376,#249377,#249378,#249379,#249380,#249381,#249382,#249383,
#249384,#249385,#249386,#249387,#249388,#249389,#249390,#249391,#249392,
#249393,#249394,#249395,#249396,#249397,#249398,#249399,#249400,#249401,
#249402,#249403,#249404,#249405,#249406,#249407,#249408,#249409,#249410,
#249411,#249412,#249413,#249414,#249415,#249416,#249417,#249418,#249419,
#249420,#249421,#249422,#249423,#249424,#249425,#249426,#249427,#249428,
#249429,#249430,#249431,#249432,#249433,#249434,#249435,#249436,#249437,
#249438,#249439,#249440,#249441,#249442,#249443,#249444,#249445,#249446,
#249447,#249448,#249449,#249450,#249451,#249452,#249453,#249454,#249455,
#249456,#249457,#249458,#249459,#249460,#249461,#249462,#249463,#249464,
#249465,#249466,#249467,#249468,#249469,#249470,#249471,#249472,#249473,
#249474,#249475,#249476,#249477,#249478,#249479,#249480,#249481,#249482,
#249483,#249484,#249485,#249486,#249487,#249488,#249489,#249490,#249491,
#249492,#249493,#249494,#249495,#249496,#249497,#249498,#249499,#249500,
#249501,#249502,#249503,#249504,#249505,#249506,#249507,#249508,#249509,
#249510,#249511,#249512,#249513,#249514,#249515,#249516,#249517,#249518,
#249519,#249520,#249521,#249522,#249523,#249524,#249525,#249526,#249527,
#249528,#249529,#249530,#249531,#249532,#249533,#249534,#249535,#249536,
#249537,#249538,#249539,#249540,#249541,#249542,#249543,#249544,#249545,
#249546,#249547,#249548,#249549,#249550,#249551,#249552,#249553,#249554,
#249555,#249556,#249557,#249558,#249559,#249560,#249561,#249562,#249563,
#249564,#249565,#249566,#249567,#249568,#249569,#249570,#249571,#249572,
#249573,#249574,#249575,#249576),.UNSPECIFIED.,.F.,.F.,(4,2,2,2,2,2,2,2,
2,2,2,2,2,2,2,2,2,2,2,2,2,2,2,2,2,2,2,2,2,2,2,2,2,2,2,2,2,2,2,2,2,2,2,2,
2,2,2,2,2,2,2,2,2,2,2,2,2,2,2,2,2,2,2,2,2,2,2,2,2,2,2,2,2,2,2,2,2,2,2,2,
2,2,2,2,2,2,2,2,2,2,2,2,2,2,2,2,2,2,2,2,2,2,2,2,2,2,2,4),(-4.05954993223484,
-4.03036658012576,-4.01419262699979,-4.00699249478495,-4.00162895680077,
-3.99619715841623,-3.99050054573201,-3.98171219325065,-3.95584406383671,
-3.91403273066718,-3.85485065504541,-3.84330114932281,-3.83888578137858,
-3.83581573520925,-3.83253893153171,-3.82714535955158,-3.80890416335039,
-3.7317456495446,-3.70576206967119,-3.68780535047242,-3.68034835524555,
-3.67491473193295,-3.66922214860698,-3.66045211764536,-3.63474778210027,
-3.5610604622095,-3.53701802348523,-3.52278306230362,-3.51800671128323,
-3.51486456277623,-3.51206834900636,-3.5074748479715,-3.49562123656505,
-3.40600188302322,-3.38255741141337,-3.36589733553926,-3.35865211972301,
-3.35325363156675,-3.34818598108828,-3.33971239162828,-3.31635224500923,
-3.24738524241934,-3.21810866031752,-3.20717967433171,-3.19913833956825,
-3.1953117517077,-3.19260726036538,-3.18913975460874,-3.18303743350277,
-3.15419949137435,-3.10423333769317,-3.05123106355611,-3.04088709210085,
-3.03485668838411,-3.02952674852438,-3.02281299073591,-3.0095724076287,
-2.94236152114677,-2.9012386406383,-2.88787845967648,-2.87851995234048,
-2.87445436931095,-2.87144041807952,-2.86800965219237,-2.86206940361582,
-2.83620509408032,-2.78412689397127,-2.73825444409505,-2.72282544493743,
-2.71579257671991,-2.71042533747878,-2.70456923923268,-2.69503518639547,
-2.66210816528481,-2.60011382638448,-2.56504820208316,-2.55676522229272,
-2.5528929921763,-2.54989910955309,-2.54634423166144,-2.53985158079507,
-2.49465637908026,-2.46118071676765,-2.41319521535961,-2.40024513492375,
-2.39367620166703,-2.38835757318798,-2.38222630339106,-2.37169434992307,
-2.31339905265122,-2.27119761953275,-2.25027629054823,-2.23733446527528,
-2.23272381567628,-2.22961608560992,-2.22640054770862,-2.22128527680501,
-2.20555801949651,-2.18417559509424,-2.16802161501854,-2.1281766541877,
-2.10055041396245,-2.08178712661103,-2.07420436149142,-2.0687484915808,
-2.06309369451128,-2.05450376131022,-2.03049264206931),.UNSPECIFIED.);
#3659=B_SPLINE_CURVE_WITH_KNOTS('',3,(#249578,#249579,#249580,#249581,#249582,
#249583,#249584,#249585,#249586,#249587,#249588,#249589,#249590,#249591,
#249592,#249593,#249594,#249595,#249596,#249597,#249598,#249599,#249600,
#249601,#249602,#249603,#249604,#249605,#249606,#249607,#249608,#249609,
#249610,#249611,#249612,#249613,#249614,#249615,#249616,#249617,#249618,
#249619,#249620,#249621,#249622,#249623,#249624,#249625,#249626,#249627,
#249628,#249629,#249630,#249631,#249632,#249633,#249634,#249635,#249636,
#249637,#249638,#249639,#249640,#249641,#249642,#249643,#249644,#249645,
#249646,#249647,#249648,#249649,#249650,#249651,#249652,#249653,#249654,
#249655,#249656,#249657,#249658,#249659,#249660,#249661,#249662,#249663,
#249664,#249665,#249666,#249667,#249668,#249669,#249670,#249671,#249672,
#249673,#249674,#249675,#249676,#249677,#249678,#249679,#249680,#249681,
#249682,#249683,#249684,#249685,#249686,#249687,#249688,#249689,#249690,
#249691,#249692,#249693,#249694,#249695,#249696,#249697,#249698,#249699,
#249700,#249701,#249702,#249703,#249704,#249705,#249706,#249707,#249708,
#249709,#249710,#249711,#249712,#249713,#249714,#249715,#249716,#249717,
#249718,#249719,#249720,#249721,#249722,#249723,#249724,#249725,#249726,
#249727,#249728,#249729,#249730,#249731,#249732,#249733,#249734,#249735,
#249736,#249737,#249738,#249739,#249740,#249741,#249742,#249743,#249744,
#249745,#249746,#249747,#249748,#249749,#249750,#249751,#249752,#249753,
#249754,#249755,#249756,#249757,#249758,#249759,#249760,#249761,#249762,
#249763,#249764,#249765,#249766,#249767,#249768,#249769,#249770,#249771,
#249772,#249773,#249774,#249775,#249776,#249777,#249778,#249779,#249780,
#249781,#249782,#249783,#249784,#249785,#249786,#249787),.UNSPECIFIED.,
 .F.,.F.,(4,2,2,2,2,2,2,2,2,2,2,2,2,2,2,2,2,2,2,2,2,2,2,2,2,2,2,2,2,2,2,
2,2,2,2,2,2,2,2,2,2,2,2,2,2,2,2,2,2,2,2,2,2,2,2,2,2,2,2,2,2,2,2,2,2,2,2,
2,2,2,2,2,2,2,2,2,2,2,2,2,2,2,2,2,2,2,2,2,2,2,2,2,2,2,2,2,2,2,2,2,2,2,2,
2,4),(-2.03039724048114,-2.00074720145003,-1.92955318715566,-1.90877531220974,
-1.9005693611473,-1.89547004600393,-1.88988559509671,-1.88210828687461,
-1.86273783696658,-1.83399757922457,-1.80792591584767,-1.74910430934334,
-1.74031283091048,-1.73633725382342,-1.73326727718626,-1.72968033876686,
-1.72307513175734,-1.67748815478831,-1.60074575991067,-1.5866040858316,
-1.57960239709298,-1.57447553018519,-1.56891448228211,-1.56126842276891,
-1.54274868794605,-1.51576955837716,-1.47550725754844,-1.46020926457178,
-1.42435803464802,-1.4179085105867,-1.41431605879151,-1.41127632709393,
-1.40725899701873,-1.39847161994737,-1.35940923906924,-1.29055053678822,
-1.26732534227102,-1.25875861906537,-1.25359414387355,-1.24805953717539,
-1.24057010554252,-1.22302703982024,-1.19800073084897,-1.15511790842254,
-1.14566430713688,-1.10348248273422,-1.09690688970201,-1.09328640627237,
-1.09022120327229,-1.08622741373684,-1.07756814365768,-1.03973191826394,
-0.974318161318125,-0.94724249695607,-0.93820557911344,-0.932369533309311,
-0.92681778025944,-0.919224918735237,-0.901040637390619,-0.874740023720986,
-0.833425054458958,-0.818296125792496,-0.782198550243678,-0.775742876228114,
-0.772149138589994,-0.769109736992565,-0.765094687434443,-0.756319259193837,
-0.717370734785041,-0.648833846917342,-0.625266130947525,-0.616651890874911,
-0.611478751113957,-0.605949821022574,-0.598494462199108,-0.581157523267402,
-0.498111001494814,-0.461066589618979,-0.454585969209858,-0.450986495855608,
-0.447918412873352,-0.44389388786784,-0.435067518805084,-0.395627296426434,
-0.325692929561808,-0.303608986675095,-0.295206201158356,-0.290071687656267,
-0.284780187635255,-0.284571792168612,-0.2843685221861,-0.277709813699694,
-0.269679867835412,-0.255927836998914,-0.225289734371868,-0.167052378029449,
-0.13932200039344,-0.133189449986556,-0.129668282391417,-0.126586247529304,
-0.122435349254635,-0.112896430227072,-0.0992675105548785,-0.0569890199881752,
-0.000938351556276533),.UNSPECIFIED.);
#3660=B_SPLINE_CURVE_WITH_KNOTS('',3,(#249788,#249789,#249790,#249791),
 .UNSPECIFIED.,.F.,.F.,(4,4),(-4.05918925078444,-4.05903826007612),
 .UNSPECIFIED.);
#3661=B_SPLINE_CURVE_WITH_KNOTS('',3,(#249797,#249798,#249799,#249800,#249801,
#249802,#249803,#249804,#249805,#249806,#249807,#249808,#249809,#249810,
#249811,#249812,#249813,#249814,#249815,#249816,#249817,#249818,#249819,
#249820,#249821,#249822,#249823,#249824,#249825,#249826,#249827,#249828,
#249829,#249830,#249831,#249832,#249833,#249834,#249835,#249836,#249837,
#249838,#249839,#249840,#249841,#249842,#249843,#249844,#249845,#249846,
#249847,#249848,#249849,#249850,#249851,#249852,#249853,#249854,#249855,
#249856,#249857,#249858,#249859,#249860,#249861,#249862,#249863,#249864,
#249865,#249866,#249867,#249868,#249869,#249870,#249871,#249872,#249873,
#249874,#249875,#249876,#249877,#249878,#249879,#249880,#249881,#249882,
#249883,#249884,#249885,#249886,#249887,#249888,#249889,#249890,#249891,
#249892,#249893,#249894,#249895,#249896,#249897,#249898,#249899,#249900,
#249901,#249902,#249903,#249904,#249905,#249906,#249907,#249908,#249909,
#249910,#249911,#249912,#249913,#249914,#249915,#249916,#249917,#249918,
#249919,#249920,#249921,#249922,#249923,#249924,#249925,#249926,#249927,
#249928,#249929,#249930,#249931,#249932,#249933,#249934,#249935,#249936,
#249937,#249938,#249939,#249940,#249941,#249942,#249943,#249944,#249945,
#249946,#249947,#249948,#249949,#249950,#249951,#249952,#249953,#249954,
#249955,#249956,#249957,#249958,#249959,#249960,#249961,#249962,#249963,
#249964,#249965,#249966,#249967,#249968,#249969,#249970,#249971,#249972,
#249973,#249974,#249975,#249976,#249977,#249978,#249979,#249980,#249981,
#249982,#249983,#249984,#249985,#249986,#249987,#249988,#249989,#249990,
#249991,#249992,#249993,#249994,#249995,#249996,#249997,#249998,#249999,
#250000),.UNSPECIFIED.,.F.,.F.,(4,2,2,2,2,2,2,2,2,2,2,2,2,2,2,2,2,2,2,2,
2,2,2,2,2,2,2,2,2,2,2,2,2,2,2,2,2,2,2,2,2,2,2,2,2,2,2,2,2,2,2,2,2,2,2,2,
2,2,2,2,2,2,2,2,2,2,2,2,2,2,2,2,2,2,2,2,2,2,2,2,2,2,2,2,2,2,2,2,2,2,2,2,
2,2,2,2,2,2,2,2,2,4),(-2.03058182286514,-2.03057883788715,-2.02734955910508,
-2.02424962838836,-2.0196817282572,-2.00706295052508,-1.92652991392495,
-1.88424374243307,-1.87409887347353,-1.86810999671337,-1.86277140426693,
-1.85598513505474,-1.84191311198418,-1.82319953202033,-1.77160036950882,
-1.72068441842592,-1.71181442524786,-1.70781394313925,-1.70479849962751,
-1.70136904563078,-1.69527965431392,-1.66382948213334,-1.6219633310418,
-1.56370323797362,-1.55324667243251,-1.54713124246375,-1.54180953841587,
-1.53521509085457,-1.52214110235948,-1.47318239345337,-1.42211194256197,
-1.394745771292,-1.38871553467375,-1.38526368448638,-1.38255540671093,-1.37870262487658,
-1.37052694392871,-1.33642960942612,-1.33479820517616,-1.27242439971672,
-1.2403371997795,-1.23083284168761,-1.22498193714512,-1.21961087693604,
-1.21256048135147,-1.19704038290564,-1.11290404198645,-1.07403761799863,
-1.06760091513295,-1.06405761398891,-1.06106114262109,-1.05716963570628,
-1.04878820037972,-1.01284740879893,-0.92521322875506,-0.912206363931,-0.905539362378852,
-0.900211937743628,-0.894147196728197,-0.883648945741923,-0.825307225790441,
-0.765904447006784,-0.750026394419319,-0.744891955008563,-0.741671477271295,
-0.73856534074901,-0.733966560722513,-0.721120601361326,-0.700427160583973,
-0.65805882884072,-0.599442475378507,-0.58899180375374,-0.582877392065725,
-0.577555115409264,-0.570958069949591,-0.557872491131587,-0.508825287905069,
-0.457565922127511,-0.430458798873896,-0.424441750222474,-0.420992721558942,
-0.418283655092944,-0.41442582696834,-0.406224355672079,-0.371902409167053,
-0.286343269570671,-0.272142474163376,-0.264434349407393,-0.259008946664582,
-0.254013730620893,-0.247231869556841,-0.229823697111821,-0.204727606379191,
-0.157924025102434,-0.113591846603902,-0.10465810026743,-0.10070885090533,
-0.0976999811722273,-0.0942401188870639,-0.0880095632349312,-0.0530658769367188,
-0.000941250914017463),.UNSPECIFIED.);
#3662=B_SPLINE_CURVE_WITH_KNOTS('',3,(#250001,#250002,#250003,#250004),
 .UNSPECIFIED.,.F.,.F.,(4,4),(-4.05981130541024,-4.05954993223484),
 .UNSPECIFIED.);
#3663=B_SPLINE_CURVE_WITH_KNOTS('',3,(#250005,#250006,#250007,#250008,#250009,
#250010,#250011,#250012,#250013,#250014,#250015,#250016,#250017,#250018,
#250019,#250020,#250021,#250022,#250023,#250024,#250025,#250026,#250027,
#250028,#250029,#250030,#250031,#250032,#250033,#250034,#250035,#250036,
#250037,#250038,#250039,#250040,#250041,#250042,#250043,#250044,#250045,
#250046,#250047,#250048,#250049,#250050,#250051,#250052,#250053,#250054,
#250055,#250056,#250057,#250058,#250059,#250060,#250061,#250062,#250063,
#250064,#250065,#250066,#250067,#250068,#250069,#250070,#250071,#250072,
#250073,#250074,#250075,#250076,#250077,#250078,#250079,#250080,#250081,
#250082,#250083,#250084,#250085,#250086,#250087,#250088,#250089,#250090,
#250091,#250092,#250093,#250094,#250095,#250096,#250097,#250098,#250099,
#250100,#250101,#250102,#250103,#250104,#250105,#250106,#250107,#250108,
#250109,#250110,#250111,#250112,#250113,#250114,#250115,#250116,#250117,
#250118,#250119,#250120,#250121,#250122,#250123,#250124,#250125,#250126,
#250127,#250128,#250129,#250130,#250131,#250132,#250133,#250134,#250135,
#250136,#250137,#250138,#250139,#250140,#250141,#250142,#250143,#250144,
#250145,#250146,#250147,#250148,#250149,#250150,#250151,#250152,#250153,
#250154,#250155,#250156,#250157,#250158,#250159,#250160,#250161,#250162,
#250163,#250164,#250165,#250166,#250167,#250168,#250169,#250170,#250171,
#250172,#250173,#250174,#250175,#250176,#250177,#250178,#250179,#250180,
#250181,#250182,#250183,#250184,#250185,#250186,#250187,#250188,#250189,
#250190,#250191,#250192,#250193,#250194,#250195,#250196,#250197,#250198,
#250199,#250200,#250201,#250202,#250203,#250204,#250205,#250206,#250207,
#250208,#250209,#250210,#250211,#250212,#250213,#250214,#250215,#250216,
#250217,#250218,#250219,#250220),.UNSPECIFIED.,.F.,.F.,(4,2,2,2,2,2,2,2,
2,2,2,2,2,2,2,2,2,2,2,2,2,2,2,2,2,2,2,2,2,2,2,2,2,2,2,2,2,2,2,2,2,2,2,2,
2,2,2,2,2,2,2,2,2,2,2,2,2,2,2,2,2,2,2,2,2,2,2,2,2,2,2,2,2,2,2,2,2,2,2,2,
2,2,2,2,2,2,2,2,2,2,2,2,2,2,2,2,2,2,2,2,2,2,2,2,2,2,2,4),(-4.05903826007612,
-4.04597790593254,-4.03596969919603,-4.03061706022468,-4.02538357229182,
-4.01946089423376,-4.0100089105106,-3.97890101285379,-3.91973109898298,
-3.88072795593345,-3.87194922368865,-3.86793467907121,-3.86489657033458,
-3.86130540175457,-3.85485682694083,-3.81891217513851,-3.80373650436185,
-3.7634255595225,-3.73654524591903,-3.71807505689601,-3.71043917246118,
-3.70488197880268,-3.69975617936139,-3.69139158091948,-3.669549036397,-3.59938693653689,
-3.55986933777879,-3.55103751200743,-3.54701315832674,-3.54394641282536,
-3.54034988069102,-3.53387781926496,-3.49704153653491,-3.48258636613612,
-3.43782139527663,-3.41365940731507,-3.39656053812398,-3.38914644784391,
-3.38362569345179,-3.37844401436517,-3.36977686191264,-3.34580905418622,
-3.27763206358795,-3.23880993600112,-3.23004943670116,-3.22603797690813,
-3.22299989564504,-3.21940598813428,-3.21294613441084,-3.17658908037883,
-3.16172415219348,-3.12107990492158,-3.09445994343133,-3.07611756811528,
-3.06850134013622,-3.06294709424354,-3.05712154920507,-3.04812779651883,
-3.02143747181968,-2.9556777918362,-2.91771689366382,-2.90904618163467,
-2.90505108407026,-2.90198670201232,-2.89836930683124,-2.89180440882497,
-2.85050153536521,-2.84026365344427,-2.79751355728265,-2.77241609077581,
-2.7548368125169,-2.74734299397284,-2.74180906074834,-2.73664797669383,
-2.72809347598532,-2.70494362640618,-2.63600083403551,-2.59690735574113,
-2.5881183752321,-2.58410148739711,-2.58106263162405,-2.57747181151553,
-2.57102668232514,-2.53525606673819,-2.51996684847196,-2.47992193149385,
-2.43910914034588,-2.42919496588705,-2.42317208171714,-2.41769231191204,
-2.41068539927334,-2.39604491955083,-2.31833134451679,-2.27240273667403,
-2.26579265937188,-2.26220532119914,-2.25913641303872,-2.2551640576646,
-2.24638662646662,-2.18847539947846,-2.14205726266983,-2.12433071740527,
-2.11077447323354,-2.10399815802401,-2.09860448757189,-2.09239161765776,
-2.08187029123698,-2.03033138896571),.UNSPECIFIED.);
#3664=B_SPLINE_CURVE_WITH_KNOTS('',3,(#250226,#250227,#250228,#250229),
 .UNSPECIFIED.,.F.,.F.,(4,4),(-0.00120239128176678,-0.000939850288917991),
 .UNSPECIFIED.);
#3665=B_SPLINE_CURVE_WITH_KNOTS('',3,(#250230,#250231,#250232,#250233,#250234,
#250235,#250236,#250237,#250238,#250239,#250240,#250241,#250242,#250243,
#250244,#250245,#250246,#250247,#250248,#250249,#250250,#250251,#250252,
#250253,#250254,#250255,#250256,#250257,#250258,#250259,#250260,#250261,
#250262,#250263,#250264,#250265,#250266,#250267,#250268,#250269,#250270,
#250271,#250272,#250273,#250274,#250275,#250276,#250277,#250278,#250279,
#250280,#250281,#250282,#250283,#250284,#250285,#250286,#250287,#250288,
#250289,#250290,#250291,#250292,#250293,#250294,#250295,#250296,#250297,
#250298,#250299,#250300,#250301,#250302,#250303,#250304,#250305,#250306,
#250307,#250308,#250309,#250310,#250311,#250312,#250313,#250314,#250315,
#250316,#250317,#250318,#250319,#250320,#250321,#250322,#250323,#250324,
#250325,#250326,#250327,#250328,#250329,#250330,#250331,#250332,#250333,
#250334,#250335,#250336,#250337,#250338,#250339,#250340,#250341,#250342,
#250343,#250344,#250345,#250346,#250347,#250348,#250349,#250350,#250351,
#250352,#250353,#250354,#250355,#250356,#250357,#250358,#250359,#250360,
#250361,#250362,#250363,#250364,#250365,#250366,#250367,#250368,#250369,
#250370,#250371,#250372,#250373,#250374,#250375,#250376,#250377,#250378,
#250379,#250380,#250381,#250382,#250383,#250384,#250385,#250386,#250387,
#250388,#250389,#250390,#250391,#250392,#250393,#250394,#250395,#250396,
#250397,#250398,#250399,#250400,#250401,#250402,#250403,#250404,#250405,
#250406,#250407,#250408,#250409,#250410,#250411,#250412,#250413,#250414,
#250415,#250416,#250417,#250418,#250419,#250420,#250421,#250422,#250423,
#250424,#250425,#250426,#250427,#250428,#250429,#250430,#250431,#250432,
#250433,#250434,#250435,#250436,#250437),.UNSPECIFIED.,.F.,.F.,(4,2,2,2,
2,2,2,2,2,2,2,2,2,2,2,2,2,2,2,2,2,2,2,2,2,2,2,2,2,2,2,2,2,2,2,2,2,2,2,2,
2,2,2,2,2,2,2,2,2,2,2,2,2,2,2,2,2,2,2,2,2,2,2,2,2,2,2,2,2,2,2,2,2,2,2,2,
2,2,2,2,2,2,2,2,2,2,2,2,2,2,2,2,2,2,2,2,2,2,2,2,2,2,2,4),(-4.05986983129597,
-3.99181327440633,-3.97381836660338,-3.9621811725854,-3.95775289382385,
-3.95468043230858,-3.95140805248172,-3.9460346986115,-3.92799029834988,
-3.90940947514947,-3.89329789548272,-3.84212150885882,-3.82101482597013,
-3.80571472003521,-3.79927328357972,-3.79910183904098,-3.79892374102063,
-3.79352547522316,-3.78845576058314,-3.77997325987689,-3.75655264393949,
-3.68044103212314,-3.64742986514537,-3.63937985161934,-3.63555127889657,
-3.63284623469308,-3.62937920582057,-3.62328033491758,-3.59452732199759,
-3.53308176206738,-3.49057192432417,-3.48069218534804,-3.47476107857106,
-3.46941223143004,-3.46252696897282,-3.45130358759924,-3.37257162566693,
-3.32622125425776,-3.31807599117137,-3.31422925167252,-3.31152201093935,
-3.30806695226786,-3.30202139916676,-3.27434008220855,-3.22354124241745,
-3.17471672227241,-3.16165999075327,-3.15506943292488,-3.14974858276697,
-3.14363161622601,-3.13316619249863,-3.07580251468088,-3.03392111546468,
-3.0120986782409,-2.99877292745343,-2.99411114289614,-2.99099266179133,
-2.98817604992191,-2.98424765940126,-2.97611561910698,-2.92556713508906,
-2.87379319925098,-2.85504803476284,-2.84095720685412,-2.83416797320819,
-2.82882968284655,-2.82284389100876,-2.81271106153646,-2.77061734359409,
-2.68992108935853,-2.68127722570045,-2.67456505107889,-2.67100327749087,
-2.66800916930287,-2.66414387156366,-2.65590116776557,-2.59063071069953,
-2.53678030992871,-2.52058908646574,-2.5134221389193,-2.50803443852083,
-2.50223462437102,-2.49296674228541,-2.46271973351095,-2.39976947629276,
-2.36273551909781,-2.35423669176454,-2.35032377485134,-2.34732585853618,
-2.34379856546825,-2.33743258685057,-2.30141371420175,-2.28598536984817,
-2.24462880482309,-2.20488724970749,-2.19517231321176,-2.18927608202312,
-2.18391776994754,-2.17707776635535,-2.16575725333272,-2.08787415652705,
-2.0536225374624,-2.03575359151365,-2.03058182286514),.UNSPECIFIED.);
#3666=B_SPLINE_CURVE_WITH_KNOTS('',3,(#250439,#250440,#250441,#250442,#250443,
#250444,#250445,#250446,#250447,#250448,#250449,#250450,#250451,#250452,
#250453,#250454,#250455,#250456,#250457,#250458,#250459,#250460,#250461,
#250462,#250463,#250464,#250465,#250466,#250467,#250468,#250469,#250470,
#250471,#250472,#250473,#250474,#250475,#250476,#250477,#250478,#250479,
#250480,#250481,#250482,#250483,#250484,#250485,#250486,#250487,#250488,
#250489,#250490,#250491,#250492,#250493,#250494,#250495,#250496,#250497,
#250498,#250499,#250500,#250501,#250502,#250503,#250504,#250505,#250506,
#250507,#250508,#250509,#250510,#250511,#250512,#250513,#250514,#250515,
#250516,#250517,#250518,#250519,#250520,#250521,#250522,#250523,#250524,
#250525,#250526,#250527,#250528,#250529,#250530,#250531,#250532,#250533,
#250534,#250535,#250536,#250537,#250538,#250539,#250540,#250541,#250542,
#250543,#250544,#250545,#250546,#250547,#250548,#250549,#250550,#250551,
#250552,#250553,#250554,#250555,#250556,#250557,#250558,#250559,#250560,
#250561,#250562,#250563,#250564,#250565,#250566,#250567,#250568,#250569,
#250570,#250571,#250572,#250573,#250574,#250575,#250576,#250577,#250578,
#250579,#250580,#250581,#250582,#250583,#250584,#250585,#250586,#250587,
#250588,#250589,#250590,#250591,#250592,#250593,#250594,#250595,#250596,
#250597,#250598,#250599,#250600,#250601,#250602,#250603,#250604,#250605,
#250606,#250607,#250608,#250609,#250610,#250611,#250612,#250613,#250614,
#250615,#250616,#250617,#250618,#250619,#250620,#250621,#250622,#250623,
#250624,#250625,#250626,#250627,#250628,#250629,#250630,#250631,#250632,
#250633,#250634,#250635,#250636,#250637,#250638,#250639,#250640,#250641,
#250642,#250643,#250644,#250645,#250646),.UNSPECIFIED.,.F.,.F.,(4,2,2,2,
2,2,2,2,2,2,2,2,2,2,2,2,2,2,2,2,2,2,2,2,2,2,2,2,2,2,2,2,2,2,2,2,2,2,2,2,
2,2,2,2,2,2,2,2,2,2,2,2,2,2,2,2,2,2,2,2,2,2,2,2,2,2,2,2,2,2,2,2,2,2,2,2,
2,2,2,2,2,2,2,2,2,2,2,2,2,2,2,2,2,2,2,2,2,2,2,2,2,2,2,4),(-2.03033138896571,
-2.03004475095578,-1.95484454428,-1.94601038089878,-1.94202760776874,-1.93895741764169,
-1.93537663409036,-1.92879841290792,-1.8846143032805,-1.81171614604089,
-1.79268949781134,-1.78476170987519,-1.77920647951301,-1.77347948396448,
-1.7649627804795,-1.74009358124814,-1.69826083666401,-1.63289842784909,
-1.62462343667328,-1.62070171262031,-1.61764202451515,-1.61396800297792,
-1.60694417349348,-1.59782753623496,-1.57595030953848,-1.53429232050904,
-1.47734666840118,-1.46674781319756,-1.46051730470633,-1.45512524866261,
-1.44837297732227,-1.43494172115453,-1.38398918534725,-1.32872975590806,
-1.30759407527396,-1.30185565666621,-1.29845641745498,-1.29533686327393,
-1.29093303090463,-1.27984412963497,-1.26311514491643,-1.19874296522546,
-1.15554767863535,-1.1452146479462,-1.13910101718287,-1.13364007682602,
-1.12667987756694,-1.11215982968773,-1.09275832860198,-1.03788722598818,
-1.02758849370523,-0.988098826979995,-0.981560793837528,-0.977948841660985,
-0.974882904176124,-0.970877810412923,-0.962155910267061,-0.923719655786981,
-0.856625978313642,-0.831482876241476,-0.822660986141599,-0.816870578928996,
-0.811293956695655,-0.803556039818518,-0.784438908085983,-0.75622722174661,
-0.695409069765793,-0.666413251311307,-0.660218404506081,-0.656683408920067,
-0.653913933282333,-0.649971841764152,-0.641589488048009,-0.606302982244557,
-0.544006199202803,-0.512038662238862,-0.502420107102914,-0.496460052925732,
-0.490960389662207,-0.483695906419145,-0.467485579927382,-0.416390175078096,
-0.353805927807226,-0.342090273559588,-0.337461308658229,-0.334331800474152,
-0.331021305907723,-0.325687262211454,-0.30689904523175,-0.269892876830737,
-0.197168796855664,-0.18530800974726,-0.178235859933491,-0.172746236021974,
-0.166754120374895,-0.156986342178952,-0.118456738247924,-0.0392440781129341,
-0.0223793449285437,-0.0170639986491465,-0.013757500959231,-0.0108711009658924,
-0.00772048351218813,-0.000937009717170368),.UNSPECIFIED.);
#3667=B_SPLINE_CURVE_WITH_KNOTS('',3,(#250647,#250648,#250649,#250650),
 .UNSPECIFIED.,.F.,.F.,(4,4),(-4.06006436020849,-4.05997090679314),
 .UNSPECIFIED.);
#3668=B_SPLINE_CURVE_WITH_KNOTS('',3,(#250655,#250656,#250657,#250658,#250659,
#250660,#250661,#250662,#250663,#250664,#250665,#250666,#250667,#250668,
#250669,#250670,#250671,#250672,#250673,#250674,#250675,#250676,#250677,
#250678,#250679,#250680,#250681,#250682,#250683,#250684,#250685,#250686,
#250687,#250688,#250689,#250690,#250691,#250692,#250693,#250694,#250695,
#250696,#250697,#250698,#250699,#250700,#250701,#250702,#250703,#250704,
#250705,#250706,#250707,#250708,#250709,#250710,#250711,#250712,#250713,
#250714,#250715,#250716,#250717,#250718,#250719,#250720,#250721,#250722,
#250723,#250724,#250725,#250726,#250727,#250728,#250729,#250730,#250731,
#250732,#250733,#250734,#250735,#250736,#250737,#250738,#250739,#250740,
#250741,#250742,#250743,#250744,#250745,#250746,#250747,#250748,#250749,
#250750,#250751,#250752,#250753,#250754,#250755,#250756,#250757,#250758,
#250759,#250760,#250761,#250762,#250763,#250764,#250765,#250766,#250767,
#250768,#250769,#250770,#250771,#250772,#250773,#250774,#250775,#250776,
#250777,#250778,#250779,#250780,#250781,#250782,#250783,#250784,#250785,
#250786,#250787,#250788,#250789,#250790,#250791,#250792,#250793,#250794,
#250795,#250796,#250797,#250798,#250799,#250800,#250801,#250802,#250803,
#250804,#250805,#250806,#250807,#250808,#250809,#250810,#250811,#250812,
#250813,#250814,#250815,#250816,#250817,#250818,#250819,#250820,#250821,
#250822,#250823,#250824,#250825,#250826,#250827,#250828,#250829,#250830,
#250831,#250832,#250833,#250834,#250835,#250836,#250837,#250838,#250839,
#250840,#250841,#250842,#250843,#250844,#250845,#250846,#250847,#250848,
#250849,#250850,#250851,#250852,#250853,#250854),.UNSPECIFIED.,.F.,.F.,
(4,2,2,2,2,2,2,2,2,2,2,2,2,2,2,2,2,2,2,2,2,2,2,2,2,2,2,2,2,2,2,2,2,2,2,
2,2,2,2,2,2,2,2,2,2,2,2,2,2,2,2,2,2,2,2,2,2,2,2,2,2,2,2,2,2,2,2,2,2,2,2,
2,2,2,2,2,2,2,2,2,2,2,2,2,2,2,2,2,2,2,2,2,2,2,2,2,2,2,2,4),(-2.03106147693124,
-2.00135992172458,-1.99213232428103,-1.98634111809768,-1.98095012196117,
-1.97376177043868,-1.95744594529994,-1.9021958880149,-1.83867193668762,
-1.83027464040683,-1.82642168933958,-1.82342321020104,-1.81989931713118,
-1.81336799840513,-1.76637047091445,-1.68518531261994,-1.67425504855372,
-1.6674548948778,-1.66211510973925,-1.65613502393256,-1.64603002272997,
-1.59914584237983,-1.54056139226403,-1.51350426281483,-1.50749041072096,
-1.50404236158618,-1.50133352220733,-1.49747530862163,-1.48927028776032,
-1.45491224318001,-1.3937104958698,-1.35937728697544,-1.34974719630998,
-1.3438693372301,-1.3385063130127,-1.33151387965844,-1.31631860837556,-1.23166592646812,
-1.192835566198,-1.18639987277859,-1.18285687532182,-1.17986049743235,-1.17596890052114,
-1.16758650831909,-1.13163542957096,-1.04402649750223,-1.03101499033604,
-1.02434717787059,-1.01901986369826,-1.01295606600793,-1.00246155857587,
-0.944265486605784,-0.885123604310577,-0.868916151471909,-0.863743230656771,
-0.860514390684492,-0.857414254977698,-0.852845128538774,-0.840217016180446,
-0.75966812682607,-0.717409466946983,-0.707266345854092,-0.701277911584229,
-0.695939353344808,-0.689152635575111,-0.675077842874266,-0.656359318764803,
-0.604733883981113,-0.553860813128715,-0.544987711052228,-0.540986689889558,
-0.537971217104552,-0.534542170901426,-0.528454495061337,-0.497040858222865,
-0.455148512029609,-0.396740512103912,-0.38635845080893,-0.380259808636969,
-0.37493653904309,-0.368319119861507,-0.355127391117024,-0.305216354839862,
-0.252123495642277,-0.227608386494145,-0.221680648527473,-0.218286264343582,
-0.215261657679254,-0.211123763955944,-0.201344435291602,-0.187173611779952,
-0.128413363064338,-0.0891715966497953,-0.0700127803815348,-0.0621605980149476,
-0.0567084908522559,-0.0517050497910303,-0.0462407742051427,-0.0387693217578128,
-0.00120239128176678),.UNSPECIFIED.);
#3669=B_SPLINE_CURVE_WITH_KNOTS('',3,(#250855,#250856,#250857,#250858,#250859,
#250860,#250861,#250862,#250863,#250864,#250865,#250866,#250867,#250868,
#250869,#250870,#250871,#250872,#250873,#250874,#250875,#250876,#250877,
#250878,#250879,#250880,#250881,#250882,#250883,#250884,#250885,#250886,
#250887,#250888,#250889,#250890,#250891,#250892,#250893,#250894,#250895,
#250896,#250897,#250898,#250899,#250900,#250901,#250902,#250903,#250904,
#250905,#250906,#250907,#250908,#250909,#250910,#250911,#250912,#250913,
#250914,#250915,#250916,#250917,#250918,#250919,#250920,#250921,#250922,
#250923,#250924,#250925,#250926,#250927,#250928,#250929,#250930,#250931,
#250932,#250933,#250934,#250935,#250936,#250937,#250938,#250939,#250940,
#250941,#250942,#250943,#250944,#250945,#250946,#250947,#250948,#250949,
#250950,#250951,#250952,#250953,#250954,#250955,#250956,#250957,#250958,
#250959,#250960,#250961,#250962,#250963,#250964,#250965,#250966,#250967,
#250968,#250969,#250970,#250971,#250972,#250973,#250974,#250975,#250976,
#250977,#250978,#250979,#250980,#250981,#250982,#250983,#250984,#250985,
#250986,#250987,#250988,#250989,#250990,#250991,#250992,#250993,#250994,
#250995,#250996,#250997,#250998,#250999,#251000,#251001,#251002,#251003,
#251004,#251005,#251006,#251007,#251008,#251009,#251010,#251011,#251012,
#251013,#251014,#251015,#251016,#251017,#251018,#251019,#251020,#251021,
#251022,#251023,#251024,#251025,#251026,#251027,#251028,#251029,#251030,
#251031,#251032,#251033,#251034,#251035,#251036,#251037,#251038,#251039,
#251040,#251041,#251042,#251043,#251044,#251045,#251046,#251047,#251048,
#251049,#251050,#251051,#251052,#251053,#251054,#251055,#251056,#251057,
#251058,#251059,#251060,#251061,#251062,#251063,#251064,#251065,#251066,
#251067,#251068,#251069,#251070,#251071,#251072,#251073,#251074,#251075,
#251076,#251077,#251078,#251079,#251080,#251081,#251082,#251083,#251084,
#251085,#251086,#251087,#251088,#251089,#251090),.UNSPECIFIED.,.F.,.F.,
(4,2,2,2,2,2,2,2,2,2,2,2,2,2,2,2,2,2,2,2,2,2,2,2,2,2,2,2,2,2,2,2,2,2,2,
2,2,2,2,2,2,2,2,2,2,2,2,2,2,2,2,2,2,2,2,2,2,2,2,2,2,2,2,2,2,2,2,2,2,2,2,
2,2,2,2,2,2,2,2,2,2,2,2,2,2,2,2,2,2,2,2,2,2,2,2,2,2,2,2,2,2,2,2,2,2,2,2,
2,2,2,2,2,2,2,2,2,2,4),(-4.05997090679314,-4.01824280524362,-3.98687820213071,
-3.93567680536283,-3.92221607379754,-3.91545857828971,-3.9100667041386,
-3.90384125480551,-3.89326288243562,-3.83379071636708,-3.79039717101627,
-3.77117286398523,-3.7628048578411,-3.75806037807277,-3.75403284670643,
-3.75399524448692,-3.75395761696416,-3.75391995276596,-3.75388224034229,
-3.75384446795469,-3.75380662366009,-3.75378647922505,-3.75376589425216,
-3.75374484599186,-3.7537233102051,-3.75370126101515,-3.75367867075903,
-3.75365550983221,-3.75363174651384,-3.7536073467604,-3.7535822739617,-3.75059286505521,
-3.7470433830799,-3.74078279001646,-3.71079648955641,-3.65141336595605,
-3.62306408252607,-3.60388024650983,-3.59613295659654,-3.59055530968897,
-3.58476885748337,-3.57596298369627,-3.55094764193656,-3.48371062514029,
-3.44521975611649,-3.43649296022556,-3.43248729823112,-3.42942170645355,
-3.42581103830104,-3.41927747384724,-3.37994071568165,-3.33766468344431,
-3.29242302373853,-3.27971694565728,-3.27310866655302,-3.2682024023488,
-3.26203632357425,-3.25145635106178,-3.20282122787205,-3.12413374002489,
-3.11541562818334,-3.11141132827631,-3.1083455959236,-3.10473336208792,
-3.09819368643935,-3.05858209371425,-3.04847588473183,-3.01012868331876,
-2.98129042974709,-2.96187292823813,-2.95408952134713,-2.94850478413205,
-2.9427274692977,-2.93396807540726,-2.90932289779428,-2.84173855942869,
-2.80312206711941,-2.79438150030537,-2.79037296617171,-2.78730672768343,
-2.78369713235045,-2.77716979624726,-2.73816263352102,-2.72570333766245,
-2.68378172487325,-2.65809912475973,-2.64022262190217,-2.6326793675314,
-2.62713618021893,-2.62128392945349,-2.61216965207654,-2.58437009485361,
-2.50441818312249,-2.486278178061,-2.47452505500896,-2.4700206488298,-2.46688314408606,
-2.46352171999791,-2.45795646743631,-2.43872975858396,-2.3821312035586,
-2.33046750641607,-2.3169495053076,-2.3101798968261,-2.30478592652532,-2.29856646011958,
-2.28801874964022,-2.23447937724356,-2.19680162310392,-2.15729804585081,
-2.15082868883574,-2.14727082617008,-2.14419638797228,-2.14017778601563,
-2.1311439958556,-2.08103734388464,-2.03096923846931,-2.03076530206895),
 .UNSPECIFIED.);
#3670=B_SPLINE_CURVE_WITH_KNOTS('',3,(#251095,#251096,#251097,#251098,#251099,
#251100,#251101,#251102,#251103,#251104,#251105,#251106,#251107,#251108,
#251109,#251110,#251111,#251112,#251113,#251114,#251115,#251116,#251117,
#251118,#251119,#251120,#251121,#251122,#251123,#251124,#251125,#251126,
#251127,#251128,#251129,#251130,#251131,#251132,#251133,#251134,#251135,
#251136,#251137,#251138,#251139,#251140,#251141,#251142,#251143,#251144,
#251145,#251146,#251147,#251148,#251149,#251150,#251151,#251152,#251153,
#251154,#251155,#251156,#251157,#251158,#251159,#251160,#251161,#251162,
#251163,#251164,#251165,#251166,#251167,#251168,#251169,#251170,#251171,
#251172,#251173,#251174,#251175,#251176,#251177,#251178,#251179,#251180,
#251181,#251182,#251183,#251184,#251185,#251186,#251187,#251188,#251189,
#251190,#251191,#251192,#251193,#251194,#251195,#251196,#251197,#251198,
#251199,#251200,#251201,#251202,#251203,#251204,#251205,#251206,#251207,
#251208,#251209,#251210,#251211,#251212,#251213,#251214,#251215,#251216,
#251217,#251218,#251219,#251220,#251221,#251222,#251223,#251224,#251225,
#251226,#251227,#251228,#251229,#251230,#251231,#251232,#251233,#251234,
#251235,#251236,#251237,#251238,#251239,#251240,#251241,#251242,#251243,
#251244,#251245,#251246,#251247,#251248,#251249,#251250,#251251,#251252,
#251253,#251254,#251255,#251256,#251257,#251258,#251259,#251260,#251261,
#251262,#251263,#251264,#251265,#251266,#251267,#251268,#251269,#251270,
#251271,#251272,#251273,#251274,#251275,#251276,#251277,#251278,#251279,
#251280,#251281,#251282,#251283,#251284,#251285,#251286,#251287,#251288,
#251289,#251290,#251291,#251292,#251293,#251294,#251295,#251296,#251297,
#251298,#251299,#251300,#251301,#251302,#251303,#251304,#251305,#251306,
#251307,#251308,#251309,#251310,#251311,#251312,#251313,#251314,#251315,
#251316,#251317,#251318,#251319,#251320,#251321,#251322,#251323,#251324,
#251325,#251326,#251327,#251328,#251329,#251330,#251331,#251332,#251333,
#251334,#251335,#251336,#251337,#251338,#251339,#251340),.UNSPECIFIED.,
 .F.,.F.,(4,2,2,2,2,2,2,2,2,2,2,2,2,2,2,2,2,2,2,2,2,2,2,2,2,2,2,2,2,2,2,
2,2,2,2,2,2,2,2,2,2,2,2,2,2,2,2,2,2,2,2,2,2,2,2,2,2,2,2,2,2,2,2,2,2,2,2,
2,2,2,2,2,2,2,2,2,2,2,2,2,2,2,2,2,2,2,2,2,2,2,2,2,2,2,2,2,2,2,2,2,2,2,2,
2,2,2,2,2,2,2,2,2,2,2,2,2,2,2,2,2,2,2,4),(-4.06053628618758,-4.02160247291763,
-3.99254683092489,-3.94078145176954,-3.92468553480843,-3.91753559308151,
-3.91215105573062,-3.90634545210276,-3.89704809315843,-3.86653684379152,
-3.78910608080314,-3.77122073374161,-3.76329128620407,-3.7587466357091,
-3.75487015269569,-3.75483572564846,-3.75480121917029,-3.75476662258901,
-3.75473192502075,-3.754697115353,-3.75466218222167,-3.75462711399698,-3.75459189877042,
-3.75455652431483,-3.75452097807844,-3.75448524716045,-3.75444931828298,
-3.75441317776608,-3.75437681150701,-3.75435519816047,-3.75433274655183,
-3.75430940496138,-3.75428511718236,-3.75425982198671,-3.75423345255093,
-3.75420593578835,-3.75417719158038,-3.75294776784094,-3.7500168695276,
-3.74634417547087,-3.73758276643462,-3.69013558696533,-3.64883285407783,
-3.62241490918712,-3.60424142541614,-3.59674922343819,-3.59130860400187,
-3.585625339043,-3.57690335952019,-3.55163669929627,-3.4843768107486,-3.44225958124779,
-3.43581928664967,-3.43231475839618,-3.42931372430127,-3.42543356403228,
-3.41719368116728,-3.35301731613637,-3.29682186137098,-3.2815835430287,
-3.27458350148761,-3.26921953700484,-3.26334549319698,-3.25373284769265,
-3.21965731681177,-3.15825003951293,-3.12348786216106,-3.11544659629313,
-3.11161938113049,-3.10891418459862,-3.10544540928693,-3.09934004856297,
-3.07046652620577,-3.02050594871814,-2.96749872286672,-2.95715219177907,
-2.95112017528144,-2.94578873786866,-2.93907299711668,-2.92582818514412,
-2.858612474182,-2.81746821286857,-2.8041025137039,-2.79474045861759,-2.79067357942079,
-2.78765876631303,-2.78422713260338,-2.77828561980348,-2.75242075918696,
-2.70032330346211,-2.65089668712429,-2.63776444477846,-2.63115872055616,
-2.62583636273981,-2.61972945265415,-2.60931038224313,-2.55538901087016,
-2.51760177539952,-2.48137900891173,-2.47296769060748,-2.46907098140614,
-2.46607449701136,-2.46253587019646,-2.45611883001515,-2.41804728966191,
-2.37429494020325,-2.33316458200083,-2.3177041657883,-2.31066454265426,
-2.30529515955346,-2.29943967706842,-2.28991335248799,-2.25711112030618,
-2.19502710042522,-2.15988190638871,-2.15158886887443,-2.14771411582957,
-2.14471929685586,-2.14116451478505,-2.134674937849,-2.09148426352191,-2.03126909524015,
-2.03106147693124),.UNSPECIFIED.);
#3671=B_SPLINE_CURVE_WITH_KNOTS('',3,(#251341,#251342,#251343,#251344,#251345,
#251346,#251347,#251348,#251349,#251350,#251351,#251352,#251353,#251354,
#251355,#251356,#251357,#251358,#251359,#251360,#251361,#251362,#251363,
#251364,#251365,#251366,#251367,#251368,#251369,#251370,#251371,#251372,
#251373,#251374,#251375,#251376,#251377,#251378,#251379,#251380,#251381,
#251382,#251383,#251384,#251385,#251386,#251387,#251388,#251389,#251390,
#251391,#251392,#251393,#251394,#251395,#251396,#251397,#251398,#251399,
#251400,#251401,#251402,#251403,#251404,#251405,#251406,#251407,#251408,
#251409,#251410,#251411,#251412,#251413,#251414,#251415,#251416,#251417,
#251418,#251419,#251420,#251421,#251422,#251423,#251424,#251425,#251426,
#251427,#251428,#251429,#251430,#251431,#251432,#251433,#251434,#251435,
#251436,#251437,#251438,#251439,#251440,#251441,#251442,#251443,#251444,
#251445,#251446,#251447,#251448,#251449,#251450,#251451,#251452,#251453,
#251454,#251455,#251456,#251457,#251458,#251459,#251460,#251461,#251462,
#251463,#251464,#251465,#251466,#251467,#251468,#251469,#251470,#251471,
#251472,#251473,#251474,#251475,#251476,#251477,#251478,#251479,#251480,
#251481,#251482,#251483,#251484,#251485,#251486,#251487,#251488,#251489,
#251490,#251491,#251492,#251493,#251494,#251495,#251496,#251497,#251498,
#251499,#251500,#251501,#251502,#251503,#251504,#251505,#251506,#251507,
#251508,#251509,#251510,#251511,#251512,#251513,#251514,#251515,#251516,
#251517,#251518,#251519,#251520,#251521,#251522,#251523,#251524,#251525,
#251526,#251527,#251528,#251529,#251530,#251531,#251532,#251533,#251534,
#251535,#251536,#251537,#251538,#251539,#251540,#251541,#251542,#251543,
#251544,#251545,#251546,#251547,#251548,#251549,#251550,#251551,#251552,
#251553,#251554),.UNSPECIFIED.,.F.,.F.,(4,2,2,2,2,2,2,2,2,2,2,2,2,2,2,2,
2,2,2,2,2,2,2,2,2,2,2,2,2,2,2,2,2,2,2,2,2,2,2,2,2,2,2,2,2,2,2,2,2,2,2,2,
2,2,2,2,2,2,2,2,2,2,2,2,2,2,2,2,2,2,2,2,2,2,2,2,2,2,2,2,2,2,2,2,2,2,2,2,
2,2,2,2,2,2,2,2,2,2,2,2,2,2,2,2,2,2,4),(-2.03076530206895,-2.00184929588146,
-1.99258929123149,-1.98670572754556,-1.98117633945776,-1.97371943523126,
-1.95637448636026,-1.87331725589928,-1.83628719771598,-1.82980668022375,
-1.82620712525286,-1.82313888050872,-1.81911402297132,-1.81028647188528,
-1.77083697219452,-1.70087529691708,-1.67881462779443,-1.67041501911654,
-1.66528090856498,-1.65972482221062,-1.65210891533437,-1.63378221316232,
-1.60719539209839,-1.56650157569052,-1.55188859119328,-1.51515420245962,
-1.50868151336268,-1.5050837720035,-1.50201538732481,-1.49798814456081,
-1.48914706762221,-1.44956375975893,-1.37921568115567,-1.35756336950096,
-1.34922455609283,-1.34410157751239,-1.33853730561561,-1.33087318092118,
-1.31223862523505,-1.28502532630068,-1.24507245639649,-1.22970943597816,
-1.19399821820182,-1.18755220669189,-1.18396049483954,-1.18092058176281,
-1.1769019610738,-1.16810778724459,-1.12898041849121,-1.05993755001622,
-1.03690774624279,-1.02836846217224,-1.02320898308664,-1.01767101111008,
-1.01016152930244,-0.992496209942183,-0.967229510164724,-0.92459077779838,
-0.912442463860844,-0.873056484973561,-0.866519986760633,-0.862908153379994,
-0.859841837981553,-0.855835627967705,-0.84710899334885,-0.808632034232486,
-0.741428228832295,-0.716398485270796,-0.70758956561908,-0.701801466671953,
-0.696222485495031,-0.688473767196113,-0.669289100914378,-0.640937633221003,
-0.58120570412414,-0.551414956244729,-0.54517950726272,-0.541635124093891,
-0.538866951905071,-0.53493798638522,-0.526626545469866,-0.491976675198403,
-0.430338647544821,-0.397089734202491,-0.38740132175486,-0.381425856999087,
-0.375930390633862,-0.368698565405506,-0.352678299055561,-0.307504527255256,
-0.255236804070178,-0.229874200022828,-0.223812117060306,-0.220341881036696,
-0.217246816139825,-0.21299982827083,-0.202892974719206,-0.188158233440947,
-0.134975612643627,-0.0937919592940926,-0.0729182784888145,-0.0646976557608329,
-0.0595958187794864,-0.0540138417708553,-0.0484812902795008,-0.0409878253526347,
-0.00120365178948661),.UNSPECIFIED.);
#3672=B_SPLINE_CURVE_WITH_KNOTS('',3,(#251560,#251561,#251562,#251563,#251564,
#251565,#251566,#251567,#251568,#251569,#251570,#251571,#251572,#251573,
#251574,#251575,#251576,#251577,#251578,#251579,#251580,#251581,#251582,
#251583,#251584,#251585,#251586,#251587,#251588,#251589,#251590,#251591,
#251592,#251593,#251594,#251595,#251596,#251597,#251598,#251599,#251600,
#251601,#251602,#251603,#251604,#251605,#251606,#251607,#251608,#251609,
#251610,#251611,#251612,#251613,#251614,#251615,#251616,#251617,#251618,
#251619,#251620,#251621,#251622,#251623,#251624,#251625,#251626,#251627,
#251628,#251629,#251630,#251631,#251632,#251633,#251634,#251635,#251636,
#251637,#251638,#251639,#251640,#251641,#251642,#251643,#251644,#251645,
#251646,#251647,#251648,#251649,#251650,#251651,#251652,#251653,#251654,
#251655,#251656,#251657,#251658,#251659,#251660,#251661,#251662,#251663,
#251664,#251665,#251666,#251667,#251668,#251669,#251670,#251671,#251672,
#251673,#251674,#251675,#251676,#251677,#251678,#251679,#251680,#251681,
#251682,#251683,#251684,#251685,#251686,#251687,#251688,#251689,#251690,
#251691,#251692,#251693,#251694,#251695,#251696,#251697,#251698,#251699,
#251700,#251701,#251702,#251703,#251704,#251705,#251706,#251707,#251708,
#251709,#251710,#251711,#251712,#251713,#251714,#251715,#251716,#251717,
#251718,#251719,#251720,#251721,#251722,#251723,#251724,#251725,#251726,
#251727,#251728,#251729,#251730,#251731,#251732,#251733,#251734,#251735,
#251736,#251737,#251738,#251739,#251740,#251741,#251742,#251743,#251744,
#251745,#251746,#251747,#251748,#251749,#251750,#251751,#251752,#251753,
#251754,#251755,#251756,#251757,#251758,#251759,#251760,#251761,#251762,
#251763,#251764,#251765,#251766,#251767,#251768,#251769,#251770,#251771),
 .UNSPECIFIED.,.F.,.F.,(4,2,2,2,2,2,2,2,2,2,2,2,2,2,2,2,2,2,2,2,2,2,2,2,
2,2,2,2,2,2,2,2,2,2,2,2,2,2,2,2,2,2,2,2,2,2,2,2,2,2,2,2,2,2,2,2,2,2,2,2,
2,2,2,2,2,2,2,2,2,2,2,2,2,2,2,2,2,2,2,2,2,2,2,2,2,2,2,2,2,2,2,2,2,2,2,2,
2,2,2,2,2,2,2,2,2,4),(-2.03033861750309,-2.03004890790123,-1.97725081667204,
-1.95233290066491,-1.94638146170912,-1.94298227338569,-1.93995968753833,
-1.93583311881427,-1.92611879437715,-1.91207401587518,-1.86700227208894,
-1.80523064461586,-1.79167148688881,-1.78498347339538,-1.77965514151353,
-1.77360641467977,-1.76317965540511,-1.70755274188579,-1.65276286404174,
-1.63066459086127,-1.62490887902268,-1.62155231165956,-1.61851625743412,
-1.61430025160995,-1.60404417042071,-1.58892856999398,-1.53692741944389,
-1.47892155205336,-1.46846374162645,-1.46234850852207,-1.45702753090137,
-1.45043470166669,-1.43736636858799,-1.38844594465325,-1.33745235432084,
-1.30999013023625,-1.30395549116173,-1.30050290674528,-1.29779518352488,
-1.29394466635748,-1.28577944189796,-1.25176934640795,-1.25037174513555,
-1.18830152261266,-1.15561157943863,-1.14609847045106,-1.14024615927711,
-1.13487642244268,-1.12783158130633,-1.11233983627481,-1.04825006012616,
-0.993049229854669,-0.98419737340668,-0.9802627974761,-0.977255923398685,
-0.97378746893247,-0.967515912823084,-0.931390358403826,-0.871366329964801,
-0.834827211812955,-0.825025294135688,-0.819110637173888,-0.813757444881677,
-0.806839532021044,-0.792054850474799,-0.772079883573775,-0.713470265297573,
-0.668144925532808,-0.661649560864759,-0.658093619007614,-0.655099081845828,
-0.651226357692079,-0.642943488258302,-0.607889369135181,-0.545973991822587,
-0.512998893886362,-0.503459139491535,-0.497600916532352,-0.492232620730419,
-0.485199668798438,-0.46977612463057,-0.402480440426757,-0.350486227358892,
-0.341558546899066,-0.337610477554837,-0.334601871076583,-0.331141559895353,
-0.324908444431098,-0.317048802723645,-0.299397739084804,-0.224787816605238,
-0.19164212908942,-0.182086975423961,-0.176225481514923,-0.170858231737986,
-0.163832526640007,-0.148449489014628,-0.103627271110006,-0.0398122519758747,
-0.0229961981578295,-0.0177548958133785,-0.0145111855666649,-0.0116827105219521,
-0.00861350243500196,-0.00485913010226856,-0.000939989750838741),
 .UNSPECIFIED.);
#3673=B_SPLINE_CURVE_WITH_KNOTS('',3,(#251772,#251773,#251774,#251775),
 .UNSPECIFIED.,.F.,.F.,(4,4),(-4.06063413645091,-4.06053628618758),
 .UNSPECIFIED.);
#3674=B_SPLINE_CURVE_WITH_KNOTS('',3,(#251777,#251778,#251779,#251780),
 .UNSPECIFIED.,.F.,.F.,(4,4),(-0.00120365178948661,-0.000936875117553324),
 .UNSPECIFIED.);
#3675=B_SPLINE_CURVE_WITH_KNOTS('',3,(#251781,#251782,#251783,#251784,#251785,
#251786,#251787,#251788,#251789,#251790,#251791,#251792,#251793,#251794,
#251795,#251796,#251797,#251798,#251799,#251800,#251801,#251802,#251803,
#251804,#251805,#251806,#251807,#251808,#251809,#251810,#251811,#251812,
#251813,#251814,#251815,#251816,#251817,#251818,#251819,#251820,#251821,
#251822,#251823,#251824,#251825,#251826,#251827,#251828,#251829,#251830,
#251831,#251832,#251833,#251834,#251835,#251836,#251837,#251838,#251839,
#251840,#251841,#251842,#251843,#251844,#251845,#251846,#251847,#251848,
#251849,#251850,#251851,#251852,#251853,#251854,#251855,#251856,#251857,
#251858,#251859,#251860,#251861,#251862,#251863,#251864,#251865,#251866,
#251867,#251868,#251869,#251870,#251871,#251872,#251873,#251874,#251875,
#251876,#251877,#251878,#251879,#251880,#251881,#251882,#251883,#251884,
#251885,#251886,#251887,#251888,#251889,#251890,#251891,#251892,#251893,
#251894,#251895,#251896,#251897,#251898,#251899,#251900,#251901,#251902,
#251903,#251904,#251905,#251906,#251907,#251908,#251909,#251910,#251911,
#251912,#251913,#251914,#251915,#251916,#251917,#251918,#251919,#251920,
#251921,#251922,#251923,#251924,#251925,#251926,#251927,#251928,#251929,
#251930,#251931,#251932,#251933,#251934,#251935,#251936,#251937,#251938,
#251939,#251940,#251941,#251942,#251943,#251944,#251945,#251946,#251947,
#251948,#251949,#251950,#251951,#251952,#251953,#251954,#251955,#251956,
#251957,#251958,#251959,#251960,#251961,#251962,#251963,#251964,#251965,
#251966,#251967,#251968,#251969,#251970,#251971,#251972,#251973,#251974,
#251975,#251976,#251977,#251978,#251979,#251980,#251981,#251982,#251983,
#251984,#251985,#251986,#251987,#251988,#251989,#251990,#251991,#251992,
#251993,#251994),.UNSPECIFIED.,.F.,.F.,(4,2,2,2,2,2,2,2,2,2,2,2,2,2,2,2,
2,2,2,2,2,2,2,2,2,2,2,2,2,2,2,2,2,2,2,2,2,2,2,2,2,2,2,2,2,2,2,2,2,2,2,2,
2,2,2,2,2,2,2,2,2,2,2,2,2,2,2,2,2,2,2,2,2,2,2,2,2,2,2,2,2,2,2,2,2,2,2,2,
2,2,2,2,2,2,2,2,2,2,2,2,2,2,2,2,2,2,4),(-4.0599101953197,-4.00818357316239,
-3.96848897714484,-3.96201432955781,-3.95845532602245,-3.95538107042525,
-3.95136419111971,-3.94234021348775,-3.89717804213648,-3.84622964427985,
-3.82426867843098,-3.80844400713818,-3.80187225425212,-3.80168047385455,
-3.80148213101809,-3.80127617050302,-3.80106138751048,-3.79557221084531,
-3.78957591183097,-3.77979061913736,-3.74508986309689,-3.67242665755617,
-3.65487630702403,-3.6433978906777,-3.63893423301607,-3.63580391938678,
-3.63242722551226,-3.62679307065948,-3.60683947182472,-3.55076296493494,
-3.49937562309541,-3.48589036399379,-3.47912688421341,-3.47373312016505,
-3.46750869606673,-3.45693990121842,-3.40237029577803,-3.34793162685712,
-3.33240903194856,-3.32190862337254,-3.31759725465209,-3.31449246914492,
-3.31105274047838,-3.3051308486166,-3.28188038301354,-3.22816291101631,
-3.1821667155189,-3.16612570560703,-3.15889020164693,-3.15339412819943,
-3.14742013006937,-3.13773892965905,-3.10509942446152,-3.04309570937919,
-3.00505178392451,-2.99862448983653,-2.9950754315408,-2.99199906495436,
-2.98796579128925,-2.97884994529758,-2.93043268046179,-2.88612384596614,
-2.86232604214216,-2.84541401282776,-2.83802888568189,-2.83251040561381,
-2.82731687151801,-2.81859609520331,-2.79425091077692,-2.72637372076309,
-2.68765019412936,-2.67889749283997,-2.67488622334734,-2.67181916350439,
-2.66821010365552,-2.66168724177889,-2.62293329508153,-2.61022219244065,
-2.56832925760348,-2.54260605300121,-2.52470807088446,-2.51716035829978,
-2.51161551293607,-2.50646466546695,-2.49797487877086,-2.47529728885201,
-2.40586981792854,-2.3665992951441,-2.35778985391995,-2.35376809743213,
-2.35069994637586,-2.34709777315226,-2.34060632564289,-2.3031502477248,
-2.22029973512685,-2.20315539231148,-2.19573135357903,-2.19020677283707,
-2.18431006848756,-2.17499034084613,-2.14530686814059,-2.07570090638503,
-2.05243480010754,-2.03845346521758,-2.03364385250762,-2.03044625802384,
-2.03042678336567),.UNSPECIFIED.);
#3676=B_SPLINE_CURVE_WITH_KNOTS('',3,(#251999,#252000,#252001,#252002,#252003,
#252004,#252005,#252006,#252007,#252008,#252009,#252010,#252011,#252012,
#252013,#252014,#252015,#252016,#252017,#252018,#252019,#252020,#252021,
#252022,#252023,#252024,#252025,#252026,#252027,#252028,#252029,#252030,
#252031,#252032,#252033,#252034,#252035,#252036,#252037,#252038,#252039,
#252040,#252041,#252042,#252043,#252044,#252045,#252046,#252047,#252048,
#252049,#252050,#252051,#252052,#252053,#252054,#252055,#252056,#252057,
#252058,#252059,#252060,#252061,#252062,#252063,#252064,#252065,#252066,
#252067,#252068,#252069,#252070,#252071,#252072,#252073,#252074,#252075,
#252076,#252077,#252078,#252079,#252080,#252081,#252082,#252083,#252084,
#252085,#252086,#252087,#252088,#252089,#252090,#252091,#252092,#252093,
#252094,#252095,#252096,#252097,#252098,#252099,#252100,#252101,#252102,
#252103,#252104,#252105,#252106,#252107,#252108,#252109,#252110,#252111,
#252112,#252113,#252114,#252115,#252116,#252117,#252118,#252119,#252120,
#252121,#252122,#252123,#252124,#252125,#252126,#252127,#252128,#252129,
#252130,#252131,#252132,#252133,#252134,#252135,#252136,#252137,#252138,
#252139,#252140,#252141,#252142,#252143,#252144,#252145,#252146,#252147,
#252148,#252149,#252150,#252151,#252152,#252153,#252154,#252155,#252156,
#252157,#252158,#252159,#252160,#252161,#252162,#252163,#252164,#252165,
#252166,#252167,#252168,#252169,#252170,#252171,#252172,#252173,#252174,
#252175,#252176,#252177,#252178,#252179,#252180,#252181,#252182,#252183,
#252184,#252185,#252186,#252187,#252188,#252189,#252190,#252191,#252192,
#252193,#252194,#252195,#252196,#252197,#252198,#252199,#252200,#252201,
#252202,#252203,#252204,#252205,#252206,#252207,#252208),.UNSPECIFIED.,
 .F.,.F.,(4,2,2,2,2,2,2,2,2,2,2,2,2,2,2,2,2,2,2,2,2,2,2,2,2,2,2,2,2,2,2,
2,2,2,2,2,2,2,2,2,2,2,2,2,2,2,2,2,2,2,2,2,2,2,2,2,2,2,2,2,2,2,2,2,2,2,2,
2,2,2,2,2,2,2,2,2,2,2,2,2,2,2,2,2,2,2,2,2,2,2,2,2,2,2,2,2,2,2,2,2,2,2,2,
2,4),(-4.05973564480636,-4.04895947790271,-4.0401996181676,-4.03494287370566,
-4.02984221445363,-4.02408797733691,-4.01502963392216,-3.98662498898566,
-3.91606292588892,-3.88075592232649,-3.87451271351252,-3.87105049960473,
-3.86804268648183,-3.86409885109718,-3.85519352795782,-3.80194757114214,
-3.76071477880727,-3.73757296729003,-3.72107073082661,-3.71385122584619,
-3.70845589758762,-3.70267799484809,-3.69351053999885,-3.66414748249112,
-3.60043996107158,-3.56313425657547,-3.55460687359398,-3.55068891719227,
-3.54769079323628,-3.54416756471351,-3.53781894825693,-3.50277854541742,
-3.48715005152721,-3.41477399173373,-3.39927276359096,-3.39222642535054,
-3.38685663215876,-3.38100531866879,-3.37149626296092,-3.33884974262725,
-3.27668657388353,-3.2414624056373,-3.23316111798039,-3.22928509610191,
-3.22629049860871,-3.22273741019866,-3.21625435554874,-3.17432317272511,
-3.11313447998543,-3.09274612496387,-3.07773039038647,-3.07077077691878,
-3.06541255190526,-3.05951962503591,-3.04981764551578,-3.01486792364621,
-2.95021733255777,-2.92754371839915,-2.91386344192486,-2.90915599912745,
-2.90602806947897,-2.90321976458621,-2.89856160549191,-2.88626966783993,
-2.79716247480215,-2.77374822616665,-2.75710342367256,-2.74986023312093,
-2.74446154544535,-2.73939247289678,-2.73091354072414,-2.70751918734115,
-2.63857280271443,-2.60930087306103,-2.59837246371469,-2.59033122126131,
-2.58650437219777,-2.58379957522817,-2.58033150873631,-2.57422782863558,
-2.54627516752496,-2.49572519841999,-2.44242335787306,-2.43206848472008,
-2.42603528544164,-2.42070500237664,-2.41399366075304,-2.40076721530869,
-2.33314605476252,-2.29230350270686,-2.27899342472995,-2.26966085701216,
-2.26559946195761,-2.26258574704101,-2.25915196628226,-2.25319957139567,
-2.22713745340132,-2.17519092797079,-2.1258391842483,-2.11271731757875,
-2.10611425967868,-2.10079285651173,-2.09468573206507,-2.08426306240254,
-2.03033861750309),.UNSPECIFIED.);
#3677=B_SPLINE_CURVE_WITH_KNOTS('',3,(#252210,#252211,#252212,#252213,#252214,
#252215,#252216,#252217,#252218,#252219,#252220,#252221,#252222,#252223,
#252224,#252225,#252226,#252227,#252228,#252229,#252230,#252231,#252232,
#252233,#252234,#252235,#252236,#252237,#252238,#252239,#252240,#252241,
#252242,#252243,#252244,#252245,#252246,#252247,#252248,#252249,#252250,
#252251,#252252,#252253,#252254,#252255,#252256,#252257,#252258,#252259,
#252260,#252261,#252262,#252263,#252264,#252265,#252266,#252267,#252268,
#252269,#252270,#252271,#252272,#252273,#252274,#252275,#252276,#252277,
#252278,#252279,#252280,#252281,#252282,#252283,#252284,#252285,#252286,
#252287,#252288,#252289,#252290,#252291,#252292,#252293,#252294,#252295,
#252296,#252297,#252298,#252299,#252300,#252301,#252302,#252303,#252304,
#252305,#252306,#252307,#252308,#252309,#252310,#252311,#252312,#252313,
#252314,#252315,#252316,#252317,#252318,#252319,#252320,#252321,#252322,
#252323,#252324,#252325,#252326,#252327,#252328,#252329,#252330,#252331,
#252332,#252333,#252334,#252335,#252336,#252337,#252338,#252339,#252340,
#252341,#252342,#252343,#252344,#252345,#252346,#252347,#252348,#252349,
#252350,#252351,#252352,#252353,#252354,#252355,#252356,#252357,#252358,
#252359,#252360,#252361,#252362,#252363,#252364,#252365,#252366,#252367,
#252368,#252369,#252370,#252371,#252372,#252373,#252374,#252375,#252376,
#252377,#252378,#252379,#252380,#252381,#252382,#252383,#252384,#252385,
#252386,#252387,#252388,#252389,#252390,#252391,#252392,#252393,#252394,
#252395,#252396,#252397,#252398,#252399,#252400,#252401,#252402,#252403,
#252404,#252405,#252406,#252407,#252408,#252409,#252410,#252411,#252412,
#252413,#252414,#252415,#252416,#252417),.UNSPECIFIED.,.F.,.F.,(4,2,2,2,
2,2,2,2,2,2,2,2,2,2,2,2,2,2,2,2,2,2,2,2,2,2,2,2,2,2,2,2,2,2,2,2,2,2,2,2,
2,2,2,2,2,2,2,2,2,2,2,2,2,2,2,2,2,2,2,2,2,2,2,2,2,2,2,2,2,2,2,2,2,2,2,2,
2,2,2,2,2,2,2,2,2,2,2,2,2,2,2,2,2,2,2,2,2,2,2,2,2,2,2,4),(-2.03042678336567,
-2.0271766588524,-2.02203124980944,-2.0051458401705,-1.97410420040719,-1.8983471496252,
-1.88194887337186,-1.87527230136595,-1.86971819800052,-1.86398637017759,
-1.85545094609828,-1.83043654458003,-1.78821497586018,-1.72349046635426,
-1.71596304215994,-1.71213856459357,-1.70902427697767,-1.70568624623425,
-1.70022852577767,-1.68007541875722,-1.63825152741114,-1.5725631157043,
-1.55917563529424,-1.55234271647675,-1.54689320264598,-1.540698152456,-1.5299883956653,
-1.4683449077896,-1.40204814226571,-1.39386969266444,-1.38996566352539,
-1.38690615867673,-1.38321588183987,-1.37611615019736,-1.32466139905582,
-1.25050211353124,-1.23875638341914,-1.23171607523815,-1.22623002787951,
-1.2202204108632,-1.21037483196101,-1.17069668646326,-1.1297146466336,-1.11587137626313,
-1.0782767140547,-1.07178171329455,-1.06817893057478,-1.06511112774005,
-1.06109101375384,-1.05228949017911,-1.01309364175023,-0.94385817082773,
-0.92102801903239,-0.912516790358778,-0.907362255448577,-0.901820484742364,
-0.894289602703367,-0.87649425666982,-0.850971087847861,-0.808827028893174,
-0.797495569084699,-0.757256865535598,-0.750703862772229,-0.747088223416008,
-0.744022157884542,-0.740020796105065,-0.731321409729111,-0.693107749684921,
-0.626644615330917,-0.600769395450082,-0.59186221652949,-0.586053248380764,
-0.580486091914029,-0.572805790259274,-0.554067797396065,-0.526642613777348,
-0.486669839395028,-0.471872491107209,-0.435976748210515,-0.429525873433119,
-0.425933042778938,-0.422893238264779,-0.418876134260448,-0.410090469243235,
-0.37104633952984,-0.302257086552059,-0.278958774535814,-0.270381610934319,
-0.265215074810287,-0.259681442734589,-0.259485331154416,-0.252978685183491,
-0.237566609476168,-0.216356965085827,-0.164580847592149,-0.156574339676578,
-0.11506810328143,-0.108497881713489,-0.104878488866221,-0.101812992052141,
-0.0978172403445724,-0.0891479295199449,-0.0512186982902751,-0.000938329146361453),
 .UNSPECIFIED.);
#3678=B_SPLINE_CURVE_WITH_KNOTS('',3,(#252418,#252419,#252420,#252421),
 .UNSPECIFIED.,.F.,.F.,(4,4),(-4.0607596339126,-4.06051280328589),
 .UNSPECIFIED.);
#3679=B_SPLINE_CURVE_WITH_KNOTS('',3,(#252427,#252428,#252429,#252430,#252431,
#252432,#252433,#252434,#252435,#252436,#252437,#252438,#252439,#252440,
#252441,#252442,#252443,#252444,#252445,#252446,#252447,#252448,#252449,
#252450,#252451,#252452,#252453,#252454,#252455,#252456,#252457,#252458,
#252459,#252460,#252461,#252462,#252463,#252464,#252465,#252466,#252467,
#252468,#252469,#252470,#252471,#252472,#252473,#252474,#252475,#252476,
#252477,#252478,#252479,#252480,#252481,#252482,#252483,#252484,#252485,
#252486,#252487,#252488,#252489,#252490,#252491,#252492,#252493,#252494,
#252495,#252496,#252497,#252498,#252499,#252500,#252501,#252502,#252503,
#252504,#252505,#252506,#252507,#252508,#252509,#252510,#252511,#252512,
#252513,#252514,#252515,#252516,#252517,#252518,#252519,#252520,#252521,
#252522,#252523,#252524,#252525,#252526,#252527,#252528,#252529,#252530,
#252531,#252532,#252533,#252534,#252535,#252536,#252537,#252538,#252539,
#252540,#252541,#252542,#252543,#252544,#252545,#252546,#252547,#252548,
#252549,#252550,#252551,#252552,#252553,#252554,#252555,#252556,#252557,
#252558,#252559,#252560,#252561,#252562,#252563,#252564,#252565,#252566,
#252567,#252568,#252569,#252570,#252571,#252572,#252573,#252574,#252575,
#252576,#252577,#252578,#252579,#252580,#252581,#252582,#252583,#252584,
#252585,#252586,#252587,#252588,#252589,#252590,#252591,#252592,#252593,
#252594,#252595,#252596,#252597,#252598,#252599,#252600,#252601,#252602,
#252603,#252604,#252605,#252606,#252607,#252608,#252609,#252610,#252611,
#252612,#252613,#252614,#252615,#252616,#252617,#252618,#252619,#252620,
#252621,#252622,#252623,#252624,#252625,#252626,#252627,#252628,#252629,
#252630,#252631,#252632,#252633,#252634,#252635,#252636),.UNSPECIFIED.,
 .F.,.F.,(4,2,2,2,2,2,2,2,2,2,2,2,2,2,2,2,2,2,2,2,2,2,2,2,2,2,2,2,2,2,2,
2,2,2,2,2,2,2,2,2,2,2,2,2,2,2,2,2,2,2,2,2,2,2,2,2,2,2,2,2,2,2,2,2,2,2,2,
2,2,2,2,2,2,2,2,2,2,2,2,2,2,2,2,2,2,2,2,2,2,2,2,2,2,2,2,2,2,2,2,2,2,2,2,
2,4),(-2.03032387244298,-1.985810352188,-1.92354028603898,-1.90998856667296,
-1.90330182203253,-1.8979734141344,-1.89192343591164,-1.88149153535254,
-1.82569392074198,-1.77061721719319,-1.74891965200316,-1.74319588344627,
-1.73984622431255,-1.73680753612006,-1.7325755580415,-1.7222209776748,-1.70690750334284,
-1.65350623116215,-1.59730564184874,-1.58680678975198,-1.58068220046311,
-1.57536184162547,-1.56878108118556,-1.55577502540947,-1.50735400480745,
-1.45747415578814,-1.42843560360286,-1.4223220933579,-1.41885158443418,
-1.4161467978325,-1.41232251572522,-1.40429607663505,-1.33816476365675,
-1.2809630757481,-1.26734742409785,-1.26064828923641,-1.25531865135497,
-1.24927651969447,-1.23888175498732,-1.18436757511404,-1.1315368358298,
-1.10665560378847,-1.10070616779897,-1.0973072172321,-1.0942841922768,-1.09015614018212,
-1.08043438714862,-1.06637559166544,-1.02122315479132,-0.959546581143472,
-0.945984702377664,-0.939295782185956,-0.933966925025547,-0.927917813081183,
-0.917490930616126,-0.861889115931241,-0.807145595013794,-0.784972499816132,
-0.779210543216743,-0.775852412722177,-0.772816509082223,-0.768602873731845,
-0.758362927624136,-0.743280187726051,-0.691512814550863,-0.633198624710415,
-0.622743016026284,-0.616627923709213,-0.611306380242599,-0.604711959246729,
-0.591637435762296,-0.542672612896766,-0.491586934217922,-0.464245534626607,
-0.458216737563347,-0.454765281665521,-0.452057040883249,-0.448203956006191,
-0.44002626839897,-0.405910018304364,-0.347346149265129,-0.310495490934644,
-0.300656135244878,-0.294733106429359,-0.289638493607166,-0.289413176345763,
-0.289197912242156,-0.288991140798167,-0.288791522621203,-0.288597893934967,
-0.288409231141944,-0.281854747281621,-0.274014556102258,-0.260610926794667,
-0.230924903372333,-0.168249844613081,-0.142728446000465,-0.13679928309122,
-0.133370386324583,-0.13035474928407,-0.126282497862192,-0.116889819551263,
-0.103467134916947,-0.0620033227178036,-0.000941319676076269),
 .UNSPECIFIED.);
#3680=B_SPLINE_CURVE_WITH_KNOTS('',3,(#252637,#252638,#252639,#252640),
 .UNSPECIFIED.,.F.,.F.,(4,4),(-4.05986998617981,-4.05973564480636),
 .UNSPECIFIED.);
#3681=B_SPLINE_CURVE_WITH_KNOTS('',3,(#252641,#252642,#252643,#252644,#252645,
#252646,#252647,#252648,#252649,#252650,#252651,#252652,#252653,#252654,
#252655,#252656,#252657,#252658,#252659,#252660,#252661,#252662,#252663,
#252664,#252665,#252666,#252667,#252668,#252669,#252670,#252671,#252672,
#252673,#252674,#252675,#252676,#252677,#252678,#252679,#252680,#252681,
#252682,#252683,#252684,#252685,#252686,#252687,#252688,#252689,#252690,
#252691,#252692,#252693,#252694,#252695,#252696,#252697,#252698,#252699,
#252700,#252701,#252702,#252703,#252704,#252705,#252706,#252707,#252708,
#252709,#252710,#252711,#252712,#252713,#252714,#252715,#252716,#252717,
#252718,#252719,#252720,#252721,#252722,#252723,#252724,#252725,#252726,
#252727,#252728,#252729,#252730,#252731,#252732,#252733,#252734,#252735,
#252736,#252737,#252738,#252739,#252740,#252741,#252742,#252743,#252744,
#252745,#252746,#252747,#252748,#252749,#252750,#252751,#252752,#252753,
#252754,#252755,#252756,#252757,#252758,#252759,#252760,#252761,#252762,
#252763,#252764,#252765,#252766,#252767,#252768,#252769,#252770,#252771,
#252772,#252773,#252774,#252775,#252776,#252777,#252778,#252779,#252780,
#252781,#252782,#252783,#252784,#252785,#252786,#252787,#252788,#252789,
#252790,#252791,#252792,#252793,#252794,#252795,#252796,#252797,#252798,
#252799,#252800,#252801,#252802,#252803,#252804,#252805,#252806,#252807,
#252808,#252809,#252810,#252811,#252812,#252813,#252814,#252815,#252816,
#252817,#252818,#252819,#252820,#252821,#252822,#252823,#252824,#252825,
#252826,#252827,#252828,#252829,#252830,#252831,#252832,#252833,#252834,
#252835,#252836,#252837,#252838,#252839,#252840,#252841,#252842,#252843,
#252844,#252845,#252846,#252847,#252848,#252849,#252850,#252851,#252852,
#252853,#252854),.UNSPECIFIED.,.F.,.F.,(4,2,2,2,2,2,2,2,2,2,2,2,2,2,2,2,
2,2,2,2,2,2,2,2,2,2,2,2,2,2,2,2,2,2,2,2,2,2,2,2,2,2,2,2,2,2,2,2,2,2,2,2,
2,2,2,2,2,2,2,2,2,2,2,2,2,2,2,2,2,2,2,2,2,2,2,2,2,2,2,2,2,2,2,2,2,2,2,2,
2,2,2,2,2,2,2,2,2,2,2,2,2,2,2,2,2,2,4),(-4.06051280328589,-4.03349125568929,
-4.01797158672048,-4.01142748395604,-4.00620981613182,-4.0007717472446,
-3.99447020809177,-3.98355486818143,-3.94287798577048,-3.86239817469966,
-3.84984294219378,-3.84522336059247,-3.84206413072108,-3.83874119466294,
-3.83335134071936,-3.81582217360265,-3.73852180782294,-3.71233298024723,
-3.6942027536992,-3.68661855630653,-3.68106827117857,-3.67592736286728,
-3.6674886887581,-3.6451584869305,-3.57541814088679,-3.53604066839924,-3.5272210190726,
-3.52319778988702,-3.52012993408766,-3.51652978031027,-3.51004584196845,
-3.47284742515918,-3.45869316300082,-3.41789830071261,-3.3914337616427,
-3.37316622438791,-3.36555993514114,-3.36000566748489,-3.35417355568086,
-3.34515625505989,-3.3182694035266,-3.25264379989367,-3.21472527649837,
-3.20605714684187,-3.2020615546724,-3.1989960283176,-3.19537637525836,-3.18880524111753,
-3.14713488154956,-3.13723108008066,-3.0944370688264,-3.06935563307476,
-3.05178256520013,-3.04428789401309,-3.03875207945414,-3.03358834981565,
-3.02502736287699,-3.0018466361948,-2.9328960461705,-2.8937938222999,-2.88500201710137,
-2.88098363879058,-2.8779435680964,-2.87435120757464,-2.86790307356932,
-2.83210261136269,-2.81681513458398,-2.77672309287494,-2.74964031211071,
-2.73106756802185,-2.7234127576404,-2.71784974674643,-2.71272409566563,
-2.70437229440999,-2.68263635170562,-2.612317957888,-2.57273690714379,-2.56389572095591,
-2.55986821272448,-2.5567995561936,-2.55320136360772,-2.54672765371147,
-2.50995534786278,-2.49541633557083,-2.45390009997454,-2.42781272325173,
-2.4097320755428,-2.4021548468511,-2.39660487459141,-2.3914608972026,-2.38300941636734,
-2.36059842024774,-2.29091604761021,-2.25155574557122,-2.24273688908833,
-2.23871331543739,-2.23564488271078,-2.23204368132547,-2.22555699918416,
-2.18829553169727,-2.10536409910089,-2.08812972904022,-2.08069053433702,
-2.07516337189089,-2.06927202045497,-2.0599781067523,-2.03077402217095),
 .UNSPECIFIED.);
#3682=B_SPLINE_CURVE_WITH_KNOTS('',3,(#252860,#252861,#252862,#252863),
 .UNSPECIFIED.,.F.,.F.,(4,4),(-0.00122902991741216,-0.000941425455351654),
 .UNSPECIFIED.);
#3683=B_SPLINE_CURVE_WITH_KNOTS('',3,(#252864,#252865,#252866,#252867,#252868,
#252869,#252870,#252871,#252872,#252873,#252874,#252875,#252876,#252877,
#252878,#252879,#252880,#252881,#252882,#252883,#252884,#252885,#252886,
#252887,#252888,#252889,#252890,#252891,#252892,#252893,#252894,#252895,
#252896,#252897,#252898,#252899,#252900,#252901,#252902,#252903,#252904,
#252905,#252906,#252907,#252908,#252909,#252910,#252911,#252912,#252913,
#252914,#252915,#252916,#252917,#252918,#252919,#252920,#252921,#252922,
#252923,#252924,#252925,#252926,#252927,#252928,#252929,#252930,#252931,
#252932,#252933,#252934,#252935,#252936,#252937,#252938,#252939,#252940,
#252941,#252942,#252943,#252944,#252945,#252946,#252947,#252948,#252949,
#252950,#252951,#252952,#252953,#252954,#252955,#252956,#252957,#252958,
#252959,#252960,#252961,#252962,#252963,#252964,#252965,#252966,#252967,
#252968,#252969,#252970,#252971,#252972,#252973,#252974,#252975,#252976,
#252977,#252978,#252979,#252980,#252981,#252982,#252983,#252984,#252985,
#252986,#252987,#252988,#252989,#252990,#252991,#252992,#252993,#252994,
#252995,#252996,#252997,#252998,#252999,#253000,#253001,#253002,#253003,
#253004,#253005,#253006,#253007,#253008,#253009,#253010,#253011,#253012,
#253013,#253014,#253015,#253016,#253017,#253018,#253019,#253020,#253021,
#253022,#253023,#253024,#253025,#253026,#253027,#253028,#253029,#253030,
#253031,#253032,#253033,#253034,#253035,#253036,#253037,#253038,#253039,
#253040,#253041,#253042,#253043,#253044,#253045,#253046,#253047,#253048,
#253049,#253050,#253051,#253052,#253053,#253054,#253055,#253056,#253057,
#253058,#253059,#253060,#253061,#253062,#253063,#253064,#253065,#253066,
#253067,#253068,#253069,#253070,#253071,#253072,#253073,#253074,#253075),
 .UNSPECIFIED.,.F.,.F.,(4,2,2,2,2,2,2,2,2,2,2,2,2,2,2,2,2,2,2,2,2,2,2,2,
2,2,2,2,2,2,2,2,2,2,2,2,2,2,2,2,2,2,2,2,2,2,2,2,2,2,2,2,2,2,2,2,2,2,2,2,
2,2,2,2,2,2,2,2,2,2,2,2,2,2,2,2,2,2,2,2,2,2,2,2,2,2,2,2,2,2,2,2,2,2,2,2,
2,2,2,2,2,2,2,2,2,4),(-4.05943251925004,-4.01250822828506,-3.99869180488384,
-3.99431174770842,-3.99036929249612,-3.98739604133786,-3.98390133402738,
-3.97767895338795,-3.94666864821514,-3.91381217739116,-3.86853671793411,
-3.84258318432119,-3.83468588315656,-3.82890593503146,-3.82351208450195,
-3.81642464002805,-3.80024123070016,-3.72023387395155,-3.69145300066394,
-3.68063901099352,-3.67266207567129,-3.6688474473133,-3.66614394447111,
-3.66266726220235,-3.65652563605165,-3.62696882539559,-3.5662552977107,
-3.52388031345365,-3.51400818717552,-3.50807871213459,-3.50272948635832,
-3.49584114035094,-3.48460717483407,-3.4059691569951,-3.37216683792621,
-3.35444193777202,-3.3492818534785,-3.34605614430662,-3.34299124926135,
-3.33917602137439,-3.33151435548724,-3.26989190052413,-3.21166273216861,
-3.19623443672209,-3.189200932372,-3.18383282620497,-3.17797540741489,-3.16843835097828,
-3.135491160719,-3.07349378708838,-3.03842960767292,-3.03014601281479,-3.02627325645761,
-3.02327885567791,-3.01972322998573,-3.01322889528417,-2.96789483302572,
-2.90934516297389,-2.8893826137384,-2.87460369712268,-2.8676869804542,-2.86233406007126,
-2.85641904047069,-2.84661498570669,-2.81004558422709,-2.74996973025211,
-2.71679557872491,-2.70872644586684,-2.70489411555978,-2.70218852576888,
-2.69872373791196,-2.69263527019818,-2.66409989525194,-2.61390539088448,
-2.56078224175002,-2.55043257266201,-2.54440019526658,-2.53906931699561,
-2.53235545667524,-2.51911822540249,-2.45173970619264,-2.41071836577752,
-2.39737538857587,-2.38802541442379,-2.38396082180492,-2.38094650606853,
-2.37751406816091,-2.37156827607295,-2.34562464238657,-2.29358874690308,
-2.24419313259982,-2.23106529814149,-2.22446076464558,-2.21918777663066,
-2.21309862063046,-2.20275723842207,-2.1534136935319,-2.09409657721453,
-2.07800990117234,-2.06727669991833,-2.06298478229787,-2.05993625966779,
-2.05661209101579,-2.05100447384093,-2.03050942068758,-2.03032387244298),
 .UNSPECIFIED.);
#3684=B_SPLINE_CURVE_WITH_KNOTS('',3,(#253076,#253077,#253078,#253079,#253080,
#253081,#253082,#253083,#253084,#253085,#253086,#253087,#253088,#253089,
#253090,#253091,#253092,#253093,#253094,#253095,#253096,#253097,#253098,
#253099,#253100,#253101,#253102,#253103,#253104,#253105,#253106,#253107,
#253108,#253109,#253110,#253111,#253112,#253113,#253114,#253115,#253116,
#253117,#253118,#253119,#253120,#253121,#253122,#253123,#253124,#253125,
#253126,#253127,#253128,#253129,#253130,#253131,#253132,#253133,#253134,
#253135,#253136,#253137,#253138,#253139,#253140,#253141,#253142,#253143,
#253144,#253145,#253146,#253147,#253148,#253149,#253150,#253151,#253152,
#253153,#253154,#253155,#253156,#253157,#253158,#253159,#253160,#253161,
#253162,#253163,#253164,#253165,#253166,#253167,#253168,#253169,#253170,
#253171,#253172,#253173,#253174,#253175,#253176,#253177,#253178,#253179,
#253180,#253181,#253182,#253183,#253184,#253185,#253186,#253187,#253188,
#253189,#253190,#253191,#253192,#253193,#253194,#253195,#253196,#253197,
#253198,#253199,#253200,#253201,#253202,#253203,#253204,#253205,#253206,
#253207,#253208,#253209,#253210,#253211,#253212,#253213,#253214,#253215,
#253216,#253217,#253218,#253219,#253220,#253221,#253222,#253223,#253224,
#253225,#253226,#253227,#253228,#253229,#253230,#253231,#253232,#253233,
#253234,#253235,#253236,#253237,#253238,#253239,#253240,#253241,#253242,
#253243,#253244,#253245,#253246,#253247,#253248,#253249,#253250,#253251,
#253252,#253253,#253254,#253255,#253256,#253257,#253258,#253259,#253260,
#253261,#253262,#253263,#253264,#253265,#253266,#253267,#253268,#253269,
#253270,#253271,#253272,#253273,#253274,#253275,#253276,#253277,#253278,
#253279,#253280,#253281,#253282,#253283,#253284,#253285,#253286,#253287,
#253288,#253289,#253290,#253291,#253292,#253293,#253294,#253295,#253296,
#253297,#253298,#253299,#253300,#253301,#253302,#253303,#253304,#253305,
#253306,#253307,#253308,#253309,#253310,#253311,#253312,#253313,#253314,
#253315,#253316,#253317,#253318,#253319,#253320,#253321,#253322,#253323,
#253324,#253325,#253326,#253327,#253328,#253329,#253330,#253331,#253332,
#253333,#253334,#253335,#253336,#253337,#253338,#253339,#253340,#253341,
#253342,#253343,#253344,#253345,#253346,#253347,#253348,#253349,#253350,
#253351,#253352,#253353,#253354,#253355,#253356,#253357,#253358,#253359,
#253360,#253361),.UNSPECIFIED.,.F.,.F.,(4,2,2,2,2,2,2,2,2,2,2,2,2,2,2,2,
2,2,2,2,2,2,2,2,2,2,2,2,2,2,2,2,2,2,2,2,2,2,2,2,2,2,2,2,2,2,2,2,2,2,2,2,
2,2,2,2,2,2,2,2,2,2,2,2,2,2,2,2,2,2,2,2,2,2,2,2,2,2,2,2,2,2,2,2,2,2,2,2,
2,2,2,2,2,2,2,2,2,2,2,2,2,2,2,2,2,2,2,2,2,2,2,2,2,2,2,2,2,2,2,2,2,2,2,2,
2,2,2,2,2,2,2,2,2,2,2,2,2,2,2,2,2,2,4),(-2.03077402217095,-2.03054329316223,
-1.97950585915411,-1.93073468173083,-1.92164973112131,-1.91762170578921,
-1.91454578935731,-1.91099296232783,-1.90454882531797,-1.86593920117148,
-1.77779666055522,-1.76604576490879,-1.75900419718089,-1.75351822575622,
-1.74750976437705,-1.73766855481353,-1.69805145397977,-1.65673369875796,
-1.64160362689499,-1.60550368697605,-1.59904757017494,-1.59545358493151,
-1.59241397319969,-1.58839864511556,-1.57962260455279,-1.54067133170504,
-1.47212954737459,-1.44856037273098,-1.43994556085159,-1.4347720679502,
-1.42924275314098,-1.42178686272413,-1.40444862657257,-1.32139627239894,
-1.28434952425307,-1.27786846171124,-1.2742687408577,-1.27120044555993,
-1.26717564031127,-1.25834865026321,-1.21890559621116,-1.14896332429741,
-1.12688025601084,-1.11847724295872,-1.11334243874796,-1.10778667194497,
-1.10017314680449,-1.08186211223756,-1.05530717594241,-1.01457391612522,
-1.00004092705399,-0.963213367338413,-0.956738149084022,-0.953139798652997,
-0.950071424547374,-0.946044887688408,-0.937207968424374,-0.897666354508307,
-0.827439310204909,-0.805658349468258,-0.797300224416531,-0.792173679241101,
-0.786611982132833,-0.778963205191546,-0.76042741658232,-0.733416031009266,
-0.693192610916315,-0.677879780903844,-0.642051895967409,-0.635602743905788,
-0.632010284501868,-0.628970404021135,-0.624952692052985,-0.616163779156102,
-0.577088448558739,-0.508194685334339,-0.485003014050021,-0.476440777667917,
-0.471276981678272,-0.465741576980334,-0.45824835991361,-0.440683342348332,
-0.415614311212734,-0.37277173621231,-0.324923390426804,-0.315880989057198,
-0.311860761365656,-0.308896579504256,-0.308834430346243,-0.308789475798928,
-0.308720948683653,-0.308656605274084,-0.308596018595368,-0.308538820093903,
-0.308484689679083,-0.308433347778783,-0.308384548947327,-0.308338076656965,
-0.308293739044644,-0.308251365395575,-0.308210803230603,-0.308171915865701,
-0.308134580350116,-0.308098685760015,-0.308064131705786,-0.308030827072463,
-0.30799868895484,-0.307967641715317,-0.307937616183952,-0.307908548967409,
-0.307880381834737,-0.30785306118997,-0.307826537601013,-0.307800765381932,
-0.30777570225921,-0.307751309031958,-0.307727549284388,-0.307704389134684,
-0.307681797019091,-0.307659743486991,-0.3076382010022,-0.307617143810173,
-0.307596547766604,-0.307576390229745,-0.307538527833294,-0.307500736275751,
-0.307463003621433,-0.307425318134875,-0.307387668267892,-0.303382625934521,
-0.298671112517162,-0.290390078420425,-0.271467109705538,-0.229540664352217,
-0.168239170202113,-0.157611171051473,-0.151373578930371,-0.145929509675019,
-0.139159569306342,-0.125640660345811,-0.0739691429210548,-0.0428284470474373,
-0.000993735616496565),.UNSPECIFIED.);
#3685=B_SPLINE_CURVE_WITH_KNOTS('',3,(#253366,#253367,#253368,#253369,#253370,
#253371,#253372,#253373,#253374,#253375,#253376,#253377,#253378,#253379,
#253380,#253381,#253382,#253383,#253384,#253385,#253386,#253387,#253388,
#253389,#253390,#253391,#253392,#253393,#253394,#253395,#253396,#253397,
#253398,#253399,#253400,#253401,#253402,#253403,#253404,#253405,#253406,
#253407,#253408,#253409,#253410,#253411,#253412,#253413,#253414,#253415,
#253416,#253417,#253418,#253419,#253420,#253421,#253422,#253423,#253424,
#253425,#253426,#253427,#253428,#253429,#253430,#253431,#253432,#253433,
#253434,#253435,#253436,#253437,#253438,#253439,#253440,#253441,#253442,
#253443,#253444,#253445,#253446,#253447,#253448,#253449,#253450,#253451,
#253452,#253453,#253454,#253455,#253456,#253457,#253458,#253459,#253460,
#253461,#253462,#253463,#253464,#253465,#253466,#253467,#253468,#253469,
#253470,#253471,#253472,#253473,#253474,#253475,#253476,#253477,#253478,
#253479,#253480,#253481,#253482,#253483,#253484,#253485,#253486,#253487,
#253488,#253489,#253490,#253491,#253492,#253493,#253494,#253495,#253496,
#253497,#253498,#253499,#253500,#253501,#253502,#253503,#253504,#253505,
#253506,#253507,#253508,#253509,#253510,#253511,#253512,#253513,#253514,
#253515,#253516,#253517,#253518,#253519,#253520,#253521,#253522,#253523,
#253524,#253525,#253526,#253527,#253528,#253529,#253530,#253531,#253532,
#253533,#253534,#253535,#253536,#253537,#253538,#253539,#253540,#253541,
#253542,#253543,#253544,#253545,#253546,#253547,#253548,#253549,#253550,
#253551,#253552,#253553,#253554,#253555,#253556,#253557,#253558,#253559,
#253560,#253561,#253562,#253563,#253564,#253565,#253566,#253567,#253568,
#253569,#253570,#253571),.UNSPECIFIED.,.F.,.F.,(4,2,2,2,2,2,2,2,2,2,2,2,
2,2,2,2,2,2,2,2,2,2,2,2,2,2,2,2,2,2,2,2,2,2,2,2,2,2,2,2,2,2,2,2,2,2,2,2,
2,2,2,2,2,2,2,2,2,2,2,2,2,2,2,2,2,2,2,2,2,2,2,2,2,2,2,2,2,2,2,2,2,2,2,2,
2,2,2,2,2,2,2,2,2,2,2,2,2,2,2,2,2,2,4),(-2.03071434728601,-2.02406353587364,
-2.01908685646972,-2.01362036552204,-2.00598027294809,-1.98684159483128,
-1.95843052180122,-1.89658083920336,-1.89528978875892,-1.86831400199091,
-1.8623051670069,-1.85885859650199,-1.85615003054387,-1.85229105765456,
-1.84408001077536,-1.80966252041393,-1.74840407813406,-1.71419939256671,
-1.70457929248984,-1.69870419392353,-1.69334152724426,-1.68634644716821,
-1.67113260672148,-1.61240722870165,-1.55091232302111,-1.5432430068348,
-1.53942597866863,-1.53636067767775,-1.53313574560849,-1.5279791761728,
-1.51028871772211,-1.47659588702326,-1.39783732428557,-1.38662317591827,
-1.37974055820503,-1.37439201637046,-1.3684594627284,-1.35857307600554,
-1.31595351180966,-1.25412522186513,-1.22577419175953,-1.21969463139117,
-1.21623193311996,-1.21352608969297,-1.20969099567397,-1.20160678144858,
-1.16830230027922,-1.10816681240579,-1.07185565381104,-1.06206729328405,
-1.05615578902976,-1.05080225455898,-1.04387937690591,-1.02906606648274,
-1.0090394273269,-0.950114599950162,-0.905204604022645,-0.898711062141302,
-0.895155656839439,-0.89216127447609,-0.888288370641051,-0.880003777188907,
-0.844931766851071,-0.782999404528137,-0.750063418814445,-0.740527639791859,
-0.734670505290375,-0.729302321317867,-0.722268227158778,-0.706836768310102,
-0.662882551525829,-0.587324587877297,-0.579408214725877,-0.575531178003882,
-0.572727493736941,-0.569593497403912,-0.564857878698352,-0.55095592115304,
-0.527744458004199,-0.45850658474406,-0.428180345289793,-0.418902371277761,
-0.413100484883986,-0.407713718237056,-0.400552308899267,-0.384392958971016,
-0.331219995956714,-0.264939614330755,-0.256841801552086,-0.25300381065856,
-0.250011517639456,-0.246428651366949,-0.240067262257872,-0.19709964013155,
-0.1506644438478,-0.108485130216251,-0.0983466391663633,-0.092359187068013,
-0.0870204334487193,-0.0802320040166418,-0.0728770014022373,-0.053460858918564,
-0.00122902991741216),.UNSPECIFIED.);
#3686=B_SPLINE_CURVE_WITH_KNOTS('',3,(#253573,#253574,#253575,#253576),
 .UNSPECIFIED.,.F.,.F.,(4,4),(-0.000993735616496565,-0.000938146623603337),
 .UNSPECIFIED.);
#3687=B_SPLINE_CURVE_WITH_KNOTS('',3,(#253577,#253578,#253579,#253580,#253581,
#253582,#253583,#253584,#253585,#253586,#253587,#253588,#253589,#253590,
#253591,#253592,#253593,#253594,#253595,#253596,#253597,#253598,#253599,
#253600,#253601,#253602,#253603,#253604,#253605,#253606,#253607,#253608,
#253609,#253610,#253611,#253612,#253613,#253614,#253615,#253616,#253617,
#253618,#253619,#253620,#253621,#253622,#253623,#253624,#253625,#253626,
#253627,#253628,#253629,#253630,#253631,#253632,#253633,#253634,#253635,
#253636,#253637,#253638,#253639,#253640,#253641,#253642,#253643,#253644,
#253645,#253646,#253647,#253648,#253649,#253650,#253651,#253652,#253653,
#253654,#253655,#253656,#253657,#253658,#253659,#253660,#253661,#253662,
#253663,#253664,#253665,#253666,#253667,#253668,#253669,#253670,#253671,
#253672,#253673,#253674,#253675,#253676,#253677,#253678,#253679,#253680,
#253681,#253682,#253683,#253684,#253685,#253686,#253687,#253688,#253689,
#253690,#253691,#253692,#253693,#253694,#253695,#253696,#253697,#253698,
#253699,#253700,#253701,#253702,#253703,#253704,#253705,#253706,#253707,
#253708,#253709,#253710,#253711,#253712,#253713,#253714,#253715,#253716,
#253717,#253718,#253719,#253720,#253721,#253722,#253723,#253724,#253725,
#253726,#253727,#253728,#253729,#253730,#253731,#253732,#253733,#253734,
#253735,#253736,#253737,#253738,#253739,#253740,#253741,#253742,#253743,
#253744,#253745,#253746,#253747,#253748,#253749,#253750,#253751,#253752,
#253753,#253754,#253755,#253756,#253757,#253758,#253759,#253760,#253761,
#253762,#253763,#253764,#253765,#253766,#253767,#253768,#253769,#253770,
#253771,#253772,#253773,#253774,#253775,#253776,#253777,#253778,#253779,
#253780,#253781,#253782,#253783,#253784),.UNSPECIFIED.,.F.,.F.,(4,2,2,2,
2,2,2,2,2,2,2,2,2,2,2,2,2,2,2,2,2,2,2,2,2,2,2,2,2,2,2,2,2,2,2,2,2,2,2,2,
2,2,2,2,2,2,2,2,2,2,2,2,2,2,2,2,2,2,2,2,2,2,2,2,2,2,2,2,2,2,2,2,2,2,2,2,
2,2,2,2,2,2,2,2,2,2,2,2,2,2,2,2,2,2,2,2,2,2,2,2,2,2,2,4),(-4.0605796293872,
-4.05409653814727,-4.05094574927176,-4.04805958206979,-4.04475364936424,
-4.03944020767741,-4.02258933328322,-3.96312384572504,-3.91146372269416,
-3.89794667649816,-3.89117755144233,-3.88578396873489,-3.87956495193356,
-3.86901801060594,-3.81548323498542,-3.77780937643852,-3.73830672729257,
-3.7318377827319,-3.72828016492804,-3.72520595107168,-3.72118765843364,
-3.71215462673145,-3.66472314858551,-3.62396546582613,-3.59747481512421,
-3.57919480194637,-3.57158696240612,-3.5660328166401,-3.56089772232263,
-3.55249020429396,-3.5303715943021,-3.46043424058787,-3.42098855318837,
-3.41216208958356,-3.40813770658865,-3.40506983786599,-3.40147068841176,
-3.3949909237573,-3.3579464086148,-3.27495018129301,-3.25762678725453,-3.25017394098637,
-3.2446456298785,-3.23947215267957,-3.2308552501926,-3.20726693857718,-3.13871064020466,
-3.09974982394642,-3.09097343904006,-3.0869582952316,-3.08389140175189,
-3.08028623487374,-3.07377900089017,-3.03563950788253,-3.02378990676986,
-2.98525145487083,-2.95665356403366,-2.93734984990228,-2.92958330183846,
-2.92400130200861,-2.91821864982873,-2.90943502643838,-2.884608077925,-2.8171822791253,
-2.77862105721687,-2.76988590975396,-2.76587819919882,-2.762811845006,-2.75920123468644,
-2.75267000458885,-2.713502205214,-2.7028713199414,-2.66429069312906,-2.63562296125547,
-2.61628571449468,-2.6085138464603,-2.60293068291467,-2.59714914719821,
-2.58837180865543,-2.56359502834578,-2.49611955358164,-2.45753996298766,
-2.44880265565485,-2.44479442018048,-2.44172785734091,-2.43811721072124,
-2.43158646864904,-2.39245684384723,-2.34981146838474,-2.30057356491377,
-2.29022508293843,-2.28410754981459,-2.27864633148644,-2.27169017715562,
-2.26049701804941,-2.18099474896332,-2.1330416947955,-2.12639875716953,
-2.12280375566951,-2.11973482762843,-2.11577064317526,-2.1070425078828,
-2.03134880387602,-2.03107347865865),.UNSPECIFIED.);
#3688=B_SPLINE_CURVE_WITH_KNOTS('',3,(#253789,#253790,#253791,#253792,#253793,
#253794,#253795,#253796,#253797,#253798,#253799,#253800,#253801,#253802,
#253803,#253804,#253805,#253806,#253807,#253808,#253809,#253810,#253811,
#253812,#253813,#253814,#253815,#253816,#253817,#253818,#253819,#253820,
#253821,#253822,#253823,#253824,#253825,#253826,#253827,#253828,#253829,
#253830,#253831,#253832,#253833,#253834,#253835,#253836,#253837,#253838,
#253839,#253840,#253841,#253842,#253843,#253844,#253845,#253846,#253847,
#253848,#253849,#253850,#253851,#253852,#253853,#253854,#253855,#253856,
#253857,#253858,#253859,#253860,#253861,#253862,#253863,#253864,#253865,
#253866,#253867,#253868,#253869,#253870,#253871,#253872,#253873,#253874,
#253875,#253876,#253877,#253878,#253879,#253880,#253881,#253882,#253883,
#253884,#253885,#253886,#253887,#253888,#253889,#253890,#253891,#253892,
#253893,#253894,#253895,#253896,#253897,#253898,#253899,#253900,#253901,
#253902,#253903,#253904,#253905,#253906,#253907,#253908,#253909,#253910,
#253911,#253912,#253913,#253914,#253915,#253916,#253917,#253918,#253919,
#253920,#253921,#253922,#253923,#253924,#253925,#253926,#253927,#253928,
#253929,#253930,#253931,#253932,#253933,#253934,#253935,#253936,#253937,
#253938,#253939,#253940,#253941,#253942,#253943,#253944,#253945,#253946,
#253947,#253948,#253949,#253950,#253951,#253952,#253953,#253954,#253955,
#253956,#253957,#253958,#253959,#253960,#253961,#253962,#253963,#253964,
#253965,#253966,#253967,#253968,#253969,#253970,#253971,#253972,#253973,
#253974,#253975,#253976,#253977,#253978,#253979,#253980,#253981,#253982,
#253983,#253984,#253985,#253986,#253987,#253988,#253989,#253990,#253991,
#253992,#253993,#253994,#253995,#253996,#253997,#253998,#253999,#254000,
#254001,#254002,#254003,#254004,#254005,#254006,#254007,#254008,#254009,
#254010,#254011,#254012,#254013,#254014,#254015,#254016),.UNSPECIFIED.,
 .F.,.F.,(4,2,2,2,2,2,2,2,2,2,2,2,2,2,2,2,2,2,2,2,2,2,2,2,2,2,2,2,2,2,2,
2,2,2,2,2,2,2,2,2,2,2,2,2,2,2,2,2,2,2,2,2,2,2,2,2,2,2,2,2,2,2,2,2,2,2,2,
2,2,2,2,2,2,2,2,2,2,2,2,2,2,2,2,2,2,2,2,2,2,2,2,2,2,2,2,2,2,2,2,2,2,2,2,
2,2,2,2,2,2,2,2,2,2,4),(-4.06010073944462,-4.00327381972928,-3.96354321613332,
-3.95382913717875,-3.94793261272819,-3.94257345686202,-3.93573155962147,
-3.92440621706684,-3.84644538263637,-3.81217588003557,-3.80014661742054,
-3.79165397931317,-3.78785687065285,-3.78782741753919,-3.78779774106567,
-3.78776783213994,-3.78773768139857,-3.78770727920272,-3.78767661562042,
-3.78764568041245,-3.78761446301772,-3.78758295253458,-3.78755113770363,
-3.78751900689269,-3.78748654807848,-3.78745374882245,-3.78446082116079,
-3.78091495024047,-3.77445452154205,-3.73152093672186,-3.67108319396295,
-3.65081826413086,-3.6358742218668,-3.62893220238744,-3.62358128586204,
-3.6176902729464,-3.60797748721511,-3.57278083568718,-3.51198929032935,
-3.4780773912706,-3.46992745463897,-3.46608259880066,-3.46337725259315,
-3.4599244489104,-3.45388855361422,-3.42639083462642,-3.375467653324,-3.32658438507309,
-3.31351883544498,-3.30692550601872,-3.30160314019417,-3.29548516284331,
-3.28501958727846,-3.22786620357478,-3.18631516943313,-3.16420952710604,
-3.1507647081687,-3.14608612238395,-3.14296317251842,-3.14014902650046,
-3.1354598512689,-3.12294655100966,-3.03412819164323,-3.01073693376364,
-2.99410510255792,-2.98686475848883,-2.98146714681414,-2.97569927442377,
-2.96657460111911,-2.93760591624089,-2.86688601835713,-2.83238166636915,
-2.82616880991931,-2.82271365554672,-2.81970550700989,-2.81575297569686,
-2.80679421059303,-2.75557752525019,-2.70425262343495,-2.68559656333056,
-2.67155765210389,-2.66477944844609,-2.6594437432434,-2.65345450536128,
-2.64330020421297,-2.60080367279707,-2.52038715406851,-2.50783714237644,
-2.50327974661355,-2.50018274011633,-2.49695169062712,-2.49176663044955,
-2.4754470752176,-2.41644688862484,-2.36654683849256,-2.35099536903007,
-2.34394025165896,-2.33856932025821,-2.3327221861508,-2.32323217569013,
-2.29129199238619,-2.22878774728127,-2.1932389719582,-2.18490191505006,
-2.18101919654915,-2.17802413799751,-2.17447613384317,-2.16801536993754,
-2.127813068444,-2.11636009937467,-2.07437677528396,-2.04861021427306,-2.03076150463163,
-2.03071434728601),.UNSPECIFIED.);
#3689=B_SPLINE_CURVE_WITH_KNOTS('',3,(#254017,#254018,#254019,#254020,#254021,
#254022,#254023,#254024,#254025,#254026,#254027,#254028,#254029,#254030,
#254031,#254032,#254033,#254034,#254035,#254036,#254037,#254038,#254039,
#254040,#254041,#254042,#254043,#254044,#254045,#254046,#254047,#254048,
#254049,#254050,#254051,#254052,#254053,#254054,#254055,#254056,#254057,
#254058,#254059,#254060,#254061,#254062,#254063,#254064,#254065,#254066,
#254067,#254068,#254069,#254070,#254071,#254072,#254073,#254074,#254075,
#254076,#254077,#254078,#254079,#254080,#254081,#254082,#254083,#254084,
#254085,#254086,#254087,#254088,#254089,#254090,#254091,#254092,#254093,
#254094,#254095,#254096,#254097,#254098,#254099,#254100,#254101,#254102,
#254103,#254104,#254105,#254106,#254107,#254108,#254109,#254110,#254111,
#254112,#254113,#254114,#254115,#254116,#254117,#254118,#254119,#254120,
#254121,#254122,#254123,#254124,#254125,#254126,#254127,#254128,#254129,
#254130,#254131,#254132,#254133,#254134,#254135,#254136,#254137,#254138,
#254139,#254140,#254141,#254142,#254143,#254144,#254145,#254146,#254147,
#254148,#254149,#254150,#254151,#254152,#254153,#254154,#254155,#254156,
#254157,#254158,#254159,#254160,#254161,#254162,#254163,#254164,#254165,
#254166,#254167,#254168,#254169,#254170,#254171,#254172,#254173,#254174,
#254175,#254176,#254177,#254178,#254179,#254180,#254181,#254182,#254183,
#254184,#254185,#254186,#254187,#254188,#254189,#254190,#254191,#254192,
#254193,#254194,#254195,#254196,#254197,#254198,#254199,#254200,#254201,
#254202,#254203,#254204,#254205,#254206,#254207,#254208,#254209,#254210,
#254211,#254212,#254213,#254214),.UNSPECIFIED.,.F.,.F.,(4,2,2,2,2,2,2,2,
2,2,2,2,2,2,2,2,2,2,2,2,2,2,2,2,2,2,2,2,2,2,2,2,2,2,2,2,2,2,2,2,2,2,2,2,
2,2,2,2,2,2,2,2,2,2,2,2,2,2,2,2,2,2,2,2,2,2,2,2,2,2,2,2,2,2,2,2,2,2,2,2,
2,2,2,2,2,2,2,2,2,2,2,2,2,2,2,2,2,2,4),(-2.03107347865865,-1.97987140276865,
-1.96935418936223,-1.96314124982904,-1.95774600484078,-1.95096573060103,
-1.93739473676935,-1.91964251984052,-1.87311767327197,-1.81524548508242,
-1.80647004637097,-1.80249736955979,-1.79942770421053,-1.7958388269116,
-1.78922439505932,-1.74309306716707,-1.6647820322584,-1.6504859861263,-1.64356723128021,
-1.63810996876968,-1.63197024785478,-1.62151806627189,-1.56961476231467,
-1.49396957897866,-1.48522263387823,-1.48125497303931,-1.47818557264391,
-1.47459253849214,-1.46795984212665,-1.42069163022611,-1.3403609399169,
-1.32927419322384,-1.3223489672679,-1.3168906606756,-1.31075401261354,-1.30031762959146,
-1.24886537199474,-1.23445353129113,-1.17245050089247,-1.16475124987323,
-1.16088437433675,-1.15775942943671,-1.15444086660573,-1.14906999593193,
-1.12988481612895,-1.09153056410051,-1.02085667034282,-1.00769791181744,
-1.00091296824315,-0.995468306777088,-0.989242551512734,-0.978385278680229,
-0.910769964633354,-0.851601209292436,-0.842842660399556,-0.838873334059304,
-0.835804313932795,-0.832213870076595,-0.82559113737444,-0.778929064482799,
-0.697753264600984,-0.686766790816478,-0.6798713303275,-0.674416387165562,
-0.668262339198706,-0.657743213899477,-0.603856541579402,-0.551966623724773,
-0.526073966225798,-0.519980961073066,-0.516503654286094,-0.51340870629343,
-0.509171369945661,-0.49913246482896,-0.484533614802463,-0.43641812230889,
-0.379164040841241,-0.365641442919304,-0.358779333173023,-0.353325360989467,
-0.347145290395334,-0.336512593794242,-0.278706986746644,-0.22010626409411,
-0.203474162443042,-0.198183901363649,-0.19488245296827,-0.191711808758821,
-0.18702436267922,-0.173953674365784,-0.152858000224886,-0.0816886554492921,
-0.050513571115412,-0.0410564845528834,-0.0351342931714837,-0.0299017612655023,
-0.0245521852369908,-0.0144938878548919,-0.0009418500334415),
 .UNSPECIFIED.);
#3690=B_SPLINE_CURVE_WITH_KNOTS('',3,(#254218,#254219,#254220,#254221,#254222,
#254223,#254224,#254225,#254226,#254227,#254228,#254229,#254230,#254231,
#254232,#254233,#254234,#254235,#254236,#254237,#254238,#254239,#254240,
#254241,#254242,#254243,#254244,#254245,#254246,#254247,#254248,#254249,
#254250,#254251,#254252,#254253,#254254,#254255,#254256,#254257,#254258,
#254259,#254260,#254261,#254262,#254263,#254264,#254265,#254266,#254267,
#254268,#254269,#254270,#254271,#254272,#254273,#254274,#254275,#254276,
#254277,#254278,#254279,#254280,#254281,#254282,#254283,#254284,#254285,
#254286,#254287,#254288,#254289,#254290,#254291,#254292,#254293,#254294,
#254295,#254296,#254297,#254298,#254299,#254300,#254301,#254302,#254303,
#254304,#254305,#254306,#254307,#254308,#254309,#254310,#254311,#254312,
#254313,#254314,#254315,#254316,#254317,#254318,#254319,#254320,#254321,
#254322,#254323,#254324,#254325,#254326,#254327,#254328,#254329,#254330,
#254331,#254332,#254333,#254334,#254335,#254336,#254337,#254338,#254339,
#254340,#254341,#254342,#254343,#254344,#254345,#254346,#254347,#254348,
#254349,#254350,#254351,#254352,#254353,#254354,#254355,#254356,#254357,
#254358,#254359,#254360,#254361,#254362,#254363,#254364,#254365,#254366,
#254367,#254368,#254369,#254370,#254371,#254372,#254373,#254374,#254375,
#254376,#254377,#254378,#254379,#254380,#254381,#254382,#254383,#254384,
#254385,#254386,#254387,#254388,#254389,#254390,#254391,#254392,#254393,
#254394,#254395,#254396,#254397,#254398,#254399,#254400,#254401,#254402,
#254403,#254404,#254405,#254406,#254407,#254408,#254409,#254410,#254411,
#254412,#254413,#254414,#254415,#254416,#254417,#254418,#254419),
 .UNSPECIFIED.,.F.,.F.,(4,3,3,3,3,3,3,3,3,3,3,3,3,3,3,3,3,3,3,3,3,3,3,3,
3,3,3,3,3,3,3,3,3,3,3,3,3,3,3,3,3,3,3,3,3,3,3,3,3,3,3,3,3,3,3,3,3,3,3,3,
3,3,3,3,3,3,3,4),(103.672557568463,103.818264882234,103.911421475433,104.004453418626,
104.097388222185,104.190256550746,104.283090631506,104.375915182229,104.468754906163,
104.561693127135,104.654683645779,104.747826170789,104.813093341946,104.906094866231,
104.998971156067,105.091749927756,105.184462290313,105.277140494718,105.369809440183,
105.462494011671,105.555278725024,105.648116417002,105.741108778493,105.807921801659,
105.901228431653,105.994409634355,106.087492733004,106.180507314493,106.273486338418,
106.366454353206,106.459435891529,106.552512528404,106.645639768258,106.738914907065,
106.802750261371,106.896007663259,106.989142157043,107.082181088458,107.175155441427,
107.268096669001,107.36102934722,107.453978038381,107.547025821459,107.640126395497,
107.733378630147,107.797578721083,107.889714279306,107.981724267907,108.073637374533,
108.165488259454,108.257307641196,108.349121268857,108.440954881136,108.53290045036,
108.62490406731,108.717079415847,108.792407180795,108.88812029801,108.983691451607,
109.08413447522,109.17946841731,109.274736986051,109.369960264623,109.465158289751,
109.560375980784,109.655603167526,109.750891777179,109.787235640508),
 .UNSPECIFIED.);
#3691=B_SPLINE_CURVE_WITH_KNOTS('',3,(#254420,#254421,#254422,#254423,#254424,
#254425,#254426,#254427,#254428,#254429,#254430,#254431,#254432,#254433,
#254434,#254435,#254436,#254437,#254438,#254439,#254440,#254441,#254442,
#254443,#254444,#254445,#254446,#254447,#254448,#254449,#254450,#254451,
#254452,#254453,#254454,#254455,#254456,#254457,#254458,#254459,#254460,
#254461,#254462,#254463,#254464,#254465,#254466,#254467,#254468,#254469,
#254470,#254471,#254472,#254473,#254474,#254475,#254476,#254477,#254478,
#254479,#254480,#254481,#254482,#254483,#254484,#254485,#254486,#254487,
#254488,#254489,#254490,#254491,#254492,#254493,#254494,#254495,#254496,
#254497,#254498,#254499,#254500,#254501,#254502,#254503,#254504,#254505,
#254506,#254507,#254508,#254509,#254510,#254511,#254512,#254513,#254514,
#254515,#254516,#254517,#254518,#254519,#254520,#254521,#254522,#254523,
#254524,#254525,#254526,#254527,#254528,#254529,#254530,#254531,#254532,
#254533,#254534,#254535,#254536,#254537,#254538,#254539,#254540,#254541,
#254542,#254543,#254544,#254545,#254546,#254547,#254548,#254549,#254550,
#254551,#254552,#254553,#254554,#254555,#254556,#254557,#254558,#254559,
#254560,#254561,#254562,#254563,#254564,#254565,#254566,#254567,#254568,
#254569,#254570,#254571,#254572,#254573,#254574,#254575,#254576,#254577,
#254578,#254579,#254580,#254581,#254582,#254583,#254584,#254585,#254586,
#254587,#254588,#254589,#254590,#254591,#254592,#254593,#254594,#254595,
#254596,#254597,#254598,#254599,#254600,#254601,#254602,#254603,#254604,
#254605,#254606,#254607,#254608,#254609,#254610,#254611,#254612,#254613,
#254614,#254615,#254616,#254617,#254618,#254619,#254620,#254621,#254622,
#254623,#254624,#254625,#254626,#254627),.UNSPECIFIED.,.F.,.F.,(4,3,3,3,
3,3,3,3,3,3,3,3,3,3,3,3,3,3,3,3,3,3,3,3,3,3,3,3,3,3,3,3,3,3,3,3,3,3,3,3,
3,3,3,3,3,3,3,3,3,3,3,3,3,3,3,3,3,3,3,3,3,3,3,3,3,3,3,3,3,4),(103.672557568638,
103.775261298986,103.878304277879,103.981841562232,104.067724430369,104.160884025681,
104.253918755596,104.346856130719,104.439726668314,104.532562751129,104.625389096472,
104.71823040696,104.811169702776,104.904161123854,104.997303785972,105.061837443301,
105.155002762704,105.24804360184,105.340987457664,105.433864999584,105.526708405513,
105.619542381756,105.712391620173,105.805339248105,105.89833923927,105.991490764735,
106.055950456232,106.148960347062,106.241845173368,106.334632639107,106.427353861026,
106.520041040157,106.612719065257,106.705412810912,106.79820660008,106.891053440063,
106.984054484014,107.050063469163,107.143377911911,107.236567096213,107.329658332532,
107.422681216068,107.51566865497,107.608645186738,107.701635333198,107.794720482451,
107.887856302815,107.98113957308,108.044176482095,108.137443386498,108.230587553017,
108.323636312462,108.416620648389,108.509571966454,108.602514829852,108.695473788108,
108.78853171488,108.881642489695,108.974904434524,109.038289495026,109.129533207633,
109.220652399344,109.31253870885,109.403501420215,109.494435465899,109.585367240415,
109.677961149161,109.769019124106,109.862380999752,109.955742875397),
 .UNSPECIFIED.);
#3692=B_SPLINE_CURVE_WITH_KNOTS('',3,(#254631,#254632,#254633,#254634,#254635,
#254636),.UNSPECIFIED.,.F.,.F.,(4,1,1,4),(-4.09274904019424,-3.97645205172536,
-2.98233903879402,-2.06157629883971),.UNSPECIFIED.);
#3693=B_SPLINE_CURVE_WITH_KNOTS('',3,(#254640,#254641,#254642,#254643,#254644),
 .UNSPECIFIED.,.F.,.F.,(4,1,4),(0.,0.994828459712242,1.11004521091125),
 .UNSPECIFIED.);
#3694=B_SPLINE_CURVE_WITH_KNOTS('',3,(#254646,#254647,#254648,#254649,#254650,
#254651,#254652,#254653,#254654,#254655,#254656,#254657,#254658,#254659,
#254660,#254661,#254662,#254663,#254664,#254665,#254666,#254667,#254668,
#254669,#254670,#254671,#254672,#254673,#254674,#254675,#254676,#254677,
#254678,#254679,#254680,#254681,#254682,#254683,#254684,#254685,#254686,
#254687,#254688,#254689,#254690,#254691,#254692,#254693,#254694,#254695,
#254696,#254697,#254698,#254699,#254700,#254701,#254702,#254703,#254704,
#254705,#254706,#254707,#254708,#254709,#254710,#254711,#254712,#254713,
#254714,#254715,#254716,#254717,#254718,#254719,#254720,#254721,#254722,
#254723,#254724,#254725,#254726,#254727,#254728,#254729,#254730,#254731,
#254732,#254733,#254734,#254735,#254736,#254737,#254738,#254739,#254740,
#254741,#254742,#254743,#254744,#254745,#254746,#254747,#254748,#254749,
#254750,#254751,#254752,#254753,#254754,#254755,#254756,#254757,#254758,
#254759,#254760,#254761,#254762,#254763,#254764,#254765,#254766,#254767,
#254768,#254769,#254770,#254771,#254772,#254773,#254774,#254775,#254776,
#254777,#254778,#254779,#254780,#254781,#254782,#254783,#254784,#254785,
#254786,#254787,#254788,#254789,#254790,#254791,#254792,#254793,#254794,
#254795,#254796,#254797,#254798,#254799,#254800,#254801,#254802,#254803,
#254804,#254805,#254806,#254807,#254808,#254809,#254810,#254811,#254812,
#254813,#254814,#254815,#254816,#254817,#254818,#254819,#254820,#254821,
#254822,#254823,#254824,#254825,#254826,#254827,#254828,#254829,#254830,
#254831,#254832,#254833,#254834,#254835,#254836,#254837,#254838,#254839,
#254840,#254841,#254842,#254843,#254844,#254845,#254846,#254847,#254848,
#254849,#254850,#254851,#254852,#254853,#254854,#254855,#254856,#254857,
#254858,#254859,#254860,#254861,#254862,#254863,#254864,#254865,#254866,
#254867,#254868,#254869,#254870,#254871,#254872,#254873,#254874),
 .UNSPECIFIED.,.F.,.F.,(4,3,3,3,3,3,3,3,3,3,3,3,3,3,3,3,3,3,3,3,3,3,3,3,
3,3,3,3,3,3,3,3,3,3,3,3,3,3,3,3,3,3,3,3,3,3,3,3,3,3,3,3,3,3,3,3,3,3,3,3,
3,3,3,3,3,3,3,3,3,3,3,3,3,3,3,3,4),(1.11004521091125,1.19658618195254,1.28302206104525,
1.37135141834266,1.45765852628216,1.54394367013426,1.63022970115781,1.72008650572448,
1.8064919221077,1.89295545020592,1.97954245262436,1.9896569194245,2.07839354757622,
2.16701659509698,2.25554962299147,2.34666659250964,2.43509828185352,2.5235164115662,
2.61194213703314,2.70039661379871,2.78894866238135,2.87755943927535,2.96629553894112,
2.98448537913676,3.0732431575045,3.16189000871733,3.2504494542818,3.3415575023527,
3.43002198667484,3.51847523453205,3.60693837515941,3.70003224108181,3.78862983616903,
3.87728906280227,3.96607484431248,3.97931383884901,4.06780433717442,4.15617965886143,
4.24446368224824,4.33567350928737,4.42385463612318,4.51202206901021,4.6001972411382,
4.6884015861779,4.77670539429878,4.86506874564576,4.95356048372003,4.97414229856127,
5.0627748690265,5.15129384270911,5.23972291607954,5.33087889635379,5.41920764213421,
5.50752339531487,5.59584743246272,5.68420103088712,5.77265392246731,5.86116643802116,
5.94980632727041,5.96897075827352,6.05759525793551,6.14610639539864,6.23452787596184,
6.32568679371483,6.41400860712589,6.50231768646847,6.59063531702913,6.67898278504305,
6.76742998783123,6.85593706670144,6.94457192822607,6.96379921798578,7.06027097853904,
7.15639479474065,7.25229694340983,7.34786388506623,7.39323051792991),
 .UNSPECIFIED.);
#3695=B_SPLINE_CURVE_WITH_KNOTS('',3,(#254876,#254877,#254878,#254879,#254880,
#254881,#254882,#254883,#254884,#254885,#254886,#254887,#254888,#254889,
#254890,#254891,#254892,#254893,#254894,#254895,#254896,#254897,#254898,
#254899,#254900,#254901,#254902,#254903,#254904,#254905,#254906,#254907,
#254908,#254909,#254910,#254911,#254912,#254913,#254914,#254915,#254916,
#254917,#254918,#254919,#254920,#254921,#254922,#254923,#254924,#254925,
#254926,#254927,#254928,#254929,#254930,#254931,#254932,#254933,#254934,
#254935,#254936,#254937,#254938,#254939,#254940,#254941,#254942,#254943,
#254944,#254945,#254946,#254947,#254948,#254949,#254950,#254951,#254952,
#254953,#254954,#254955,#254956,#254957,#254958,#254959,#254960,#254961,
#254962,#254963,#254964,#254965,#254966,#254967,#254968,#254969,#254970,
#254971,#254972,#254973,#254974,#254975,#254976,#254977,#254978,#254979,
#254980,#254981,#254982,#254983,#254984,#254985,#254986,#254987,#254988,
#254989,#254990,#254991,#254992,#254993,#254994,#254995,#254996,#254997,
#254998,#254999,#255000,#255001,#255002,#255003,#255004,#255005,#255006,
#255007,#255008,#255009,#255010,#255011,#255012,#255013,#255014,#255015,
#255016,#255017,#255018,#255019,#255020,#255021,#255022,#255023,#255024,
#255025,#255026,#255027,#255028,#255029,#255030,#255031,#255032,#255033,
#255034,#255035,#255036,#255037,#255038,#255039,#255040,#255041,#255042,
#255043,#255044,#255045,#255046,#255047,#255048,#255049,#255050,#255051,
#255052,#255053,#255054,#255055,#255056,#255057,#255058,#255059,#255060,
#255061,#255062,#255063,#255064,#255065,#255066,#255067,#255068,#255069,
#255070,#255071,#255072,#255073,#255074,#255075,#255076,#255077,#255078,
#255079,#255080,#255081,#255082,#255083,#255084,#255085,#255086,#255087,
#255088,#255089,#255090,#255091,#255092,#255093,#255094,#255095,#255096,
#255097,#255098,#255099,#255100,#255101,#255102,#255103,#255104),
 .UNSPECIFIED.,.F.,.F.,(4,3,3,3,3,3,3,3,3,3,3,3,3,3,3,3,3,3,3,3,3,3,3,3,
3,3,3,3,3,3,3,3,3,3,3,3,3,3,3,3,3,3,3,3,3,3,3,3,3,3,3,3,3,3,3,3,3,3,3,3,
3,3,3,3,3,3,3,3,3,3,3,3,3,3,3,3,4),(7.39323051809083,7.48347022309097,7.57375978939412,
7.66411673584461,7.75462047802957,7.84520966702015,7.93595807272466,7.95862767769803,
8.04723962034107,8.13573789041722,8.22414621052771,8.31530995138803,8.40361795631955,
8.49191300997709,8.58021641201351,8.66854946288955,8.75698204080424,8.84547435567409,
8.93409436213729,8.95345613741028,9.04206509863056,9.13056039468739,9.2189657518448,
9.31013060750452,9.39843569670434,9.48672785736798,9.57502839244658,9.6633586057217,
9.75178840399521,9.84027796987582,9.92889529292322,9.94828459712254,10.0368893664816,
10.1253803957387,10.2137814167579,10.3049478717675,10.3932484794336,10.4815361122486,
10.5698320779018,10.6581576848853,10.7465828452453,10.8350677491512,10.9236804104514,
10.9431130568348,11.0317210210924,11.120215285819,11.2086195786997,11.2997848209307,
11.3880887702342,11.4763797648196,11.5646791087858,11.6530081070455,11.7414366608764,
11.829924963588,11.9185410057114,11.937941516547,12.0265488062092,12.1150423936802,
12.2034460074971,12.2946115035923,12.3829147737558,12.4712050903673,12.5595037582774,
12.6478320831516,12.7362599709608,12.8247476111719,12.9133630009563,12.9327699762593,
13.0203928491707,13.1078750269985,13.1952767025933,13.2826202103428,13.3699278286532,
13.4572453849245,13.5445677094498,13.63195244959,13.6764158252704),
 .UNSPECIFIED.);
#3696=B_SPLINE_CURVE_WITH_KNOTS('',3,(#255106,#255107,#255108,#255109,#255110,
#255111,#255112,#255113,#255114,#255115,#255116,#255117,#255118,#255119,
#255120,#255121,#255122,#255123,#255124,#255125,#255126,#255127,#255128,
#255129,#255130,#255131,#255132,#255133,#255134,#255135,#255136,#255137,
#255138,#255139,#255140,#255141,#255142,#255143,#255144,#255145,#255146,
#255147,#255148,#255149,#255150,#255151,#255152,#255153,#255154,#255155,
#255156,#255157,#255158,#255159,#255160,#255161,#255162,#255163,#255164,
#255165,#255166,#255167,#255168,#255169,#255170,#255171,#255172,#255173,
#255174,#255175,#255176,#255177,#255178,#255179,#255180,#255181,#255182,
#255183,#255184,#255185,#255186,#255187,#255188,#255189,#255190,#255191,
#255192,#255193,#255194,#255195,#255196,#255197,#255198,#255199,#255200,
#255201,#255202,#255203,#255204,#255205,#255206,#255207,#255208,#255209,
#255210,#255211,#255212,#255213,#255214,#255215,#255216,#255217,#255218,
#255219,#255220,#255221,#255222,#255223,#255224,#255225,#255226,#255227,
#255228,#255229,#255230,#255231,#255232,#255233,#255234,#255235,#255236,
#255237,#255238,#255239,#255240,#255241,#255242,#255243,#255244,#255245,
#255246,#255247,#255248,#255249,#255250,#255251,#255252,#255253,#255254,
#255255,#255256,#255257,#255258,#255259,#255260,#255261,#255262,#255263,
#255264,#255265,#255266,#255267,#255268,#255269,#255270,#255271,#255272,
#255273,#255274,#255275,#255276,#255277,#255278,#255279,#255280,#255281,
#255282,#255283,#255284,#255285,#255286,#255287,#255288,#255289,#255290,
#255291,#255292,#255293,#255294,#255295,#255296,#255297,#255298,#255299,
#255300,#255301,#255302,#255303,#255304,#255305,#255306,#255307,#255308,
#255309,#255310,#255311,#255312,#255313,#255314,#255315,#255316,#255317,
#255318,#255319,#255320,#255321,#255322,#255323,#255324,#255325,#255326,
#255327,#255328,#255329,#255330,#255331,#255332,#255333,#255334),
 .UNSPECIFIED.,.F.,.F.,(4,3,3,3,3,3,3,3,3,3,3,3,3,3,3,3,3,3,3,3,3,3,3,3,
3,3,3,3,3,3,3,3,3,3,3,3,3,3,3,3,3,3,3,3,3,3,3,3,3,3,3,3,3,3,3,3,3,3,3,3,
3,3,3,3,3,3,3,3,3,3,3,3,3,3,3,3,4),(13.676415825492,13.7891574344351,13.9043053450487,
13.9275984359716,14.016205699341,14.1046992571262,14.1931028379146,14.2842683451358,
14.372571574107,14.4608618465555,14.5491604673653,14.6374887422324,14.7259165759653,
14.8144041596502,14.9030194897623,14.9224268956838,15.0110340298656,15.0995274575668,
15.1879309075392,15.2790964635213,15.3673995607014,15.4556897012271,15.5439881901263,
15.6323163332399,15.7207440361164,15.8092314893145,15.8978466904685,15.9172553553961,
16.0058624376068,16.0943558121718,16.1827592079139,16.2739247838132,16.3622278243749,
16.4505179074917,16.5388163382506,16.6271444225509,16.7155720659096,16.804059459106,
16.8926746000073,16.9120838151083,17.0006909620515,17.0891844022555,17.1775878644579,
17.2687534157532,17.3570565243985,17.4453466760841,17.5336451758243,17.6219733294457,
17.7104010422817,17.7988885051298,17.8875037154091,17.9069122748205,17.9955193991191,
18.0840128164805,18.1724162556715,18.2635818155292,18.3518849008906,18.4401750292317,
18.5284735055923,18.6168016358241,18.7052293253736,18.7937167649678,18.8823319522173,
18.9017407345328,18.9903478540733,19.0788412665423,19.1672447007132,19.2584102624047,
19.3467133424586,19.4350034653947,19.5233019362577,19.6116300609052,19.7000577447692,
19.7885451786117,19.8771603600567,19.896569194245,19.95960113245),
 .UNSPECIFIED.);
#3697=B_SPLINE_CURVE_WITH_KNOTS('',3,(#255336,#255337,#255338,#255339,#255340,
#255341,#255342,#255343,#255344,#255345,#255346,#255347,#255348,#255349,
#255350,#255351,#255352,#255353,#255354,#255355,#255356,#255357,#255358,
#255359,#255360,#255361,#255362,#255363,#255364,#255365,#255366,#255367,
#255368,#255369,#255370,#255371,#255372,#255373,#255374,#255375,#255376,
#255377,#255378,#255379,#255380,#255381,#255382,#255383,#255384,#255385,
#255386,#255387,#255388,#255389,#255390,#255391,#255392,#255393,#255394,
#255395,#255396,#255397,#255398,#255399,#255400,#255401,#255402,#255403,
#255404,#255405,#255406,#255407,#255408,#255409,#255410,#255411,#255412,
#255413,#255414,#255415,#255416,#255417,#255418,#255419,#255420,#255421,
#255422,#255423,#255424,#255425,#255426,#255427,#255428,#255429,#255430,
#255431,#255432,#255433,#255434,#255435,#255436,#255437,#255438,#255439,
#255440,#255441,#255442,#255443,#255444,#255445,#255446,#255447,#255448,
#255449,#255450,#255451,#255452,#255453,#255454,#255455,#255456,#255457,
#255458,#255459,#255460,#255461,#255462,#255463,#255464,#255465,#255466,
#255467,#255468,#255469,#255470,#255471,#255472,#255473,#255474,#255475,
#255476,#255477,#255478,#255479,#255480,#255481,#255482,#255483,#255484,
#255485,#255486,#255487,#255488,#255489,#255490,#255491,#255492,#255493,
#255494,#255495,#255496,#255497,#255498,#255499,#255500,#255501,#255502,
#255503,#255504,#255505,#255506,#255507,#255508,#255509,#255510,#255511,
#255512,#255513,#255514,#255515,#255516,#255517,#255518,#255519,#255520,
#255521,#255522,#255523,#255524,#255525,#255526,#255527,#255528,#255529,
#255530,#255531,#255532,#255533,#255534,#255535,#255536,#255537,#255538,
#255539,#255540,#255541,#255542,#255543,#255544,#255545,#255546,#255547,
#255548,#255549,#255550,#255551,#255552,#255553,#255554,#255555,#255556,
#255557,#255558,#255559,#255560,#255561),.UNSPECIFIED.,.F.,.F.,(4,3,3,3,
3,3,3,3,3,3,3,3,3,3,3,3,3,3,3,3,3,3,3,3,3,3,3,3,3,3,3,3,3,3,3,3,3,3,3,3,
3,3,3,3,3,3,3,3,3,3,3,3,3,3,3,3,3,3,3,3,3,3,3,3,3,3,3,3,3,3,3,3,3,3,3,4),
(19.9596011326339,20.0473762095346,20.1350428488705,20.2226256406632,20.3101531325818,
20.3976527830734,20.4851466858016,20.5726569253986,20.6602579030711,20.7479081347566,
20.8356943412198,20.8913976539573,20.9800047786225,21.0684981963089,21.1569016357831,
21.2480671955189,21.3363702810569,21.4246604095348,21.5129588859916,21.6012870162792,
21.6897147058233,21.7782021453768,21.8668173325332,21.8862261136696,21.9748332380488,
22.0633266554348,22.151730094595,22.2428956544434,22.3311987396352,22.4194888677553,
22.5077873438435,22.596115473751,22.6845431629013,22.773030602052,22.8616457887963,
22.8810545733818,22.9696616989445,23.0581551175325,23.1465585579113,23.2377241173092,
23.3260272037533,23.4143173331362,23.5026158104959,23.5909439416836,23.6793716321186,
23.7678590725585,23.856474260589,23.8758830330941,23.9644901580618,24.0529835760482,
24.1413870158199,24.2325525754432,24.3208556612698,24.4091457900321,24.4974442667698,
24.5857723973327,24.6742000871445,24.7626875269612,24.8513027143727,24.8707114928063,
24.9593186177899,25.0478120357911,25.1362154755763,25.227381035194,25.3156841210307,
25.4039742498019,25.4922727265469,25.5806008571162,25.6690285469324,25.7575159867526,
25.8461311741657,25.8655399525186,25.9654106279957,26.0649637746012,26.1639285591376,
26.2427864394061),.UNSPECIFIED.);
#3698=B_SPLINE_CURVE_WITH_KNOTS('',3,(#255563,#255564,#255565,#255566,#255567,
#255568,#255569,#255570,#255571,#255572,#255573,#255574,#255575,#255576,
#255577,#255578,#255579,#255580,#255581,#255582,#255583,#255584,#255585,
#255586,#255587,#255588,#255589,#255590,#255591,#255592,#255593,#255594,
#255595,#255596,#255597,#255598,#255599,#255600,#255601,#255602,#255603,
#255604,#255605,#255606,#255607,#255608,#255609,#255610,#255611,#255612,
#255613,#255614,#255615,#255616,#255617,#255618,#255619,#255620,#255621,
#255622,#255623,#255624,#255625,#255626,#255627,#255628,#255629,#255630,
#255631,#255632,#255633,#255634,#255635,#255636,#255637,#255638,#255639,
#255640,#255641,#255642,#255643,#255644,#255645,#255646,#255647,#255648,
#255649,#255650,#255651,#255652,#255653,#255654,#255655,#255656,#255657,
#255658,#255659,#255660,#255661,#255662,#255663,#255664,#255665,#255666,
#255667,#255668,#255669,#255670,#255671,#255672,#255673,#255674,#255675,
#255676,#255677,#255678,#255679,#255680,#255681,#255682,#255683,#255684,
#255685,#255686,#255687,#255688,#255689,#255690,#255691,#255692,#255693,
#255694,#255695,#255696,#255697,#255698,#255699,#255700,#255701,#255702,
#255703,#255704,#255705,#255706,#255707,#255708,#255709,#255710,#255711,
#255712,#255713,#255714,#255715,#255716,#255717,#255718,#255719,#255720,
#255721,#255722,#255723,#255724,#255725,#255726,#255727,#255728,#255729,
#255730,#255731,#255732,#255733,#255734,#255735,#255736,#255737,#255738,
#255739,#255740,#255741,#255742,#255743,#255744,#255745,#255746,#255747,
#255748,#255749,#255750,#255751,#255752,#255753,#255754,#255755,#255756,
#255757,#255758,#255759,#255760,#255761,#255762,#255763,#255764,#255765,
#255766,#255767,#255768,#255769,#255770,#255771,#255772,#255773,#255774,
#255775,#255776,#255777,#255778,#255779,#255780,#255781,#255782,#255783,
#255784,#255785,#255786,#255787,#255788),.UNSPECIFIED.,.F.,.F.,(4,3,3,3,
3,3,3,3,3,3,3,3,3,3,3,3,3,3,3,3,3,3,3,3,3,3,3,3,3,3,3,3,3,3,3,3,3,3,3,3,
3,3,3,3,3,3,3,3,3,3,3,3,3,3,3,3,3,3,3,3,3,3,3,3,3,3,3,3,3,3,3,3,3,3,3,4),
(26.2427864396296,26.3318193218316,26.4208635005913,26.5099390761185,26.5991295140694,
26.6883785209592,26.7777899169144,26.8603684122308,26.9489755372762,27.0374689553405,
27.1258723951899,27.217037954784,27.305341040688,27.3936311695276,27.4819296463415,
27.5702577769808,27.6586854668681,27.7471729067595,27.8357880942444,27.8551968719431,
27.9438039969987,28.032297415073,28.1207008549323,28.2118664145227,28.3001695004365,
28.3884596292859,28.4767581061098,28.5650862367584,28.6535139266547,28.7420013665553,
28.830616554049,28.8500253316553,28.9386324567299,29.0271258748237,29.1155293147029,
29.206694874286,29.2949979602201,29.3832880890899,29.4715865659343,29.5599146966042,
29.6483423865216,29.7368298264431,29.825445013958,29.8448537913676,29.9334609164285,
30.0219543345085,30.1103577743733,30.2015233339616,30.2898264198815,30.3781165487372,
30.4664150255671,30.5547431562226,30.6431708461254,30.7316582860327,30.8202734735329,
30.8396822510798,30.9282893761434,31.016782794226,31.1051862340936,31.1963517936809,
31.2846548796033,31.3729450084614,31.4612434852935,31.5495716159513,31.6379993058566,
31.7264867457661,31.8151019332689,31.8345107107921,31.9226441977953,32.0106702726248,
32.0986108681665,32.1864878426814,32.2743354198353,32.3621629675877,32.4500259983624,
32.5259717468092),.UNSPECIFIED.);
#3699=B_SPLINE_CURVE_WITH_KNOTS('',3,(#255790,#255791,#255792,#255793,#255794,
#255795,#255796,#255797,#255798,#255799,#255800,#255801,#255802,#255803,
#255804,#255805,#255806,#255807,#255808,#255809,#255810,#255811,#255812,
#255813,#255814,#255815,#255816,#255817,#255818,#255819,#255820,#255821,
#255822,#255823,#255824,#255825,#255826,#255827,#255828,#255829,#255830,
#255831,#255832,#255833,#255834,#255835,#255836,#255837,#255838,#255839,
#255840,#255841,#255842,#255843,#255844,#255845,#255846,#255847,#255848,
#255849,#255850,#255851,#255852,#255853,#255854,#255855,#255856,#255857,
#255858,#255859,#255860,#255861,#255862,#255863,#255864,#255865,#255866,
#255867,#255868,#255869,#255870,#255871,#255872,#255873,#255874,#255875,
#255876,#255877,#255878,#255879,#255880,#255881,#255882,#255883,#255884,
#255885,#255886,#255887,#255888,#255889,#255890,#255891,#255892,#255893,
#255894,#255895,#255896,#255897,#255898,#255899,#255900,#255901,#255902,
#255903,#255904,#255905,#255906,#255907,#255908,#255909,#255910,#255911,
#255912,#255913,#255914,#255915,#255916,#255917,#255918,#255919,#255920,
#255921,#255922,#255923,#255924,#255925,#255926,#255927,#255928,#255929,
#255930,#255931,#255932,#255933,#255934,#255935,#255936,#255937,#255938,
#255939,#255940,#255941,#255942,#255943,#255944,#255945,#255946,#255947,
#255948,#255949,#255950,#255951,#255952,#255953,#255954,#255955,#255956,
#255957,#255958,#255959,#255960,#255961,#255962,#255963,#255964,#255965,
#255966,#255967,#255968,#255969,#255970,#255971,#255972,#255973,#255974,
#255975,#255976,#255977,#255978,#255979,#255980,#255981,#255982,#255983,
#255984,#255985,#255986,#255987,#255988,#255989,#255990,#255991,#255992,
#255993,#255994,#255995,#255996,#255997,#255998,#255999,#256000,#256001,
#256002,#256003,#256004,#256005,#256006,#256007,#256008,#256009,#256010,
#256011,#256012,#256013,#256014,#256015,#256016,#256017,#256018),
 .UNSPECIFIED.,.F.,.F.,(4,3,3,3,3,3,3,3,3,3,3,3,3,3,3,3,3,3,3,3,3,3,3,3,
3,3,3,3,3,3,3,3,3,3,3,3,3,3,3,3,3,3,3,3,3,3,3,3,3,3,3,3,3,3,3,3,3,3,3,3,
3,3,3,3,3,3,3,3,3,3,3,3,3,3,3,3,4),(32.5259717469845,32.6316063770899,32.7385526087099,
32.8293391705043,32.9179462955682,33.0064397136512,33.0948431535192,33.1860087131064,
33.2743117990292,33.3626019278877,33.4509004047208,33.5392285353792,33.6276562252851,
33.716143665195,33.8047588526984,33.8241676302166,33.9127747552809,34.0012681733644,
34.089671613233,34.18083717282,34.2691402587434,34.3574303876023,34.4457288644357,
34.5340569950947,34.622484685001,34.7109721249114,34.7995873124152,34.8189960899289,
34.9076032149935,34.9960966330771,35.0845000729459,35.1756656325328,35.2639687184563,
35.3522588473155,35.4405573241492,35.5288854548083,35.6173131447149,35.7058005846256,
35.7944157721296,35.8138245496411,35.9024316747054,35.9909250927888,36.0793285326574,
36.1704940922444,36.2587971781677,36.3470873070266,36.43538578386,36.5237139145189,
36.6121416044252,36.7006290443357,36.7892442318394,36.8086530093534,36.8972601344178,
36.9857535525013,37.07415699237,37.1653225519569,37.2536256378803,37.3419157667393,
37.4302142435728,37.5185423742318,37.6069700641382,37.6954575040487,37.7840726915525,
37.8034814690656,37.89208859413,37.9805820122135,38.0689854520821,38.1601510116691,
38.2484540975925,38.3367442264515,38.4250427032849,38.5133708339439,38.6017985238503,
38.690285963761,38.7789011512648,38.7983099287779,38.8091570539888),
 .UNSPECIFIED.);
#3700=B_SPLINE_CURVE_WITH_KNOTS('',3,(#256020,#256021,#256022,#256023,#256024,
#256025,#256026,#256027,#256028,#256029,#256030,#256031,#256032,#256033,
#256034,#256035,#256036,#256037,#256038,#256039,#256040,#256041,#256042,
#256043,#256044,#256045,#256046,#256047,#256048,#256049,#256050,#256051,
#256052,#256053,#256054,#256055,#256056,#256057,#256058,#256059,#256060,
#256061,#256062,#256063,#256064,#256065,#256066,#256067,#256068,#256069,
#256070,#256071,#256072,#256073,#256074,#256075,#256076,#256077,#256078,
#256079,#256080,#256081,#256082,#256083,#256084,#256085,#256086,#256087,
#256088,#256089,#256090,#256091,#256092,#256093,#256094,#256095,#256096,
#256097,#256098,#256099,#256100,#256101,#256102,#256103,#256104,#256105,
#256106,#256107,#256108,#256109,#256110,#256111,#256112,#256113,#256114,
#256115,#256116,#256117,#256118,#256119,#256120,#256121,#256122,#256123,
#256124,#256125,#256126,#256127,#256128,#256129,#256130,#256131,#256132,
#256133,#256134,#256135,#256136,#256137,#256138,#256139,#256140,#256141,
#256142,#256143,#256144,#256145,#256146,#256147,#256148,#256149,#256150,
#256151,#256152,#256153,#256154,#256155,#256156,#256157,#256158,#256159,
#256160,#256161,#256162,#256163,#256164,#256165,#256166,#256167,#256168,
#256169,#256170,#256171,#256172,#256173,#256174,#256175,#256176,#256177,
#256178,#256179,#256180,#256181,#256182,#256183,#256184,#256185,#256186,
#256187,#256188,#256189,#256190,#256191,#256192,#256193,#256194,#256195,
#256196,#256197,#256198,#256199,#256200,#256201,#256202,#256203,#256204,
#256205,#256206,#256207,#256208,#256209,#256210,#256211,#256212,#256213,
#256214,#256215,#256216,#256217,#256218,#256219,#256220,#256221,#256222,
#256223,#256224,#256225,#256226,#256227,#256228,#256229,#256230,#256231,
#256232,#256233,#256234,#256235,#256236,#256237,#256238,#256239,#256240,
#256241,#256242,#256243,#256244,#256245),.UNSPECIFIED.,.F.,.F.,(4,3,3,3,
3,3,3,3,3,3,3,3,3,3,3,3,3,3,3,3,3,3,3,3,3,3,3,3,3,3,3,3,3,3,3,3,3,3,3,3,
3,3,3,3,3,3,3,3,3,3,3,3,3,3,3,3,3,3,3,3,3,3,3,3,3,3,3,3,3,3,3,3,3,3,3,4),
(38.8091570541465,38.897595286393,38.9859200585766,39.0741553025263,39.1640281882718,
39.2521650539386,39.3402896600519,39.4284234933862,39.5196022171622,39.6078681861544,
39.7005032873222,39.7931383884901,39.8817455135546,39.9702389316381,40.0586423715069,
40.1498079310938,40.2381110170172,40.3264011458762,40.4146996227097,40.5030277533687,
40.5914554432752,40.6799428831856,40.7685580706896,40.7879668482024,40.8765739732668,
40.9650673913502,41.0534708312188,41.1446363908058,41.2329394767291,41.3212296055882,
41.4095280824215,41.4978562130806,41.5862839029871,41.6747713428978,41.7633865304015,
41.7827953079146,41.871402432979,41.9598958510626,42.0482992909313,42.1394648505183,
42.2277679364417,42.3160580653006,42.4043565421341,42.492684672793,42.5811123626994,
42.6695998026096,42.7582149901136,42.7776237676269,42.8662308926912,42.9547243107747,
43.0431277506435,43.1342933102305,43.2225963961537,43.3108865250126,43.3991850018458,
43.4875131325044,43.5759408224108,43.6644282623213,43.7530434498251,43.7724522273391,
43.8610593524037,43.9495527704867,44.0379562103554,44.1291217699424,44.2174248558657,
44.3057149847247,44.3940134615584,44.4823415922176,44.5707692821241,44.6592567220348,
44.7478719095386,44.7672806870514,44.8719117025869,44.9760047942364,45.0791547761021,
45.0923423609627),.UNSPECIFIED.);
#3701=B_SPLINE_CURVE_WITH_KNOTS('',3,(#256247,#256248,#256249,#256250,#256251,
#256252,#256253,#256254,#256255,#256256,#256257,#256258,#256259,#256260,
#256261,#256262,#256263,#256264,#256265,#256266,#256267,#256268,#256269,
#256270,#256271,#256272,#256273,#256274,#256275,#256276,#256277,#256278,
#256279,#256280,#256281,#256282,#256283,#256284,#256285,#256286,#256287,
#256288,#256289,#256290,#256291,#256292,#256293,#256294,#256295,#256296,
#256297,#256298,#256299,#256300,#256301,#256302,#256303,#256304,#256305,
#256306,#256307,#256308,#256309,#256310,#256311,#256312,#256313,#256314,
#256315,#256316,#256317,#256318,#256319,#256320,#256321,#256322,#256323,
#256324,#256325,#256326,#256327,#256328,#256329,#256330,#256331,#256332,
#256333,#256334,#256335,#256336,#256337,#256338,#256339,#256340,#256341,
#256342,#256343,#256344,#256345,#256346,#256347,#256348,#256349,#256350,
#256351,#256352,#256353,#256354,#256355,#256356,#256357,#256358,#256359,
#256360,#256361,#256362,#256363,#256364,#256365,#256366,#256367,#256368,
#256369,#256370,#256371,#256372,#256373,#256374,#256375,#256376,#256377,
#256378,#256379,#256380,#256381,#256382,#256383,#256384,#256385,#256386,
#256387,#256388,#256389,#256390,#256391,#256392,#256393,#256394,#256395,
#256396,#256397,#256398,#256399,#256400,#256401,#256402,#256403,#256404,
#256405,#256406,#256407,#256408,#256409,#256410,#256411,#256412,#256413,
#256414,#256415,#256416,#256417,#256418,#256419,#256420,#256421,#256422,
#256423,#256424,#256425,#256426,#256427,#256428,#256429,#256430,#256431,
#256432,#256433,#256434,#256435,#256436,#256437,#256438,#256439,#256440,
#256441,#256442,#256443,#256444,#256445,#256446,#256447,#256448,#256449,
#256450,#256451,#256452,#256453,#256454,#256455,#256456,#256457,#256458,
#256459,#256460,#256461,#256462,#256463,#256464,#256465,#256466,#256467,
#256468,#256469,#256470,#256471,#256472,#256473,#256474,#256475),
 .UNSPECIFIED.,.F.,.F.,(4,3,3,3,3,3,3,3,3,3,3,3,3,3,3,3,3,3,3,3,3,3,3,3,
3,3,3,3,3,3,3,3,3,3,3,3,3,3,3,3,3,3,3,3,3,3,3,3,3,3,3,3,3,3,3,3,3,3,3,3,
3,3,3,3,3,3,3,3,3,3,3,3,3,3,3,3,4),(45.0923423611684,45.1804874726743,45.268615113927,
45.3567467014704,45.4449036496255,45.533162152123,45.621476590854,45.7099331199093,
45.7621091467636,45.8507162718281,45.9392096899116,46.0276131297802,46.1187786893672,
46.2070817752906,46.2953719041496,46.3836703809832,46.4719985116424,46.5604262015488,
46.6489136414594,46.7375288289634,46.7569376064759,46.8455447315403,46.9340381496237,
47.0224415894924,47.1136071490793,47.2019102350027,47.2902003638616,47.378498840695,
47.4668269713538,47.5552546612603,47.6437421011705,47.7323572886743,47.7517660661881,
47.8403731912525,47.928866609336,48.0172700492049,48.1084356087918,48.1967386947152,
48.2850288235743,48.3733273004076,48.4616554310666,48.550083120973,48.6385705608837,
48.7271857483876,48.7465945259004,48.8352016509647,48.923695069048,49.0120985089169,
49.1032640685039,49.1915671544272,49.279857283286,49.3681557601194,49.4564838907784,
49.5449115806848,49.6333990205953,49.7220142080992,49.7414229856126,49.8300301106771,
49.9185235287605,50.0069269686287,50.0980925282157,50.186395614139,50.2746857429981,
50.3629842198315,50.4513123504906,50.5397400403971,50.6282274803076,50.7168426678114,
50.7362514453249,50.8252260157582,50.9140857907327,51.0028517450659,51.0960207258864,
51.1846602000951,51.2732715330894,51.3618844535853,51.3755276683479),
 .UNSPECIFIED.);
#3702=B_SPLINE_CURVE_WITH_KNOTS('',3,(#256477,#256478,#256479,#256480,#256481,
#256482,#256483,#256484,#256485,#256486,#256487,#256488,#256489,#256490,
#256491,#256492,#256493,#256494,#256495,#256496,#256497,#256498,#256499,
#256500,#256501,#256502,#256503,#256504,#256505,#256506,#256507,#256508,
#256509,#256510,#256511,#256512,#256513,#256514,#256515,#256516,#256517,
#256518,#256519,#256520,#256521,#256522,#256523,#256524,#256525,#256526,
#256527,#256528,#256529,#256530,#256531,#256532,#256533,#256534,#256535,
#256536,#256537,#256538,#256539,#256540,#256541,#256542,#256543,#256544,
#256545,#256546,#256547,#256548,#256549,#256550,#256551,#256552,#256553,
#256554,#256555,#256556,#256557,#256558,#256559,#256560,#256561,#256562,
#256563,#256564,#256565,#256566,#256567,#256568,#256569,#256570,#256571,
#256572,#256573,#256574,#256575,#256576,#256577,#256578,#256579,#256580,
#256581,#256582,#256583,#256584,#256585,#256586,#256587,#256588,#256589,
#256590,#256591,#256592,#256593,#256594,#256595,#256596,#256597,#256598,
#256599,#256600,#256601,#256602,#256603,#256604,#256605,#256606,#256607,
#256608,#256609,#256610,#256611,#256612,#256613,#256614,#256615,#256616,
#256617,#256618,#256619,#256620,#256621,#256622,#256623,#256624,#256625,
#256626,#256627,#256628,#256629,#256630,#256631,#256632,#256633,#256634,
#256635,#256636,#256637,#256638,#256639,#256640,#256641,#256642,#256643,
#256644,#256645,#256646,#256647,#256648,#256649,#256650,#256651,#256652,
#256653,#256654,#256655,#256656,#256657,#256658,#256659,#256660,#256661,
#256662,#256663,#256664,#256665,#256666,#256667,#256668,#256669,#256670,
#256671,#256672,#256673,#256674,#256675,#256676,#256677,#256678,#256679,
#256680,#256681,#256682,#256683,#256684,#256685,#256686,#256687,#256688,
#256689,#256690,#256691,#256692,#256693,#256694,#256695,#256696,#256697,
#256698,#256699,#256700,#256701,#256702),.UNSPECIFIED.,.F.,.F.,(4,3,3,3,
3,3,3,3,3,3,3,3,3,3,3,3,3,3,3,3,3,3,3,3,3,3,3,3,3,3,3,3,3,3,3,3,3,3,3,3,
3,3,3,3,3,3,3,3,3,3,3,3,3,3,3,3,3,3,3,3,3,3,3,3,3,3,3,3,3,3,3,3,3,3,3,4),
(51.3755276685726,51.476178803125,51.5773060586414,51.6790268227341,51.7310799050371,
51.8196870301015,51.908180448185,51.9965838880539,52.0877494476408,52.1760525335642,
52.2643426624233,52.3526411392568,52.4409692699155,52.5293969598219,52.6178843997324,
52.7064995872363,52.7259083647494,52.8145154898138,52.9030089078973,52.991412347766,
53.0825779073529,53.1708809932763,53.2591711221353,53.3474695989688,53.4357977296278,
53.5242254195342,53.6127128594447,53.7013280469485,53.7207368244617,53.8093439495261,
53.8978373676095,53.9862408074781,54.0774063670651,54.1657094529885,54.2539995818474,
54.3422980586809,54.4306261893398,54.5190538792462,54.6075413191567,54.6961565066605,
54.7155652841739,54.8041724092383,54.8926658273218,54.9810692671905,55.0722348267774,
55.1605379127008,55.2488280415598,55.3371265183933,55.4254546490523,55.5138823389587,
55.6023697788692,55.6909849663731,55.7103937438862,55.7990008689506,55.8874942870341,
55.9758977269028,56.0670632864898,56.1553663724132,56.2436565012722,56.3319549781056,
56.4202831087644,56.5087107986708,56.5971982385813,56.6858134260852,56.7052222035984,
56.7932537350039,56.8811719603503,56.9690012602387,57.0567678288438,57.1445015213368,
57.2322242343352,57.3199578511882,57.4077779743433,57.495642164388,57.5836458244834,
57.6587129753877),.UNSPECIFIED.);
#3703=B_SPLINE_CURVE_WITH_KNOTS('',3,(#256704,#256705,#256706,#256707,#256708,
#256709,#256710,#256711,#256712,#256713,#256714,#256715,#256716,#256717,
#256718,#256719,#256720,#256721,#256722,#256723,#256724,#256725,#256726,
#256727,#256728,#256729,#256730,#256731,#256732,#256733,#256734,#256735,
#256736,#256737,#256738,#256739,#256740,#256741,#256742,#256743,#256744,
#256745,#256746,#256747,#256748,#256749,#256750,#256751,#256752,#256753,
#256754,#256755,#256756,#256757,#256758,#256759,#256760,#256761,#256762,
#256763,#256764,#256765,#256766,#256767,#256768,#256769,#256770,#256771,
#256772,#256773,#256774,#256775,#256776,#256777,#256778,#256779,#256780,
#256781,#256782,#256783,#256784,#256785,#256786,#256787,#256788,#256789,
#256790,#256791,#256792,#256793,#256794,#256795,#256796,#256797,#256798,
#256799,#256800,#256801,#256802,#256803,#256804,#256805,#256806,#256807,
#256808,#256809,#256810,#256811,#256812,#256813,#256814,#256815,#256816,
#256817,#256818,#256819,#256820,#256821,#256822,#256823,#256824,#256825,
#256826,#256827,#256828,#256829,#256830,#256831,#256832,#256833,#256834,
#256835,#256836,#256837,#256838,#256839,#256840,#256841,#256842,#256843,
#256844,#256845,#256846,#256847,#256848,#256849,#256850,#256851,#256852,
#256853,#256854,#256855,#256856,#256857,#256858,#256859,#256860,#256861,
#256862,#256863,#256864,#256865,#256866,#256867,#256868,#256869,#256870,
#256871,#256872,#256873,#256874,#256875,#256876,#256877,#256878,#256879,
#256880,#256881,#256882,#256883,#256884,#256885,#256886,#256887,#256888,
#256889,#256890,#256891,#256892,#256893,#256894,#256895,#256896,#256897,
#256898,#256899,#256900,#256901,#256902,#256903,#256904,#256905,#256906,
#256907,#256908,#256909,#256910,#256911,#256912,#256913,#256914,#256915,
#256916,#256917,#256918,#256919,#256920,#256921,#256922,#256923,#256924,
#256925,#256926,#256927,#256928,#256929,#256930,#256931,#256932),
 .UNSPECIFIED.,.F.,.F.,(4,3,3,3,3,3,3,3,3,3,3,3,3,3,3,3,3,3,3,3,3,3,3,3,
3,3,3,3,3,3,3,3,3,3,3,3,3,3,3,3,3,3,3,3,3,3,3,3,3,3,3,3,3,3,3,3,3,3,3,3,
3,3,3,3,3,3,3,3,3,3,3,3,3,3,3,3,4),(57.6587129755275,57.7000506633107,57.7886577883743,
57.8771512064569,57.9655546463247,58.056720205912,58.1450232918345,58.2333134206926,
58.3216118975252,58.4099400281833,58.4983677180889,58.5868551579985,58.6754703455015,
58.6948791230229,58.7834862480875,58.8719796661712,58.9603831060401,59.051548665627,
59.1398517515505,59.2281418804097,59.3164403572433,59.4047684879024,59.493196177809,
59.5816836177198,59.6702988052238,59.6897075827352,59.7783147077997,59.8668081258832,
59.9552115657519,60.0463771253389,60.1346802112623,60.2229703401214,60.3112688169549,
60.399596947614,60.4880246375204,60.576512077431,60.665127264935,60.6845360424474,
60.7731431675117,60.8616365855951,60.9500400254637,61.0412055850507,61.129508670974,
61.2177987998329,61.3060972766663,61.3944254073251,61.4828530972315,61.5713405371419,
61.6599557246456,61.6793645021597,61.7679716272241,61.8564650453076,61.9448684851763,
62.0360340447632,62.1243371306866,62.2126272595456,62.3009257363791,62.3892538670381,
62.4776815569445,62.5661689968551,62.654784184359,62.6741929618719,62.7628000869363,
62.8512935050199,62.9396969448887,63.0308625044756,63.1191655903991,63.2074557192581,
63.2957541960915,63.3840823267506,63.4725100166571,63.5609974565676,63.6496126440714,
63.6690214215842,63.7804659467197,63.8901245517755,63.9418982824832),
 .UNSPECIFIED.);
#3704=B_SPLINE_CURVE_WITH_KNOTS('',3,(#256934,#256935,#256936,#256937,#256938,
#256939,#256940,#256941,#256942,#256943,#256944,#256945,#256946,#256947,
#256948,#256949,#256950,#256951,#256952,#256953,#256954,#256955,#256956,
#256957,#256958,#256959,#256960,#256961,#256962,#256963,#256964,#256965,
#256966,#256967,#256968,#256969,#256970,#256971,#256972,#256973,#256974,
#256975,#256976,#256977,#256978,#256979,#256980,#256981,#256982,#256983,
#256984,#256985,#256986,#256987,#256988,#256989,#256990,#256991,#256992,
#256993,#256994,#256995,#256996,#256997,#256998,#256999,#257000,#257001,
#257002,#257003,#257004,#257005,#257006,#257007,#257008,#257009,#257010,
#257011,#257012,#257013,#257014,#257015,#257016,#257017,#257018,#257019,
#257020,#257021,#257022,#257023,#257024,#257025,#257026,#257027,#257028,
#257029,#257030,#257031,#257032,#257033,#257034,#257035,#257036,#257037,
#257038,#257039,#257040,#257041,#257042,#257043,#257044,#257045,#257046,
#257047,#257048,#257049,#257050,#257051,#257052,#257053,#257054,#257055,
#257056,#257057,#257058,#257059,#257060,#257061,#257062,#257063,#257064,
#257065,#257066,#257067,#257068,#257069,#257070,#257071,#257072,#257073,
#257074,#257075,#257076,#257077,#257078,#257079,#257080,#257081,#257082,
#257083,#257084,#257085,#257086,#257087,#257088,#257089,#257090,#257091,
#257092,#257093,#257094,#257095,#257096,#257097,#257098,#257099,#257100,
#257101,#257102,#257103,#257104,#257105,#257106,#257107,#257108,#257109,
#257110,#257111,#257112,#257113,#257114,#257115,#257116,#257117,#257118,
#257119,#257120,#257121,#257122,#257123,#257124,#257125,#257126,#257127,
#257128,#257129,#257130,#257131,#257132,#257133,#257134,#257135,#257136,
#257137,#257138,#257139,#257140,#257141,#257142,#257143,#257144,#257145,
#257146,#257147,#257148,#257149,#257150,#257151,#257152,#257153,#257154,
#257155,#257156,#257157,#257158,#257159,#257160,#257161,#257162),
 .UNSPECIFIED.,.F.,.F.,(4,3,3,3,3,3,3,3,3,3,3,3,3,3,3,3,3,3,3,3,3,3,3,3,
3,3,3,3,3,3,3,3,3,3,3,3,3,3,3,3,3,3,3,3,3,3,3,3,3,3,3,3,3,3,3,3,3,3,3,3,
3,3,3,3,3,3,3,3,3,3,3,3,3,3,3,3,4),(63.9418982827071,64.0321422325308,64.1196536355069,
64.2071478195229,64.2946468554795,64.3821728137796,64.4697961122042,64.5574781053708,
64.6452874718245,64.6638498812965,64.7524570063608,64.840950424444,64.9293538643125,
65.0205194238995,65.1088225098228,65.1971126386817,65.2854111155151,65.3737392461739,
65.4621669360803,65.5506543759904,65.6392695634944,65.6586783410087,65.7472854660733,
65.8357788841568,65.9241823240256,66.0153478836125,66.103650969536,66.1919410983952,
66.2802395752289,66.3685677058882,66.4569953957948,66.5454828357052,66.6340980232092,
66.6535068007209,66.7421139257853,66.8306073438688,66.9190107837375,67.0101763433245,
67.0984794292477,67.1867695581066,67.2750680349402,67.3633961655994,67.4518238555058,
67.5403112954164,67.62892648292,67.6483352604332,67.7369423854971,67.8254358035799,
67.9138392434483,68.0050048030354,68.0933078889583,68.1815980178167,68.2698964946495,
68.3582246253081,68.446652315214,68.535139755124,68.6237549426273,68.6431637201455,
68.7317708452113,68.8202642632963,68.9086677031662,68.9998332627526,69.0881363486775,
69.176426477538,69.2647249543729,69.3530530850333,69.4414807749412,69.5299682148529,
69.6185834023578,69.6379921798577,69.7281401915285,69.8181614902726,69.9080751538865,
69.9978824824515,70.0876273877454,70.1773265093766,70.2250835898867),
 .UNSPECIFIED.);
#3705=B_SPLINE_CURVE_WITH_KNOTS('',3,(#257164,#257165,#257166,#257167,#257168,
#257169,#257170,#257171,#257172,#257173,#257174,#257175,#257176,#257177,
#257178,#257179,#257180,#257181,#257182,#257183,#257184,#257185,#257186,
#257187,#257188,#257189,#257190,#257191,#257192,#257193,#257194,#257195,
#257196,#257197,#257198,#257199,#257200,#257201,#257202,#257203,#257204,
#257205,#257206,#257207,#257208,#257209,#257210,#257211,#257212,#257213,
#257214,#257215,#257216,#257217,#257218,#257219,#257220,#257221,#257222,
#257223,#257224,#257225,#257226,#257227,#257228,#257229,#257230,#257231,
#257232,#257233,#257234,#257235,#257236,#257237,#257238,#257239,#257240,
#257241,#257242,#257243,#257244,#257245,#257246,#257247,#257248,#257249,
#257250,#257251,#257252,#257253,#257254,#257255,#257256,#257257,#257258,
#257259,#257260,#257261,#257262,#257263,#257264,#257265,#257266,#257267,
#257268,#257269,#257270,#257271,#257272,#257273,#257274,#257275,#257276,
#257277,#257278,#257279,#257280,#257281,#257282,#257283,#257284,#257285,
#257286,#257287,#257288,#257289,#257290,#257291,#257292,#257293,#257294,
#257295,#257296,#257297,#257298,#257299,#257300,#257301,#257302,#257303,
#257304,#257305,#257306,#257307,#257308,#257309,#257310,#257311,#257312,
#257313,#257314,#257315,#257316,#257317,#257318,#257319,#257320,#257321,
#257322,#257323,#257324,#257325,#257326,#257327,#257328,#257329,#257330,
#257331,#257332,#257333,#257334,#257335,#257336,#257337,#257338,#257339,
#257340,#257341,#257342,#257343,#257344,#257345,#257346,#257347,#257348,
#257349,#257350,#257351,#257352,#257353,#257354,#257355,#257356,#257357,
#257358,#257359,#257360,#257361,#257362,#257363,#257364,#257365,#257366,
#257367,#257368,#257369,#257370,#257371,#257372,#257373,#257374,#257375,
#257376,#257377,#257378,#257379,#257380,#257381,#257382,#257383,#257384,
#257385,#257386,#257387,#257388,#257389,#257390,#257391,#257392),
 .UNSPECIFIED.,.F.,.F.,(4,3,3,3,3,3,3,3,3,3,3,3,3,3,3,3,3,3,3,3,3,3,3,3,
3,3,3,3,3,3,3,3,3,3,3,3,3,3,3,3,3,3,3,3,3,3,3,3,3,3,3,3,3,3,3,3,3,3,3,3,
3,3,3,3,3,3,3,3,3,3,3,3,3,3,3,3,4),(70.2250835900812,70.3218443516428,70.4190899158864,
70.5165901278083,70.6144198067222,70.6328206395699,70.7214277646309,70.809921182711,
70.8983246225762,70.9894901821644,71.0777932680843,71.1660833969398,71.2543818737698,
71.3427100044253,71.4311376943283,71.5196251342353,71.6082403217358,71.6276490992822,
71.7162562243575,71.8047496424519,71.8931530823314,71.9843186419143,72.0726217278485,
72.1609118567182,72.2492103335624,72.3375384642319,72.4259661541488,72.5144535940698,
72.6030687815839,72.6224775589944,72.7110846840487,72.7995781021221,72.8879815419807,
72.9791471015715,73.0674501874851,73.1557403163344,73.2440387931583,73.3323669238078,
73.420794613705,73.5092820536064,73.5978972411014,73.6173060187067,73.7059131437523,
73.7944065618168,73.8828100016663,73.9739755612604,74.0622786471644,74.150568776004,
74.2388672528181,74.3271953834575,74.4156230733446,74.5041105132358,74.5927257007206,
74.612134478419,74.7007416035599,74.7892350217199,74.8776384616652,74.9688040212234,
75.0571071072231,75.1453972361581,75.2336957130672,75.3220238438014,75.4104515337821,
75.4989389737664,75.5875541613426,75.6069629381312,75.6945092421715,75.7819426777027,
75.8727334550957,75.9600150315868,76.047266012454,76.1345086911532,76.2217653498227,
76.3091023023828,76.39648710581,76.4839876343942,76.5082688968469),
 .UNSPECIFIED.);
#3706=B_SPLINE_CURVE_WITH_KNOTS('',3,(#257394,#257395,#257396,#257397,#257398,
#257399,#257400,#257401,#257402,#257403,#257404,#257405,#257406,#257407,
#257408,#257409,#257410,#257411,#257412,#257413,#257414,#257415,#257416,
#257417,#257418,#257419,#257420,#257421,#257422,#257423,#257424,#257425,
#257426,#257427,#257428,#257429,#257430,#257431,#257432,#257433,#257434,
#257435,#257436,#257437,#257438,#257439,#257440,#257441,#257442,#257443,
#257444,#257445,#257446,#257447,#257448,#257449,#257450,#257451,#257452,
#257453,#257454,#257455,#257456,#257457,#257458,#257459,#257460,#257461,
#257462,#257463,#257464,#257465,#257466,#257467,#257468,#257469,#257470,
#257471,#257472,#257473,#257474,#257475,#257476,#257477,#257478,#257479,
#257480,#257481,#257482,#257483,#257484,#257485,#257486,#257487,#257488,
#257489,#257490,#257491,#257492,#257493,#257494,#257495,#257496,#257497,
#257498,#257499,#257500,#257501,#257502,#257503,#257504,#257505,#257506,
#257507,#257508,#257509,#257510,#257511,#257512,#257513,#257514,#257515,
#257516,#257517,#257518,#257519,#257520,#257521,#257522,#257523,#257524,
#257525,#257526,#257527,#257528,#257529,#257530,#257531,#257532,#257533,
#257534,#257535,#257536,#257537,#257538,#257539,#257540,#257541,#257542,
#257543,#257544,#257545,#257546,#257547,#257548,#257549,#257550,#257551,
#257552,#257553,#257554,#257555,#257556,#257557,#257558,#257559,#257560,
#257561,#257562,#257563,#257564,#257565,#257566,#257567,#257568,#257569,
#257570,#257571,#257572,#257573,#257574,#257575,#257576,#257577,#257578,
#257579,#257580,#257581,#257582,#257583,#257584,#257585,#257586,#257587,
#257588,#257589,#257590,#257591,#257592,#257593,#257594,#257595,#257596,
#257597,#257598,#257599,#257600,#257601,#257602,#257603,#257604,#257605,
#257606,#257607,#257608,#257609,#257610,#257611,#257612,#257613,#257614,
#257615,#257616,#257617,#257618,#257619),.UNSPECIFIED.,.F.,.F.,(4,3,3,3,
3,3,3,3,3,3,3,3,3,3,3,3,3,3,3,3,3,3,3,3,3,3,3,3,3,3,3,3,3,3,3,3,3,3,3,3,
3,3,3,3,3,3,3,3,3,3,3,3,3,3,3,3,3,3,3,3,3,3,3,3,3,3,3,3,3,3,3,3,3,3,3,4),
(76.5082688970663,76.6017913978435,76.6903985228155,76.7788919408056,76.8672953805797,
76.9584609402017,77.0467640260285,77.1350541547905,77.2233526315264,77.3116807620876,
77.4001084518961,77.4885958917088,77.5772110791153,77.5966198575557,77.6852269831444,
77.7737204017533,77.8621238421481,77.9532894015381,78.041592487986,78.1298826173679,
78.2181810947223,78.3065092258995,78.3949369163176,78.4834243567367,78.5720395447406,
78.591448317268,78.6800554415763,78.7685488589052,78.8569522980218,78.9481178578916,
79.0364209430736,79.1247110711964,79.2130095472997,79.3013376772352,79.3897653664317,
79.4782528056393,79.5668679924559,79.5862767769802,79.6748839016983,79.7633773194274,
79.8517807589342,79.942946318654,80.0312494041995,80.1195395326753,80.2078380091207,
80.2961661393873,80.3845938288969,80.4730812684075,80.5616964555102,80.5811052366925,
80.6697123652559,80.7582057868492,80.8466092302344,80.9377747885057,81.0260778779398,
81.1143680103014,81.2026664906256,81.2909946247595,81.3794223181006,81.4679097614261,
81.5565249522907,81.5759336964047,81.6645408154376,81.7530342274963,81.8414376613538,
81.9326032231992,82.0209063031824,82.1091964261374,82.1974948971095,82.2858230219558,
82.3742507061504,82.4627381404012,82.5513533223634,82.570762156117,82.6912110363831,
82.7914542042459),.UNSPECIFIED.);
#3707=B_SPLINE_CURVE_WITH_KNOTS('',3,(#257621,#257622,#257623,#257624,#257625,
#257626,#257627,#257628,#257629,#257630,#257631,#257632,#257633,#257634,
#257635,#257636,#257637,#257638,#257639,#257640,#257641,#257642,#257643,
#257644,#257645,#257646,#257647,#257648,#257649,#257650,#257651,#257652,
#257653,#257654,#257655,#257656,#257657,#257658,#257659,#257660,#257661,
#257662,#257663,#257664,#257665,#257666,#257667,#257668,#257669,#257670,
#257671,#257672,#257673,#257674,#257675,#257676,#257677,#257678,#257679,
#257680,#257681,#257682,#257683,#257684,#257685,#257686,#257687,#257688,
#257689,#257690,#257691,#257692,#257693,#257694,#257695,#257696,#257697,
#257698,#257699,#257700,#257701,#257702,#257703,#257704,#257705,#257706,
#257707,#257708,#257709,#257710,#257711,#257712,#257713,#257714,#257715,
#257716,#257717,#257718,#257719,#257720,#257721,#257722,#257723,#257724,
#257725,#257726,#257727,#257728,#257729,#257730,#257731,#257732,#257733,
#257734,#257735,#257736,#257737,#257738,#257739,#257740,#257741,#257742,
#257743,#257744,#257745,#257746,#257747,#257748,#257749,#257750,#257751,
#257752,#257753,#257754,#257755,#257756,#257757,#257758,#257759,#257760,
#257761,#257762,#257763,#257764,#257765,#257766,#257767,#257768,#257769,
#257770,#257771,#257772,#257773,#257774,#257775,#257776,#257777,#257778,
#257779,#257780,#257781,#257782,#257783,#257784,#257785,#257786,#257787,
#257788,#257789,#257790,#257791,#257792,#257793,#257794,#257795,#257796,
#257797,#257798,#257799,#257800,#257801,#257802,#257803,#257804,#257805,
#257806,#257807,#257808,#257809,#257810,#257811,#257812,#257813,#257814,
#257815,#257816,#257817,#257818,#257819,#257820,#257821,#257822,#257823,
#257824,#257825,#257826,#257827,#257828,#257829,#257830,#257831,#257832,
#257833,#257834,#257835,#257836,#257837,#257838,#257839,#257840,#257841,
#257842,#257843,#257844,#257845,#257846),.UNSPECIFIED.,.F.,.F.,(4,3,3,3,
3,3,3,3,3,3,3,3,3,3,3,3,3,3,3,3,3,3,3,3,3,3,3,3,3,3,3,3,3,3,3,3,3,3,3,3,
3,3,3,3,3,3,3,3,3,3,3,3,3,3,3,3,3,3,3,3,3,3,3,3,3,3,3,3,3,3,3,3,3,3,3,4),
(82.7914542044676,82.8786912064162,82.9658605008993,83.0529939686767,83.1401140002044,
83.2272429704705,83.3144574461672,83.4017150705519,83.4891135083265,83.5655906158292,
83.6541977635751,83.7426912044279,83.8310946671256,83.9222602181776,84.0105633269349,
84.0988534785905,84.1871519781585,84.2754801314657,84.3639078437791,84.4523953059819,
84.5410105154437,84.5604190755415,84.6490261542103,84.7375195259123,84.8259229194677,
84.9170884964409,85.0053915365081,85.0936816197577,85.1819800512769,85.2703081369651,
85.3587357826303,85.4472231786738,85.5358383231833,85.5552475352537,85.643854673882,
85.732348105177,85.8207515578944,85.9119171125283,86.0002202103292,86.0885103506881,
86.176808838633,86.2651369800039,86.3535646799847,86.442052129609,86.5306673262334,
86.550075994966,86.6386832620597,86.7271768228551,86.8155804059424,86.9067459120344,
86.9950491415257,87.0833394138348,87.1716380338451,87.2599663072531,87.3483941385609,
87.4368817192527,87.5254970455713,87.5449044546782,87.6335112335058,87.7220043052216,
87.8104073989971,87.9015730884213,87.9898758310873,88.0781656183221,88.1664637555268,
88.2547915489157,88.3432189067063,88.4317060171204,88.5203208814088,88.5397329143905,
88.6314471618556,88.7230153488038,88.8144085406912,88.9056990092786,88.9968741033722,
89.0746395114255),.UNSPECIFIED.);
#3708=B_SPLINE_CURVE_WITH_KNOTS('',3,(#257848,#257849,#257850,#257851,#257852,
#257853,#257854,#257855,#257856,#257857,#257858,#257859,#257860,#257861,
#257862,#257863,#257864,#257865,#257866,#257867,#257868,#257869,#257870,
#257871,#257872,#257873,#257874,#257875,#257876,#257877,#257878,#257879,
#257880,#257881,#257882,#257883,#257884,#257885,#257886,#257887,#257888,
#257889,#257890,#257891,#257892,#257893,#257894,#257895,#257896,#257897,
#257898,#257899,#257900,#257901,#257902,#257903,#257904,#257905,#257906,
#257907,#257908,#257909,#257910,#257911,#257912,#257913,#257914,#257915,
#257916,#257917,#257918,#257919,#257920,#257921,#257922,#257923,#257924,
#257925,#257926,#257927,#257928,#257929,#257930,#257931,#257932,#257933,
#257934,#257935,#257936,#257937,#257938,#257939,#257940,#257941,#257942,
#257943,#257944,#257945,#257946,#257947,#257948,#257949,#257950,#257951,
#257952,#257953,#257954,#257955,#257956,#257957,#257958,#257959,#257960,
#257961,#257962,#257963,#257964,#257965,#257966,#257967,#257968,#257969,
#257970,#257971,#257972,#257973,#257974,#257975,#257976,#257977,#257978,
#257979,#257980,#257981,#257982,#257983,#257984,#257985,#257986,#257987,
#257988,#257989,#257990,#257991,#257992,#257993,#257994,#257995,#257996,
#257997,#257998,#257999,#258000,#258001,#258002,#258003,#258004,#258005,
#258006,#258007,#258008,#258009,#258010,#258011,#258012,#258013,#258014,
#258015,#258016,#258017,#258018,#258019,#258020,#258021,#258022,#258023,
#258024,#258025,#258026,#258027,#258028,#258029,#258030,#258031,#258032,
#258033,#258034,#258035,#258036,#258037,#258038,#258039,#258040,#258041,
#258042,#258043,#258044,#258045,#258046,#258047,#258048,#258049,#258050,
#258051,#258052,#258053,#258054,#258055,#258056,#258057,#258058,#258059,
#258060,#258061,#258062,#258063,#258064,#258065,#258066,#258067,#258068,
#258069,#258070,#258071,#258072,#258073),.UNSPECIFIED.,.F.,.F.,(4,3,3,3,
3,3,3,3,3,3,3,3,3,3,3,3,3,3,3,3,3,3,3,3,3,3,3,3,3,3,3,3,3,3,3,3,3,3,3,3,
3,3,3,3,3,3,3,3,3,3,3,3,3,3,3,3,3,3,3,3,3,3,3,3,3,3,3,3,3,3,3,3,3,3,3,4),
(89.0746395116165,89.1686632146834,89.2630023574553,89.3575003593515,89.4522779338305,
89.5345613741027,89.6231693503936,89.711663624846,89.8000679251546,89.8912331637371,
89.979537114721,90.0678281088546,90.1561274502379,90.2444564437819,90.3328849897766,
90.4213732828159,90.5099893126814,90.529389833815,90.6179944436426,90.7064853439579,
90.794886266498,90.8860527698766,90.9743533552645,91.0626409940622,91.1509369939529,
91.2392626634439,91.3276879276889,91.4161729598151,91.5047857836245,91.5242182935272,
91.6128275436993,91.7013230732993,91.7897286088216,91.8808933768739,91.9691985064186,
92.0574906562365,92.1457911292899,92.2341212293331,92.3225508394298,92.4110401730542,
92.4996572017433,92.5190467532395,92.6076586787778,92.6961569350293,92.7845652445817,
92.8757289906279,92.9640369931715,93.0523320474714,93.1406354531799,93.2289685107595,
93.3174010998141,93.4058934284332,93.4945134523218,93.5138752129518,93.6024645262058,
93.6909401039031,93.7793256959558,93.8704979430443,93.9587832740915,94.0470557126769,
94.1353365826214,94.2236472086369,94.3120576318395,94.4005279235777,94.489126264354,
94.508703672664,94.5960456223258,94.6832745648956,94.7704058542892,94.8574831823146,
94.9445290257256,95.0315658284712,95.1186578056599,95.2057776856793,95.2930068060975,
95.3578248184193),.UNSPECIFIED.);
#3709=B_SPLINE_CURVE_WITH_KNOTS('',3,(#258074,#258075,#258076,#258077,#258078,
#258079,#258080,#258081,#258082,#258083,#258084,#258085,#258086,#258087,
#258088,#258089),.UNSPECIFIED.,.F.,.F.,(4,3,3,3,3,4),(95.3578248186051,
95.5035321323763,95.6067616768316,95.7095307827672,95.8114768751005,95.8411954015946),
 .UNSPECIFIED.);
#3710=B_SPLINE_CURVE_WITH_KNOTS('',3,(#258093,#258094,#258095,#258096,#258097,
#258098,#258099,#258100,#258101,#258102,#258103,#258104,#258105,#258106,
#258107,#258108,#258109,#258110,#258111,#258112,#258113,#258114,#258115,
#258116,#258117,#258118,#258119,#258120,#258121,#258122,#258123,#258124,
#258125,#258126,#258127,#258128,#258129,#258130,#258131,#258132,#258133,
#258134,#258135,#258136,#258137,#258138,#258139,#258140,#258141,#258142,
#258143,#258144,#258145,#258146,#258147,#258148,#258149,#258150,#258151,
#258152,#258153,#258154,#258155,#258156,#258157,#258158,#258159,#258160,
#258161,#258162,#258163,#258164,#258165,#258166,#258167,#258168,#258169,
#258170,#258171,#258172,#258173,#258174,#258175,#258176,#258177,#258178,
#258179,#258180,#258181,#258182,#258183,#258184,#258185,#258186,#258187,
#258188,#258189,#258190,#258191,#258192,#258193,#258194,#258195,#258196,
#258197,#258198,#258199,#258200,#258201,#258202,#258203,#258204,#258205,
#258206,#258207,#258208,#258209,#258210,#258211,#258212,#258213,#258214,
#258215,#258216,#258217,#258218,#258219,#258220,#258221,#258222,#258223,
#258224,#258225,#258226,#258227,#258228,#258229,#258230,#258231,#258232,
#258233,#258234,#258235,#258236,#258237,#258238,#258239,#258240,#258241,
#258242,#258243,#258244,#258245,#258246,#258247,#258248,#258249,#258250,
#258251,#258252,#258253,#258254,#258255,#258256,#258257,#258258,#258259,
#258260,#258261,#258262,#258263,#258264,#258265,#258266,#258267,#258268,
#258269,#258270,#258271,#258272,#258273,#258274,#258275,#258276,#258277,
#258278,#258279,#258280,#258281,#258282,#258283,#258284,#258285,#258286,
#258287,#258288,#258289,#258290,#258291,#258292,#258293,#258294,#258295,
#258296,#258297,#258298,#258299,#258300,#258301,#258302,#258303),
 .UNSPECIFIED.,.F.,.F.,(4,3,3,3,3,3,3,3,3,3,3,3,3,3,3,3,3,3,3,3,3,3,3,3,
3,3,3,3,3,3,3,3,3,3,3,3,3,3,3,3,3,3,3,3,3,3,3,3,3,3,3,3,3,3,3,3,3,3,3,3,
3,3,3,3,3,3,3,3,3,3,4),(-97.9023967967897,-97.8098768245286,-97.7131764352143,
-97.6202556022436,-97.5271946252469,-97.4339194033831,-97.4230752672713,
-97.3343296902634,-97.2456975231773,-97.1571552179489,-97.0661310974978,
-96.9776898140414,-96.8892620118076,-96.800826546421,-96.7078604734008,
-96.6192962152005,-96.5306722242695,-96.4419244412054,-96.42896225434,-96.3401970093587,
-96.2515425422849,-96.1629753425841,-96.0719595799372,-95.9834870676489,
-95.8950257250841,-95.8065544323462,-95.7136281346118,-95.6250225631976,
-95.5363553665576,-95.447561935756,-95.4348492414086,-95.3463507655028,
-95.2579673164513,-95.1696750265485,-95.0785576767896,-94.9903680015801,
-94.9021919521721,-94.8140081043174,-94.7257950332546,-94.6374826197777,
-94.5491106283321,-94.4606106255198,-94.4407362284773,-94.352095377284,
-94.2635679649133,-94.175130306476,-94.0840669201097,-93.9957292952466,
-93.9074045909461,-93.8190715404506,-93.7307088762241,-93.6422470377735,
-93.5537255403015,-93.4650770429167,-93.446623215546,-93.3579908217227,
-93.2694716376156,-93.181041968962,-93.0899754981686,-93.0016452127027,
-92.9133275920912,-92.8250013603883,-92.7366452406657,-92.6481895061684,
-92.5596738613995,-92.4710308067318,-92.4525102026146,-92.3537185416299,
-92.25549727205,-92.1564204153629,-92.0573435586757),.UNSPECIFIED.);
#3711=B_SPLINE_CURVE_WITH_KNOTS('',3,(#258305,#258306,#258307,#258308,#258309,
#258310,#258311,#258312,#258313,#258314),.UNSPECIFIED.,.F.,.F.,(4,1,1,1,
1,1,1,4),(-92.0573433407085,-91.4583971896833,-90.4642841767519,-89.4701711638206,
-88.4760581508893,-87.4819451379579,-86.4878321250266,-85.7741580335289),
 .UNSPECIFIED.);
#3712=B_SPLINE_CURVE_WITH_KNOTS('',3,(#258316,#258317,#258318,#258319,#258320,
#258321,#258322,#258323,#258324,#258325,#258326),.UNSPECIFIED.,.F.,.F.,
(4,1,1,1,1,1,1,1,4),(-85.7741580335289,-85.4937191120952,-84.4996060991639,
-83.5054930862326,-82.5113800733012,-81.5172670603699,-80.5231540474386,
-79.5290410345072,-79.4909727263493),.UNSPECIFIED.);
#3713=B_SPLINE_CURVE_WITH_KNOTS('',3,(#258328,#258329,#258330,#258331,#258332,
#258333,#258334,#258335,#258336,#258337),.UNSPECIFIED.,.F.,.F.,(4,1,1,1,
1,1,1,4),(-79.4909727263493,-78.5349280215759,-77.5408150086445,-76.5467019957132,
-75.5525889827818,-74.5584759698505,-73.5643629569192,-73.2077947719134),
 .UNSPECIFIED.);
#3714=B_SPLINE_CURVE_WITH_KNOTS('',3,(#258339,#258340,#258341,#258342,#258343,
#258344,#258345,#258346,#258347,#258348,#258349,#258350,#258351,#258352,
#258353,#258354,#258355,#258356,#258357,#258358,#258359,#258360,#258361,
#258362,#258363,#258364,#258365,#258366,#258367,#258368,#258369,#258370,
#258371,#258372,#258373,#258374,#258375,#258376,#258377,#258378,#258379,
#258380,#258381,#258382,#258383,#258384,#258385,#258386,#258387,#258388,
#258389,#258390,#258391,#258392,#258393,#258394,#258395,#258396,#258397,
#258398,#258399,#258400,#258401,#258402,#258403,#258404,#258405,#258406,
#258407,#258408,#258409,#258410,#258411,#258412,#258413,#258414,#258415,
#258416,#258417,#258418,#258419,#258420,#258421,#258422,#258423,#258424,
#258425,#258426,#258427,#258428,#258429,#258430,#258431,#258432,#258433,
#258434,#258435,#258436,#258437,#258438,#258439,#258440,#258441,#258442,
#258443,#258444,#258445,#258446,#258447,#258448,#258449,#258450,#258451,
#258452,#258453,#258454,#258455,#258456,#258457,#258458,#258459,#258460,
#258461,#258462,#258463,#258464,#258465,#258466,#258467,#258468,#258469,
#258470,#258471,#258472,#258473,#258474,#258475,#258476,#258477,#258478,
#258479,#258480,#258481,#258482,#258483,#258484,#258485,#258486,#258487,
#258488,#258489,#258490,#258491,#258492,#258493,#258494,#258495,#258496,
#258497,#258498,#258499,#258500,#258501,#258502,#258503,#258504,#258505,
#258506,#258507,#258508,#258509,#258510,#258511,#258512,#258513,#258514,
#258515,#258516,#258517,#258518,#258519,#258520,#258521,#258522,#258523,
#258524,#258525,#258526,#258527,#258528,#258529,#258530,#258531,#258532,
#258533,#258534,#258535,#258536,#258537,#258538,#258539,#258540,#258541,
#258542,#258543,#258544,#258545,#258546,#258547,#258548,#258549,#258550,
#258551,#258552,#258553,#258554,#258555,#258556,#258557,#258558,#258559,
#258560,#258561,#258562,#258563,#258564,#258565,#258566,#258567),
 .UNSPECIFIED.,.F.,.F.,(4,3,3,3,3,3,3,3,3,3,3,3,3,3,3,3,3,3,3,3,3,3,3,3,
3,3,3,3,3,3,3,3,3,3,3,3,3,3,3,3,3,3,3,3,3,3,3,3,3,3,3,3,3,3,3,3,3,3,3,3,
3,3,3,3,3,3,3,3,3,3,3,3,3,3,3,3,4),(-73.2077874191697,-73.1191307791567,
-73.0304750182465,-72.9417994239236,-72.8489120539397,-72.7600798965587,
-72.6711787100487,-72.5821422240396,-72.5702499439878,-72.4816347896643,
-72.3931331886022,-72.3047214231813,-72.2136483616657,-72.1253366635817,
-72.0370378526932,-71.9487306333893,-71.8603937092123,-71.7719573456623,
-71.6834611976276,-71.5948376755639,-71.5761369310565,-71.4875217767217,
-71.3990201756487,-71.3106084102167,-71.2195353487053,-71.1312236506104,
-71.042924839711,-70.9546176203965,-70.8662806962091,-70.7778443326487,
-70.6893481846037,-70.6007246625301,-70.5820239181251,-70.4934087637716,
-70.4049071626793,-70.3164953972278,-70.2254223357235,-70.1371106376086,
-70.0488118266889,-69.9605046073539,-69.8721676831462,-69.7837313195652,
-69.6952351714996,-69.6066116494054,-69.5879109051938,-69.4992957508541,
-69.4107941497758,-69.3223823843386,-69.2313093228291,-69.1429976247286,
-69.0546988138235,-68.9663915945029,-68.8780546703097,-68.7896183067433,
-68.7011221586918,-68.6124986366122,-68.5937978922625,-68.50518273792,-68.416681136839,
-68.328269371399,-68.2371963098905,-68.1488846117874,-68.0605858008793,
-67.9722785815559,-67.88394165736,-67.7955052937909,-67.7070091457367,-67.6183856236545,
-67.5996848793311,-67.5113193348893,-67.4230629416262,-67.3348940028069,
-67.2467908959305,-67.1587233843022,-67.0706780149519,-66.9826080226754,
-66.9246021119901),.UNSPECIFIED.);
#3715=B_SPLINE_CURVE_WITH_KNOTS('',3,(#258569,#258570,#258571,#258572,#258573,
#258574,#258575,#258576,#258577,#258578,#258579,#258580,#258581,#258582,
#258583,#258584,#258585,#258586,#258587,#258588,#258589,#258590,#258591,
#258592,#258593,#258594,#258595,#258596,#258597,#258598,#258599,#258600,
#258601,#258602,#258603,#258604,#258605,#258606,#258607,#258608,#258609,
#258610,#258611,#258612,#258613,#258614,#258615,#258616,#258617,#258618,
#258619,#258620,#258621,#258622,#258623,#258624,#258625,#258626,#258627,
#258628,#258629,#258630,#258631,#258632,#258633,#258634,#258635,#258636,
#258637,#258638,#258639,#258640,#258641,#258642,#258643,#258644,#258645,
#258646,#258647,#258648,#258649,#258650,#258651,#258652,#258653,#258654,
#258655,#258656,#258657,#258658,#258659,#258660,#258661,#258662,#258663,
#258664,#258665,#258666,#258667,#258668,#258669,#258670,#258671,#258672,
#258673,#258674,#258675,#258676,#258677,#258678,#258679,#258680,#258681,
#258682,#258683,#258684,#258685,#258686,#258687,#258688,#258689,#258690,
#258691,#258692,#258693,#258694,#258695,#258696,#258697,#258698,#258699,
#258700,#258701,#258702,#258703,#258704,#258705,#258706,#258707,#258708,
#258709,#258710,#258711,#258712,#258713,#258714,#258715,#258716,#258717,
#258718,#258719,#258720,#258721,#258722,#258723,#258724,#258725,#258726,
#258727,#258728,#258729,#258730,#258731,#258732,#258733,#258734,#258735,
#258736,#258737,#258738,#258739,#258740,#258741,#258742,#258743,#258744,
#258745,#258746,#258747,#258748,#258749,#258750,#258751,#258752,#258753,
#258754,#258755,#258756,#258757,#258758,#258759,#258760,#258761,#258762,
#258763,#258764,#258765,#258766,#258767,#258768,#258769,#258770,#258771,
#258772,#258773,#258774,#258775,#258776,#258777,#258778,#258779,#258780,
#258781,#258782,#258783,#258784,#258785,#258786,#258787,#258788,#258789,
#258790,#258791,#258792,#258793,#258794),.UNSPECIFIED.,.F.,.F.,(4,3,3,3,
3,3,3,3,3,3,3,3,3,3,3,3,3,3,3,3,3,3,3,3,3,3,3,3,3,3,3,3,3,3,3,3,3,3,3,3,
3,3,3,3,3,3,3,3,3,3,3,3,3,3,3,3,3,3,3,3,3,3,3,3,3,3,3,3,3,3,3,3,3,3,3,4),
(-66.9246021117923,-66.8206773626048,-66.7131246145023,-66.6055718663998,
-66.5169567120572,-66.4284551109757,-66.3400433455352,-66.2489702840269,
-66.1606585859232,-66.0723597750149,-65.9840525556914,-65.8957156314953,
-65.8072792679258,-65.7187831198716,-65.6301595977888,-65.6114588534684,
-65.5228436991252,-65.4343420980434,-65.3459303326026,-65.2548572710944,
-65.1665455729903,-65.0782467620815,-64.9899395427575,-64.9016026185607,
-64.8131662549907,-64.7246701069361,-64.6360465848529,-64.6173458405371,
-64.5287306861937,-64.4402290851117,-64.3518173196705,-64.2607442581624,
-64.1724325600581,-64.0841337491491,-63.9958265298249,-63.9074896056279,
-63.8190532420577,-63.7305570940027,-63.6419335719193,-63.6232328276058,
-63.5346176732626,-63.4461160721808,-63.3577043067398,-63.2666312452317,
-63.1783195471276,-63.0900207362188,-63.0017135168948,-62.913376592698,
-62.824940229128,-62.7364440810733,-62.6478205589901,-62.6291198146744,
-62.5405046603312,-62.4520030592493,-62.3635912938083,-62.2725182323002,
-62.184206534196,-62.0959077232872,-62.0076005039631,-61.9192635797663,
-61.8308272161963,-61.7423310681415,-61.6537075460582,-61.6350068017431,
-61.5464000329724,-61.4579068136205,-61.3695034155933,-61.2784925892747,
-61.190189177838,-61.1018986244542,-61.0135996241492,-60.9252708710678,
-60.8368426762851,-60.7483546362475,-60.6597393331835,-60.6414168050444),
 .UNSPECIFIED.);
#3716=B_SPLINE_CURVE_WITH_KNOTS('',3,(#258796,#258797,#258798,#258799,#258800,
#258801,#258802,#258803,#258804,#258805,#258806,#258807,#258808,#258809,
#258810,#258811,#258812,#258813,#258814,#258815,#258816,#258817,#258818,
#258819,#258820,#258821,#258822,#258823,#258824,#258825,#258826,#258827,
#258828,#258829,#258830,#258831,#258832,#258833,#258834,#258835,#258836,
#258837,#258838,#258839,#258840,#258841,#258842,#258843,#258844,#258845,
#258846,#258847,#258848,#258849,#258850,#258851,#258852,#258853,#258854,
#258855,#258856,#258857,#258858,#258859,#258860,#258861,#258862,#258863,
#258864,#258865,#258866,#258867,#258868,#258869,#258870,#258871,#258872,
#258873,#258874,#258875,#258876,#258877,#258878,#258879,#258880,#258881,
#258882,#258883,#258884,#258885,#258886,#258887,#258888,#258889,#258890,
#258891,#258892,#258893,#258894,#258895,#258896,#258897,#258898,#258899,
#258900,#258901,#258902,#258903,#258904,#258905,#258906,#258907,#258908,
#258909,#258910,#258911,#258912,#258913,#258914,#258915,#258916,#258917,
#258918,#258919,#258920,#258921,#258922,#258923,#258924,#258925,#258926,
#258927,#258928,#258929,#258930,#258931,#258932,#258933,#258934,#258935,
#258936,#258937,#258938,#258939,#258940,#258941,#258942,#258943,#258944,
#258945,#258946,#258947,#258948,#258949,#258950,#258951,#258952,#258953,
#258954,#258955,#258956,#258957,#258958,#258959,#258960,#258961,#258962,
#258963,#258964,#258965,#258966,#258967,#258968,#258969,#258970,#258971,
#258972,#258973,#258974,#258975,#258976,#258977,#258978,#258979,#258980,
#258981,#258982,#258983,#258984,#258985,#258986,#258987,#258988,#258989,
#258990,#258991,#258992,#258993,#258994,#258995,#258996,#258997,#258998,
#258999,#259000,#259001,#259002,#259003,#259004,#259005,#259006,#259007,
#259008,#259009,#259010,#259011,#259012,#259013,#259014,#259015,#259016,
#259017,#259018,#259019,#259020,#259021),.UNSPECIFIED.,.F.,.F.,(4,3,3,3,
3,3,3,3,3,3,3,3,3,3,3,3,3,3,3,3,3,3,3,3,3,3,3,3,3,3,3,3,3,3,3,3,3,3,3,3,
3,3,3,3,3,3,3,3,3,3,3,3,3,3,3,3,3,3,3,3,3,3,3,3,3,3,3,3,3,3,3,3,3,3,3,4),
(-60.6414168048005,-60.5527932377506,-60.4642832273796,-60.375863066609,
-60.2847277802679,-60.1964077670923,-60.1081006701652,-60.0197852033004,
-59.9314400794989,-59.8429955189631,-59.7544912348454,-59.6658594661403,
-59.6467807758804,-59.5581656215372,-59.4696640204554,-59.3812522550144,
-59.2901791935062,-59.2018674954021,-59.1135686844933,-59.0252614651692,
-58.9369245409723,-58.8484881774023,-58.7599920293476,-58.6713685072643,
-58.6526677629491,-58.5640526086058,-58.4755510075239,-58.3871392420829,
-58.2960661805748,-58.2077544824706,-58.1194556715617,-58.0311484522376,
-57.9428115280407,-57.8543751644707,-57.7658790164159,-57.6772554943325,
-57.6585547500177,-57.5699395956745,-57.4814379945926,-57.3930262291516,
-57.3019531676434,-57.2136414695393,-57.1253426586305,-57.0370354393064,
-56.9486985151095,-56.8602621515395,-56.7717660034847,-56.6831424814014,
-56.6644417370864,-56.5758265827432,-56.4873249816614,-56.3989132162204,
-56.3078401547122,-56.2195284566081,-56.1312296456993,-56.0429224263752,
-55.9545855021785,-55.8661491386085,-55.7776529905539,-55.6890294684706,
-55.6703287241551,-55.5817135698118,-55.4932119687299,-55.4048002032889,
-55.3137271417808,-55.2254154436766,-55.1371166327677,-55.0488094134437,
-54.9604724892468,-54.8720361256767,-54.7835399776221,-54.6949164555388,
-54.6762157112237,-54.5708557136836,-54.4645436057556,-54.3582314978275),
 .UNSPECIFIED.);
#3717=B_SPLINE_CURVE_WITH_KNOTS('',3,(#259023,#259024,#259025,#259026,#259027,
#259028,#259029,#259030,#259031,#259032,#259033,#259034,#259035,#259036,
#259037,#259038,#259039,#259040,#259041,#259042,#259043,#259044,#259045,
#259046,#259047,#259048,#259049,#259050,#259051,#259052,#259053,#259054,
#259055,#259056,#259057,#259058,#259059,#259060,#259061,#259062,#259063,
#259064,#259065,#259066,#259067,#259068,#259069,#259070,#259071,#259072,
#259073,#259074,#259075,#259076,#259077,#259078,#259079,#259080,#259081,
#259082,#259083,#259084,#259085,#259086,#259087,#259088,#259089,#259090,
#259091,#259092,#259093,#259094,#259095,#259096,#259097,#259098,#259099,
#259100,#259101,#259102,#259103,#259104,#259105,#259106,#259107,#259108,
#259109,#259110,#259111,#259112,#259113,#259114,#259115,#259116,#259117,
#259118,#259119,#259120,#259121,#259122,#259123,#259124,#259125,#259126,
#259127,#259128,#259129,#259130,#259131,#259132,#259133,#259134,#259135,
#259136,#259137,#259138,#259139,#259140,#259141,#259142,#259143,#259144,
#259145,#259146,#259147,#259148,#259149,#259150,#259151,#259152,#259153,
#259154,#259155,#259156,#259157,#259158,#259159,#259160,#259161,#259162,
#259163,#259164,#259165,#259166,#259167,#259168,#259169,#259170,#259171,
#259172,#259173,#259174,#259175,#259176,#259177,#259178,#259179,#259180,
#259181,#259182,#259183,#259184,#259185,#259186,#259187,#259188,#259189,
#259190,#259191,#259192,#259193,#259194,#259195,#259196,#259197,#259198,
#259199,#259200,#259201,#259202,#259203,#259204,#259205,#259206,#259207,
#259208,#259209,#259210,#259211,#259212,#259213,#259214,#259215,#259216,
#259217,#259218,#259219,#259220,#259221,#259222,#259223,#259224,#259225,
#259226,#259227,#259228,#259229,#259230,#259231,#259232,#259233,#259234,
#259235,#259236,#259237,#259238,#259239,#259240,#259241,#259242,#259243,
#259244,#259245,#259246,#259247,#259248,#259249,#259250,#259251),
 .UNSPECIFIED.,.F.,.F.,(4,3,3,3,3,3,3,3,3,3,3,3,3,3,3,3,3,3,3,3,3,3,3,3,
3,3,3,3,3,3,3,3,3,3,3,3,3,3,3,3,3,3,3,3,3,3,3,3,3,3,3,3,3,3,3,3,3,3,3,3,
3,3,3,3,3,3,3,3,3,3,3,3,3,3,3,3,4),(-54.358231497631,-54.2701712613679,
-54.1821317164641,-54.094091339317,-54.0060286107654,-53.9178668301822,
-53.8296515905965,-53.7412933384214,-53.6821026982924,-53.5934875439491,
-53.5049859428671,-53.416574177426,-53.3255011159179,-53.2371894178138,
-53.148890606905,-53.0605833875811,-52.9722464633841,-52.8838100998141,
-52.7953139517594,-52.7066904296761,-52.687989685361,-52.5993745310178,
-52.5108729299358,-52.4224611644946,-52.3313881029865,-52.2430764048823,
-52.1547775939733,-52.0664703746491,-51.9781334504521,-51.8896970868823,
-51.8012009388273,-51.712577416744,-51.6938766724297,-51.6052615180865,
-51.5167599170046,-51.4283481515637,-51.3372750900555,-51.2489633919514,
-51.1606645810424,-51.0723573617186,-50.9840204375214,-50.8955840739514,
-50.8070879258966,-50.7184644038133,-50.6997636594984,-50.6111485051552,
-50.5226469040735,-50.4342351386325,-50.3431620771243,-50.2548503790201,
-50.1665515681111,-50.0782443487871,-49.98990742459,-49.90147106102,-49.8129749129652,
-49.7243513908818,-49.705650646567,-49.6170354922239,-49.528533891142,-49.4401221257014,
-49.3490490641932,-49.2607373660889,-49.1724385551802,-49.0841313358561,
-48.9957944116597,-48.9073580480896,-48.818861900035,-48.7302383779515,
-48.7115376336357,-48.622510573146,-48.5335985669592,-48.4447807108149,
-48.352347080724,-48.2636567565059,-48.1749951783338,-48.0863334765725,
-48.0750461904514),.UNSPECIFIED.);
#3718=B_SPLINE_CURVE_WITH_KNOTS('',3,(#259253,#259254,#259255,#259256,#259257,
#259258,#259259,#259260,#259261,#259262,#259263,#259264,#259265,#259266,
#259267,#259268,#259269,#259270,#259271,#259272,#259273,#259274,#259275,
#259276,#259277,#259278,#259279,#259280,#259281,#259282,#259283,#259284,
#259285,#259286,#259287,#259288,#259289,#259290,#259291,#259292,#259293,
#259294,#259295,#259296,#259297,#259298,#259299,#259300,#259301,#259302,
#259303,#259304,#259305,#259306,#259307,#259308,#259309,#259310,#259311,
#259312,#259313,#259314,#259315,#259316,#259317,#259318,#259319,#259320,
#259321,#259322,#259323,#259324,#259325,#259326,#259327,#259328,#259329,
#259330,#259331,#259332,#259333,#259334,#259335,#259336,#259337,#259338,
#259339,#259340,#259341,#259342,#259343,#259344,#259345,#259346,#259347,
#259348,#259349,#259350,#259351,#259352,#259353,#259354,#259355,#259356,
#259357,#259358,#259359,#259360,#259361,#259362,#259363,#259364,#259365,
#259366,#259367,#259368,#259369,#259370,#259371,#259372,#259373,#259374,
#259375,#259376,#259377,#259378,#259379,#259380,#259381,#259382,#259383,
#259384,#259385,#259386,#259387,#259388,#259389,#259390,#259391,#259392,
#259393,#259394,#259395,#259396,#259397,#259398,#259399,#259400,#259401,
#259402,#259403,#259404,#259405,#259406,#259407,#259408,#259409,#259410,
#259411,#259412,#259413,#259414,#259415,#259416,#259417,#259418,#259419,
#259420,#259421,#259422,#259423,#259424,#259425,#259426,#259427,#259428,
#259429,#259430,#259431,#259432,#259433,#259434,#259435,#259436,#259437,
#259438,#259439,#259440,#259441,#259442,#259443,#259444,#259445,#259446,
#259447,#259448,#259449,#259450,#259451,#259452,#259453,#259454,#259455,
#259456,#259457,#259458,#259459,#259460,#259461,#259462,#259463,#259464,
#259465,#259466,#259467,#259468,#259469,#259470,#259471,#259472,#259473,
#259474,#259475,#259476,#259477,#259478),.UNSPECIFIED.,.F.,.F.,(4,3,3,3,
3,3,3,3,3,3,3,3,3,3,3,3,3,3,3,3,3,3,3,3,3,3,3,3,3,3,3,3,3,3,3,3,3,3,3,3,
3,3,3,3,3,3,3,3,3,3,3,3,3,3,3,3,3,3,3,3,3,3,3,3,3,3,3,3,3,3,3,3,3,3,3,4),
(-48.075046190225,-47.9745922065697,-47.8736760615069,-47.7721776295322,
-47.7174246207043,-47.6288094663611,-47.5403078652793,-47.4518960998384,
-47.3608230383303,-47.2725113402262,-47.1842125293174,-47.0959053099934,
-47.0075683857966,-46.9191320222266,-46.830635874172,-46.7420123520887,
-46.723311607773,-46.6346964534298,-46.5461948523479,-46.4577830869068,
-46.3667100253987,-46.2783983272945,-46.1900995163857,-46.1017922970616,
-46.0134553728647,-45.9250190092947,-45.8365228612399,-45.7478993391567,
-45.7291985948417,-45.6405834404984,-45.5520818394165,-45.4636700739755,
-45.3725970124673,-45.2842853143631,-45.1959865034543,-45.1076792841302,
-45.0193423599333,-44.9309059963632,-44.8424098483084,-44.7537863262251,
-44.7350855819103,-44.6464704275671,-44.5579688264852,-44.4695570610442,
-44.378483999536,-44.2901723014319,-44.2018734905231,-44.1135662711991,
-44.0252293470023,-43.9367929834323,-43.8482968353776,-43.7596733132943,
-43.740972568979,-43.6523574146358,-43.5638558135539,-43.4754440481129,
-43.3843709866047,-43.2960592885005,-43.2077604775917,-43.1194532582676,
-43.0311163340706,-42.9426799705006,-42.8541838224459,-42.7655603003626,
-42.7468595560476,-42.6587931162129,-42.5708398586021,-42.4829754395242,
-42.3951736725909,-42.3074047672152,-42.2196468586651,-42.1318780954865,
-42.0440227241161,-41.9561233914437,-41.8680841239335,-41.7918608832718),
 .UNSPECIFIED.);
#3719=B_SPLINE_CURVE_WITH_KNOTS('',3,(#259480,#259481,#259482,#259483,#259484,
#259485,#259486,#259487,#259488,#259489,#259490),.UNSPECIFIED.,.F.,.F.,
(4,1,1,1,1,1,1,1,4),(-41.7918608832718,-41.7527465431163,-40.758633530185,
-39.7645205172536,-38.7704075043223,-37.7762944913909,-36.7821814784596,
-35.7880684655282,-35.5086755760922),.UNSPECIFIED.);
#3720=B_SPLINE_CURVE_WITH_KNOTS('',3,(#259492,#259493,#259494,#259495,#259496,
#259497,#259498,#259499,#259500,#259501),.UNSPECIFIED.,.F.,.F.,(4,1,1,1,
1,1,1,4),(-35.5086755760922,-34.7939554525969,-33.7998424396656,-32.8057294267342,
-31.8116164138029,-30.8175034008716,-29.8233903879402,-29.2254902689126),
 .UNSPECIFIED.);
#3721=B_SPLINE_CURVE_WITH_KNOTS('',3,(#259503,#259504,#259505,#259506,#259507,
#259508,#259509,#259510,#259511,#259512),.UNSPECIFIED.,.F.,.F.,(4,1,1,1,
1,1,1,4),(-29.2254902689126,-28.8292773750089,-27.8351643620775,-26.8410513491462,
-25.8469383362148,-24.8528253232835,-23.8587123103522,-22.942304961733),
 .UNSPECIFIED.);
#3722=B_SPLINE_CURVE_WITH_KNOTS('',3,(#259514,#259515,#259516,#259517,#259518,
#259519,#259520,#259521,#259522,#259523,#259524),.UNSPECIFIED.,.F.,.F.,
(4,1,1,1,1,1,1,1,4),(-22.942304961733,-22.8645992974208,-21.8704862844895,
-20.8763732715581,-19.8822602586268,-18.8881472456955,-17.8940342327641,
-16.8999212198328,-16.6591196545534),.UNSPECIFIED.);
#3723=B_SPLINE_CURVE_WITH_KNOTS('',3,(#259526,#259527,#259528,#259529,#259530,
#259531,#259532,#259533,#259534,#259535),.UNSPECIFIED.,.F.,.F.,(4,1,1,1,
1,1,1,4),(-16.6591196545534,-15.9058082069014,-14.9116951939701,-13.9175821810388,
-12.9234691681074,-11.9293561551761,-10.9352431422447,-10.3759343473738),
 .UNSPECIFIED.);
#3724=B_SPLINE_CURVE_WITH_KNOTS('',3,(#259536,#259537,#259538,#259539,#259540,
#259541,#259542,#259543,#259544,#259545),.UNSPECIFIED.,.F.,.F.,(4,1,1,1,
1,1,1,4),(-10.3759343473738,-9.9411301293134,-8.94701711638206,-7.95290410345072,
-6.95879109051938,-5.96467807758804,-4.9705650646567,-4.09274904019424),
 .UNSPECIFIED.);
#3725=B_SPLINE_CURVE_WITH_KNOTS('',3,(#259547,#259548,#259549,#259550,#259551,
#259552,#259553,#259554,#259555,#259556,#259557,#259558,#259559,#259560,
#259561,#259562,#259563,#259564,#259565,#259566,#259567,#259568,#259569,
#259570,#259571,#259572,#259573,#259574,#259575,#259576,#259577,#259578,
#259579,#259580,#259581,#259582,#259583),.UNSPECIFIED.,.F.,.F.,(4,3,3,3,
3,3,3,3,3,3,3,3,4),(109.955742875643,110.032402507957,110.128120593318,
110.223696942156,110.324049264497,110.419388953009,110.514663397292,110.609892664551,
110.705096775639,110.800320560765,110.895553903767,110.990848473115,111.026515520889),
 .UNSPECIFIED.);
#3726=B_SPLINE_CURVE_WITH_KNOTS('',3,(#259585,#259586,#259587,#259588,#259589,
#259590,#259591,#259592,#259593,#259594,#259595,#259596,#259597,#259598,
#259599,#259600,#259601,#259602,#259603,#259604,#259605,#259606,#259607,
#259608,#259609),.UNSPECIFIED.,.F.,.F.,(4,3,3,3,3,3,3,3,4),(-0.549622632142507,
-0.513017594085634,-0.477058007630391,-0.4417375777789,-0.426178763214292,
-0.417876160218151,-0.412493643783751,-0.408624068330263,-0.379508346512894),
 .UNSPECIFIED.);
#3727=B_SPLINE_CURVE_WITH_KNOTS('',3,(#260022,#260023,#260024,#260025,#260026,
#260027,#260028,#260029,#260030,#260031,#260032,#260033,#260034,#260035,
#260036,#260037,#260038,#260039,#260040,#260041,#260042,#260043,#260044,
#260045,#260046,#260047,#260048,#260049,#260050,#260051,#260052,#260053,
#260054,#260055,#260056,#260057,#260058,#260059,#260060,#260061,#260062,
#260063,#260064,#260065,#260066,#260067,#260068,#260069,#260070,#260071,
#260072,#260073,#260074,#260075,#260076,#260077,#260078,#260079,#260080,
#260081,#260082,#260083,#260084,#260085,#260086,#260087,#260088,#260089,
#260090,#260091,#260092,#260093,#260094,#260095,#260096,#260097,#260098,
#260099,#260100,#260101,#260102,#260103,#260104,#260105,#260106,#260107,
#260108,#260109,#260110,#260111,#260112,#260113,#260114,#260115),
 .UNSPECIFIED.,.F.,.F.,(4,3,3,3,3,3,3,3,3,3,3,3,3,3,3,3,3,3,3,3,3,3,3,3,
3,3,3,3,3,3,3,4),(-0.741270768406358,-0.712628874131324,-0.676115879403475,
-0.645170516354468,-0.634510439317648,-0.598376433025019,-0.562201275520222,
-0.552334427207448,-0.544010451928663,-0.537620481368847,-0.502220944134419,
-0.467072958588553,-0.432961270314914,-0.409685081650182,-0.401126444594882,
-0.393612449446962,-0.360002546520967,-0.339856515655984,-0.305586608063842,
-0.281392336058492,-0.269295200055818,-0.261473488331155,-0.257198064053143,
-0.223773286179016,-0.190288603318019,-0.157388277993465,-0.128292725468663,
-0.123232979734184,-0.0910310892017754,-0.0592806646549281,-0.0285050479878524,
0.),.UNSPECIFIED.);
#3728=B_SPLINE_CURVE_WITH_KNOTS('',3,(#260536,#260537,#260538,#260539,#260540,
#260541,#260542,#260543,#260544,#260545,#260546,#260547,#260548,#260549,
#260550,#260551,#260552,#260553,#260554,#260555,#260556,#260557,#260558,
#260559,#260560,#260561,#260562,#260563,#260564,#260565,#260566,#260567,
#260568,#260569,#260570,#260571,#260572,#260573,#260574,#260575,#260576,
#260577,#260578,#260579,#260580,#260581,#260582,#260583,#260584,#260585,
#260586,#260587,#260588,#260589,#260590,#260591,#260592,#260593,#260594,
#260595,#260596,#260597,#260598,#260599,#260600,#260601,#260602,#260603,
#260604,#260605,#260606,#260607,#260608,#260609,#260610,#260611,#260612,
#260613,#260614,#260615,#260616,#260617,#260618,#260619,#260620,#260621,
#260622,#260623,#260624,#260625,#260626),.UNSPECIFIED.,.F.,.F.,(4,3,3,3,
3,3,3,3,3,3,3,3,3,3,3,3,3,3,3,3,3,3,3,3,3,3,3,3,3,3,4),(-0.744397949170608,
-0.721015353144527,-0.689663353689886,-0.660791961248297,-0.655129677496236,
-0.623063100944602,-0.590176459395623,-0.57188783490759,-0.566327003320675,
-0.532731534257962,-0.498780580187938,-0.465742657817175,-0.449223696631794,
-0.440358610599788,-0.433480268257869,-0.432704735446413,-0.397791832207206,
-0.377365240725741,-0.343711753671548,-0.309316447784973,-0.297483911038414,
-0.292610347577743,-0.25715627413548,-0.221728826073117,-0.185872338321595,
-0.15079405380869,-0.145699899549763,-0.108961750383309,-0.0721608531336355,
-0.036054100646489,-9.78674087907486E-15),.UNSPECIFIED.);
#4472=LINE('',#247352,#5109);
#4473=LINE('',#247633,#5110);
#4474=LINE('',#247689,#5111);
#4475=LINE('',#248010,#5112);
#4476=LINE('',#248430,#5113);
#4477=LINE('',#248863,#5114);
#4478=LINE('',#249360,#5115);
#4479=LINE('',#249795,#5116);
#4480=LINE('',#250224,#5117);
#4481=LINE('',#250654,#5118);
#4482=LINE('',#251094,#5119);
#4483=LINE('',#251558,#5120);
#4484=LINE('',#251998,#5121);
#4485=LINE('',#252425,#5122);
#4486=LINE('',#252858,#5123);
#4487=LINE('',#253365,#5124);
#4488=LINE('',#253788,#5125);
#4489=LINE('',#254217,#5126);
#4490=LINE('',#260630,#5127);
#4491=LINE('',#260632,#5128);
#4492=LINE('',#260634,#5129);
#4493=LINE('',#260635,#5130);
#4494=LINE('',#260638,#5131);
#4495=LINE('',#260640,#5132);
#4496=LINE('',#260641,#5133);
#4497=LINE('',#260644,#5134);
#4498=LINE('',#260646,#5135);
#4499=LINE('',#260647,#5136);
#4500=LINE('',#260650,#5137);
#4501=LINE('',#260652,#5138);
#4502=LINE('',#260653,#5139);
#4503=LINE('',#260656,#5140);
#4504=LINE('',#260658,#5141);
#4505=LINE('',#260659,#5142);
#4506=LINE('',#260661,#5143);
#4507=LINE('',#260662,#5144);
#4508=LINE('',#260669,#5145);
#5109=VECTOR('',#19826,3.5);
#5110=VECTOR('',#19831,3.5);
#5111=VECTOR('',#19838,3.22275);
#5112=VECTOR('',#19843,3.22275);
#5113=VECTOR('',#19846,3.22275);
#5114=VECTOR('',#19849,3.22275);
#5115=VECTOR('',#19852,3.22275);
#5116=VECTOR('',#19855,3.22275);
#5117=VECTOR('',#19858,3.22275);
#5118=VECTOR('',#19861,3.22275);
#5119=VECTOR('',#19864,3.22275);
#5120=VECTOR('',#19867,3.22275);
#5121=VECTOR('',#19870,3.22275);
#5122=VECTOR('',#19873,3.22275);
#5123=VECTOR('',#19876,3.22275);
#5124=VECTOR('',#19879,3.22275);
#5125=VECTOR('',#19882,3.22275);
#5126=VECTOR('',#19885,3.22275);
#5127=VECTOR('',#19898,10.);
#5128=VECTOR('',#19899,10.);
#5129=VECTOR('',#19900,10.);
#5130=VECTOR('',#19901,10.);
#5131=VECTOR('',#19904,10.);
#5132=VECTOR('',#19905,10.);
#5133=VECTOR('',#19906,10.);
#5134=VECTOR('',#19909,10.);
#5135=VECTOR('',#19910,10.);
#5136=VECTOR('',#19911,10.);
#5137=VECTOR('',#19914,10.);
#5138=VECTOR('',#19915,10.);
#5139=VECTOR('',#19916,10.);
#5140=VECTOR('',#19919,10.);
#5141=VECTOR('',#19920,10.);
#5142=VECTOR('',#19921,10.);
#5143=VECTOR('',#19924,10.);
#5144=VECTOR('',#19925,10.);
#5145=VECTOR('',#19934,6.5);
#7047=VERTEX_POINT('',#247350);
#7048=VERTEX_POINT('',#247351);
#7049=VERTEX_POINT('',#247353);
#7050=VERTEX_POINT('',#247355);
#7051=VERTEX_POINT('',#247630);
#7052=VERTEX_POINT('',#247632);
#7053=VERTEX_POINT('',#247635);
#7054=VERTEX_POINT('',#247687);
#7055=VERTEX_POINT('',#247688);
#7056=VERTEX_POINT('',#247690);
#7057=VERTEX_POINT('',#247869);
#7058=VERTEX_POINT('',#248008);
#7059=VERTEX_POINT('',#248009);
#7060=VERTEX_POINT('',#248428);
#7061=VERTEX_POINT('',#248429);
#7062=VERTEX_POINT('',#248431);
#7063=VERTEX_POINT('',#248861);
#7064=VERTEX_POINT('',#248862);
#7065=VERTEX_POINT('',#249134);
#7066=VERTEX_POINT('',#249358);
#7067=VERTEX_POINT('',#249359);
#7068=VERTEX_POINT('',#249577);
#7069=VERTEX_POINT('',#249793);
#7070=VERTEX_POINT('',#249794);
#7071=VERTEX_POINT('',#249796);
#7072=VERTEX_POINT('',#250222);
#7073=VERTEX_POINT('',#250223);
#7074=VERTEX_POINT('',#250225);
#7075=VERTEX_POINT('',#250438);
#7076=VERTEX_POINT('',#250652);
#7077=VERTEX_POINT('',#250653);
#7078=VERTEX_POINT('',#251092);
#7079=VERTEX_POINT('',#251093);
#7080=VERTEX_POINT('',#251556);
#7081=VERTEX_POINT('',#251557);
#7082=VERTEX_POINT('',#251559);
#7083=VERTEX_POINT('',#251776);
#7084=VERTEX_POINT('',#251996);
#7085=VERTEX_POINT('',#251997);
#7086=VERTEX_POINT('',#252209);
#7087=VERTEX_POINT('',#252423);
#7088=VERTEX_POINT('',#252424);
#7089=VERTEX_POINT('',#252426);
#7090=VERTEX_POINT('',#252856);
#7091=VERTEX_POINT('',#252857);
#7092=VERTEX_POINT('',#252859);
#7093=VERTEX_POINT('',#253363);
#7094=VERTEX_POINT('',#253364);
#7095=VERTEX_POINT('',#253572);
#7096=VERTEX_POINT('',#253786);
#7097=VERTEX_POINT('',#253787);
#7098=VERTEX_POINT('',#254216);
#7099=VERTEX_POINT('',#254629);
#7100=VERTEX_POINT('',#254630);
#7101=VERTEX_POINT('',#254637);
#7102=VERTEX_POINT('',#254639);
#7103=VERTEX_POINT('',#254645);
#7104=VERTEX_POINT('',#254875);
#7105=VERTEX_POINT('',#255105);
#7106=VERTEX_POINT('',#255335);
#7107=VERTEX_POINT('',#255562);
#7108=VERTEX_POINT('',#255789);
#7109=VERTEX_POINT('',#256019);
#7110=VERTEX_POINT('',#256246);
#7111=VERTEX_POINT('',#256476);
#7112=VERTEX_POINT('',#256703);
#7113=VERTEX_POINT('',#256933);
#7114=VERTEX_POINT('',#257163);
#7115=VERTEX_POINT('',#257393);
#7116=VERTEX_POINT('',#257620);
#7117=VERTEX_POINT('',#257847);
#7118=VERTEX_POINT('',#258090);
#7119=VERTEX_POINT('',#258092);
#7120=VERTEX_POINT('',#258304);
#7121=VERTEX_POINT('',#258315);
#7122=VERTEX_POINT('',#258327);
#7123=VERTEX_POINT('',#258338);
#7124=VERTEX_POINT('',#258568);
#7125=VERTEX_POINT('',#258795);
#7126=VERTEX_POINT('',#259022);
#7127=VERTEX_POINT('',#259252);
#7128=VERTEX_POINT('',#259479);
#7129=VERTEX_POINT('',#259491);
#7130=VERTEX_POINT('',#259502);
#7131=VERTEX_POINT('',#259513);
#7132=VERTEX_POINT('',#259525);
#7133=VERTEX_POINT('',#260628);
#7134=VERTEX_POINT('',#260629);
#7135=VERTEX_POINT('',#260631);
#7136=VERTEX_POINT('',#260633);
#7137=VERTEX_POINT('',#260637);
#7138=VERTEX_POINT('',#260639);
#7139=VERTEX_POINT('',#260643);
#7140=VERTEX_POINT('',#260645);
#7141=VERTEX_POINT('',#260649);
#7142=VERTEX_POINT('',#260651);
#7143=VERTEX_POINT('',#260655);
#7144=VERTEX_POINT('',#260657);
#7145=VERTEX_POINT('',#260665);
#7146=VERTEX_POINT('',#260668);
#9734=EDGE_CURVE('',#7047,#7048,#4472,.T.);
#9735=EDGE_CURVE('',#7049,#7047,#1963,.T.);
#9736=EDGE_CURVE('',#7050,#7049,#3646,.T.);
#9737=EDGE_CURVE('',#7051,#7050,#1964,.T.);
#9738=EDGE_CURVE('',#7051,#7052,#4473,.T.);
#9739=EDGE_CURVE('',#7052,#7052,#1965,.T.);
#9740=EDGE_CURVE('',#7053,#7051,#1966,.T.);
#9741=EDGE_CURVE('',#7048,#7053,#3647,.T.);
#9742=EDGE_CURVE('',#7054,#7055,#4474,.T.);
#9743=EDGE_CURVE('',#7056,#7054,#3648,.T.);
#9744=EDGE_CURVE('',#7057,#7056,#1967,.T.);
#9745=EDGE_CURVE('',#7057,#7055,#3649,.T.);
#9746=EDGE_CURVE('',#7058,#7059,#4475,.T.);
#9747=EDGE_CURVE('',#7054,#7058,#3650,.F.);
#9748=EDGE_CURVE('',#7055,#7059,#3651,.T.);
#9749=EDGE_CURVE('',#7060,#7061,#4476,.T.);
#9750=EDGE_CURVE('',#7062,#7060,#3652,.F.);
#9751=EDGE_CURVE('',#7058,#7062,#3653,.F.);
#9752=EDGE_CURVE('',#7059,#7061,#3654,.T.);
#9753=EDGE_CURVE('',#7063,#7064,#4477,.T.);
#9754=EDGE_CURVE('',#7060,#7063,#3655,.F.);
#9755=EDGE_CURVE('',#7061,#7065,#3656,.T.);
#9756=EDGE_CURVE('',#7065,#7064,#3657,.T.);
#9757=EDGE_CURVE('',#7066,#7067,#4478,.T.);
#9758=EDGE_CURVE('',#7063,#7066,#3658,.F.);
#9759=EDGE_CURVE('',#7064,#7068,#3659,.T.);
#9760=EDGE_CURVE('',#7068,#7067,#3660,.T.);
#9761=EDGE_CURVE('',#7069,#7070,#4479,.T.);
#9762=EDGE_CURVE('',#7071,#7069,#3661,.F.);
#9763=EDGE_CURVE('',#7066,#7071,#3662,.F.);
#9764=EDGE_CURVE('',#7067,#7070,#3663,.T.);
#9765=EDGE_CURVE('',#7072,#7073,#4480,.T.);
#9766=EDGE_CURVE('',#7074,#7072,#3664,.F.);
#9767=EDGE_CURVE('',#7069,#7074,#3665,.F.);
#9768=EDGE_CURVE('',#7070,#7075,#3666,.T.);
#9769=EDGE_CURVE('',#7075,#7073,#3667,.T.);
#9770=EDGE_CURVE('',#7076,#7077,#4481,.T.);
#9771=EDGE_CURVE('',#7072,#7076,#3668,.F.);
#9772=EDGE_CURVE('',#7073,#7077,#3669,.T.);
#9773=EDGE_CURVE('',#7078,#7079,#4482,.T.);
#9774=EDGE_CURVE('',#7076,#7078,#3670,.F.);
#9775=EDGE_CURVE('',#7077,#7079,#3671,.T.);
#9776=EDGE_CURVE('',#7080,#7081,#4483,.T.);
#9777=EDGE_CURVE('',#7082,#7080,#3672,.F.);
#9778=EDGE_CURVE('',#7078,#7082,#3673,.F.);
#9779=EDGE_CURVE('',#7079,#7083,#3674,.T.);
#9780=EDGE_CURVE('',#7083,#7081,#3675,.T.);
#9781=EDGE_CURVE('',#7084,#7085,#4484,.T.);
#9782=EDGE_CURVE('',#7080,#7084,#3676,.F.);
#9783=EDGE_CURVE('',#7081,#7086,#3677,.T.);
#9784=EDGE_CURVE('',#7086,#7085,#3678,.T.);
#9785=EDGE_CURVE('',#7087,#7088,#4485,.T.);
#9786=EDGE_CURVE('',#7089,#7087,#3679,.F.);
#9787=EDGE_CURVE('',#7084,#7089,#3680,.F.);
#9788=EDGE_CURVE('',#7085,#7088,#3681,.T.);
#9789=EDGE_CURVE('',#7090,#7091,#4486,.T.);
#9790=EDGE_CURVE('',#7092,#7090,#3682,.F.);
#9791=EDGE_CURVE('',#7087,#7092,#3683,.F.);
#9792=EDGE_CURVE('',#7088,#7091,#3684,.T.);
#9793=EDGE_CURVE('',#7093,#7094,#4487,.T.);
#9794=EDGE_CURVE('',#7090,#7093,#3685,.F.);
#9795=EDGE_CURVE('',#7091,#7095,#3686,.T.);
#9796=EDGE_CURVE('',#7095,#7094,#3687,.T.);
#9797=EDGE_CURVE('',#7096,#7097,#4488,.T.);
#9798=EDGE_CURVE('',#7093,#7096,#3688,.F.);
#9799=EDGE_CURVE('',#7094,#7097,#3689,.T.);
#9800=EDGE_CURVE('',#7051,#7098,#4489,.T.);
#9801=EDGE_CURVE('',#7096,#7050,#3690,.T.);
#9802=EDGE_CURVE('',#7097,#7098,#3691,.T.);
#9803=EDGE_CURVE('',#7099,#7100,#3692,.T.);
#9804=EDGE_CURVE('',#7100,#7101,#1968,.F.);
#9805=EDGE_CURVE('',#7101,#7102,#3693,.T.);
#9806=EDGE_CURVE('',#7102,#7103,#3694,.T.);
#9807=EDGE_CURVE('',#7103,#7104,#3695,.T.);
#9808=EDGE_CURVE('',#7104,#7105,#3696,.T.);
#9809=EDGE_CURVE('',#7105,#7106,#3697,.T.);
#9810=EDGE_CURVE('',#7106,#7107,#3698,.T.);
#9811=EDGE_CURVE('',#7107,#7108,#3699,.T.);
#9812=EDGE_CURVE('',#7108,#7109,#3700,.T.);
#9813=EDGE_CURVE('',#7109,#7110,#3701,.T.);
#9814=EDGE_CURVE('',#7110,#7111,#3702,.T.);
#9815=EDGE_CURVE('',#7111,#7112,#3703,.T.);
#9816=EDGE_CURVE('',#7112,#7113,#3704,.T.);
#9817=EDGE_CURVE('',#7113,#7114,#3705,.T.);
#9818=EDGE_CURVE('',#7114,#7115,#3706,.T.);
#9819=EDGE_CURVE('',#7115,#7116,#3707,.T.);
#9820=EDGE_CURVE('',#7116,#7117,#3708,.T.);
#9821=EDGE_CURVE('',#7117,#7049,#3709,.T.);
#9822=EDGE_CURVE('',#7047,#7118,#1969,.T.);
#9823=EDGE_CURVE('',#7118,#7119,#3710,.T.);
#9824=EDGE_CURVE('',#7119,#7120,#3711,.T.);
#9825=EDGE_CURVE('',#7120,#7121,#3712,.T.);
#9826=EDGE_CURVE('',#7121,#7122,#3713,.T.);
#9827=EDGE_CURVE('',#7122,#7123,#3714,.T.);
#9828=EDGE_CURVE('',#7123,#7124,#3715,.T.);
#9829=EDGE_CURVE('',#7124,#7125,#3716,.T.);
#9830=EDGE_CURVE('',#7125,#7126,#3717,.T.);
#9831=EDGE_CURVE('',#7126,#7127,#3718,.T.);
#9832=EDGE_CURVE('',#7127,#7128,#3719,.T.);
#9833=EDGE_CURVE('',#7128,#7129,#3720,.T.);
#9834=EDGE_CURVE('',#7129,#7130,#3721,.T.);
#9835=EDGE_CURVE('',#7130,#7131,#3722,.T.);
#9836=EDGE_CURVE('',#7131,#7132,#3723,.T.);
#9837=EDGE_CURVE('',#7132,#7099,#3724,.T.);
#9838=EDGE_CURVE('',#7098,#7053,#3725,.T.);
#9839=EDGE_CURVE('',#7118,#7048,#3726,.T.);
#9840=EDGE_CURVE('',#7100,#7057,#3727,.T.);
#9841=EDGE_CURVE('',#7056,#7101,#3728,.T.);
#9842=EDGE_CURVE('',#7133,#7134,#4490,.T.);
#9843=EDGE_CURVE('',#7133,#7135,#4491,.T.);
#9844=EDGE_CURVE('',#7135,#7136,#4492,.T.);
#9845=EDGE_CURVE('',#7134,#7136,#4493,.T.);
#9846=EDGE_CURVE('',#7137,#7133,#4494,.T.);
#9847=EDGE_CURVE('',#7137,#7138,#4495,.T.);
#9848=EDGE_CURVE('',#7138,#7135,#4496,.T.);
#9849=EDGE_CURVE('',#7139,#7137,#4497,.T.);
#9850=EDGE_CURVE('',#7139,#7140,#4498,.T.);
#9851=EDGE_CURVE('',#7140,#7138,#4499,.T.);
#9852=EDGE_CURVE('',#7141,#7139,#4500,.T.);
#9853=EDGE_CURVE('',#7141,#7142,#4501,.T.);
#9854=EDGE_CURVE('',#7142,#7140,#4502,.T.);
#9855=EDGE_CURVE('',#7143,#7141,#4503,.T.);
#9856=EDGE_CURVE('',#7143,#7144,#4504,.T.);
#9857=EDGE_CURVE('',#7144,#7142,#4505,.T.);
#9858=EDGE_CURVE('',#7134,#7143,#4506,.T.);
#9859=EDGE_CURVE('',#7136,#7144,#4507,.T.);
#9860=EDGE_CURVE('',#7145,#7145,#1970,.T.);
#9861=EDGE_CURVE('',#7145,#7146,#4508,.T.);
#9862=EDGE_CURVE('',#7146,#7146,#1971,.T.);
#14845=ORIENTED_EDGE('',*,*,#9734,.F.);
#14846=ORIENTED_EDGE('',*,*,#9735,.F.);
#14847=ORIENTED_EDGE('',*,*,#9736,.F.);
#14848=ORIENTED_EDGE('',*,*,#9737,.F.);
#14849=ORIENTED_EDGE('',*,*,#9738,.T.);
#14850=ORIENTED_EDGE('',*,*,#9739,.F.);
#14851=ORIENTED_EDGE('',*,*,#9738,.F.);
#14852=ORIENTED_EDGE('',*,*,#9740,.F.);
#14853=ORIENTED_EDGE('',*,*,#9741,.F.);
#14854=ORIENTED_EDGE('',*,*,#9742,.F.);
#14855=ORIENTED_EDGE('',*,*,#9743,.F.);
#14856=ORIENTED_EDGE('',*,*,#9744,.F.);
#14857=ORIENTED_EDGE('',*,*,#9745,.T.);
#14858=ORIENTED_EDGE('',*,*,#9746,.F.);
#14859=ORIENTED_EDGE('',*,*,#9747,.F.);
#14860=ORIENTED_EDGE('',*,*,#9742,.T.);
#14861=ORIENTED_EDGE('',*,*,#9748,.T.);
#14862=ORIENTED_EDGE('',*,*,#9749,.F.);
#14863=ORIENTED_EDGE('',*,*,#9750,.F.);
#14864=ORIENTED_EDGE('',*,*,#9751,.F.);
#14865=ORIENTED_EDGE('',*,*,#9746,.T.);
#14866=ORIENTED_EDGE('',*,*,#9752,.T.);
#14867=ORIENTED_EDGE('',*,*,#9753,.F.);
#14868=ORIENTED_EDGE('',*,*,#9754,.F.);
#14869=ORIENTED_EDGE('',*,*,#9749,.T.);
#14870=ORIENTED_EDGE('',*,*,#9755,.T.);
#14871=ORIENTED_EDGE('',*,*,#9756,.T.);
#14872=ORIENTED_EDGE('',*,*,#9757,.F.);
#14873=ORIENTED_EDGE('',*,*,#9758,.F.);
#14874=ORIENTED_EDGE('',*,*,#9753,.T.);
#14875=ORIENTED_EDGE('',*,*,#9759,.T.);
#14876=ORIENTED_EDGE('',*,*,#9760,.T.);
#14877=ORIENTED_EDGE('',*,*,#9761,.F.);
#14878=ORIENTED_EDGE('',*,*,#9762,.F.);
#14879=ORIENTED_EDGE('',*,*,#9763,.F.);
#14880=ORIENTED_EDGE('',*,*,#9757,.T.);
#14881=ORIENTED_EDGE('',*,*,#9764,.T.);
#14882=ORIENTED_EDGE('',*,*,#9765,.F.);
#14883=ORIENTED_EDGE('',*,*,#9766,.F.);
#14884=ORIENTED_EDGE('',*,*,#9767,.F.);
#14885=ORIENTED_EDGE('',*,*,#9761,.T.);
#14886=ORIENTED_EDGE('',*,*,#9768,.T.);
#14887=ORIENTED_EDGE('',*,*,#9769,.T.);
#14888=ORIENTED_EDGE('',*,*,#9770,.F.);
#14889=ORIENTED_EDGE('',*,*,#9771,.F.);
#14890=ORIENTED_EDGE('',*,*,#9765,.T.);
#14891=ORIENTED_EDGE('',*,*,#9772,.T.);
#14892=ORIENTED_EDGE('',*,*,#9773,.F.);
#14893=ORIENTED_EDGE('',*,*,#9774,.F.);
#14894=ORIENTED_EDGE('',*,*,#9770,.T.);
#14895=ORIENTED_EDGE('',*,*,#9775,.T.);
#14896=ORIENTED_EDGE('',*,*,#9776,.F.);
#14897=ORIENTED_EDGE('',*,*,#9777,.F.);
#14898=ORIENTED_EDGE('',*,*,#9778,.F.);
#14899=ORIENTED_EDGE('',*,*,#9773,.T.);
#14900=ORIENTED_EDGE('',*,*,#9779,.T.);
#14901=ORIENTED_EDGE('',*,*,#9780,.T.);
#14902=ORIENTED_EDGE('',*,*,#9781,.F.);
#14903=ORIENTED_EDGE('',*,*,#9782,.F.);
#14904=ORIENTED_EDGE('',*,*,#9776,.T.);
#14905=ORIENTED_EDGE('',*,*,#9783,.T.);
#14906=ORIENTED_EDGE('',*,*,#9784,.T.);
#14907=ORIENTED_EDGE('',*,*,#9785,.F.);
#14908=ORIENTED_EDGE('',*,*,#9786,.F.);
#14909=ORIENTED_EDGE('',*,*,#9787,.F.);
#14910=ORIENTED_EDGE('',*,*,#9781,.T.);
#14911=ORIENTED_EDGE('',*,*,#9788,.T.);
#14912=ORIENTED_EDGE('',*,*,#9789,.F.);
#14913=ORIENTED_EDGE('',*,*,#9790,.F.);
#14914=ORIENTED_EDGE('',*,*,#9791,.F.);
#14915=ORIENTED_EDGE('',*,*,#9785,.T.);
#14916=ORIENTED_EDGE('',*,*,#9792,.T.);
#14917=ORIENTED_EDGE('',*,*,#9793,.F.);
#14918=ORIENTED_EDGE('',*,*,#9794,.F.);
#14919=ORIENTED_EDGE('',*,*,#9789,.T.);
#14920=ORIENTED_EDGE('',*,*,#9795,.T.);
#14921=ORIENTED_EDGE('',*,*,#9796,.T.);
#14922=ORIENTED_EDGE('',*,*,#9797,.F.);
#14923=ORIENTED_EDGE('',*,*,#9798,.F.);
#14924=ORIENTED_EDGE('',*,*,#9793,.T.);
#14925=ORIENTED_EDGE('',*,*,#9799,.T.);
#14926=ORIENTED_EDGE('',*,*,#9800,.F.);
#14927=ORIENTED_EDGE('',*,*,#9737,.T.);
#14928=ORIENTED_EDGE('',*,*,#9801,.F.);
#14929=ORIENTED_EDGE('',*,*,#9797,.T.);
#14930=ORIENTED_EDGE('',*,*,#9802,.T.);
#14931=ORIENTED_EDGE('',*,*,#9803,.T.);
#14932=ORIENTED_EDGE('',*,*,#9804,.T.);
#14933=ORIENTED_EDGE('',*,*,#9805,.T.);
#14934=ORIENTED_EDGE('',*,*,#9806,.T.);
#14935=ORIENTED_EDGE('',*,*,#9807,.T.);
#14936=ORIENTED_EDGE('',*,*,#9808,.T.);
#14937=ORIENTED_EDGE('',*,*,#9809,.T.);
#14938=ORIENTED_EDGE('',*,*,#9810,.T.);
#14939=ORIENTED_EDGE('',*,*,#9811,.T.);
#14940=ORIENTED_EDGE('',*,*,#9812,.T.);
#14941=ORIENTED_EDGE('',*,*,#9813,.T.);
#14942=ORIENTED_EDGE('',*,*,#9814,.T.);
#14943=ORIENTED_EDGE('',*,*,#9815,.T.);
#14944=ORIENTED_EDGE('',*,*,#9816,.T.);
#14945=ORIENTED_EDGE('',*,*,#9817,.T.);
#14946=ORIENTED_EDGE('',*,*,#9818,.T.);
#14947=ORIENTED_EDGE('',*,*,#9819,.T.);
#14948=ORIENTED_EDGE('',*,*,#9820,.T.);
#14949=ORIENTED_EDGE('',*,*,#9821,.T.);
#14950=ORIENTED_EDGE('',*,*,#9735,.T.);
#14951=ORIENTED_EDGE('',*,*,#9822,.T.);
#14952=ORIENTED_EDGE('',*,*,#9823,.T.);
#14953=ORIENTED_EDGE('',*,*,#9824,.T.);
#14954=ORIENTED_EDGE('',*,*,#9825,.T.);
#14955=ORIENTED_EDGE('',*,*,#9826,.T.);
#14956=ORIENTED_EDGE('',*,*,#9827,.T.);
#14957=ORIENTED_EDGE('',*,*,#9828,.T.);
#14958=ORIENTED_EDGE('',*,*,#9829,.T.);
#14959=ORIENTED_EDGE('',*,*,#9830,.T.);
#14960=ORIENTED_EDGE('',*,*,#9831,.T.);
#14961=ORIENTED_EDGE('',*,*,#9832,.T.);
#14962=ORIENTED_EDGE('',*,*,#9833,.T.);
#14963=ORIENTED_EDGE('',*,*,#9834,.T.);
#14964=ORIENTED_EDGE('',*,*,#9835,.T.);
#14965=ORIENTED_EDGE('',*,*,#9836,.T.);
#14966=ORIENTED_EDGE('',*,*,#9837,.T.);
#14967=ORIENTED_EDGE('',*,*,#9800,.T.);
#14968=ORIENTED_EDGE('',*,*,#9838,.T.);
#14969=ORIENTED_EDGE('',*,*,#9740,.T.);
#14970=ORIENTED_EDGE('',*,*,#9734,.T.);
#14971=ORIENTED_EDGE('',*,*,#9839,.F.);
#14972=ORIENTED_EDGE('',*,*,#9822,.F.);
#14973=ORIENTED_EDGE('',*,*,#9839,.T.);
#14974=ORIENTED_EDGE('',*,*,#9741,.T.);
#14975=ORIENTED_EDGE('',*,*,#9838,.F.);
#14976=ORIENTED_EDGE('',*,*,#9802,.F.);
#14977=ORIENTED_EDGE('',*,*,#9799,.F.);
#14978=ORIENTED_EDGE('',*,*,#9796,.F.);
#14979=ORIENTED_EDGE('',*,*,#9795,.F.);
#14980=ORIENTED_EDGE('',*,*,#9792,.F.);
#14981=ORIENTED_EDGE('',*,*,#9788,.F.);
#14982=ORIENTED_EDGE('',*,*,#9784,.F.);
#14983=ORIENTED_EDGE('',*,*,#9783,.F.);
#14984=ORIENTED_EDGE('',*,*,#9780,.F.);
#14985=ORIENTED_EDGE('',*,*,#9779,.F.);
#14986=ORIENTED_EDGE('',*,*,#9775,.F.);
#14987=ORIENTED_EDGE('',*,*,#9772,.F.);
#14988=ORIENTED_EDGE('',*,*,#9769,.F.);
#14989=ORIENTED_EDGE('',*,*,#9768,.F.);
#14990=ORIENTED_EDGE('',*,*,#9764,.F.);
#14991=ORIENTED_EDGE('',*,*,#9760,.F.);
#14992=ORIENTED_EDGE('',*,*,#9759,.F.);
#14993=ORIENTED_EDGE('',*,*,#9756,.F.);
#14994=ORIENTED_EDGE('',*,*,#9755,.F.);
#14995=ORIENTED_EDGE('',*,*,#9752,.F.);
#14996=ORIENTED_EDGE('',*,*,#9748,.F.);
#14997=ORIENTED_EDGE('',*,*,#9745,.F.);
#14998=ORIENTED_EDGE('',*,*,#9840,.F.);
#14999=ORIENTED_EDGE('',*,*,#9803,.F.);
#15000=ORIENTED_EDGE('',*,*,#9837,.F.);
#15001=ORIENTED_EDGE('',*,*,#9836,.F.);
#15002=ORIENTED_EDGE('',*,*,#9835,.F.);
#15003=ORIENTED_EDGE('',*,*,#9834,.F.);
#15004=ORIENTED_EDGE('',*,*,#9833,.F.);
#15005=ORIENTED_EDGE('',*,*,#9832,.F.);
#15006=ORIENTED_EDGE('',*,*,#9831,.F.);
#15007=ORIENTED_EDGE('',*,*,#9830,.F.);
#15008=ORIENTED_EDGE('',*,*,#9829,.F.);
#15009=ORIENTED_EDGE('',*,*,#9828,.F.);
#15010=ORIENTED_EDGE('',*,*,#9827,.F.);
#15011=ORIENTED_EDGE('',*,*,#9826,.F.);
#15012=ORIENTED_EDGE('',*,*,#9825,.F.);
#15013=ORIENTED_EDGE('',*,*,#9824,.F.);
#15014=ORIENTED_EDGE('',*,*,#9823,.F.);
#15015=ORIENTED_EDGE('',*,*,#9736,.T.);
#15016=ORIENTED_EDGE('',*,*,#9821,.F.);
#15017=ORIENTED_EDGE('',*,*,#9820,.F.);
#15018=ORIENTED_EDGE('',*,*,#9819,.F.);
#15019=ORIENTED_EDGE('',*,*,#9818,.F.);
#15020=ORIENTED_EDGE('',*,*,#9817,.F.);
#15021=ORIENTED_EDGE('',*,*,#9816,.F.);
#15022=ORIENTED_EDGE('',*,*,#9815,.F.);
#15023=ORIENTED_EDGE('',*,*,#9814,.F.);
#15024=ORIENTED_EDGE('',*,*,#9813,.F.);
#15025=ORIENTED_EDGE('',*,*,#9812,.F.);
#15026=ORIENTED_EDGE('',*,*,#9811,.F.);
#15027=ORIENTED_EDGE('',*,*,#9810,.F.);
#15028=ORIENTED_EDGE('',*,*,#9809,.F.);
#15029=ORIENTED_EDGE('',*,*,#9808,.F.);
#15030=ORIENTED_EDGE('',*,*,#9807,.F.);
#15031=ORIENTED_EDGE('',*,*,#9806,.F.);
#15032=ORIENTED_EDGE('',*,*,#9805,.F.);
#15033=ORIENTED_EDGE('',*,*,#9841,.F.);
#15034=ORIENTED_EDGE('',*,*,#9743,.T.);
#15035=ORIENTED_EDGE('',*,*,#9747,.T.);
#15036=ORIENTED_EDGE('',*,*,#9751,.T.);
#15037=ORIENTED_EDGE('',*,*,#9750,.T.);
#15038=ORIENTED_EDGE('',*,*,#9754,.T.);
#15039=ORIENTED_EDGE('',*,*,#9758,.T.);
#15040=ORIENTED_EDGE('',*,*,#9763,.T.);
#15041=ORIENTED_EDGE('',*,*,#9762,.T.);
#15042=ORIENTED_EDGE('',*,*,#9767,.T.);
#15043=ORIENTED_EDGE('',*,*,#9766,.T.);
#15044=ORIENTED_EDGE('',*,*,#9771,.T.);
#15045=ORIENTED_EDGE('',*,*,#9774,.T.);
#15046=ORIENTED_EDGE('',*,*,#9778,.T.);
#15047=ORIENTED_EDGE('',*,*,#9777,.T.);
#15048=ORIENTED_EDGE('',*,*,#9782,.T.);
#15049=ORIENTED_EDGE('',*,*,#9787,.T.);
#15050=ORIENTED_EDGE('',*,*,#9786,.T.);
#15051=ORIENTED_EDGE('',*,*,#9791,.T.);
#15052=ORIENTED_EDGE('',*,*,#9790,.T.);
#15053=ORIENTED_EDGE('',*,*,#9794,.T.);
#15054=ORIENTED_EDGE('',*,*,#9798,.T.);
#15055=ORIENTED_EDGE('',*,*,#9801,.T.);
#15056=ORIENTED_EDGE('',*,*,#9842,.F.);
#15057=ORIENTED_EDGE('',*,*,#9843,.T.);
#15058=ORIENTED_EDGE('',*,*,#9844,.T.);
#15059=ORIENTED_EDGE('',*,*,#9845,.F.);
#15060=ORIENTED_EDGE('',*,*,#9846,.F.);
#15061=ORIENTED_EDGE('',*,*,#9847,.T.);
#15062=ORIENTED_EDGE('',*,*,#9848,.T.);
#15063=ORIENTED_EDGE('',*,*,#9843,.F.);
#15064=ORIENTED_EDGE('',*,*,#9849,.F.);
#15065=ORIENTED_EDGE('',*,*,#9850,.T.);
#15066=ORIENTED_EDGE('',*,*,#9851,.T.);
#15067=ORIENTED_EDGE('',*,*,#9847,.F.);
#15068=ORIENTED_EDGE('',*,*,#9852,.F.);
#15069=ORIENTED_EDGE('',*,*,#9853,.T.);
#15070=ORIENTED_EDGE('',*,*,#9854,.T.);
#15071=ORIENTED_EDGE('',*,*,#9850,.F.);
#15072=ORIENTED_EDGE('',*,*,#9855,.F.);
#15073=ORIENTED_EDGE('',*,*,#9856,.T.);
#15074=ORIENTED_EDGE('',*,*,#9857,.T.);
#15075=ORIENTED_EDGE('',*,*,#9853,.F.);
#15076=ORIENTED_EDGE('',*,*,#9858,.F.);
#15077=ORIENTED_EDGE('',*,*,#9845,.T.);
#15078=ORIENTED_EDGE('',*,*,#9859,.T.);
#15079=ORIENTED_EDGE('',*,*,#9856,.F.);
#15080=ORIENTED_EDGE('',*,*,#9859,.F.);
#15081=ORIENTED_EDGE('',*,*,#9844,.F.);
#15082=ORIENTED_EDGE('',*,*,#9848,.F.);
#15083=ORIENTED_EDGE('',*,*,#9851,.F.);
#15084=ORIENTED_EDGE('',*,*,#9854,.F.);
#15085=ORIENTED_EDGE('',*,*,#9857,.F.);
#15086=ORIENTED_EDGE('',*,*,#9860,.T.);
#15087=ORIENTED_EDGE('',*,*,#9840,.T.);
#15088=ORIENTED_EDGE('',*,*,#9744,.T.);
#15089=ORIENTED_EDGE('',*,*,#9841,.T.);
#15090=ORIENTED_EDGE('',*,*,#9804,.F.);
#15091=ORIENTED_EDGE('',*,*,#9860,.F.);
#15092=ORIENTED_EDGE('',*,*,#9861,.T.);
#15093=ORIENTED_EDGE('',*,*,#9862,.T.);
#15094=ORIENTED_EDGE('',*,*,#9861,.F.);
#15095=ORIENTED_EDGE('',*,*,#9862,.F.);
#15096=ORIENTED_EDGE('',*,*,#9842,.T.);
#15097=ORIENTED_EDGE('',*,*,#9858,.T.);
#15098=ORIENTED_EDGE('',*,*,#9855,.T.);
#15099=ORIENTED_EDGE('',*,*,#9852,.T.);
#15100=ORIENTED_EDGE('',*,*,#9849,.T.);
#15101=ORIENTED_EDGE('',*,*,#9846,.T.);
#15102=ORIENTED_EDGE('',*,*,#9739,.T.);
#16138=CYLINDRICAL_SURFACE('',#17753,3.22275);
#16139=CYLINDRICAL_SURFACE('',#17755,3.22275);
#16140=CYLINDRICAL_SURFACE('',#17756,3.22275);
#16141=CYLINDRICAL_SURFACE('',#17757,3.22275);
#16142=CYLINDRICAL_SURFACE('',#17758,3.22275);
#16143=CYLINDRICAL_SURFACE('',#17759,3.22275);
#16144=CYLINDRICAL_SURFACE('',#17760,3.22275);
#16145=CYLINDRICAL_SURFACE('',#17761,3.22275);
#16146=CYLINDRICAL_SURFACE('',#17762,3.22275);
#16147=CYLINDRICAL_SURFACE('',#17763,3.22275);
#16148=CYLINDRICAL_SURFACE('',#17764,3.22275);
#16149=CYLINDRICAL_SURFACE('',#17765,3.22275);
#16150=CYLINDRICAL_SURFACE('',#17766,3.22275);
#16151=CYLINDRICAL_SURFACE('',#17767,3.22275);
#16152=CYLINDRICAL_SURFACE('',#17768,3.22275);
#16153=CYLINDRICAL_SURFACE('',#17769,3.22275);
#16154=CYLINDRICAL_SURFACE('',#17770,3.933);
#16155=CYLINDRICAL_SURFACE('',#17773,3.22275);
#16156=CYLINDRICAL_SURFACE('',#17784,6.5);
#16747=ADVANCED_FACE('',(#979),#114,.T.);
#16748=ADVANCED_FACE('',(#980),#16138,.T.);
#16749=ADVANCED_FACE('',(#981),#16139,.T.);
#16750=ADVANCED_FACE('',(#982),#16140,.T.);
#16751=ADVANCED_FACE('',(#983),#16141,.T.);
#16752=ADVANCED_FACE('',(#984),#16142,.T.);
#16753=ADVANCED_FACE('',(#985),#16143,.T.);
#16754=ADVANCED_FACE('',(#986),#16144,.T.);
#16755=ADVANCED_FACE('',(#987),#16145,.T.);
#16756=ADVANCED_FACE('',(#988),#16146,.T.);
#16757=ADVANCED_FACE('',(#989),#16147,.T.);
#16758=ADVANCED_FACE('',(#990),#16148,.T.);
#16759=ADVANCED_FACE('',(#991),#16149,.T.);
#16760=ADVANCED_FACE('',(#992),#16150,.T.);
#16761=ADVANCED_FACE('',(#993),#16151,.T.);
#16762=ADVANCED_FACE('',(#994),#16152,.T.);
#16763=ADVANCED_FACE('',(#995),#16153,.T.);
#16764=ADVANCED_FACE('',(#996),#16154,.T.);
#16765=ADVANCED_FACE('',(#997),#16155,.T.);
#16766=ADVANCED_FACE('',(#998),#115,.T.);
#16767=ADVANCED_FACE('',(#999),#297,.F.);
#16768=ADVANCED_FACE('',(#1000),#298,.F.);
#16769=ADVANCED_FACE('',(#1001),#393,.F.);
#16770=ADVANCED_FACE('',(#1002),#394,.F.);
#16771=ADVANCED_FACE('',(#1003),#395,.F.);
#16772=ADVANCED_FACE('',(#1004),#396,.F.);
#16773=ADVANCED_FACE('',(#1005),#397,.F.);
#16774=ADVANCED_FACE('',(#1006),#398,.F.);
#16775=ADVANCED_FACE('',(#1007),#399,.F.);
#16776=ADVANCED_FACE('',(#1008,#267),#400,.T.);
#16777=ADVANCED_FACE('',(#1009),#16156,.T.);
#16778=ADVANCED_FACE('',(#1010,#268),#401,.F.);
#16779=ADVANCED_FACE('',(#1011),#402,.T.);
#16855=CLOSED_SHELL('',(#16747,#16748,#16749,#16750,#16751,#16752,#16753,
#16754,#16755,#16756,#16757,#16758,#16759,#16760,#16761,#16762,#16763,#16764,
#16765,#16766,#16767,#16768,#16769,#16770,#16771,#16772,#16773,#16774,#16775,
#16776,#16777,#16778,#16779));
#17747=AXIS2_PLACEMENT_3D('',#247348,#19822,#19823);
#17748=AXIS2_PLACEMENT_3D('',#247349,#19824,#19825);
#17749=AXIS2_PLACEMENT_3D('',#247354,#19827,#19828);
#17750=AXIS2_PLACEMENT_3D('',#247631,#19829,#19830);
#17751=AXIS2_PLACEMENT_3D('',#247634,#19832,#19833);
#17752=AXIS2_PLACEMENT_3D('',#247636,#19834,#19835);
#17753=AXIS2_PLACEMENT_3D('',#247686,#19836,#19837);
#17754=AXIS2_PLACEMENT_3D('',#247870,#19839,#19840);
#17755=AXIS2_PLACEMENT_3D('',#248007,#19841,#19842);
#17756=AXIS2_PLACEMENT_3D('',#248427,#19844,#19845);
#17757=AXIS2_PLACEMENT_3D('',#248860,#19847,#19848);
#17758=AXIS2_PLACEMENT_3D('',#249357,#19850,#19851);
#17759=AXIS2_PLACEMENT_3D('',#249792,#19853,#19854);
#17760=AXIS2_PLACEMENT_3D('',#250221,#19856,#19857);
#17761=AXIS2_PLACEMENT_3D('',#250651,#19859,#19860);
#17762=AXIS2_PLACEMENT_3D('',#251091,#19862,#19863);
#17763=AXIS2_PLACEMENT_3D('',#251555,#19865,#19866);
#17764=AXIS2_PLACEMENT_3D('',#251995,#19868,#19869);
#17765=AXIS2_PLACEMENT_3D('',#252422,#19871,#19872);
#17766=AXIS2_PLACEMENT_3D('',#252855,#19874,#19875);
#17767=AXIS2_PLACEMENT_3D('',#253362,#19877,#19878);
#17768=AXIS2_PLACEMENT_3D('',#253785,#19880,#19881);
#17769=AXIS2_PLACEMENT_3D('',#254215,#19883,#19884);
#17770=AXIS2_PLACEMENT_3D('',#254628,#19886,#19887);
#17771=AXIS2_PLACEMENT_3D('',#254638,#19888,#19889);
#17772=AXIS2_PLACEMENT_3D('',#258091,#19890,#19891);
#17773=AXIS2_PLACEMENT_3D('',#259546,#19892,#19893);
#17774=AXIS2_PLACEMENT_3D('',#259584,#19894,#19895);
#17775=AXIS2_PLACEMENT_3D('',#260627,#19896,#19897);
#17776=AXIS2_PLACEMENT_3D('',#260636,#19902,#19903);
#17777=AXIS2_PLACEMENT_3D('',#260642,#19907,#19908);
#17778=AXIS2_PLACEMENT_3D('',#260648,#19912,#19913);
#17779=AXIS2_PLACEMENT_3D('',#260654,#19917,#19918);
#17780=AXIS2_PLACEMENT_3D('',#260660,#19922,#19923);
#17781=AXIS2_PLACEMENT_3D('',#260663,#19926,#19927);
#17782=AXIS2_PLACEMENT_3D('',#260664,#19928,#19929);
#17783=AXIS2_PLACEMENT_3D('',#260666,#19930,#19931);
#17784=AXIS2_PLACEMENT_3D('',#260667,#19932,#19933);
#17785=AXIS2_PLACEMENT_3D('',#260670,#19935,#19936);
#17786=AXIS2_PLACEMENT_3D('',#260671,#19937,#19938);
#17787=AXIS2_PLACEMENT_3D('',#260672,#19939,#19940);
#19822=DIRECTION('axis',(0.,0.,1.));
#19823=DIRECTION('refdir',(1.,0.,0.));
#19824=DIRECTION('center_axis',(0.,0.,-1.));
#19825=DIRECTION('ref_axis',(1.,0.,0.));
#19826=DIRECTION('',(0.707106781186547,-8.65956056235493E-17,0.707106781186548));
#19827=DIRECTION('center_axis',(0.,0.,-1.));
#19828=DIRECTION('ref_axis',(1.,0.,0.));
#19829=DIRECTION('center_axis',(0.,0.,-1.));
#19830=DIRECTION('ref_axis',(1.,1.08690987399044E-13,0.));
#19831=DIRECTION('',(0.707106781186547,-8.65956056235493E-17,0.707106781186548));
#19832=DIRECTION('center_axis',(0.,0.,1.));
#19833=DIRECTION('ref_axis',(1.,0.,0.));
#19834=DIRECTION('center_axis',(0.,0.,-1.));
#19835=DIRECTION('ref_axis',(1.,1.08690987399044E-13,0.));
#19836=DIRECTION('center_axis',(0.,0.,1.));
#19837=DIRECTION('ref_axis',(1.,1.08690987399044E-13,0.));
#19838=DIRECTION('',(0.,0.,-1.));
#19839=DIRECTION('center_axis',(0.,0.,-1.));
#19840=DIRECTION('ref_axis',(1.,1.08690987399044E-13,0.));
#19841=DIRECTION('center_axis',(0.,0.,1.));
#19842=DIRECTION('ref_axis',(1.,1.08690987399044E-13,0.));
#19843=DIRECTION('',(0.,0.,-1.));
#19844=DIRECTION('center_axis',(0.,0.,1.));
#19845=DIRECTION('ref_axis',(1.,1.08690987399044E-13,0.));
#19846=DIRECTION('',(0.,0.,-1.));
#19847=DIRECTION('center_axis',(0.,0.,1.));
#19848=DIRECTION('ref_axis',(1.,1.08690987399044E-13,0.));
#19849=DIRECTION('',(0.,0.,-1.));
#19850=DIRECTION('center_axis',(0.,0.,1.));
#19851=DIRECTION('ref_axis',(1.,1.08690987399044E-13,0.));
#19852=DIRECTION('',(0.,0.,-1.));
#19853=DIRECTION('center_axis',(0.,0.,1.));
#19854=DIRECTION('ref_axis',(1.,1.08690987399044E-13,0.));
#19855=DIRECTION('',(0.,0.,-1.));
#19856=DIRECTION('center_axis',(0.,0.,1.));
#19857=DIRECTION('ref_axis',(1.,1.08690987399044E-13,0.));
#19858=DIRECTION('',(0.,0.,-1.));
#19859=DIRECTION('center_axis',(0.,0.,1.));
#19860=DIRECTION('ref_axis',(1.,1.08690987399044E-13,0.));
#19861=DIRECTION('',(0.,0.,-1.));
#19862=DIRECTION('center_axis',(0.,0.,1.));
#19863=DIRECTION('ref_axis',(1.,1.08690987399044E-13,0.));
#19864=DIRECTION('',(0.,0.,-1.));
#19865=DIRECTION('center_axis',(0.,0.,1.));
#19866=DIRECTION('ref_axis',(1.,1.08690987399044E-13,0.));
#19867=DIRECTION('',(0.,0.,-1.));
#19868=DIRECTION('center_axis',(0.,0.,1.));
#19869=DIRECTION('ref_axis',(1.,1.08690987399044E-13,0.));
#19870=DIRECTION('',(0.,0.,-1.));
#19871=DIRECTION('center_axis',(0.,0.,1.));
#19872=DIRECTION('ref_axis',(1.,1.08690987399044E-13,0.));
#19873=DIRECTION('',(0.,0.,-1.));
#19874=DIRECTION('center_axis',(0.,0.,1.));
#19875=DIRECTION('ref_axis',(1.,1.08690987399044E-13,0.));
#19876=DIRECTION('',(0.,0.,-1.));
#19877=DIRECTION('center_axis',(0.,0.,1.));
#19878=DIRECTION('ref_axis',(1.,1.08690987399044E-13,0.));
#19879=DIRECTION('',(0.,0.,-1.));
#19880=DIRECTION('center_axis',(0.,0.,1.));
#19881=DIRECTION('ref_axis',(1.,1.08690987399044E-13,0.));
#19882=DIRECTION('',(0.,0.,-1.));
#19883=DIRECTION('center_axis',(0.,0.,1.));
#19884=DIRECTION('ref_axis',(1.,1.08690987399044E-13,0.));
#19885=DIRECTION('',(0.,0.,-1.));
#19886=DIRECTION('center_axis',(0.,0.,1.));
#19887=DIRECTION('ref_axis',(1.,0.,0.));
#19888=DIRECTION('center_axis',(0.,0.,-1.));
#19889=DIRECTION('ref_axis',(1.,0.,0.));
#19890=DIRECTION('center_axis',(0.,0.,-1.));
#19891=DIRECTION('ref_axis',(1.,0.,0.));
#19892=DIRECTION('center_axis',(0.,0.,1.));
#19893=DIRECTION('ref_axis',(1.,1.08690987399044E-13,0.));
#19894=DIRECTION('center_axis',(0.,0.,-1.));
#19895=DIRECTION('ref_axis',(1.,0.,0.));
#19896=DIRECTION('center_axis',(-1.60246890531964E-16,-1.,0.));
#19897=DIRECTION('ref_axis',(1.,-1.60246890531964E-16,0.));
#19898=DIRECTION('',(1.,-1.60246890531964E-16,0.));
#19899=DIRECTION('',(0.,0.,1.));
#19900=DIRECTION('',(1.,-1.60246890531964E-16,0.));
#19901=DIRECTION('',(0.,0.,1.));
#19902=DIRECTION('center_axis',(-0.866025403784439,-0.5,0.));
#19903=DIRECTION('ref_axis',(0.5,-0.866025403784439,0.));
#19904=DIRECTION('',(0.5,-0.866025403784439,0.));
#19905=DIRECTION('',(0.,0.,1.));
#19906=DIRECTION('',(0.5,-0.866025403784439,0.));
#19907=DIRECTION('center_axis',(-0.866025403784439,0.5,0.));
#19908=DIRECTION('ref_axis',(-0.5,-0.866025403784439,0.));
#19909=DIRECTION('',(-0.5,-0.866025403784439,0.));
#19910=DIRECTION('',(0.,0.,1.));
#19911=DIRECTION('',(-0.5,-0.866025403784439,0.));
#19912=DIRECTION('center_axis',(1.60246890531964E-16,1.,0.));
#19913=DIRECTION('ref_axis',(-1.,1.60246890531964E-16,0.));
#19914=DIRECTION('',(-1.,1.60246890531964E-16,0.));
#19915=DIRECTION('',(0.,0.,1.));
#19916=DIRECTION('',(-1.,1.60246890531964E-16,0.));
#19917=DIRECTION('center_axis',(0.866025403784439,0.5,0.));
#19918=DIRECTION('ref_axis',(-0.5,0.866025403784439,0.));
#19919=DIRECTION('',(-0.5,0.866025403784439,0.));
#19920=DIRECTION('',(0.,0.,1.));
#19921=DIRECTION('',(-0.5,0.866025403784439,0.));
#19922=DIRECTION('center_axis',(0.866025403784439,-0.5,0.));
#19923=DIRECTION('ref_axis',(0.5,0.866025403784439,0.));
#19924=DIRECTION('',(0.5,0.866025403784439,0.));
#19925=DIRECTION('',(0.5,0.866025403784439,0.));
#19926=DIRECTION('center_axis',(0.,0.,1.));
#19927=DIRECTION('ref_axis',(1.,0.,0.));
#19928=DIRECTION('center_axis',(0.,0.,1.));
#19929=DIRECTION('ref_axis',(1.,0.,0.));
#19930=DIRECTION('center_axis',(0.,0.,1.));
#19931=DIRECTION('ref_axis',(1.,0.,0.));
#19932=DIRECTION('center_axis',(0.,0.,1.));
#19933=DIRECTION('ref_axis',(1.,0.,0.));
#19934=DIRECTION('',(0.,0.,-1.));
#19935=DIRECTION('center_axis',(0.,0.,1.));
#19936=DIRECTION('ref_axis',(1.,0.,0.));
#19937=DIRECTION('center_axis',(0.,0.,1.));
#19938=DIRECTION('ref_axis',(1.,0.,0.));
#19939=DIRECTION('center_axis',(0.,0.,1.));
#19940=DIRECTION('ref_axis',(1.,0.,0.));
#247348=CARTESIAN_POINT('',(0.,0.,0.));
#247349=CARTESIAN_POINT('Origin',(0.,0.,19.5));
#247350=CARTESIAN_POINT('',(-3.933,4.81653586104654E-16,19.067));
#247351=CARTESIAN_POINT('',(-3.72907923291372,-0.00301811260641736,19.2709195457389));
#247352=CARTESIAN_POINT('',(-3.5,4.28626379701574E-16,19.5));
#247353=CARTESIAN_POINT('',(-3.48351403049219,-1.825212838262,19.0672818680215));
#247354=CARTESIAN_POINT('Origin',(0.,0.,19.067));
#247355=CARTESIAN_POINT('',(-3.1771036721075,0.540490350682607,19.77725));
#247356=CARTESIAN_POINT('Ctrl Pts',(-3.17710367210751,0.54049035068261,
19.77725));
#247357=CARTESIAN_POINT('Ctrl Pts',(-3.16458988313419,0.636662782213618,
19.7734573799255));
#247358=CARTESIAN_POINT('Ctrl Pts',(-3.14759826787415,0.732018576300735,
19.7698475455261));
#247359=CARTESIAN_POINT('Ctrl Pts',(-3.12629674287792,0.826357140292361,
19.7663337451368));
#247360=CARTESIAN_POINT('Ctrl Pts',(-3.12487753074456,0.832642438395861,
19.7660996385107));
#247361=CARTESIAN_POINT('Ctrl Pts',(-3.12343917326921,0.838923233893048,
19.7658659581679));
#247362=CARTESIAN_POINT('Ctrl Pts',(-3.12198171393402,0.845199472642916,
19.7656326784525));
#247363=CARTESIAN_POINT('Ctrl Pts',(-3.09807584703403,0.948145005711887,
19.7618063255022));
#247364=CARTESIAN_POINT('Ctrl Pts',(-3.06903398719535,1.04986083335664,
19.7580872627407));
#247365=CARTESIAN_POINT('Ctrl Pts',(-3.03503853293981,1.15004696575645,
19.7543772677843));
#247366=CARTESIAN_POINT('Ctrl Pts',(-3.01733595934536,1.20221724618924,
19.7524453489384));
#247367=CARTESIAN_POINT('Ctrl Pts',(-2.9982896999218,1.25397207251287,19.7505161810263));
#247368=CARTESIAN_POINT('Ctrl Pts',(-2.97792340270646,1.30526499304348,
19.7485780811387));
#247369=CARTESIAN_POINT('Ctrl Pts',(-2.96193234297344,1.34553879183044,
19.7470563380971));
#247370=CARTESIAN_POINT('Ctrl Pts',(-2.94512745587406,1.38552777067492,
19.7455291174391));
#247371=CARTESIAN_POINT('Ctrl Pts',(-2.9275198572165,1.42520831898889,19.7439915130774));
#247372=CARTESIAN_POINT('Ctrl Pts',(-2.91989399705739,1.44239398515292,
19.7433255758266));
#247373=CARTESIAN_POINT('Ctrl Pts',(-2.9121206622458,1.4595147225641,19.7426579721191));
#247374=CARTESIAN_POINT('Ctrl Pts',(-2.90420365992811,1.476563460031,19.7419885589767));
#247375=CARTESIAN_POINT('Ctrl Pts',(-2.85856365692285,1.57484616830884,
19.7381295203403));
#247376=CARTESIAN_POINT('Ctrl Pts',(-2.80812532886755,1.67079266491046,
19.7342056102415));
#247377=CARTESIAN_POINT('Ctrl Pts',(-2.75316165124206,1.76405727156329,
19.7301686381061));
#247378=CARTESIAN_POINT('Ctrl Pts',(-2.69776993998212,1.85804818311921,
19.7261002277566));
#247379=CARTESIAN_POINT('Ctrl Pts',(-2.6377820652722,1.94931490144401,19.7219168766214));
#247380=CARTESIAN_POINT('Ctrl Pts',(-2.57346776037294,2.03749724942546,
19.7176028035755));
#247381=CARTESIAN_POINT('Ctrl Pts',(-2.5312628736305,2.09536502884201,19.7147717854282));
#247382=CARTESIAN_POINT('Ctrl Pts',(-2.48719471026825,2.15190447451021,
19.7118851719569));
#247383=CARTESIAN_POINT('Ctrl Pts',(-2.44133692549877,2.20701319668367,
19.7089464856767));
#247384=CARTESIAN_POINT('Ctrl Pts',(-2.43027421564794,2.22030759820611,
19.7082375584177));
#247385=CARTESIAN_POINT('Ctrl Pts',(-2.41910619342676,2.23351998459099,
19.7075255580821));
#247386=CARTESIAN_POINT('Ctrl Pts',(-2.40784488962212,2.24663635551648,
19.7068112829041));
#247387=CARTESIAN_POINT('Ctrl Pts',(-2.33286625983243,2.3339661653562,19.7020555836467));
#247388=CARTESIAN_POINT('Ctrl Pts',(-2.25365629340451,2.41715985411514,
19.697189593479));
#247389=CARTESIAN_POINT('Ctrl Pts',(-2.17061375920421,2.49590001164361,
19.6922695152463));
#247390=CARTESIAN_POINT('Ctrl Pts',(-2.09136398447513,2.5710439099646,19.6875741492468));
#247391=CARTESIAN_POINT('Ctrl Pts',(-2.00862409412524,2.64213271644402,
19.6828301060477));
#247392=CARTESIAN_POINT('Ctrl Pts',(-1.92269565758021,2.70890454420114,
19.6781146285172));
#247393=CARTESIAN_POINT('Ctrl Pts',(-1.83796886681413,2.77474261721767,
19.6734650934604));
#247394=CARTESIAN_POINT('Ctrl Pts',(-1.7501425366723,2.8363847262143,19.6688437473422));
#247395=CARTESIAN_POINT('Ctrl Pts',(-1.65945464450637,2.89357888006934,
19.664345873392));
#247396=CARTESIAN_POINT('Ctrl Pts',(-1.60622192399477,2.92715117218405,
19.6617056745609));
#247397=CARTESIAN_POINT('Ctrl Pts',(-1.55200223306352,2.95919081438473,
19.6591083913824));
#247398=CARTESIAN_POINT('Ctrl Pts',(-1.49683447506739,2.98964404084263,
19.6565758664662));
#247399=CARTESIAN_POINT('Ctrl Pts',(-1.4744877757989,3.00197967161917,19.6555500213939));
#247400=CARTESIAN_POINT('Ctrl Pts',(-1.45198543586043,3.01405496715234,
19.6545348200898));
#247401=CARTESIAN_POINT('Ctrl Pts',(-1.42932970158584,3.02586618074696,
19.6535317811723));
#247402=CARTESIAN_POINT('Ctrl Pts',(-1.41605565619611,3.03278639721237,
19.6529440984269));
#247403=CARTESIAN_POINT('Ctrl Pts',(-1.40273752971901,3.03961148194378,
19.6523609716114));
#247404=CARTESIAN_POINT('Ctrl Pts',(-1.38937624925342,3.04634086757255,
19.6517827066583));
#247405=CARTESIAN_POINT('Ctrl Pts',(-1.36924390684754,3.05648048675114,
19.6509113958534));
#247406=CARTESIAN_POINT('Ctrl Pts',(-1.34901337628808,3.06640295336509,
19.6500511133982));
#247407=CARTESIAN_POINT('Ctrl Pts',(-1.3286867018512,3.0761068082297,19.6492028638974));
#247408=CARTESIAN_POINT('Ctrl Pts',(-1.23897459210359,3.11893493022734,
19.645459100866));
#247409=CARTESIAN_POINT('Ctrl Pts',(-1.14738809682255,3.1575087790561,19.6419487793584));
#247410=CARTESIAN_POINT('Ctrl Pts',(-1.05419368277925,3.19185082210001,
19.6385663785593));
#247411=CARTESIAN_POINT('Ctrl Pts',(-1.04888030346469,3.19380879675978,
19.6383735346144));
#247412=CARTESIAN_POINT('Ctrl Pts',(-1.04356168380452,3.1957530126226,19.6381811064871));
#247413=CARTESIAN_POINT('Ctrl Pts',(-1.03823786832269,3.19768347263257,
19.6379890746212));
#247414=CARTESIAN_POINT('Ctrl Pts',(-0.936912661247142,3.23442483997126,
19.6343342393538));
#247415=CARTESIAN_POINT('Ctrl Pts',(-0.833710131733674,3.26618357112524,
19.6308224475133));
#247416=CARTESIAN_POINT('Ctrl Pts',(-0.728987945023351,3.2929368227092,
19.6273369064872));
#247417=CARTESIAN_POINT('Ctrl Pts',(-0.618230512283943,3.32123189136611,
19.62365049019));
#247418=CARTESIAN_POINT('Ctrl Pts',(-0.505772563389774,3.34392695068221,
19.619992753164));
#247419=CARTESIAN_POINT('Ctrl Pts',(-0.392069459542977,3.36095412422278,
19.6162548727429));
#247420=CARTESIAN_POINT('Ctrl Pts',(-0.342324351610006,3.36840351264678,
19.6146195500586));
#247421=CARTESIAN_POINT('Ctrl Pts',(-0.292341372829587,3.37476761591482,
19.6129693154895));
#247422=CARTESIAN_POINT('Ctrl Pts',(-0.242160814847883,3.38003919219647,
19.6112971801835));
#247423=CARTESIAN_POINT('Ctrl Pts',(-0.221494449192876,3.38221023866141,
19.610608527824));
#247424=CARTESIAN_POINT('Ctrl Pts',(-0.200794587116868,3.38419597077201,
19.6099161769195));
#247425=CARTESIAN_POINT('Ctrl Pts',(-0.180064107341896,3.38599585119609,
19.6092197082279));
#247426=CARTESIAN_POINT('Ctrl Pts',(-0.164827432646491,3.38731874351745,
19.6087078113976));
#247427=CARTESIAN_POINT('Ctrl Pts',(-0.149584229007586,3.3885403673882,
19.60819402712));
#247428=CARTESIAN_POINT('Ctrl Pts',(-0.134335760330162,3.38966089776966,
19.6076782142061));
#247429=CARTESIAN_POINT('Ctrl Pts',(-0.0228498841094028,3.39785341296919,
19.603906959801));
#247430=CARTESIAN_POINT('Ctrl Pts',(0.0889175554404967,3.40064237400044,
19.600024130958));
#247431=CARTESIAN_POINT('Ctrl Pts',(0.20049137098505,3.39809487625733,19.595995655425));
#247432=CARTESIAN_POINT('Ctrl Pts',(0.31333184657006,3.39551845762827,19.5919214459627));
#247433=CARTESIAN_POINT('Ctrl Pts',(0.425973809192178,3.38748379911017,
19.5876982574808));
#247434=CARTESIAN_POINT('Ctrl Pts',(0.537937125635622,3.37405655392717,
19.5833299866338));
#247435=CARTESIAN_POINT('Ctrl Pts',(0.649538927040108,3.36067266357876,
19.5789758203672));
#247436=CARTESIAN_POINT('Ctrl Pts',(0.760466169508123,3.34193148245174,
19.5744776729821));
#247437=CARTESIAN_POINT('Ctrl Pts',(0.87026043105589,3.31788976175756,19.56987672393));
#247438=CARTESIAN_POINT('Ctrl Pts',(0.918145898551613,3.3074042498682,19.5678700744642));
#247439=CARTESIAN_POINT('Ctrl Pts',(0.965816099665759,3.29591033247577,
19.565844335427));
#247440=CARTESIAN_POINT('Ctrl Pts',(1.01323416596061,3.28341171682478,19.5638050146634));
#247441=CARTESIAN_POINT('Ctrl Pts',(1.05147591420847,3.27333182638387,19.5621603421297));
#247442=CARTESIAN_POINT('Ctrl Pts',(1.08955368553102,3.2625984600994,19.5605068605029));
#247443=CARTESIAN_POINT('Ctrl Pts',(1.12744847290062,3.25121313328311,19.5588480276107));
#247444=CARTESIAN_POINT('Ctrl Pts',(1.14260692398368,3.24665884147706,19.5581844709847));
#247445=CARTESIAN_POINT('Ctrl Pts',(1.15773540097485,3.24200036908579,19.5575200931108));
#247446=CARTESIAN_POINT('Ctrl Pts',(1.17281990695688,3.23724205230611,19.5568557045379));
#247447=CARTESIAN_POINT('Ctrl Pts',(1.28139605346562,3.20299235924881,19.5520735292964));
#247448=CARTESIAN_POINT('Ctrl Pts',(1.38786500384221,3.16352193443418,19.5472812256798));
#247449=CARTESIAN_POINT('Ctrl Pts',(1.49184806016234,3.11899167315108,19.5425848250758));
#247450=CARTESIAN_POINT('Ctrl Pts',(1.59436475009484,3.07508937646806,19.5379546529925));
#247451=CARTESIAN_POINT('Ctrl Pts',(1.69446626847233,3.02627009263741,19.5334182553453));
#247452=CARTESIAN_POINT('Ctrl Pts',(1.79182717787839,2.9726309517123,19.5290953037484));
#247453=CARTESIAN_POINT('Ctrl Pts',(1.83747794464135,2.94748053018609,19.5270683500533));
#247454=CARTESIAN_POINT('Ctrl Pts',(1.88252662676428,2.92126953380817,19.5250885318974));
#247455=CARTESIAN_POINT('Ctrl Pts',(1.92694138741515,2.89400248501213,19.5231690444041));
#247456=CARTESIAN_POINT('Ctrl Pts',(2.01674297995926,2.83887161477934,19.5192880590911));
#247457=CARTESIAN_POINT('Ctrl Pts',(2.10395873229359,2.77942316276847,19.5156532043811));
#247458=CARTESIAN_POINT('Ctrl Pts',(2.18842314999436,2.71585528229139,19.5121545622288));
#247459=CARTESIAN_POINT('Ctrl Pts',(2.1929279567887,2.71246496684649,19.5119679664129));
#247460=CARTESIAN_POINT('Ctrl Pts',(2.19742493888665,2.70906292154206,19.5117817580525));
#247461=CARTESIAN_POINT('Ctrl Pts',(2.2019140715046,2.70564917233842,19.5115959204723));
#247462=CARTESIAN_POINT('Ctrl Pts',(2.23107014013917,2.68347751590652,19.5103889404821));
#247463=CARTESIAN_POINT('Ctrl Pts',(2.25989446870579,2.66081260713164,19.5091976772753));
#247464=CARTESIAN_POINT('Ctrl Pts',(2.28837856765338,2.63766240727529,19.5080178345747));
#247465=CARTESIAN_POINT('Ctrl Pts',(2.30709383064093,2.62245174256993,19.5072426278017));
#247466=CARTESIAN_POINT('Ctrl Pts',(2.32566732334985,2.60702707649191,19.5064721401425));
#247467=CARTESIAN_POINT('Ctrl Pts',(2.34406866120866,2.59141470798129,19.5057063550408));
#247468=CARTESIAN_POINT('Ctrl Pts',(2.42801257768479,2.52019361697664,19.5022129677061));
#247469=CARTESIAN_POINT('Ctrl Pts',(2.50846443703766,2.44499936367937,19.49881193032));
#247470=CARTESIAN_POINT('Ctrl Pts',(2.58523998813779,2.36616437098485,19.4954030721373));
#247471=CARTESIAN_POINT('Ctrl Pts',(2.66463705873511,2.28463753866887,19.4918778176792));
#247472=CARTESIAN_POINT('Ctrl Pts',(2.74010185284196,2.19921651126464,19.4883437781998));
#247473=CARTESIAN_POINT('Ctrl Pts',(2.81139933026821,2.11026813746333,19.4847193844267));
#247474=CARTESIAN_POINT('Ctrl Pts',(2.88320120511787,2.02069049412569,19.481069349706));
#247475=CARTESIAN_POINT('Ctrl Pts',(2.95077593728325,1.9275352101032,19.4773274483407));
#247476=CARTESIAN_POINT('Ctrl Pts',(3.01386241038701,1.83118227639482,19.4734442924964));
#247477=CARTESIAN_POINT('Ctrl Pts',(3.05935422153283,1.76170193856714,19.4706441392523));
#247478=CARTESIAN_POINT('Ctrl Pts',(3.10251176849141,1.69055902194563,19.4677712482316));
#247479=CARTESIAN_POINT('Ctrl Pts',(3.14323283105931,1.61789790696629,19.4648187786741));
#247480=CARTESIAN_POINT('Ctrl Pts',(3.15256575919984,1.60124458502554,19.4641420972597));
#247481=CARTESIAN_POINT('Ctrl Pts',(3.1617706898004,1.58451151903962,19.463461277159));
#247482=CARTESIAN_POINT('Ctrl Pts',(3.1708463718576,1.56770045508266,19.4627763103263));
#247483=CARTESIAN_POINT('Ctrl Pts',(3.17845206332653,1.5536122835364,19.46220228775));
#247484=CARTESIAN_POINT('Ctrl Pts',(3.18596647279068,1.53947016049922,19.4616253866984));
#247485=CARTESIAN_POINT('Ctrl Pts',(3.1933829871923,1.52528680237208,19.4610460963189));
#247486=CARTESIAN_POINT('Ctrl Pts',(3.24720725577905,1.42235315511455,19.4568419811125));
#247487=CARTESIAN_POINT('Ctrl Pts',(3.2959619462958,1.31709019069266,19.4525025542234));
#247488=CARTESIAN_POINT('Ctrl Pts',(3.33950590367559,1.2099581232903,19.4480571033869));
#247489=CARTESIAN_POINT('Ctrl Pts',(3.38315102057343,1.10257717110673,19.4436013250632));
#247490=CARTESIAN_POINT('Ctrl Pts',(3.42156183143616,0.993318922576536,
19.4390392975554));
#247491=CARTESIAN_POINT('Ctrl Pts',(3.45459938143664,0.882610076888688,
19.4344344860811));
#247492=CARTESIAN_POINT('Ctrl Pts',(3.48721345282509,0.773320308230192,
19.4298886995396));
#247493=CARTESIAN_POINT('Ctrl Pts',(3.51459215543077,0.662617111471497,
19.4253016032098));
#247494=CARTESIAN_POINT('Ctrl Pts',(3.5365922265338,0.550869944812617,19.420762333558));
#247495=CARTESIAN_POINT('Ctrl Pts',(3.55580037483495,0.453304071531322,
19.416799120701));
#247496=CARTESIAN_POINT('Ctrl Pts',(3.57090886825469,0.354941774153412,
19.4128729457123));
#247497=CARTESIAN_POINT('Ctrl Pts',(3.58180565188396,0.256001776248793,
19.4090574165951));
#247498=CARTESIAN_POINT('Ctrl Pts',(3.58371650043283,0.238651761982868,
19.4083883294108));
#247499=CARTESIAN_POINT('Ctrl Pts',(3.58549782885556,0.221282662292161,
19.407722627683));
#247500=CARTESIAN_POINT('Ctrl Pts',(3.58714748111238,0.20391333437368,19.4070614117152));
#247501=CARTESIAN_POINT('Ctrl Pts',(3.59490511742215,0.122232526567783,
19.4039519848771));
#247502=CARTESIAN_POINT('Ctrl Pts',(3.59976225922983,0.0404590842984835,
19.4009381638359));
#247503=CARTESIAN_POINT('Ctrl Pts',(3.60169878861074,-0.0412946177144568,
19.3980644912308));
#247504=CARTESIAN_POINT('Ctrl Pts',(3.60419581238684,-0.146710491970134,
19.3943590845945));
#247505=CARTESIAN_POINT('Ctrl Pts',(3.60183841423843,-0.252098971576584,
19.3908860908306));
#247506=CARTESIAN_POINT('Ctrl Pts',(3.5947512689982,-0.357225533988951,
19.3875428351193));
#247507=CARTESIAN_POINT('Ctrl Pts',(3.59431849705639,-0.363645019551776,
19.3873386813709));
#247508=CARTESIAN_POINT('Ctrl Pts',(3.59386807825058,-0.370063540736907,
19.387135011397));
#247509=CARTESIAN_POINT('Ctrl Pts',(3.59340003682488,-0.376481048737694,
19.3869318018183));
#247510=CARTESIAN_POINT('Ctrl Pts',(3.58507504193675,-0.49062846896029,
19.383317338204));
#247511=CARTESIAN_POINT('Ctrl Pts',(3.57117718051369,-0.60445132204649,
19.3798480308315));
#247512=CARTESIAN_POINT('Ctrl Pts',(3.55182373931981,-0.717609841555423,
19.3764084446653));
#247513=CARTESIAN_POINT('Ctrl Pts',(3.53219721908766,-0.832365039369245,
19.3729203255859));
#247514=CARTESIAN_POINT('Ctrl Pts',(3.50695892089234,-0.946437013077343,
19.3694623301513));
#247515=CARTESIAN_POINT('Ctrl Pts',(3.4762079922568,-1.05942782808591,19.3659376273442));
#247516=CARTESIAN_POINT('Ctrl Pts',(3.46821757599952,-1.08878771037984,
19.3650217576823));
#247517=CARTESIAN_POINT('Ctrl Pts',(3.45985488460338,-1.11807437117177,
19.3641015253591));
#247518=CARTESIAN_POINT('Ctrl Pts',(3.45112154213351,-1.14728036824038,
19.3631755415022));
#247519=CARTESIAN_POINT('Ctrl Pts',(3.44618411254059,-1.16379209381565,
19.3626520328784));
#247520=CARTESIAN_POINT('Ctrl Pts',(3.44113041057629,-1.18027058518833,
19.3621269237154));
#247521=CARTESIAN_POINT('Ctrl Pts',(3.43596296363524,-1.19670873142764,
19.3616001765408));
#247522=CARTESIAN_POINT('Ctrl Pts',(3.40077392169046,-1.30864846184167,
19.3580131579157));
#247523=CARTESIAN_POINT('Ctrl Pts',(3.36028536534138,-1.41880322069132,
19.3543445904448));
#247524=CARTESIAN_POINT('Ctrl Pts',(3.31473956815417,-1.52677068406583,
19.3505442698383));
#247525=CARTESIAN_POINT('Ctrl Pts',(3.26862550536591,-1.63608523541021,
19.3466965334086));
#247526=CARTESIAN_POINT('Ctrl Pts',(3.21732720295,-1.74315713587502,19.3427136455698));
#247527=CARTESIAN_POINT('Ctrl Pts',(3.16108829899971,-1.84756939818066,
19.3385806146842));
#247528=CARTESIAN_POINT('Ctrl Pts',(3.10490387238151,-1.95188051873053,
19.3344515873704));
#247529=CARTESIAN_POINT('Ctrl Pts',(3.04378877524706,-2.05353694145685,
19.3301727796814));
#247530=CARTESIAN_POINT('Ctrl Pts',(2.97797551513044,-2.15212844821212,
19.3257660626574));
#247531=CARTESIAN_POINT('Ctrl Pts',(2.94523482079766,-2.20117562169605,
19.3235738148514));
#247532=CARTESIAN_POINT('Ctrl Pts',(2.91133120733824,-2.24946438412975,
19.321350476985));
#247533=CARTESIAN_POINT('Ctrl Pts',(2.87629176279623,-2.29694484308792,
19.3191020230224));
#247534=CARTESIAN_POINT('Ctrl Pts',(2.85048071464791,-2.33192029513323,
19.3174457480944));
#247535=CARTESIAN_POINT('Ctrl Pts',(2.82405331952821,-2.366457154258,19.3157758898878));
#247536=CARTESIAN_POINT('Ctrl Pts',(2.79701991565477,-2.40053558605405,
19.3140955643857));
#247537=CARTESIAN_POINT('Ctrl Pts',(2.78698082964753,-2.41319090350478,
19.3134715611224));
#247538=CARTESIAN_POINT('Ctrl Pts',(2.77685873720404,-2.42578219237878,
19.3128461579201));
#247539=CARTESIAN_POINT('Ctrl Pts',(2.76666237134247,-2.4382986711196,19.3122200327859));
#247540=CARTESIAN_POINT('Ctrl Pts',(2.69091998260967,-2.53127571914085,
19.3075689429799));
#247541=CARTESIAN_POINT('Ctrl Pts',(2.61096786415274,-2.62026940316246,
19.3028686272558));
#247542=CARTESIAN_POINT('Ctrl Pts',(2.5271193507041,-2.70497870613519,19.2982109712535));
#247543=CARTESIAN_POINT('Ctrl Pts',(2.44454139689091,-2.78840440589686,
19.2936238928854));
#247544=CARTESIAN_POINT('Ctrl Pts',(2.35818486874117,-2.86767578697296,
19.2890786950165));
#247545=CARTESIAN_POINT('Ctrl Pts',(2.26829076229067,-2.9425204355399,19.284684468869));
#247546=CARTESIAN_POINT('Ctrl Pts',(2.18040734951895,-3.01569100704323,
19.2803885299518));
#247547=CARTESIAN_POINT('Ctrl Pts',(2.08914318404235,-3.08463203363021,
19.2762373832327));
#247548=CARTESIAN_POINT('Ctrl Pts',(1.99466030529637,-3.14908455620803,
19.2723461432594));
#247549=CARTESIAN_POINT('Ctrl Pts',(1.93019574293449,-3.19305975802495,
19.2696911957679));
#247550=CARTESIAN_POINT('Ctrl Pts',(1.86422998226858,-3.2349460604959,19.2671574695618));
#247551=CARTESIAN_POINT('Ctrl Pts',(1.79684706521249,-3.27471586875336,
19.2647057148294));
#247552=CARTESIAN_POINT('Ctrl Pts',(1.76306020003609,-3.29465708246733,
19.2634763660537));
#247553=CARTESIAN_POINT('Ctrl Pts',(1.72891707848498,-3.314065937121,19.2622676486185));
#247554=CARTESIAN_POINT('Ctrl Pts',(1.69442865360166,-3.33293762892873,
19.2610747934098));
#247555=CARTESIAN_POINT('Ctrl Pts',(1.67966120721037,-3.34101821532914,
19.2605640300042));
#247556=CARTESIAN_POINT('Ctrl Pts',(1.66483933557783,-3.34899543928581,
19.260056483811));
#247557=CARTESIAN_POINT('Ctrl Pts',(1.64996551745785,-3.35686853107841,
19.2595518258176));
#247558=CARTESIAN_POINT('Ctrl Pts',(1.54790692001615,-3.41089075317367,
19.25608905072));
#247559=CARTESIAN_POINT('Ctrl Pts',(1.44338102079118,-3.46002494558198,
19.2527598044352));
#247560=CARTESIAN_POINT('Ctrl Pts',(1.33675738679763,-3.50423623360503,
19.2494544540736));
#247561=CARTESIAN_POINT('Ctrl Pts',(1.22748680308684,-3.5495450743183,19.2460670478311));
#247562=CARTESIAN_POINT('Ctrl Pts',(1.11601262685197,-3.5896826848128,19.2427043407588));
#247563=CARTESIAN_POINT('Ctrl Pts',(1.00274554376078,-3.62457714481419,
19.2392742583058));
#247564=CARTESIAN_POINT('Ctrl Pts',(0.887418485001359,-3.66010622642493,
19.23578179333));
#247565=CARTESIAN_POINT('Ctrl Pts',(0.770232609504335,-3.6901989429599,
19.2322191475815));
#247566=CARTESIAN_POINT('Ctrl Pts',(0.651638599037863,-3.71475692682424,
19.2285212596192));
#247567=CARTESIAN_POINT('Ctrl Pts',(0.557481316903401,-3.73425464855801,
19.2255853349565));
#247568=CARTESIAN_POINT('Ctrl Pts',(0.462436821599179,-3.75026305735668,
19.2225647675566));
#247569=CARTESIAN_POINT('Ctrl Pts',(0.366737966434126,-3.76272714493643,
19.2194428580875));
#247570=CARTESIAN_POINT('Ctrl Pts',(0.348578568571863,-3.76509227589814,
19.2188504581466));
#247571=CARTESIAN_POINT('Ctrl Pts',(0.330395625607895,-3.76732977506375,
19.2182544512168));
#247572=CARTESIAN_POINT('Ctrl Pts',(0.312190750748018,-3.76943925243843,
19.2176547827206));
#247573=CARTESIAN_POINT('Ctrl Pts',(0.295454775339816,-3.77137852209772,
19.2171034997658));
#247574=CARTESIAN_POINT('Ctrl Pts',(0.27870457594682,-3.77320905523334,
19.2165492635453));
#247575=CARTESIAN_POINT('Ctrl Pts',(0.261950803658832,-3.77492987456066,
19.2159923650463));
#247576=CARTESIAN_POINT('Ctrl Pts',(0.140494854890857,-3.78740490051092,
19.2119551467765));
#247577=CARTESIAN_POINT('Ctrl Pts',(0.0187071285680933,-3.79413133586308,
19.2077701623785));
#247578=CARTESIAN_POINT('Ctrl Pts',(-0.102919377231485,-3.79515191457483,
19.2034528248801));
#247579=CARTESIAN_POINT('Ctrl Pts',(-0.225323696673865,-3.7961790199893,
19.1991078775775));
#247580=CARTESIAN_POINT('Ctrl Pts',(-0.347564405183152,-3.7914276864069,
19.1946290698833));
#247581=CARTESIAN_POINT('Ctrl Pts',(-0.469169014359218,-3.78093380970734,
19.1900682371697));
#247582=CARTESIAN_POINT('Ctrl Pts',(-0.588890599908213,-3.77060242863931,
19.1855780280601));
#247583=CARTESIAN_POINT('Ctrl Pts',(-0.707995692757366,-3.75470586367773,
19.1810086717632));
#247584=CARTESIAN_POINT('Ctrl Pts',(-0.826064256043132,-3.73325957207986,
19.1764402466238));
#247585=CARTESIAN_POINT('Ctrl Pts',(-0.893094062371818,-3.72108409765832,
19.173846663338));
#247586=CARTESIAN_POINT('Ctrl Pts',(-0.95979036063892,-3.70711950966395,
19.1712539125421));
#247587=CARTESIAN_POINT('Ctrl Pts',(-1.02608048299624,-3.69136401974347,
19.1686804513533));
#247588=CARTESIAN_POINT('Ctrl Pts',(-1.0731344302124,-3.68018048342282,
19.166853761303));
#247589=CARTESIAN_POINT('Ctrl Pts',(-1.1199837936364,-3.66809454403529,
19.1650368471905));
#247590=CARTESIAN_POINT('Ctrl Pts',(-1.16660340215532,-3.65510416442421,
19.1632370478864));
#247591=CARTESIAN_POINT('Ctrl Pts',(-1.18354551570129,-3.65038330782828,
19.1625829796705));
#247592=CARTESIAN_POINT('Ctrl Pts',(-1.20044812808266,-3.64554552754666,
19.1619315314114));
#247593=CARTESIAN_POINT('Ctrl Pts',(-1.21730683248261,-3.64059209559565,
19.1612831921432));
#247594=CARTESIAN_POINT('Ctrl Pts',(-1.33463995018198,-3.6061172272822,
19.1567708840881));
#247595=CARTESIAN_POINT('Ctrl Pts',(-1.4498950175503,-3.56603139636547,
19.1524063055148));
#247596=CARTESIAN_POINT('Ctrl Pts',(-1.56273946469582,-3.5204123978789,
19.1483174993703));
#247597=CARTESIAN_POINT('Ctrl Pts',(-1.57762987331034,-3.51439273501348,
19.1477779602456));
#247598=CARTESIAN_POINT('Ctrl Pts',(-1.5924783670239,-3.50827662342372,
19.1472432353143));
#247599=CARTESIAN_POINT('Ctrl Pts',(-1.60728423194846,-3.50206414269901,
19.1467136283624));
#247600=CARTESIAN_POINT('Ctrl Pts',(-1.71029567872433,-3.45884095845543,
19.1430289008153));
#247601=CARTESIAN_POINT('Ctrl Pts',(-1.81124821300518,-3.41095457478404,
19.139591140223));
#247602=CARTESIAN_POINT('Ctrl Pts',(-1.90996741658097,-3.35860925792791,
19.1362930132009));
#247603=CARTESIAN_POINT('Ctrl Pts',(-1.91638568915619,-3.35520600405785,
19.1360785840174));
#247604=CARTESIAN_POINT('Ctrl Pts',(-1.9227945286344,-3.35178388555094,
19.1358647450661));
#247605=CARTESIAN_POINT('Ctrl Pts',(-1.92919388980695,-3.34834295154984,
19.1356514668496));
#247606=CARTESIAN_POINT('Ctrl Pts',(-2.03589817023458,-3.2909681016724,
19.1320952214654));
#247607=CARTESIAN_POINT('Ctrl Pts',(-2.13996474276898,-3.22836590874485,
19.1286943674431));
#247608=CARTESIAN_POINT('Ctrl Pts',(-2.2411130948938,-3.16077460424877,
19.1253278844567));
#247609=CARTESIAN_POINT('Ctrl Pts',(-2.30453714555583,-3.11839216073272,
19.1232169653662));
#247610=CARTESIAN_POINT('Ctrl Pts',(-2.36681264127981,-3.07404780448213,
19.1211199056681));
#247611=CARTESIAN_POINT('Ctrl Pts',(-2.42785977746311,-3.02779966215665,
19.1190112222297));
#247612=CARTESIAN_POINT('Ctrl Pts',(-2.44551288664286,-3.01442600440831,
19.1184014504813));
#247613=CARTESIAN_POINT('Ctrl Pts',(-2.4630632314328,-3.00089315573997,
19.1177907308758));
#247614=CARTESIAN_POINT('Ctrl Pts',(-2.48050876672247,-2.98720253689442,
19.1171785080672));
#247615=CARTESIAN_POINT('Ctrl Pts',(-2.49385060611702,-2.97673234868774,
19.1167102978202));
#247616=CARTESIAN_POINT('Ctrl Pts',(-2.50713106880999,-2.96616986439984,
19.116241209721));
#247617=CARTESIAN_POINT('Ctrl Pts',(-2.52033810050941,-2.95552493019762,
19.1157714081302));
#247618=CARTESIAN_POINT('Ctrl Pts',(-2.61722856965942,-2.87743072308156,
19.1123248125906));
#247619=CARTESIAN_POINT('Ctrl Pts',(-2.71032158081448,-2.79478006848099,
19.1088315555871));
#247620=CARTESIAN_POINT('Ctrl Pts',(-2.79933067258955,-2.70796263286715,
19.1052196678753));
#247621=CARTESIAN_POINT('Ctrl Pts',(-2.8882857381335,-2.62119789320547,
19.1016099724865));
#247622=CARTESIAN_POINT('Ctrl Pts',(-2.97316127057925,-2.53027135578799,
19.0978817066295));
#247623=CARTESIAN_POINT('Ctrl Pts',(-3.05366149423723,-2.43556820923745,
19.0939993569848));
#247624=CARTESIAN_POINT('Ctrl Pts',(-3.13423505475908,-2.34077878675562,
19.0901134704636));
#247625=CARTESIAN_POINT('Ctrl Pts',(-3.21042506006765,-2.24220613355532,
19.0860732072219));
#247626=CARTESIAN_POINT('Ctrl Pts',(-3.28193146579411,-2.14023119209007,
19.081880080732));
#247627=CARTESIAN_POINT('Ctrl Pts',(-3.35343787152057,-2.03825625062482,
19.0776869542421));
#247628=CARTESIAN_POINT('Ctrl Pts',(-3.4202607872896,-1.93287950230611,
19.0733410316596));
#247629=CARTESIAN_POINT('Ctrl Pts',(-3.48209799042183,-1.8244708936356,
19.0688805084781));
#247630=CARTESIAN_POINT('',(-3.22275,-3.50678552687464E-13,19.77725));
#247631=CARTESIAN_POINT('Origin',(0.,0.,19.77725));
#247632=CARTESIAN_POINT('',(-3.,-3.67394039744206E-16,20.));
#247633=CARTESIAN_POINT('',(-3.5,4.28626379701574E-16,19.5));
#247634=CARTESIAN_POINT('Origin',(0.,0.,20.));
#247635=CARTESIAN_POINT('',(-1.54513563095215,-2.82819261091993,19.77725));
#247636=CARTESIAN_POINT('Origin',(0.,0.,19.77725));
#247637=CARTESIAN_POINT('Ctrl Pts',(-3.72907923291372,-0.00301811260641736,
19.2709195457389));
#247638=CARTESIAN_POINT('Ctrl Pts',(-3.71732607315158,-0.0973557598520273,
19.2825963499489));
#247639=CARTESIAN_POINT('Ctrl Pts',(-3.70184284765992,-0.19102707851843,
19.2944247832023));
#247640=CARTESIAN_POINT('Ctrl Pts',(-3.68258976228466,-0.283865185503344,
19.3064858466733));
#247641=CARTESIAN_POINT('Ctrl Pts',(-3.65909155554632,-0.397173208015436,
19.3212062593969));
#247642=CARTESIAN_POINT('Ctrl Pts',(-3.62997830197441,-0.509247625521539,
19.3362734645736));
#247643=CARTESIAN_POINT('Ctrl Pts',(-3.59537764216538,-0.619795875562299,
19.3515911252785));
#247644=CARTESIAN_POINT('Ctrl Pts',(-3.56079454951504,-0.730287998966675,
19.3669010090283));
#247645=CARTESIAN_POINT('Ctrl Pts',(-3.52072781136372,-0.839255856288323,
19.3824605958806));
#247646=CARTESIAN_POINT('Ctrl Pts',(-3.47527674613691,-0.946329469354909,
19.3981826910836));
#247647=CARTESIAN_POINT('Ctrl Pts',(-3.46098767994945,-0.97999164946893,
19.4031254588239));
#247648=CARTESIAN_POINT('Ctrl Pts',(-3.44616634251706,-1.01346601192478,
19.4080843853173));
#247649=CARTESIAN_POINT('Ctrl Pts',(-3.43081567631547,-1.04673941322125,
19.4130570670775));
#247650=CARTESIAN_POINT('Ctrl Pts',(-3.42493621336561,-1.05948346794626,
19.4149616553075));
#247651=CARTESIAN_POINT('Ctrl Pts',(-3.41897973743929,-1.0721965657576,
19.4168680465519));
#247652=CARTESIAN_POINT('Ctrl Pts',(-3.41295050270049,-1.08486973062788,
19.4187748651731));
#247653=CARTESIAN_POINT('Ctrl Pts',(-3.3645837579527,-1.18653432936764,
19.4340714348914));
#247654=CARTESIAN_POINT('Ctrl Pts',(-3.31146599038082,-1.28578496005253,
19.4494162238301));
#247655=CARTESIAN_POINT('Ctrl Pts',(-3.25379544256635,-1.38229577327628,
19.4647593594095));
#247656=CARTESIAN_POINT('Ctrl Pts',(-3.19622520881502,-1.47863871239134,
19.4800758066301));
#247657=CARTESIAN_POINT('Ctrl Pts',(-3.13411702103349,-1.57225100599859,
19.4953903618227));
#247658=CARTESIAN_POINT('Ctrl Pts',(-3.0676673887165,-1.66276180456701,
19.5106791453749));
#247659=CARTESIAN_POINT('Ctrl Pts',(-3.0021465554394,-1.75200748939619,
19.5257542301151));
#247660=CARTESIAN_POINT('Ctrl Pts',(-2.93240420076956,-1.83823724984042,
19.5408041109178));
#247661=CARTESIAN_POINT('Ctrl Pts',(-2.85863980690601,-1.92105686787767,
19.5558337677679));
#247662=CARTESIAN_POINT('Ctrl Pts',(-2.81383532908736,-1.97136148701632,
19.5649627782795));
#247663=CARTESIAN_POINT('Ctrl Pts',(-2.76754725817361,-2.02040726935002,
19.574084881253));
#247664=CARTESIAN_POINT('Ctrl Pts',(-2.71982338200487,-2.06810000982114,
19.5832066378075));
#247665=CARTESIAN_POINT('Ctrl Pts',(-2.69328594074255,-2.09462013770045,
19.5882789013831));
#247666=CARTESIAN_POINT('Ctrl Pts',(-2.6663045863994,-2.12072182447228,
19.5933511331322));
#247667=CARTESIAN_POINT('Ctrl Pts',(-2.63888788001173,-2.14638835604203,
19.5984250385703));
#247668=CARTESIAN_POINT('Ctrl Pts',(-2.62778918242003,-2.1567785563853,
19.6004790322656));
#247669=CARTESIAN_POINT('Ctrl Pts',(-2.61662239946336,-2.16709434556364,
19.6025326982287));
#247670=CARTESIAN_POINT('Ctrl Pts',(-2.60539419598218,-2.17732943764041,
19.6045850921466));
#247671=CARTESIAN_POINT('Ctrl Pts',(-2.52605958296763,-2.2496470680111,
19.6190865996673));
#247672=CARTESIAN_POINT('Ctrl Pts',(-2.44357065075068,-2.31802061246615,
19.6335390243701));
#247673=CARTESIAN_POINT('Ctrl Pts',(-2.35818713366859,-2.38218174582851,
19.6480100794366));
#247674=CARTESIAN_POINT('Ctrl Pts',(-2.27399720972799,-2.44544595796592,
19.6622788407505));
#247675=CARTESIAN_POINT('Ctrl Pts',(-2.18699327598033,-2.50461492306674,
19.6765659173718));
#247676=CARTESIAN_POINT('Ctrl Pts',(-2.09740996719078,-2.55941822033091,
19.6909593237566));
#247677=CARTESIAN_POINT('Ctrl Pts',(-2.01001005421766,-2.61288580794571,
19.7050019225668));
#247678=CARTESIAN_POINT('Ctrl Pts',(-1.92015522309492,-2.66219835190401,
19.7191460218339));
#247679=CARTESIAN_POINT('Ctrl Pts',(-1.82804613218824,-2.7070875228198,
19.7334918463878));
#247680=CARTESIAN_POINT('Ctrl Pts',(-1.74640674880859,-2.74687430388468,
19.7462070329033));
#247681=CARTESIAN_POINT('Ctrl Pts',(-1.66299749211945,-2.7831858303728,
19.7590809473144));
#247682=CARTESIAN_POINT('Ctrl Pts',(-1.57794048331916,-2.81581954168268,
19.7721933359912));
#247683=CARTESIAN_POINT('Ctrl Pts',(-1.56703248807982,-2.82000459794824,
19.773874912563));
#247684=CARTESIAN_POINT('Ctrl Pts',(-1.55609743761987,-2.8241291126961,
19.7755604111672));
#247685=CARTESIAN_POINT('Ctrl Pts',(-1.54513563095217,-2.82819261092003,
19.7772499999999));
#247686=CARTESIAN_POINT('Origin',(0.,0.,-2.31077344927308));
#247687=CARTESIAN_POINT('',(-3.22274978348675,0.00118132810417647,1.06077344921939));
#247688=CARTESIAN_POINT('',(-3.22274921729244,0.00224609459589272,0.814226550726902));
#247689=CARTESIAN_POINT('',(-3.22275,-3.50678552687464E-13,-2.31077344927308));
#247690=CARTESIAN_POINT('',(-1.87152083515305,-2.62364771379239,7.67940544457724E-5));
#247691=CARTESIAN_POINT('Ctrl Pts',(-1.87152083515305,-2.62364771379239,
7.67940544461609E-5));
#247692=CARTESIAN_POINT('Ctrl Pts',(-1.79128701262451,-2.68088072939763,
0.00619382745291832));
#247693=CARTESIAN_POINT('Ctrl Pts',(-1.70827916512899,-2.73453404989049,
0.01231086085139));
#247694=CARTESIAN_POINT('Ctrl Pts',(-1.62285367642187,-2.78432460525421,
0.0184278942498621));
#247695=CARTESIAN_POINT('Ctrl Pts',(-1.53753803913513,-2.83405113331987,
0.0245370615557027));
#247696=CARTESIAN_POINT('Ctrl Pts',(-1.44981131701081,-2.8799245447086,
0.0306462288615435));
#247697=CARTESIAN_POINT('Ctrl Pts',(-1.36006067539097,-2.92170370191008,
0.0367553961673841));
#247698=CARTESIAN_POINT('Ctrl Pts',(-1.27012268459411,-2.96357007064094,
0.0428773160000743));
#247699=CARTESIAN_POINT('Ctrl Pts',(-1.17815268266129,-3.00132481674489,
0.0489992358327648));
#247700=CARTESIAN_POINT('Ctrl Pts',(-1.08456726970077,-3.03477040317613,
0.0551211556654549));
#247701=CARTESIAN_POINT('Ctrl Pts',(-0.991325256568774,-3.0680932652609,
0.0612206118881195));
#247702=CARTESIAN_POINT('Ctrl Pts',(-0.896480082078013,-3.09713837625361,
0.0673200681107845));
#247703=CARTESIAN_POINT('Ctrl Pts',(-0.800464647125199,-3.12175814425185,
0.073419524333449));
#247704=CARTESIAN_POINT('Ctrl Pts',(-0.704476256382932,-3.14637097771721,
0.0795172625513117));
#247705=CARTESIAN_POINT('Ctrl Pts',(-0.607318688578545,-3.16656083456988,
0.0856150007691736));
#247706=CARTESIAN_POINT('Ctrl Pts',(-0.509439092134675,-3.18223025155393,
0.0917127389870362));
#247707=CARTESIAN_POINT('Ctrl Pts',(-0.4115597591698,-3.19789962635798,
0.09781046079059));
#247708=CARTESIAN_POINT('Ctrl Pts',(-0.312958838800098,-3.20904851669443,
0.103908182594144));
#247709=CARTESIAN_POINT('Ctrl Pts',(-0.214091622340587,-3.21563093960479,
0.110005904397697));
#247710=CARTESIAN_POINT('Ctrl Pts',(-0.114544904462395,-3.22225860264495,
0.116145535043885));
#247711=CARTESIAN_POINT('Ctrl Pts',(-0.0147286687435439,-3.22425674435509,
0.122285165690072));
#247712=CARTESIAN_POINT('Ctrl Pts',(0.0848907776275571,-3.22163174779083,
0.12842479633626));
#247713=CARTESIAN_POINT('Ctrl Pts',(0.183965536554572,-3.21902110387278,
0.134530857435074));
#247714=CARTESIAN_POINT('Ctrl Pts',(0.282845212155482,-3.2118378409206,
0.140636918533888));
#247715=CARTESIAN_POINT('Ctrl Pts',(0.381076252659278,-3.20014038007072,
0.146742979632702));
#247716=CARTESIAN_POINT('Ctrl Pts',(0.480117366510128,-3.18834645479153,
0.152899395052576));
#247717=CARTESIAN_POINT('Ctrl Pts',(0.578498646385012,-3.17196361674406,
0.15905581047245));
#247718=CARTESIAN_POINT('Ctrl Pts',(0.675767254513531,-3.15110396214204,
0.165212225892324));
#247719=CARTESIAN_POINT('Ctrl Pts',(0.773035862642052,-3.13024430754001,
0.171368641312199));
#247720=CARTESIAN_POINT('Ctrl Pts',(0.869191376290511,-3.1049080144529,
0.177525056732073));
#247721=CARTESIAN_POINT('Ctrl Pts',(0.963799540515554,-3.07525738893544,
0.183681472151948));
#247722=CARTESIAN_POINT('Ctrl Pts',(1.0588688509138,-3.04546223812672,0.18986789563122));
#247723=CARTESIAN_POINT('Ctrl Pts',(1.15271366098345,-3.01120482551079,
0.196054319110491));
#247724=CARTESIAN_POINT('Ctrl Pts',(1.24488592317186,-2.97260434649291,
0.202240742589763));
#247725=CARTESIAN_POINT('Ctrl Pts',(1.33693776245938,-2.93405429893401,
0.208419083517474));
#247726=CARTESIAN_POINT('Ctrl Pts',(1.42732100254314,-2.89117263032656,
0.214597424445185));
#247727=CARTESIAN_POINT('Ctrl Pts',(1.51560286257366,-2.84412825404526,
0.220775765372896));
#247728=CARTESIAN_POINT('Ctrl Pts',(1.60379510779988,-2.79713163245073,
0.226947834674558));
#247729=CARTESIAN_POINT('Ctrl Pts',(1.68988983509325,-2.7459809074072,0.23311990397622));
#247730=CARTESIAN_POINT('Ctrl Pts',(1.77347523023534,-2.69089263446941,
0.239291973277882));
#247731=CARTESIAN_POINT('Ctrl Pts',(1.85700387082497,-2.63584176651452,
0.245459851739382));
#247732=CARTESIAN_POINT('Ctrl Pts',(1.93802620718757,-2.57685890354785,
0.251627730200881));
#247733=CARTESIAN_POINT('Ctrl Pts',(2.01615675376923,-2.51420554186222,
0.25779560866238));
#247734=CARTESIAN_POINT('Ctrl Pts',(2.09426018272848,-2.45157392596335,
0.263961346370915));
#247735=CARTESIAN_POINT('Ctrl Pts',(2.16947347983138,-2.38527461311472,
0.27012708407945));
#247736=CARTESIAN_POINT('Ctrl Pts',(2.24144250557063,-2.31561073082702,
0.276292821787985));
#247737=CARTESIAN_POINT('Ctrl Pts',(2.31340554305196,-2.24595264499537,
0.282458046469877));
#247738=CARTESIAN_POINT('Ctrl Pts',(2.38212453560621,-2.17293084695873,
0.288623271151769));
#247739=CARTESIAN_POINT('Ctrl Pts',(2.44728135326857,-2.0968861534294,0.294788495833661));
#247740=CARTESIAN_POINT('Ctrl Pts',(2.51244994239862,-2.02082772138913,
0.30095483434747));
#247741=CARTESIAN_POINT('Ctrl Pts',(2.57405479696641,-1.94174563691404,
0.30712117286128));
#247742=CARTESIAN_POINT('Ctrl Pts',(2.63181795262218,-1.86001393187137,
0.313287511375088));
#247743=CARTESIAN_POINT('Ctrl Pts',(2.68964329587142,-1.77819423478622,
0.319460488545465));
#247744=CARTESIAN_POINT('Ctrl Pts',(2.74361843185147,-1.6937195746257,0.325633465715842));
#247745=CARTESIAN_POINT('Ctrl Pts',(2.79350871979648,-1.60699302889622,
0.331806442886218));
#247746=CARTESIAN_POINT('Ctrl Pts',(2.8434276369906,-1.52021671564714,0.337982962383338));
#247747=CARTESIAN_POINT('Ctrl Pts',(2.88925683988024,-1.43118632719822,
0.344159481880458));
#247748=CARTESIAN_POINT('Ctrl Pts',(2.93080860004921,-1.34032776304067,
0.350336001377578));
#247749=CARTESIAN_POINT('Ctrl Pts',(2.97242830962644,-1.24932061827797,
0.356522621309513));
#247750=CARTESIAN_POINT('Ctrl Pts',(3.00975644428611,-1.15647972746503,
0.362709241241448));
#247751=CARTESIAN_POINT('Ctrl Pts',(3.04265413891859,-1.06224919553822,
0.368895861173383));
#247752=CARTESIAN_POINT('Ctrl Pts',(3.06516591177251,-0.997767585068575,
0.37312934270445));
#247753=CARTESIAN_POINT('Ctrl Pts',(3.08560412160844,-0.93263559411187,
0.377362824235516));
#247754=CARTESIAN_POINT('Ctrl Pts',(3.10393805760351,-0.86699832586953,
0.381596305766583));
#247755=CARTESIAN_POINT('Ctrl Pts',(3.13064891965725,-0.771370850237589,
0.387764099807853));
#247756=CARTESIAN_POINT('Ctrl Pts',(3.15298395288961,-0.674337722705913,
0.393931893849122));
#247757=CARTESIAN_POINT('Ctrl Pts',(3.17079708643209,-0.576336185896548,
0.400099687890392));
#247758=CARTESIAN_POINT('Ctrl Pts',(3.18858597964063,-0.478468010798811,
0.406259088720728));
#247759=CARTESIAN_POINT('Ctrl Pts',(3.20186512627604,-0.379634469888541,
0.412418489551064));
#247760=CARTESIAN_POINT('Ctrl Pts',(3.21053835167315,-0.280287450550098,
0.4185778903814));
#247761=CARTESIAN_POINT('Ctrl Pts',(3.21920234703497,-0.18104615618158,
0.424730736385312));
#247762=CARTESIAN_POINT('Ctrl Pts',(3.22327012806913,-0.081292900734927,
0.430883582389223));
#247763=CARTESIAN_POINT('Ctrl Pts',(3.22269683317995,0.0185117236352813,
0.437036428393134));
#247764=CARTESIAN_POINT('Ctrl Pts',(3.22212396099534,0.118242759572707,
0.443184737750598));
#247765=CARTESIAN_POINT('Ctrl Pts',(3.21691681880613,0.218024655391256,
0.449333047108062));
#247766=CARTESIAN_POINT('Ctrl Pts',(3.20708255632381,0.317394138924411,
0.455481356465526));
#247767=CARTESIAN_POINT('Ctrl Pts',(3.1972520475349,0.416725693576094,0.461627319041176));
#247768=CARTESIAN_POINT('Ctrl Pts',(3.18279797050033,0.515644716249514,
0.467773281616825));
#247769=CARTESIAN_POINT('Ctrl Pts',(3.16377947627986,0.613691280669986,
0.473919244192474));
#247770=CARTESIAN_POINT('Ctrl Pts',(3.14476313435015,0.711726749326874,
0.480064511239952));
#247771=CARTESIAN_POINT('Ctrl Pts',(3.12118348507223,0.808889528923773,
0.486209778287429));
#247772=CARTESIAN_POINT('Ctrl Pts',(3.09315094070796,0.904729142062675,
0.492355045334906));
#247773=CARTESIAN_POINT('Ctrl Pts',(3.06511404127982,1.00058364459696,0.49850126709524));
#247774=CARTESIAN_POINT('Ctrl Pts',(3.03262299497265,1.09511415479859,0.504647488855574));
#247775=CARTESIAN_POINT('Ctrl Pts',(2.99583800178979,1.18788561298308,0.510793710615907));
#247776=CARTESIAN_POINT('Ctrl Pts',(2.95901401252014,1.28075541898609,0.516946448038645));
#247777=CARTESIAN_POINT('Ctrl Pts',(2.91788714758439,1.37186204419843,0.523099185461383));
#247778=CARTESIAN_POINT('Ctrl Pts',(2.87266562126227,1.46079081011549,0.529251922884121));
#247779=CARTESIAN_POINT('Ctrl Pts',(2.82741878839573,1.54976934170717,0.535408103457402));
#247780=CARTESIAN_POINT('Ctrl Pts',(2.77807294608138,1.63656720882083,0.541564284030684));
#247781=CARTESIAN_POINT('Ctrl Pts',(2.72488105641269,1.72079655709305,0.547720464603965));
#247782=CARTESIAN_POINT('Ctrl Pts',(2.67160150018635,1.80516472534443,0.553886791294679));
#247783=CARTESIAN_POINT('Ctrl Pts',(2.61446348552986,1.88695556308096,0.560053117985394));
#247784=CARTESIAN_POINT('Ctrl Pts',(2.55376191401101,1.96581221103309,0.566219444676109));
#247785=CARTESIAN_POINT('Ctrl Pts',(2.51014725235934,2.02247146932511,0.570650009577805));
#247786=CARTESIAN_POINT('Ctrl Pts',(2.46469374932749,2.07761661373107,0.575080574479501));
#247787=CARTESIAN_POINT('Ctrl Pts',(2.41752243029318,2.1311271340606,0.579511139381198));
#247788=CARTESIAN_POINT('Ctrl Pts',(2.35174975841072,2.20573878300207,0.585688835860732));
#247789=CARTESIAN_POINT('Ctrl Pts',(2.28240614186831,2.27743157497007,0.591866532340266));
#247790=CARTESIAN_POINT('Ctrl Pts',(2.20978063521303,2.34584464676106,0.598044228819799));
#247791=CARTESIAN_POINT('Ctrl Pts',(2.13725244314113,2.41416604842284,0.604213647491896));
#247792=CARTESIAN_POINT('Ctrl Pts',(2.06145141495303,2.47921617061427,0.610383066163992));
#247793=CARTESIAN_POINT('Ctrl Pts',(1.9827059515682,2.54066815466248,0.616552484836088));
#247794=CARTESIAN_POINT('Ctrl Pts',(1.90404285857504,2.60205585787751,0.622715450089655));
#247795=CARTESIAN_POINT('Ctrl Pts',(1.82244179393401,2.65985264087373,0.628878415343223));
#247796=CARTESIAN_POINT('Ctrl Pts',(1.73826629504038,2.71377004368951,0.63504138059679));
#247797=CARTESIAN_POINT('Ctrl Pts',(1.65415124531696,2.76764872666042,0.641199920024072));
#247798=CARTESIAN_POINT('Ctrl Pts',(1.56746580117371,2.81765333547917,0.647358459451355));
#247799=CARTESIAN_POINT('Ctrl Pts',(1.47860397401242,2.86353764608302,0.653516998878637));
#247800=CARTESIAN_POINT('Ctrl Pts',(1.38977507297627,2.90940495509461,0.659673256371748));
#247801=CARTESIAN_POINT('Ctrl Pts',(1.29877177613583,2.95115480101006,0.66582951386486));
#247802=CARTESIAN_POINT('Ctrl Pts',(1.2060135139842,2.9885864495757,0.671985771357971));
#247803=CARTESIAN_POINT('Ctrl Pts',(1.11326493675272,3.02601418989081,0.678141386074247));
#247804=CARTESIAN_POINT('Ctrl Pts',(1.01876216053388,3.05912446716541,0.684297000790522));
#247805=CARTESIAN_POINT('Ctrl Pts',(0.922944527480625,3.08776471929025,
0.690452615506798));
#247806=CARTESIAN_POINT('Ctrl Pts',(0.827111400001406,3.11640960275748,
0.696609225631888));
#247807=CARTESIAN_POINT('Ctrl Pts',(0.729963408681899,3.14058290113278,
0.702765835756979));
#247808=CARTESIAN_POINT('Ctrl Pts',(0.631954016389179,3.16018222317473,
0.708922445882069));
#247809=CARTESIAN_POINT('Ctrl Pts',(0.533840905623936,3.17980228620586,
0.715085571241905));
#247810=CARTESIAN_POINT('Ctrl Pts',(0.434864999483574,3.19483862244009,
0.721248696601742));
#247811=CARTESIAN_POINT('Ctrl Pts',(0.33548876722234,3.20524021713937,0.727411821961578));
#247812=CARTESIAN_POINT('Ctrl Pts',(0.23605676392719,3.21564764932793,0.733578406135113));
#247813=CARTESIAN_POINT('Ctrl Pts',(0.136224419780004,3.22141513477925,
0.739744990308648));
#247814=CARTESIAN_POINT('Ctrl Pts',(0.0364560542900044,3.2225437962277,
0.745911574482183));
#247815=CARTESIAN_POINT('Ctrl Pts',(-0.0634751617003769,3.22367429997436,
0.75208822428437));
#247816=CARTESIAN_POINT('Ctrl Pts',(-0.163341757182965,3.22015087153828,
0.758264874086558));
#247817=CARTESIAN_POINT('Ctrl Pts',(-0.262682585611081,3.21202668446523,
0.764441523888745));
#247818=CARTESIAN_POINT('Ctrl Pts',(-0.332293457323671,3.20633384142113,
0.768769673591109));
#247819=CARTESIAN_POINT('Ctrl Pts',(-0.401646275419367,3.19838303131296,
0.773097823293472));
#247820=CARTESIAN_POINT('Ctrl Pts',(-0.470585672091414,3.18820744113715,
0.777425972995835));
#247821=CARTESIAN_POINT('Ctrl Pts',(-0.568975958136059,3.173684841921,0.783603106939803));
#247822=CARTESIAN_POINT('Ctrl Pts',(-0.666863183878244,3.15457832544767,
0.789780240883771));
#247823=CARTESIAN_POINT('Ctrl Pts',(-0.763787336524841,3.13093380113095,
0.795957374827739));
#247824=CARTESIAN_POINT('Ctrl Pts',(-0.860581873702995,3.10732089634364,
0.802126248167018));
#247825=CARTESIAN_POINT('Ctrl Pts',(-0.956415480169123,3.07918214831494,
0.808295121506298));
#247826=CARTESIAN_POINT('Ctrl Pts',(-1.05083523750127,3.04661498488497,
0.814463994845578));
#247827=CARTESIAN_POINT('Ctrl Pts',(-1.14515649358677,3.01408179640144,
0.820626432649208));
#247828=CARTESIAN_POINT('Ctrl Pts',(-1.23806642539856,2.97712951833294,
0.826788870452837));
#247829=CARTESIAN_POINT('Ctrl Pts',(-1.32912518798289,2.93590595850232,
0.832951308256467));
#247830=CARTESIAN_POINT('Ctrl Pts',(-1.42011898523278,2.89471180937613,
0.839109349505372));
#247831=CARTESIAN_POINT('Ctrl Pts',(-1.50926384531011,2.84925261556918,
0.845267390754277));
#247832=CARTESIAN_POINT('Ctrl Pts',(-1.59613875285414,2.79972474435206,
0.851425432003182));
#247833=CARTESIAN_POINT('Ctrl Pts',(-1.6829817249642,2.75021507970466,0.857581209540673));
#247834=CARTESIAN_POINT('Ctrl Pts',(-1.76755602643768,2.69663992421653,
0.863736987078165));
#247835=CARTESIAN_POINT('Ctrl Pts',(-1.84946495672966,2.63924173510669,
0.869892764615657));
#247836=CARTESIAN_POINT('Ctrl Pts',(-1.93136558545734,2.58184936336933,
0.876047918258016));
#247837=CARTESIAN_POINT('Ctrl Pts',(-2.0106010251037,2.52063497727754,0.882203071900374));
#247838=CARTESIAN_POINT('Ctrl Pts',(-2.08680413946703,2.45588396427911,
0.888358225542733));
#247839=CARTESIAN_POINT('Ctrl Pts',(-2.1630198194789,2.39112227404683,0.894514394150136));
#247840=CARTESIAN_POINT('Ctrl Pts',(-2.23620185057499,2.32282307924975,
0.900670562757539));
#247841=CARTESIAN_POINT('Ctrl Pts',(-2.30601749120835,2.25131092760222,
0.906826731364942));
#247842=CARTESIAN_POINT('Ctrl Pts',(-2.3759073959641,2.17972270722374,0.912989448396951));
#247843=CARTESIAN_POINT('Ctrl Pts',(-2.44242345656973,2.10491501642267,
0.919152165428961));
#247844=CARTESIAN_POINT('Ctrl Pts',(-2.50527112082526,2.02724793097908,
0.92531488246097));
#247845=CARTESIAN_POINT('Ctrl Pts',(-2.5681542409122,1.94953702925177,0.93148107622133));
#247846=CARTESIAN_POINT('Ctrl Pts',(-2.62736458637439,1.86896386958431,
0.93764726998169));
#247847=CARTESIAN_POINT('Ctrl Pts',(-2.68265033179356,1.78591846393611,
0.94381346374205));
#247848=CARTESIAN_POINT('Ctrl Pts',(-2.73802662326239,1.7027370479408,0.949989756389243));
#247849=CARTESIAN_POINT('Ctrl Pts',(-2.78946525347622,1.61707567059967,
0.956166049036436));
#247850=CARTESIAN_POINT('Ctrl Pts',(-2.83675978469182,1.52935002090928,
0.962342341683629));
#247851=CARTESIAN_POINT('Ctrl Pts',(-2.86993806495115,1.46780831372772,
0.966675163325904));
#247852=CARTESIAN_POINT('Ctrl Pts',(-2.90107785822629,1.40525120745208,
0.971007984968179));
#247853=CARTESIAN_POINT('Ctrl Pts',(-2.93012223651133,1.34182757521295,
0.975340806610454));
#247854=CARTESIAN_POINT('Ctrl Pts',(-2.97519609107558,1.24340069385822,
0.98206489519793));
#247855=CARTESIAN_POINT('Ctrl Pts',(-3.01535773768093,1.14258916682412,
0.988788983785406));
#247856=CARTESIAN_POINT('Ctrl Pts',(-3.05037101870565,1.0398818253728,0.995513072372882));
#247857=CARTESIAN_POINT('Ctrl Pts',(-3.08525396049592,0.937556818734572,
1.00221213009969));
#247858=CARTESIAN_POINT('Ctrl Pts',(-3.11502664347812,0.83335035784085,
1.0089111878265));
#247859=CARTESIAN_POINT('Ctrl Pts',(-3.13950132278114,0.727769885853671,
1.01561024555331));
#247860=CARTESIAN_POINT('Ctrl Pts',(-3.16391653004058,0.622445968257002,
1.02229302496047));
#247861=CARTESIAN_POINT('Ctrl Pts',(-3.18305930980102,0.515754989028655,
1.02897580436762));
#247862=CARTESIAN_POINT('Ctrl Pts',(-3.19679113100839,0.408220561958983,
1.03565858377478));
#247863=CARTESIAN_POINT('Ctrl Pts',(-3.21047458455517,0.301064903924503,
1.04231782439555));
#247864=CARTESIAN_POINT('Ctrl Pts',(-3.21878502250993,0.193072023646205,
1.04897706501631));
#247865=CARTESIAN_POINT('Ctrl Pts',(-3.22163478414336,0.0847754687252713,
1.05563630563708));
#247866=CARTESIAN_POINT('Ctrl Pts',(-3.22236758214641,0.0569277013004861,
1.05734868683118));
#247867=CARTESIAN_POINT('Ctrl Pts',(-3.22273956433623,0.0290599208778919,
1.05906106802528));
#247868=CARTESIAN_POINT('Ctrl Pts',(-3.22274978348675,0.00118132810417647,
1.06077344921939));
#247869=CARTESIAN_POINT('',(1.87158653173903,-2.62360084935058,0.));
#247870=CARTESIAN_POINT('Origin',(0.,0.,0.));
#247871=CARTESIAN_POINT('Ctrl Pts',(1.87158653173902,-2.62360084935058,
-3.99680288865056E-15));
#247872=CARTESIAN_POINT('Ctrl Pts',(1.95492543847218,-2.56414974212509,
0.00631946307768746));
#247873=CARTESIAN_POINT('Ctrl Pts',(2.03548387446147,-2.50068513957169,
0.0126389261553787));
#247874=CARTESIAN_POINT('Ctrl Pts',(2.11287029831822,-2.43349474315945,
0.0189583892330702));
#247875=CARTESIAN_POINT('Ctrl Pts',(2.19021266751125,-2.36634259700056,
0.0252742547569941));
#247876=CARTESIAN_POINT('Ctrl Pts',(2.26438631500752,-2.29546914473324,
0.0315901202809182));
#247877=CARTESIAN_POINT('Ctrl Pts',(2.33503251876323,-2.22120253439848,
0.0379059858048421));
#247878=CARTESIAN_POINT('Ctrl Pts',(2.40565481867404,-2.14696105290915,
0.0442197142929191));
#247879=CARTESIAN_POINT('Ctrl Pts',(2.47275177340866,-2.06932899274331,
0.0505334427809963));
#247880=CARTESIAN_POINT('Ctrl Pts',(2.53600172914556,-1.98867111214267,
0.0568471712690735));
#247881=CARTESIAN_POINT('Ctrl Pts',(2.59926252374806,-1.90799940955721,
0.0631619817129206));
#247882=CARTESIAN_POINT('Ctrl Pts',(2.65867474659795,-1.82430116432855,
0.0694767921567673));
#247883=CARTESIAN_POINT('Ctrl Pts',(2.71395737767804,-1.7379737957308,0.0757916026006145));
#247884=CARTESIAN_POINT('Ctrl Pts',(2.7692484525325,-1.65163324163867,0.0821073775577904));
#247885=CARTESIAN_POINT('Ctrl Pts',(2.82040846123542,-1.56266310548976,
0.0884231525149662));
#247886=CARTESIAN_POINT('Ctrl Pts',(2.86720056961815,-1.4714885171422,0.0947389274721422));
#247887=CARTESIAN_POINT('Ctrl Pts',(2.91400965186176,-1.38028085516681,
0.101056993479864));
#247888=CARTESIAN_POINT('Ctrl Pts',(2.95644749454226,-1.28686750908988,
0.107375059487585));
#247889=CARTESIAN_POINT('Ctrl Pts',(2.99432422469011,-1.19169627000087,
0.113693125495307));
#247890=CARTESIAN_POINT('Ctrl Pts',(3.0322226534121,-1.09647050983308,0.120014810955479));
#247891=CARTESIAN_POINT('Ctrl Pts',(3.06555461802173,-0.999485227527157,
0.126336496415651));
#247892=CARTESIAN_POINT('Ctrl Pts',(3.09417939463669,-0.901205546091291,
0.132658181875823));
#247893=CARTESIAN_POINT('Ctrl Pts',(3.12284606342699,-0.802782032977649,
0.138989119081756));
#247894=CARTESIAN_POINT('Ctrl Pts',(3.14679167349174,-0.703060726745416,
0.14532005628769));
#247895=CARTESIAN_POINT('Ctrl Pts',(3.16592605622274,-0.602519517551057,
0.151650993493623));
#247896=CARTESIAN_POINT('Ctrl Pts',(3.18507609504922,-0.501896043734193,
0.157987110786045));
#247897=CARTESIAN_POINT('Ctrl Pts',(3.19940700326259,-0.400451730043345,
0.164323228078468));
#247898=CARTESIAN_POINT('Ctrl Pts',(3.208880426794,-0.298670335049077,0.17065934537089));
#247899=CARTESIAN_POINT('Ctrl Pts',(3.21837017823093,-0.196713514877829,
0.17700638326916));
#247900=CARTESIAN_POINT('Ctrl Pts',(3.22298570268855,-0.0944188568314729,
0.183353421167431));
#247901=CARTESIAN_POINT('Ctrl Pts',(3.22274073245243,0.00772877040364258,
0.189700459065702));
#247902=CARTESIAN_POINT('Ctrl Pts',(3.2226368829715,0.0510319007561665,
0.192391139377135));
#247903=CARTESIAN_POINT('Ctrl Pts',(3.22166017418701,0.0943086603682532,
0.195081819688569));
#247904=CARTESIAN_POINT('Ctrl Pts',(3.21981445683011,0.137522456667455,
0.197772500000002));
#247905=CARTESIAN_POINT('Ctrl Pts',(3.21562008643828,0.235725286606468,
0.203887038496331));
#247906=CARTESIAN_POINT('Ctrl Pts',(3.20691991595699,0.333942178358137,
0.21000157699266));
#247907=CARTESIAN_POINT('Ctrl Pts',(3.19370248745656,0.431719798148999,
0.216116115488989));
#247908=CARTESIAN_POINT('Ctrl Pts',(3.18050477959944,0.529351531955746,
0.222221530982858));
#247909=CARTESIAN_POINT('Ctrl Pts',(3.16280326081571,0.626544861148386,
0.228326946476726));
#247910=CARTESIAN_POINT('Ctrl Pts',(3.14063845087156,0.722846929444312,
0.234432361970594));
#247911=CARTESIAN_POINT('Ctrl Pts',(3.11849984119223,0.819035162354429,
0.240530560461333));
#247912=CARTESIAN_POINT('Ctrl Pts',(3.09190852211019,0.914333798479899,
0.246628758952073));
#247913=CARTESIAN_POINT('Ctrl Pts',(3.06095661357545,1.00829666879779,0.252726957442812));
#247914=CARTESIAN_POINT('Ctrl Pts',(3.0300317624365,1.10217739908968,0.258819825038688));
#247915=CARTESIAN_POINT('Ctrl Pts',(2.99475403662924,1.19472426481479,0.264912692634564));
#247916=CARTESIAN_POINT('Ctrl Pts',(2.95526602375376,1.28550390561313,0.27100556023044));
#247917=CARTESIAN_POINT('Ctrl Pts',(2.91579631979057,1.37624145575259,0.277095602822721));
#247918=CARTESIAN_POINT('Ctrl Pts',(2.87212038204646,1.46521300198972,0.283185645415002));
#247919=CARTESIAN_POINT('Ctrl Pts',(2.82442945658175,1.55200380389139,0.289275688007284));
#247920=CARTESIAN_POINT('Ctrl Pts',(2.77674728024902,1.63877868359877,0.295364613351662));
#247921=CARTESIAN_POINT('Ctrl Pts',(2.7250517932753,1.72337322507659,0.301453538696042));
#247922=CARTESIAN_POINT('Ctrl Pts',(2.66958033235958,1.80539702325526,0.307542464040421));
#247923=CARTESIAN_POINT('Ctrl Pts',(2.61410350441056,1.88742875748696,0.313631978506926));
#247924=CARTESIAN_POINT('Ctrl Pts',(2.55485022641688,1.96688888746183,0.319721492973432));
#247925=CARTESIAN_POINT('Ctrl Pts',(2.49210067160407,2.04341669883813,0.325811007439938));
#247926=CARTESIAN_POINT('Ctrl Pts',(2.42928653909573,2.1200232675812,0.331906788832358));
#247927=CARTESIAN_POINT('Ctrl Pts',(2.36296922687978,2.19369114808772,0.338002570224777));
#247928=CARTESIAN_POINT('Ctrl Pts',(2.29346849125129,2.2640936027774,0.344098351617197));
#247929=CARTESIAN_POINT('Ctrl Pts',(2.22393109264782,2.3345331961162,0.350197348651562));
#247930=CARTESIAN_POINT('Ctrl Pts',(2.15120725402708,2.40170363400882,0.356296345685926));
#247931=CARTESIAN_POINT('Ctrl Pts',(2.07565116067855,2.46531738761438,0.36239534272029));
#247932=CARTESIAN_POINT('Ctrl Pts',(1.99996714770689,2.52903884196289,0.368504665611479));
#247933=CARTESIAN_POINT('Ctrl Pts',(1.92144165573973,2.5891913161499,0.374613988502668));
#247934=CARTESIAN_POINT('Ctrl Pts',(1.84045931761003,2.64552963746816,0.380723311393857));
#247935=CARTESIAN_POINT('Ctrl Pts',(1.77496951785463,2.69109000861698,0.385663874262568));
#247936=CARTESIAN_POINT('Ctrl Pts',(1.70787361394654,2.73415678273328,0.39060443713128));
#247937=CARTESIAN_POINT('Ctrl Pts',(1.6393860656107,2.77462265729621,0.395544999999991));
#247938=CARTESIAN_POINT('Ctrl Pts',(1.55363981683965,2.8252858366817,0.401730573043608));
#247939=CARTESIAN_POINT('Ctrl Pts',(1.46539703945234,2.87205664003861,0.407916146087224));
#247940=CARTESIAN_POINT('Ctrl Pts',(1.37504551440431,2.91468135407914,0.414101719130841));
#247941=CARTESIAN_POINT('Ctrl Pts',(1.28481470585698,2.95724911826387,0.420279027779005));
#247942=CARTESIAN_POINT('Ctrl Pts',(1.19248113794149,2.99568162203976,0.42645633642717));
#247943=CARTESIAN_POINT('Ctrl Pts',(1.09845941233454,3.02976970774243,0.432633645075335));
#247944=CARTESIAN_POINT('Ctrl Pts',(1.00453588072825,3.06382219267849,0.438804502292774));
#247945=CARTESIAN_POINT('Ctrl Pts',(0.908928101182369,3.0935391345434,0.444975359510213));
#247946=CARTESIAN_POINT('Ctrl Pts',(0.812072143685353,3.11875879092152,
0.451146216727652));
#247947=CARTESIAN_POINT('Ctrl Pts',(0.715286187601124,3.1439602201134,0.457312614036434));
#247948=CARTESIAN_POINT('Ctrl Pts',(0.617254264392215,3.16467071848417,
0.463479011345218));
#247949=CARTESIAN_POINT('Ctrl Pts',(0.518428299268892,3.18077815337964,
0.469645408654));
#247950=CARTESIAN_POINT('Ctrl Pts',(0.419639277575774,3.1968795669436,0.475809500820927));
#247951=CARTESIAN_POINT('Ctrl Pts',(0.32005722994316,3.20838126724278,0.481973592987853));
#247952=CARTESIAN_POINT('Ctrl Pts',(0.220144143290919,3.21522225027675,
0.48813768515478));
#247953=CARTESIAN_POINT('Ctrl Pts',(0.120242016159254,3.2220624829196,0.494301101179099));
#247954=CARTESIAN_POINT('Ctrl Pts',(0.0200093533601731,3.22424298544074,
0.500464517203419));
#247955=CARTESIAN_POINT('Ctrl Pts',(-0.0800878465952649,3.22175472364482,
0.506627933227738));
#247956=CARTESIAN_POINT('Ctrl Pts',(-0.18020050520609,3.21926607757061,
0.512792301108097));
#247957=CARTESIAN_POINT('Ctrl Pts',(-0.280177227367024,3.21210724569945,
0.518956668988456));
#247958=CARTESIAN_POINT('Ctrl Pts',(-0.37955411058339,3.20032127131625,
0.525121036868815));
#247959=CARTESIAN_POINT('Ctrl Pts',(-0.47903394953257,3.18852308651157,
0.531291791113808));
#247960=CARTESIAN_POINT('Ctrl Pts',(-0.577912278700772,3.17208823786559,
0.537462545358803));
#247961=CARTESIAN_POINT('Ctrl Pts',(-0.675732526357839,3.15111140953824,
0.543633299603796));
#247962=CARTESIAN_POINT('Ctrl Pts',(-0.773606755744829,3.13012300522831,
0.549807459155943));
#247963=CARTESIAN_POINT('Ctrl Pts',(-0.870421322734032,3.10458773902362,
0.555981618708089));
#247964=CARTESIAN_POINT('Ctrl Pts',(-0.965733991792374,3.07465045486422,
0.562155778260236));
#247965=CARTESIAN_POINT('Ctrl Pts',(-1.06119901609093,3.04466531660353,
0.568339807072902));
#247966=CARTESIAN_POINT('Ctrl Pts',(-1.15515694141851,3.01026425460189,
0.574523835885568));
#247967=CARTESIAN_POINT('Ctrl Pts',(-1.24718462932257,2.97164063488194,
0.580707864698233));
#247968=CARTESIAN_POINT('Ctrl Pts',(-1.3097347681446,2.94538861410085,0.58491107646549));
#247969=CARTESIAN_POINT('Ctrl Pts',(-1.37139362992841,2.9171868686106,0.589114288232746));
#247970=CARTESIAN_POINT('Ctrl Pts',(-1.43203530093296,2.88710797501269,
0.593317500000002));
#247971=CARTESIAN_POINT('Ctrl Pts',(-1.52129718861555,2.8428331590738,0.599504443902765));
#247972=CARTESIAN_POINT('Ctrl Pts',(-1.60865229565399,2.79434124124621,
0.605691387805528));
#247973=CARTESIAN_POINT('Ctrl Pts',(-1.69367664058628,2.74182001590775,
0.611878331708291));
#247974=CARTESIAN_POINT('Ctrl Pts',(-1.77859006068519,2.6893673110404,0.618057203973193));
#247975=CARTESIAN_POINT('Ctrl Pts',(-1.86117839897765,2.6328959738107,0.624236076238095));
#247976=CARTESIAN_POINT('Ctrl Pts',(-1.94104052614948,2.5726405186783,0.630414948502997));
#247977=CARTESIAN_POINT('Ctrl Pts',(-2.02082172249445,2.51244612532799,
0.636587559211149));
#247978=CARTESIAN_POINT('Ctrl Pts',(-2.09788185801057,2.44847549797177,
0.642760169919301));
#247979=CARTESIAN_POINT('Ctrl Pts',(-2.17184795978842,2.38100693028451,
0.648932780627453));
#247980=CARTESIAN_POINT('Ctrl Pts',(-2.24576396690791,2.31358405670262,
0.655101210841876));
#247981=CARTESIAN_POINT('Ctrl Pts',(-2.31658978840695,2.24266824334093,
0.6612696410563));
#247982=CARTESIAN_POINT('Ctrl Pts',(-2.38398548044491,2.16857805751323,
0.667438071270724));
#247983=CARTESIAN_POINT('Ctrl Pts',(-2.4513578618263,2.09451349781718,0.673604367963643));
#247984=CARTESIAN_POINT('Ctrl Pts',(-2.51530218115938,2.01727706684051,
0.679770664656563));
#247985=CARTESIAN_POINT('Ctrl Pts',(-2.57551596160632,1.93722355292596,
0.685936961349482));
#247986=CARTESIAN_POINT('Ctrl Pts',(-2.63572479590579,1.85717661485638,
0.692102751523585));
#247987=CARTESIAN_POINT('Ctrl Pts',(-2.69220344112948,1.77431339925425,
0.698268541697687));
#247988=CARTESIAN_POINT('Ctrl Pts',(-2.74469087675724,1.68902029400051,
0.70443433187179));
#247989=CARTESIAN_POINT('Ctrl Pts',(-2.79718784336744,1.60371170071465,
0.710601241666945));
#247990=CARTESIAN_POINT('Ctrl Pts',(-2.84569193412304,1.51597270901757,
0.716768151462101));
#247991=CARTESIAN_POINT('Ctrl Pts',(-2.88998699003919,1.42621623883065,
0.722935061257257));
#247992=CARTESIAN_POINT('Ctrl Pts',(-2.93432967906764,1.33636324816448,
0.729108602697882));
#247993=CARTESIAN_POINT('Ctrl Pts',(-2.97445410399483,1.24448883502799,
0.735282144138506));
#247994=CARTESIAN_POINT('Ctrl Pts',(-3.01019143545741,1.15102783823802,
0.741455685579131));
#247995=CARTESIAN_POINT('Ctrl Pts',(-3.04594929758766,1.05751314922794,
0.747632773645164));
#247996=CARTESIAN_POINT('Ctrl Pts',(-3.07731491134282,0.962410471336915,
0.753809861711195));
#247997=CARTESIAN_POINT('Ctrl Pts',(-3.10416934776438,0.866169857995585,
0.759986949777228));
#247998=CARTESIAN_POINT('Ctrl Pts',(-3.13106756177693,0.769772355038621,
0.766174107614626));
#247999=CARTESIAN_POINT('Ctrl Pts',(-3.15343981370364,0.672233632573876,
0.772361265452025));
#248000=CARTESIAN_POINT('Ctrl Pts',(-3.17121828160923,0.574014087708131,
0.778548423289423));
#248001=CARTESIAN_POINT('Ctrl Pts',(-3.18323079876677,0.507649315773298,
0.782728948859614));
#248002=CARTESIAN_POINT('Ctrl Pts',(-3.19314714429896,0.440973884319493,
0.786909474429804));
#248003=CARTESIAN_POINT('Ctrl Pts',(-3.2009598565266,0.374130404277991,
0.791089999999995));
#248004=CARTESIAN_POINT('Ctrl Pts',(-3.21537265460941,0.250818351700129,
0.798802183575631));
#248005=CARTESIAN_POINT('Ctrl Pts',(-3.22266251386311,0.126650208984342,
0.806514367151267));
#248006=CARTESIAN_POINT('Ctrl Pts',(-3.22274921729245,0.00224609459589272,
0.814226550726902));
#248007=CARTESIAN_POINT('Origin',(0.,0.,-2.31077344927308));
#248008=CARTESIAN_POINT('',(-3.22275,1.20843135519762E-10,2.31096825019553));
#248009=CARTESIAN_POINT('',(-3.22275,-8.28983494685339E-13,2.06147698899067));
#248010=CARTESIAN_POINT('',(-3.22275,-3.50678552687464E-13,-2.31077344927308));
#248011=CARTESIAN_POINT('Ctrl Pts',(-3.22275,1.20843127171533E-10,2.31096825019553));
#248012=CARTESIAN_POINT('Ctrl Pts',(-3.22274999999303,0.185834148167105,
2.30055492199149));
#248013=CARTESIAN_POINT('Ctrl Pts',(-3.20667711875127,0.371301546871853,
2.29005533248189));
#248014=CARTESIAN_POINT('Ctrl Pts',(-3.16694702710074,0.598835624703661,
2.27638194280519));
#248015=CARTESIAN_POINT('Ctrl Pts',(-3.15824378544306,0.64315897761156,
2.27368177435837));
#248016=CARTESIAN_POINT('Ctrl Pts',(-3.14386419459536,0.70903539333966,
2.26960698121429));
#248017=CARTESIAN_POINT('Ctrl Pts',(-3.13889091598327,0.730737327962122,
2.26825455001991));
#248018=CARTESIAN_POINT('Ctrl Pts',(-3.12955360841005,0.769627304868333,
2.26581211517507));
#248019=CARTESIAN_POINT('Ctrl Pts',(-3.12527178862818,0.786834292470408,
2.26472477396117));
#248020=CARTESIAN_POINT('Ctrl Pts',(-3.1158281473904,0.82349100290969,2.26239369798068));
#248021=CARTESIAN_POINT('Ctrl Pts',(-3.11062573776534,0.842929395817087,
2.2611486999294));
#248022=CARTESIAN_POINT('Ctrl Pts',(-3.09596489022453,0.895723729794777,
2.25774250956016));
#248023=CARTESIAN_POINT('Ctrl Pts',(-3.08614988448032,0.928977040919678,
2.25556993721904));
#248024=CARTESIAN_POINT('Ctrl Pts',(-3.02080416833628,1.13789274972979,
2.24174391301209));
#248025=CARTESIAN_POINT('Ctrl Pts',(-2.95084136202242,1.30865338519323,
2.22961935399385));
#248026=CARTESIAN_POINT('Ctrl Pts',(-2.78409157437045,1.63328916879489,
2.20510166453211));
#248027=CARTESIAN_POINT('Ctrl Pts',(-2.6881084969062,1.78686125667515,2.192764539701));
#248028=CARTESIAN_POINT('Ctrl Pts',(-2.53445030375698,1.99208251759074,
2.17577453438));
#248029=CARTESIAN_POINT('Ctrl Pts',(-2.48702759135021,2.05098189487471,
2.17083592560627));
#248030=CARTESIAN_POINT('Ctrl Pts',(-2.42494334104917,2.12276709731408,
2.16479050166764));
#248031=CARTESIAN_POINT('Ctrl Pts',(-2.4121817380035,2.13725750944807,2.16356880163992));
#248032=CARTESIAN_POINT('Ctrl Pts',(-2.39181116471069,2.15997277960522,
2.16165266822472));
#248033=CARTESIAN_POINT('Ctrl Pts',(-2.38428844123661,2.16827389739153,
2.16095222043271));
#248034=CARTESIAN_POINT('Ctrl Pts',(-2.36990823068031,2.18397672656969,
2.15962710199718));
#248035=CARTESIAN_POINT('Ctrl Pts',(-2.36305912914913,2.19138561606638,
2.15900187270809));
#248036=CARTESIAN_POINT('Ctrl Pts',(-2.34665672816707,2.20896229125239,
2.15751829466192));
#248037=CARTESIAN_POINT('Ctrl Pts',(-2.33707187447798,2.21910055516079,
2.15666230224761));
#248038=CARTESIAN_POINT('Ctrl Pts',(-2.30414095293798,2.25348281642948,
2.15375711652164));
#248039=CARTESIAN_POINT('Ctrl Pts',(-2.28048025023812,2.27742406315151,
2.15173033578387));
#248040=CARTESIAN_POINT('Ctrl Pts',(-2.22120415615729,2.33555266750864,
2.14678634335597));
#248041=CARTESIAN_POINT('Ctrl Pts',(-2.18516934129827,2.36930149970408,
2.14389548368513));
#248042=CARTESIAN_POINT('Ctrl Pts',(-2.02415609904709,2.51330064515287,
2.13139532634657));
#248043=CARTESIAN_POINT('Ctrl Pts',(-1.89150339907874,2.61459556494731,
2.12214954774121));
#248044=CARTESIAN_POINT('Ctrl Pts',(-1.58270805408277,2.81454049097386,
2.1015329444411));
#248045=CARTESIAN_POINT('Ctrl Pts',(-1.40396381556002,2.90782993318214,
2.09014694434025));
#248046=CARTESIAN_POINT('Ctrl Pts',(-1.18552916992628,2.99697273567516,
2.07607521791467));
#248047=CARTESIAN_POINT('Ctrl Pts',(-1.15314775717085,3.00958055242416,
2.07398646532869));
#248048=CARTESIAN_POINT('Ctrl Pts',(-1.10150120430541,3.02873344380082,
2.070647709429));
#248049=CARTESIAN_POINT('Ctrl Pts',(-1.08236652200441,3.03562413013318,
2.0694091618992));
#248050=CARTESIAN_POINT('Ctrl Pts',(-1.04645230798768,3.04817464642984,
2.06708101665008));
#248051=CARTESIAN_POINT('Ctrl Pts',(-1.02968879090546,3.05387820356598,
2.0659929081853));
#248052=CARTESIAN_POINT('Ctrl Pts',(-0.992037582917555,3.06634325989044,
2.06354545814926));
#248053=CARTESIAN_POINT('Ctrl Pts',(-0.971126244388909,3.0730299921914,
2.06218373135486));
#248054=CARTESIAN_POINT('Ctrl Pts',(-0.908516881791847,3.09234746349154,
2.05809868276745));
#248055=CARTESIAN_POINT('Ctrl Pts',(-0.866630668024983,3.1043464286363,
2.05535517302565));
#248056=CARTESIAN_POINT('Ctrl Pts',(-0.666507021961941,3.15730919393773,
2.04219170297967));
#248057=CARTESIAN_POINT('Ctrl Pts',(-0.505568001477319,3.18703950065206,
2.03142454040343));
#248058=CARTESIAN_POINT('Ctrl Pts',(-0.172943013101873,3.22265257413123,
2.00897383370336));
#248059=CARTESIAN_POINT('Ctrl Pts',(-0.00161943607923983,3.22728926705032,
1.99730631365715));
#248060=CARTESIAN_POINT('Ctrl Pts',(0.258362700504717,3.21361591616483,
1.97996331485864));
#248061=CARTESIAN_POINT('Ctrl Pts',(0.347239282800383,3.20523108327493,
1.97410352360909));
#248062=CARTESIAN_POINT('Ctrl Pts',(0.455442392935602,3.19046836609113,
1.96713972125666));
#248063=CARTESIAN_POINT('Ctrl Pts',(0.475199313984088,3.18758557948713,
1.96587523460691));
#248064=CARTESIAN_POINT('Ctrl Pts',(0.506254627591664,3.18275905291123,
1.96390006194163));
#248065=CARTESIAN_POINT('Ctrl Pts',(0.51757125662516,3.18093837422369,1.96318291201767));
#248066=CARTESIAN_POINT('Ctrl Pts',(0.538762926213483,3.17741286036991,
1.96184516525283));
#248067=CARTESIAN_POINT('Ctrl Pts',(0.548639733087155,3.17572234646466,
1.96122384003476));
#248068=CARTESIAN_POINT('Ctrl Pts',(0.571756537962713,3.17165460889896,
1.95977447296951));
#248069=CARTESIAN_POINT('Ctrl Pts',(0.584989734339,3.16924052768454,1.95894849116909));
#248070=CARTESIAN_POINT('Ctrl Pts',(0.628362813461217,3.16104721843311,
1.9562522892123));
#248071=CARTESIAN_POINT('Ctrl Pts',(0.658436268177177,3.15492015390587,
1.9544003503644));
#248072=CARTESIAN_POINT('Ctrl Pts',(0.73100361309739,3.13905263567001,1.94996412959465));
#248073=CARTESIAN_POINT('Ctrl Pts',(0.773397077552878,3.12887760071118,
1.94739967786598));
#248074=CARTESIAN_POINT('Ctrl Pts',(0.943391534685824,3.08441006931795,
1.93717937191521));
#248075=CARTESIAN_POINT('Ctrl Pts',(1.06904198731469,3.0431442533812,1.92976555118161));
#248076=CARTESIAN_POINT('Ctrl Pts',(1.40575683852297,2.90912180038783,1.90947112247632));
#248077=CARTESIAN_POINT('Ctrl Pts',(1.60993626957032,2.8012915199883,1.89663243332257));
#248078=CARTESIAN_POINT('Ctrl Pts',(1.83718208045462,2.64816844871361,1.88040132025763));
#248079=CARTESIAN_POINT('Ctrl Pts',(1.87298413272379,2.62296860355975,1.87778330112054));
#248080=CARTESIAN_POINT('Ctrl Pts',(1.92621999863589,2.58385192343228,1.87379114340837));
#248081=CARTESIAN_POINT('Ctrl Pts',(1.94404172129719,2.57046999456735,1.87243740259821));
#248082=CARTESIAN_POINT('Ctrl Pts',(1.97579370959435,2.54610905317501,1.86999346151878));
#248083=CARTESIAN_POINT('Ctrl Pts',(1.98977495880697,2.5351977609488,1.86890593594071));
#248084=CARTESIAN_POINT('Ctrl Pts',(2.0194168714634,2.51166827313903,1.86657540005744));
#248085=CARTESIAN_POINT('Ctrl Pts',(2.03505084645822,2.49901781471519,1.86533113492383));
#248086=CARTESIAN_POINT('Ctrl Pts',(2.07726686553157,2.46419924528422,1.86192936715591));
#248087=CARTESIAN_POINT('Ctrl Pts',(2.10361122323009,2.44174839485416,1.85976053663779));
#248088=CARTESIAN_POINT('Ctrl Pts',(2.26631642806333,2.29850221777508,1.84606905152189));
#248089=CARTESIAN_POINT('Ctrl Pts',(2.39257068277541,2.16676934973573,1.83408649965335));
#248090=CARTESIAN_POINT('Ctrl Pts',(2.61832809354431,1.88728890325952,1.80996006108117));
#248091=CARTESIAN_POINT('Ctrl Pts',(2.7180945507089,1.74053552425201,1.79787408462959));
#248092=CARTESIAN_POINT('Ctrl Pts',(2.84503214214245,1.51605627233366,1.78074837867811));
#248093=CARTESIAN_POINT('Ctrl Pts',(2.88211767435064,1.44431106296683,1.77546345127314));
#248094=CARTESIAN_POINT('Ctrl Pts',(2.92484006044386,1.3534455855131,1.76906485332629));
#248095=CARTESIAN_POINT('Ctrl Pts',(2.93304506947218,1.33557141215259,1.76782002500611));
#248096=CARTESIAN_POINT('Ctrl Pts',(2.94569838863813,1.30732774210726,1.76587599315759));
#248097=CARTESIAN_POINT('Ctrl Pts',(2.95025660127906,1.29700841082399,1.7651704889577));
#248098=CARTESIAN_POINT('Ctrl Pts',(2.95877889849914,1.27743739216432,1.76384179621177));
#248099=CARTESIAN_POINT('Ctrl Pts',(2.96275382727595,1.26819108271962,1.76321800603394));
#248100=CARTESIAN_POINT('Ctrl Pts',(2.97207134159564,1.24623416401556,1.76174580546783));
#248101=CARTESIAN_POINT('Ctrl Pts',(2.97737577012575,1.23350767747316,1.76089966381898));
#248102=CARTESIAN_POINT('Ctrl Pts',(2.99497286578714,1.19051346270818,1.75806392603069));
#248103=CARTESIAN_POINT('Ctrl Pts',(3.00688737235722,1.16009192986447,1.75609532663598));
#248104=CARTESIAN_POINT('Ctrl Pts',(3.03495405337296,1.08508951049969,1.75132196810032));
#248105=CARTESIAN_POINT('Ctrl Pts',(3.05058930858167,1.04032238050182,1.74854126041145));
#248106=CARTESIAN_POINT('Ctrl Pts',(3.11282241047156,0.848648154921171,
1.73686014852028));
#248107=CARTESIAN_POINT('Ctrl Pts',(3.1498411885631,0.698837394319297,1.72827721712706));
#248108=CARTESIAN_POINT('Ctrl Pts',(3.20998676144822,0.349583956248182,
1.70843617187904));
#248109=CARTESIAN_POINT('Ctrl Pts',(3.22550151798466,0.149507144973904,
1.69717030154135));
#248110=CARTESIAN_POINT('Ctrl Pts',(3.22164015293346,-0.0958858230904817,
1.6826419978657));
#248111=CARTESIAN_POINT('Ctrl Pts',(3.21997910290325,-0.141044827728787,
1.67994068861445));
#248112=CARTESIAN_POINT('Ctrl Pts',(3.21608307747443,-0.208381873450195,
1.67586459848443));
#248113=CARTESIAN_POINT('Ctrl Pts',(3.21456658974851,-0.230596982437728,
1.67451203777158));
#248114=CARTESIAN_POINT('Ctrl Pts',(3.21142928796425,-0.270469681621264,
1.67206957547851));
#248115=CARTESIAN_POINT('Ctrl Pts',(3.20989270879577,-0.288133126497392,
1.67098233892588));
#248116=CARTESIAN_POINT('Ctrl Pts',(3.20630173357278,-0.325808912498398,
1.6686517159574));
#248117=CARTESIAN_POINT('Ctrl Pts',(3.20420555322548,-0.345816421981687,
1.6674070684783));
#248118=CARTESIAN_POINT('Ctrl Pts',(3.19798909186975,-0.40022998698095,
1.66400243970232));
#248119=CARTESIAN_POINT('Ctrl Pts',(3.19350108696467,-0.434590534175425,
1.66183109278558));
#248120=CARTESIAN_POINT('Ctrl Pts',(3.16174168517603,-0.650563763439772,
1.64804323223134));
#248121=CARTESIAN_POINT('Ctrl Pts',(3.11954637970748,-0.829611317695499,
1.63595872021517));
#248122=CARTESIAN_POINT('Ctrl Pts',(3.00633787649355,-1.17489035562275,
1.61155043952407));
#248123=CARTESIAN_POINT('Ctrl Pts',(2.93613513970884,-1.3407259571393,1.5992831787055));
#248124=CARTESIAN_POINT('Ctrl Pts',(2.81662257503734,-1.56802041783545,
1.58225451540949));
#248125=CARTESIAN_POINT('Ctrl Pts',(2.77833881656349,-1.63489637303071,
1.57721898607882));
#248126=CARTESIAN_POINT('Ctrl Pts',(2.72745045345081,-1.71683091533526,
1.5710744211516));
#248127=CARTESIAN_POINT('Ctrl Pts',(2.71705978094946,-1.73322836273651,
1.56984603323711));
#248128=CARTESIAN_POINT('Ctrl Pts',(2.70042800130979,-1.75895769015101,
1.567921884263));
#248129=CARTESIAN_POINT('Ctrl Pts',(2.69428539809744,-1.76835226934616,
1.56722002549472));
#248130=CARTESIAN_POINT('Ctrl Pts',(2.6825327599891,-1.78612350805862,1.56589399531724));
#248131=CARTESIAN_POINT('Ctrl Pts',(2.67693238932781,-1.79450611020295,
1.56526924879722));
#248132=CARTESIAN_POINT('Ctrl Pts',(2.66351638142086,-1.8143845454588,1.56378922303953));
#248133=CARTESIAN_POINT('Ctrl Pts',(2.65566543970209,-1.82585647887927,
1.56293626930998));
#248134=CARTESIAN_POINT('Ctrl Pts',(2.62872710706015,-1.86467789295419,
1.56005254872316));
#248135=CARTESIAN_POINT('Ctrl Pts',(2.60928883463633,-1.8917827096265,1.55804375289821));
#248136=CARTESIAN_POINT('Ctrl Pts',(2.56040741693405,-1.95775597847468,
1.55315271287891));
#248137=CARTESIAN_POINT('Ctrl Pts',(2.53049570456691,-1.99626816001729,
1.55029609571321));
#248138=CARTESIAN_POINT('Ctrl Pts',(2.39707595295957,-2.16022957901623,
1.53805738936644));
#248139=CARTESIAN_POINT('Ctrl Pts',(2.28502444493128,-2.27842818645096,
1.5290238662057));
#248140=CARTESIAN_POINT('Ctrl Pts',(2.02427330294337,-2.51481013283664,
1.50930812980629));
#248141=CARTESIAN_POINT('Ctrl Pts',(1.87311072318561,-2.62933413634705,
1.49862460989673));
#248142=CARTESIAN_POINT('Ctrl Pts',(1.67439673277888,-2.75400917292916,
1.48473888013062));
#248143=CARTESIAN_POINT('Ctrl Pts',(1.63550979971264,-2.77727894465387,
1.4820300755438));
#248144=CARTESIAN_POINT('Ctrl Pts',(1.57677962844725,-2.81076156110673,
1.47794475941962));
#248145=CARTESIAN_POINT('Ctrl Pts',(1.55729903871607,-2.82160135664181,
1.47659061411639));
#248146=CARTESIAN_POINT('Ctrl Pts',(1.52212204009938,-2.84070001647051,
1.47414627861748));
#248147=CARTESIAN_POINT('Ctrl Pts',(1.50646682273241,-2.8490331308745,1.47305876777375));
#248148=CARTESIAN_POINT('Ctrl Pts',(1.47291924660825,-2.86653635248986,
1.47072863273186));
#248149=CARTESIAN_POINT('Ctrl Pts',(1.4550083242896,-2.87566905507895,1.46948475713349));
#248150=CARTESIAN_POINT('Ctrl Pts',(1.40605605806614,-2.9000551916817,1.46608501444263));
#248151=CARTESIAN_POINT('Ctrl Pts',(1.374853435774,-2.91497712424577,1.46391784130291));
#248152=CARTESIAN_POINT('Ctrl Pts',(1.17856211937092,-3.00499617209078,
1.45027897907652));
#248153=CARTESIAN_POINT('Ctrl Pts',(1.00764509862685,-3.06653608160793,
1.43835171535599));
#248154=CARTESIAN_POINT('Ctrl Pts',(0.662712591579352,-3.15876764879831,
1.41437823961773));
#248155=CARTESIAN_POINT('Ctrl Pts',(0.489513111421216,-3.1902003461873,
1.40239070936379));
#248156=CARTESIAN_POINT('Ctrl Pts',(0.232297303174221,-3.21543105741181,
1.38521455159657));
#248157=CARTESIAN_POINT('Ctrl Pts',(0.14969206047645,-3.2203343891187,1.37979567400837));
#248158=CARTESIAN_POINT('Ctrl Pts',(0.047196217307954,-3.22246516964836,
1.37326164059696));
#248159=CARTESIAN_POINT('Ctrl Pts',(0.0274053862454179,-3.22269425210146,
1.37200877394559));
#248160=CARTESIAN_POINT('Ctrl Pts',(-0.00369587151322278,-3.22276772316502,
1.37005499926958));
#248161=CARTESIAN_POINT('Ctrl Pts',(-0.0150051466959918,-3.2227349117801,
1.36934769096479));
#248162=CARTESIAN_POINT('Ctrl Pts',(-0.0363776369577231,-3.22256039652642,
1.36801723315083));
#248163=CARTESIAN_POINT('Ctrl Pts',(-0.0464403507838753,-3.22243109123781,
1.36739346541563));
#248164=CARTESIAN_POINT('Ctrl Pts',(-0.0702477089453369,-3.2220136259795,
1.3659237086186));
#248165=CARTESIAN_POINT('Ctrl Pts',(-0.0839913474430751,-3.22168465493525,
1.36507995956881));
#248166=CARTESIAN_POINT('Ctrl Pts',(-0.130108378113417,-3.22028547166179,
1.36226333691457));
#248167=CARTESIAN_POINT('Ctrl Pts',(-0.162468757136495,-3.21881512230102,
1.36031104742288));
#248168=CARTESIAN_POINT('Ctrl Pts',(-0.241577871545698,-3.21402452114527,
1.3555856313518));
#248169=CARTESIAN_POINT('Ctrl Pts',(-0.288287846514752,-3.2101719623515,
1.35283589683806));
#248170=CARTESIAN_POINT('Ctrl Pts',(-0.484817090053177,-3.18963801145944,
1.34137611863389));
#248171=CARTESIAN_POINT('Ctrl Pts',(-0.633461135311341,-3.16347454032089,
1.33297112179323));
#248172=CARTESIAN_POINT('Ctrl Pts',(-0.977733025119387,-3.07762834499138,
1.31310656690478));
#248173=CARTESIAN_POINT('Ctrl Pts',(-1.17057182219064,-3.00956940119656,
1.30164063185059));
#248174=CARTESIAN_POINT('Ctrl Pts',(-1.39681209740821,-2.90466690125933,
1.28687937703692));
#248175=CARTESIAN_POINT('Ctrl Pts',(-1.43754228318283,-2.88472628241025,
1.28416865861869));
#248176=CARTESIAN_POINT('Ctrl Pts',(-1.49765804969568,-2.85370556054669,
1.28008071032851));
#248177=CARTESIAN_POINT('Ctrl Pts',(-1.51737222441274,-2.84327215622488,
1.27872586816672));
#248178=CARTESIAN_POINT('Ctrl Pts',(-1.55257084686608,-2.82417352901214,
1.27628036883012));
#248179=CARTESIAN_POINT('Ctrl Pts',(-1.56809516180137,-2.81558340318886,
1.27519239326876));
#248180=CARTESIAN_POINT('Ctrl Pts',(-1.60106411562954,-2.79698333063702,
1.2728613503058));
#248181=CARTESIAN_POINT('Ctrl Pts',(-1.61848750012414,-2.78693742969881,
1.27161703183881));
#248182=CARTESIAN_POINT('Ctrl Pts',(-1.66562269013185,-2.75916933919876,
1.2682162714455));
#248183=CARTESIAN_POINT('Ctrl Pts',(-1.69514431900333,-2.74113114926068,
1.26604852271925));
#248184=CARTESIAN_POINT('Ctrl Pts',(-1.75996419529829,-2.70007756466549,
1.26120260807297));
#248185=CARTESIAN_POINT('Ctrl Pts',(-1.79511250833111,-2.67683836730967,
1.25851663239158));
#248186=CARTESIAN_POINT('Ctrl Pts',(-1.90435767397843,-2.60148882229082,
1.24998107316453));
#248187=CARTESIAN_POINT('Ctrl Pts',(-1.9767144585979,-2.54694325192496,
1.24404785221202));
#248188=CARTESIAN_POINT('Ctrl Pts',(-2.14979671615801,-2.40464427824107,
1.22917084389868));
#248189=CARTESIAN_POINT('Ctrl Pts',(-2.24754758245627,-2.31353982650047,
1.22014315557297));
#248190=CARTESIAN_POINT('Ctrl Pts',(-2.37652296516427,-2.17742396870072,
1.20747204368998));
#248191=CARTESIAN_POINT('Ctrl Pts',(-2.41269218531012,-2.13727703601834,
1.2038253795197));
#248192=CARTESIAN_POINT('Ctrl Pts',(-2.52376484040837,-2.00757448416984,
1.19236200812574));
#248193=CARTESIAN_POINT('Ctrl Pts',(-2.5948288806241,-1.9148401743512,1.18462302236009));
#248194=CARTESIAN_POINT('Ctrl Pts',(-2.67263107030621,-1.80100170001078,
1.17581811928718));
#248195=CARTESIAN_POINT('Ctrl Pts',(-2.68438122846769,-1.78344089782949,
1.17447850627666));
#248196=CARTESIAN_POINT('Ctrl Pts',(-2.7023821039717,-1.75595728597366,
1.17241229148214));
#248197=CARTESIAN_POINT('Ctrl Pts',(-2.7087525713782,-1.74611412661286,
1.17167825574094));
#248198=CARTESIAN_POINT('Ctrl Pts',(-2.72043998428536,-1.72783773359812,
1.17032666087447));
#248199=CARTESIAN_POINT('Ctrl Pts',(-2.72577155502347,-1.71941454438589,
1.16970818949788));
#248200=CARTESIAN_POINT('Ctrl Pts',(-2.73797621672805,-1.69993332340838,
1.16828787422502));
#248201=CARTESIAN_POINT('Ctrl Pts',(-2.74482146869559,-1.68885824918665,
1.16748782791784));
#248202=CARTESIAN_POINT('Ctrl Pts',(-2.76634669901203,-1.65355554951443,
1.16496003184757));
#248203=CARTESIAN_POINT('Ctrl Pts',(-2.78077488274044,-1.62917500261481,
1.16324758837465));
#248204=CARTESIAN_POINT('Ctrl Pts',(-2.85652054729852,-1.49724230236028,
1.15414076963792));
#248205=CARTESIAN_POINT('Ctrl Pts',(-2.91192962534587,-1.3864040593358,
1.14705223095193));
#248206=CARTESIAN_POINT('Ctrl Pts',(-3.05217345762915,-1.06012394442053,
1.12700296264413));
#248207=CARTESIAN_POINT('Ctrl Pts',(-3.12037052170006,-0.838398476945386,
1.11429958918481));
#248208=CARTESIAN_POINT('Ctrl Pts',(-3.1798950228356,-0.53027562905916,
1.09612869278267));
#248209=CARTESIAN_POINT('Ctrl Pts',(-3.19242674030653,-0.448703095731515,
1.09127729630226));
#248210=CARTESIAN_POINT('Ctrl Pts',(-3.20508536182478,-0.338188565996296,
1.08460480267479));
#248211=CARTESIAN_POINT('Ctrl Pts',(-3.2079739522668,-0.30959122043394,
1.08286937218141));
#248212=CARTESIAN_POINT('Ctrl Pts',(-3.21212201003229,-0.262192064140319,
1.07997669986104));
#248213=CARTESIAN_POINT('Ctrl Pts',(-3.21359980576588,-0.24341066278756,
1.07882630072219));
#248214=CARTESIAN_POINT('Ctrl Pts',(-3.21608548488812,-0.207833581932038,
1.07663872469654));
#248215=CARTESIAN_POINT('Ctrl Pts',(-3.21712667406909,-0.191040806918223,
1.07560262506271));
#248216=CARTESIAN_POINT('Ctrl Pts',(-3.21899170423312,-0.156595766204148,
1.07346985434961));
#248217=CARTESIAN_POINT('Ctrl Pts',(-3.21980194232736,-0.138943363555232,
1.07237279527519));
#248218=CARTESIAN_POINT('Ctrl Pts',(-3.22120479765994,-0.101693646886477,
1.07004897222391));
#248219=CARTESIAN_POINT('Ctrl Pts',(-3.22176383201439,-0.0820958580356578,
1.06882121079411));
#248220=CARTESIAN_POINT('Ctrl Pts',(-3.22255677868777,-0.0412124644936687,
1.06624891962182));
#248221=CARTESIAN_POINT('Ctrl Pts',(-3.22275868156198,-0.0199273287497446,
1.06490347292996));
#248222=CARTESIAN_POINT('Ctrl Pts',(-3.22274971398033,0.0013577701177717,
1.06355168448669));
#248223=CARTESIAN_POINT('Ctrl Pts',(-3.22274913564885,0.00236033357308065,
0.816219464231529));
#248224=CARTESIAN_POINT('Ctrl Pts',(-3.22286909096441,-0.1614240966976,
0.825608085954441));
#248225=CARTESIAN_POINT('Ctrl Pts',(-3.21050335524459,-0.324991258301196,
0.834672913528035));
#248226=CARTESIAN_POINT('Ctrl Pts',(-3.1604140557922,-0.652708508243162,
0.85328181329922));
#248227=CARTESIAN_POINT('Ctrl Pts',(-3.1221748315376,-0.816248156505571,
0.862807257899995));
#248228=CARTESIAN_POINT('Ctrl Pts',(-3.05795698999836,-1.01832372725381,
0.875362448731364));
#248229=CARTESIAN_POINT('Ctrl Pts',(-3.04365559516214,-1.06030396559574,
0.878013951006589));
#248230=CARTESIAN_POINT('Ctrl Pts',(-3.02086567945308,-1.1229361901449,
0.882041682122287));
#248231=CARTESIAN_POINT('Ctrl Pts',(-3.01302102409625,-1.14381790956262,
0.883396701528632));
#248232=CARTESIAN_POINT('Ctrl Pts',(-2.99852262649171,-1.18122689761408,
0.885846916177238));
#248233=CARTESIAN_POINT('Ctrl Pts',(-2.99194736003148,-1.19778374506526,
0.886939451114916));
#248234=CARTESIAN_POINT('Ctrl Pts',(-2.97747966255677,-1.23335157450746,
0.889304359451952));
#248235=CARTESIAN_POINT('Ctrl Pts',(-2.96954172138339,-1.25234307634294,
0.890578230696995));
#248236=CARTESIAN_POINT('Ctrl Pts',(-2.94761568434028,-1.30342029047189,
0.894035057233538));
#248237=CARTESIAN_POINT('Ctrl Pts',(-2.93328622055922,-1.33535555929732,
0.896229506738193));
#248238=CARTESIAN_POINT('Ctrl Pts',(-2.84247298990635,-1.52922771526697,
0.909760128481584));
#248239=CARTESIAN_POINT('Ctrl Pts',(-2.75313227779475,-1.68476552146076,
0.921541139942433));
#248240=CARTESIAN_POINT('Ctrl Pts',(-2.57989828553722,-1.93546937623926,
0.942009518664005));
#248241=CARTESIAN_POINT('Ctrl Pts',(-2.50245515066346,-2.03460910653372,
0.950548576390257));
#248242=CARTESIAN_POINT('Ctrl Pts',(-2.35995172448385,-2.19655406819115,
0.965079561172328));
#248243=CARTESIAN_POINT('Ctrl Pts',(-2.29767165179909,-2.2616208468479,
0.971099045246451));
#248244=CARTESIAN_POINT('Ctrl Pts',(-2.20769722116667,-2.34806240440204,
0.979265741386672));
#248245=CARTESIAN_POINT('Ctrl Pts',(-2.18226063843599,-2.37172148008052,
0.981519837156127));
#248246=CARTESIAN_POINT('Ctrl Pts',(-2.13763166392808,-2.41190575291921,
0.985374144341918));
#248247=CARTESIAN_POINT('Ctrl Pts',(-2.11861817407881,-2.42862422282353,
0.98698576889893));
#248248=CARTESIAN_POINT('Ctrl Pts',(-2.09011423909651,-2.45309806406821,
0.989354551877601));
#248249=CARTESIAN_POINT('Ctrl Pts',(-2.08077389078241,-2.46102573559374,
0.990123385983259));
#248250=CARTESIAN_POINT('Ctrl Pts',(-2.06363511571716,-2.47540503738035,
0.991520350426597));
#248251=CARTESIAN_POINT('Ctrl Pts',(-2.0558512992925,-2.48187337163248,
0.992149645667449));
#248252=CARTESIAN_POINT('Ctrl Pts',(-2.03878123805063,-2.49592314063498,
0.993518485475008));
#248253=CARTESIAN_POINT('Ctrl Pts',(-2.02948307877546,-2.50348950550907,
0.994256974265698));
#248254=CARTESIAN_POINT('Ctrl Pts',(-2.00331018720816,-2.52454601439626,
0.996316520030707));
#248255=CARTESIAN_POINT('Ctrl Pts',(-1.98634137237403,-2.53791889036635,
0.997629659672997));
#248256=CARTESIAN_POINT('Ctrl Pts',(-1.870362177989,-2.62744454545351,1.0064656123821));
#248257=CARTESIAN_POINT('Ctrl Pts',(-1.76712041277952,-2.69796438500549,
1.0136525579085));
#248258=CARTESIAN_POINT('Ctrl Pts',(-1.42368931182879,-2.90435171005929,
1.03633485440145));
#248259=CARTESIAN_POINT('Ctrl Pts',(-1.17010894421849,-3.01545914864115,
1.05139395941233));
#248260=CARTESIAN_POINT('Ctrl Pts',(-0.850609460254013,-3.10899497450193,
1.07095055048486));
#248261=CARTESIAN_POINT('Ctrl Pts',(-0.795325361273546,-3.12359459426378,
1.07434927130283));
#248262=CARTESIAN_POINT('Ctrl Pts',(-0.715584914688503,-3.14239858749436,
1.07928660494274));
#248263=CARTESIAN_POINT('Ctrl Pts',(-0.691421098572556,-3.14780359383477,
1.08078729327755));
#248264=CARTESIAN_POINT('Ctrl Pts',(-0.649168547291423,-3.15674474312338,
1.08342030574655));
#248265=CARTESIAN_POINT('Ctrl Pts',(-0.631107100899261,-3.16040519257544,
1.08454864983804));
#248266=CARTESIAN_POINT('Ctrl Pts',(-0.593700612013165,-3.16765279303163,
1.08689178902605));
#248267=CARTESIAN_POINT('Ctrl Pts',(-0.574352166982195,-3.17121809327191,
1.08810722046468));
#248268=CARTESIAN_POINT('Ctrl Pts',(-0.524329318061336,-3.17996289879882,
1.09125897186331));
#248269=CARTESIAN_POINT('Ctrl Pts',(-0.493610947167263,-3.18487572704859,
1.09320353977833));
#248270=CARTESIAN_POINT('Ctrl Pts',(-0.364498774602229,-3.20361206652839,
1.10141729700865));
#248271=CARTESIAN_POINT('Ctrl Pts',(-0.265572432593184,-3.21332500769714,
1.10781150495507));
#248272=CARTESIAN_POINT('Ctrl Pts',(0.0628457619002177,-3.23030108781832,
1.12936495692031));
#248273=CARTESIAN_POINT('Ctrl Pts',(0.292652254680948,-3.21762809599612,
1.1450250762266));
#248274=CARTESIAN_POINT('Ctrl Pts',(0.595040875317243,-3.16827397014781,
1.16556206322948));
#248275=CARTESIAN_POINT('Ctrl Pts',(0.670488929049658,-3.15316976613957,
1.17067354019613));
#248276=CARTESIAN_POINT('Ctrl Pts',(0.790406087210058,-3.12466360155229,
1.17871030673554));
#248277=CARTESIAN_POINT('Ctrl Pts',(0.835250330174358,-3.11297635538181,
1.18169562883888));
#248278=CARTESIAN_POINT('Ctrl Pts',(0.895239014336261,-3.0959523977076,
1.18564812793372));
#248279=CARTESIAN_POINT('Ctrl Pts',(0.91061616750354,-3.09146443641764,
1.18665762036896));
#248280=CARTESIAN_POINT('Ctrl Pts',(0.936181467492968,-3.08379566625165,
1.18832909331505));
#248281=CARTESIAN_POINT('Ctrl Pts',(0.946388258718718,-3.08067861418492,
1.18899458722347));
#248282=CARTESIAN_POINT('Ctrl Pts',(0.965744116338459,-3.07466225260615,
1.19025287654708));
#248283=CARTESIAN_POINT('Ctrl Pts',(0.974896025294655,-3.07177268223002,
1.19084623869258));
#248284=CARTESIAN_POINT('Ctrl Pts',(0.999295199861494,-3.06394900129731,
1.19242424933902));
#248285=CARTESIAN_POINT('Ctrl Pts',(1.01451902155037,-3.05894190173244,
1.19340476255508));
#248286=CARTESIAN_POINT('Ctrl Pts',(1.07052557509851,-3.04005728665629,
1.19699902484583));
#248287=CARTESIAN_POINT('Ctrl Pts',(1.11106805098352,-3.02547541628464,
1.1995754965506));
#248288=CARTESIAN_POINT('Ctrl Pts',(1.3425252598494,-2.93694681478146,1.21420306013822));
#248289=CARTESIAN_POINT('Ctrl Pts',(1.5263581985784,-2.84574747986912,1.2255211208592));
#248290=CARTESIAN_POINT('Ctrl Pts',(1.84281882243856,-2.64920350034945,
1.24641299679187));
#248291=CARTESIAN_POINT('Ctrl Pts',(1.97818696215714,-2.54971157413972,
1.25589864264067));
#248292=CARTESIAN_POINT('Ctrl Pts',(2.14596027113954,-2.40496809011715,
1.2689418937264));
#248293=CARTESIAN_POINT('Ctrl Pts',(2.18584088164418,-2.36877946334564,
1.2721476541899));
#248294=CARTESIAN_POINT('Ctrl Pts',(2.24227601767943,-2.31492973162574,
1.27685182230117));
#248295=CARTESIAN_POINT('Ctrl Pts',(2.25956888668173,-2.29805348061677,
1.27831710590944));
#248296=CARTESIAN_POINT('Ctrl Pts',(2.28962635724851,-2.26805286678018,
1.28090730550712));
#248297=CARTESIAN_POINT('Ctrl Pts',(2.30247208077044,-2.25501107713496,
1.28202859099051));
#248298=CARTESIAN_POINT('Ctrl Pts',(2.32901485856407,-2.22759992209547,
1.28437597394713));
#248299=CARTESIAN_POINT('Ctrl Pts',(2.34269161247608,-2.21321205609795,
1.28560287512141));
#248300=CARTESIAN_POINT('Ctrl Pts',(2.37811067712946,-2.17525523891722,
1.28882660935714));
#248301=CARTESIAN_POINT('Ctrl Pts',(2.39963525693648,-2.1514869887129,1.29083247438135));
#248302=CARTESIAN_POINT('Ctrl Pts',(2.49135662818551,-2.0471159446422,1.2995885839805));
#248303=CARTESIAN_POINT('Ctrl Pts',(2.55786742931069,-1.96337761384278,
1.30648521295537));
#248304=CARTESIAN_POINT('Ctrl Pts',(2.74081790964209,-1.70792998602518,
1.32715013580317));
#248305=CARTESIAN_POINT('Ctrl Pts',(2.84498867706062,-1.52811435177765,
1.34126824149459));
#248306=CARTESIAN_POINT('Ctrl Pts',(2.98431136334188,-1.22325629113519,
1.36381541703847));
#248307=CARTESIAN_POINT('Ctrl Pts',(3.03050097260132,-1.10387542316613,
1.37232101091366));
#248308=CARTESIAN_POINT('Ctrl Pts',(3.07600383140691,-0.961653157438882,
1.38185624290185));
#248309=CARTESIAN_POINT('Ctrl Pts',(3.08232761205328,-0.941186971149414,
1.38321420380309));
#248310=CARTESIAN_POINT('Ctrl Pts',(3.09182174806545,-0.909337884737007,
1.38530387210902));
#248311=CARTESIAN_POINT('Ctrl Pts',(3.09513422926783,-0.897998454091546,
1.38604326429945));
#248312=CARTESIAN_POINT('Ctrl Pts',(3.10119741735548,-0.876810521145158,
1.38741592089813));
#248313=CARTESIAN_POINT('Ctrl Pts',(3.10396361827285,-0.866967110726428,
1.38805001188597));
#248314=CARTESIAN_POINT('Ctrl Pts',(3.11024361416766,-0.844204629707802,
1.38950818339774));
#248315=CARTESIAN_POINT('Ctrl Pts',(3.11372380771394,-0.83127664474951,
1.39033035500236));
#248316=CARTESIAN_POINT('Ctrl Pts',(3.12479131300124,-0.789118954564906,
1.3929930496368));
#248317=CARTESIAN_POINT('Ctrl Pts',(3.13204862016663,-0.759803305073057,
1.39481596811506));
#248318=CARTESIAN_POINT('Ctrl Pts',(3.1778339480306,-0.563037902476248,
1.40688657569195));
#248319=CARTESIAN_POINT('Ctrl Pts',(3.20333362661943,-0.392820222940303,
1.41654333773793));
#248320=CARTESIAN_POINT('Ctrl Pts',(3.22632737545772,-0.0588545063100762,
1.43529701214256));
#248321=CARTESIAN_POINT('Ctrl Pts',(3.22517869050616,0.104265513338425,
1.44437327539808));
#248322=CARTESIAN_POINT('Ctrl Pts',(3.20634029344234,0.331216995898737,
1.45747997278169));
#248323=CARTESIAN_POINT('Ctrl Pts',(3.19902690426935,0.395662625043786,
1.46125432553624));
#248324=CARTESIAN_POINT('Ctrl Pts',(3.18285836569279,0.507818739866992,
1.46794708257281));
#248325=CARTESIAN_POINT('Ctrl Pts',(3.1748605937362,0.555632156082215,1.47084005049569));
#248326=CARTESIAN_POINT('Ctrl Pts',(3.16144954117865,0.626012400680083,
1.47516587434077));
#248327=CARTESIAN_POINT('Ctrl Pts',(3.15686584343416,0.648731632404412,
1.47657273136909));
#248328=CARTESIAN_POINT('Ctrl Pts',(3.1482545924279,0.689159137741823,1.47909569553666));
#248329=CARTESIAN_POINT('Ctrl Pts',(3.14432162537363,0.70688668890667,1.48020876262159));
#248330=CARTESIAN_POINT('Ctrl Pts',(3.13567462260323,0.744361729200727,
1.4825764421999));
#248331=CARTESIAN_POINT('Ctrl Pts',(3.13092339123425,0.764099738937444,
1.4838321977915));
#248332=CARTESIAN_POINT('Ctrl Pts',(3.11765737947424,0.817008432708395,
1.48722234779076));
#248333=CARTESIAN_POINT('Ctrl Pts',(3.10880002592167,0.850089742139968,
1.48936758838151));
#248334=CARTESIAN_POINT('Ctrl Pts',(3.06059056382652,1.01930539034497,1.50047624231283));
#248335=CARTESIAN_POINT('Ctrl Pts',(3.01282259744245,1.15286117632721,1.50970740186858));
#248336=CARTESIAN_POINT('Ctrl Pts',(2.87028055090618,1.48136647401607,1.53353483465706));
#248337=CARTESIAN_POINT('Ctrl Pts',(2.7643579421497,1.670711204747,1.54835941420533));
#248338=CARTESIAN_POINT('Ctrl Pts',(2.60820843424535,1.89380336034819,1.56645291954706));
#248339=CARTESIAN_POINT('Ctrl Pts',(2.57496588790332,1.93876087956273,1.57013152444463));
#248340=CARTESIAN_POINT('Ctrl Pts',(2.51780309014676,2.01200256059984,1.57615120959206));
#248341=CARTESIAN_POINT('Ctrl Pts',(2.49453543221871,2.04077925059272,1.57852349845452));
#248342=CARTESIAN_POINT('Ctrl Pts',(2.46136382450686,2.08038953134716,1.58179162124443));
#248343=CARTESIAN_POINT('Ctrl Pts',(2.45187464107815,2.09156478318943,1.58271396603745));
#248344=CARTESIAN_POINT('Ctrl Pts',(2.43554037211883,2.11053744168677,1.58427981820621));
#248345=CARTESIAN_POINT('Ctrl Pts',(2.4287333544413,2.11836717829471,1.58492599915673));
#248346=CARTESIAN_POINT('Ctrl Pts',(2.414432304586,2.13465733460855,1.5862701676898));
#248347=CARTESIAN_POINT('Ctrl Pts',(2.40693144787051,2.14311136059401,1.58696764831078));
#248348=CARTESIAN_POINT('Ctrl Pts',(2.38666847721577,2.16570866743081,1.58883228529697));
#248349=CARTESIAN_POINT('Ctrl Pts',(2.37382496276697,2.1797787819432,1.58999360857395));
#248350=CARTESIAN_POINT('Ctrl Pts',(2.31334295070601,2.24486841920629,1.59537210001377));
#248351=CARTESIAN_POINT('Ctrl Pts',(2.26417636975943,2.29444910193913,1.5994868889855));
#248352=CARTESIAN_POINT('Ctrl Pts',(2.07956423120677,2.46889726386049,1.61420630287181));
#248353=CARTESIAN_POINT('Ctrl Pts',(1.93508744159758,2.5836963394253,1.62438682578549));
#248354=CARTESIAN_POINT('Ctrl Pts',(1.64013546441197,2.77936813423737,1.64426087883806));
#248355=CARTESIAN_POINT('Ctrl Pts',(1.49150729193875,2.86187504257026,1.65390011069732));
#248356=CARTESIAN_POINT('Ctrl Pts',(1.29638575695095,2.95084770312298,1.66659959483267));
#248357=CARTESIAN_POINT('Ctrl Pts',(1.25530823103117,2.96855506144135,1.66927423459243));
#248358=CARTESIAN_POINT('Ctrl Pts',(1.19305070731933,2.99386923752831,1.67333618648865));
#248359=CARTESIAN_POINT('Ctrl Pts',(1.17213686172049,3.00211894165499,1.67470205121285));
#248360=CARTESIAN_POINT('Ctrl Pts',(1.13437155467025,3.01656112065541,1.67717168373143));
#248361=CARTESIAN_POINT('Ctrl Pts',(1.11755128771927,3.02283292915734,1.67827276512772));
#248362=CARTESIAN_POINT('Ctrl Pts',(1.08118548346784,3.03604771401498,1.68065616503584));
#248363=CARTESIAN_POINT('Ctrl Pts',(1.06162364319364,3.0429431443542,1.68193999290455));
#248364=CARTESIAN_POINT('Ctrl Pts',(1.00861061972943,3.06105650978373,1.68542454182457));
#248365=CARTESIAN_POINT('Ctrl Pts',(0.975040313014042,3.07191447945906,
1.68763685596779));
#248366=CARTESIAN_POINT('Ctrl Pts',(0.760836642009185,3.13733158013057,
1.70179407343206));
#248367=CARTESIAN_POINT('Ctrl Pts',(0.575911226341209,3.1764803833567,1.71423224605722));
#248368=CARTESIAN_POINT('Ctrl Pts',(0.252491394646808,3.21577032382659,
1.736136452538));
#248369=CARTESIAN_POINT('Ctrl Pts',(0.11541561776743,3.22360199009643,1.74545644895553));
#248370=CARTESIAN_POINT('Ctrl Pts',(-0.0959038079811421,3.22217632773535,
1.75961368338483));
#248371=CARTESIAN_POINT('Ctrl Pts',(-0.170031068386464,3.2191161136176,
1.76453807474508));
#248372=CARTESIAN_POINT('Ctrl Pts',(-0.289039910990113,3.21008015898365,
1.77231594456876));
#248373=CARTESIAN_POINT('Ctrl Pts',(-0.334014900976881,3.20571258999861,
1.77522557184541));
#248374=CARTESIAN_POINT('Ctrl Pts',(-0.39461015545749,3.1985389029578,1.77909264104674));
#248375=CARTESIAN_POINT('Ctrl Pts',(-0.410321118918131,3.19656141684924,
1.78009043798495));
#248376=CARTESIAN_POINT('Ctrl Pts',(-0.436531574789474,3.19306596614869,
1.78174624235564));
#248377=CARTESIAN_POINT('Ctrl Pts',(-0.447039157971009,3.19161183126196,
1.78240767136716));
#248378=CARTESIAN_POINT('Ctrl Pts',(-0.468353568368802,3.18855482070454,
1.7837442922526));
#248379=CARTESIAN_POINT('Ctrl Pts',(-0.479159751276847,3.18694883087511,
1.78441930847881));
#248380=CARTESIAN_POINT('Ctrl Pts',(-0.507088242975339,3.18265289868826,
1.78615754113685));
#248381=CARTESIAN_POINT('Ctrl Pts',(-0.524197639783479,3.1798796871099,
1.78721623235103));
#248382=CARTESIAN_POINT('Ctrl Pts',(-0.593583269519605,3.16805793025572,
1.79148758048805));
#248383=CARTESIAN_POINT('Ctrl Pts',(-0.645657598670931,3.15785672839533,
1.79464227807491));
#248384=CARTESIAN_POINT('Ctrl Pts',(-0.75890352182933,3.13275340497592,
1.8014371988924));
#248385=CARTESIAN_POINT('Ctrl Pts',(-0.819938497879905,3.11733541281106,
1.80505704576313));
#248386=CARTESIAN_POINT('Ctrl Pts',(-1.06480528049328,3.04778961281511,
1.81954493158093));
#248387=CARTESIAN_POINT('Ctrl Pts',(-1.24409133614876,2.97910596002563,
1.83009498852789));
#248388=CARTESIAN_POINT('Ctrl Pts',(-1.4992891042266,2.85426036640323,1.84620476556318));
#248389=CARTESIAN_POINT('Ctrl Pts',(-1.58056814750168,2.81006630673086,
1.85151016859105));
#248390=CARTESIAN_POINT('Ctrl Pts',(-1.71378472787176,2.73002224526434,
1.8606083139029));
#248391=CARTESIAN_POINT('Ctrl Pts',(-1.76677443288491,2.6960316923153,1.86434068711323));
#248392=CARTESIAN_POINT('Ctrl Pts',(-1.83990461213528,2.64603974148246,
1.8696732421494));
#248393=CARTESIAN_POINT('Ctrl Pts',(-1.86090269025632,2.6313145792619,1.87122618433916));
#248394=CARTESIAN_POINT('Ctrl Pts',(-1.89677310922655,2.60551588685585,
1.87391806665086));
#248395=CARTESIAN_POINT('Ctrl Pts',(-1.91172994159052,2.59456159544994,
1.87505243568036));
#248396=CARTESIAN_POINT('Ctrl Pts',(-1.94206249975424,2.57194153995899,
1.87737790356021));
#248397=CARTESIAN_POINT('Ctrl Pts',(-1.95742958612638,2.56026549944559,
1.87856937156763));
#248398=CARTESIAN_POINT('Ctrl Pts',(-1.99602083014927,2.53039302202824,
1.88159595961613));
#248399=CARTESIAN_POINT('Ctrl Pts',(-2.01910131312976,2.51201468855766,
1.88343817240581));
#248400=CARTESIAN_POINT('Ctrl Pts',(-2.10762268984663,2.43951942781959,
1.89063144395813));
#248401=CARTESIAN_POINT('Ctrl Pts',(-2.1711622693735,2.3831451349451,1.8960719105151));
#248402=CARTESIAN_POINT('Ctrl Pts',(-2.39272725293461,2.17034370394175,
1.9160838496602));
#248403=CARTESIAN_POINT('Ctrl Pts',(-2.53667947232337,2.00019283811771,
1.93118385179018));
#248404=CARTESIAN_POINT('Ctrl Pts',(-2.73385635827691,1.71126127713571,
1.95475449451254));
#248405=CARTESIAN_POINT('Ctrl Pts',(-2.79944173820837,1.60172335112025,
1.9632741085455));
#248406=CARTESIAN_POINT('Ctrl Pts',(-2.87175346579648,1.46287034557162,
1.97334898230511));
#248407=CARTESIAN_POINT('Ctrl Pts',(-2.88479407301754,1.43698326596089,
1.97519756130324));
#248408=CARTESIAN_POINT('Ctrl Pts',(-2.90331503417518,1.39894844732685,
1.97786675765037));
#248409=CARTESIAN_POINT('Ctrl Pts',(-2.90907173679522,1.38693784670786,
1.9787029014807));
#248410=CARTESIAN_POINT('Ctrl Pts',(-2.91910515437681,1.36566712102551,
1.98017140532332));
#248411=CARTESIAN_POINT('Ctrl Pts',(-2.9234125790301,1.35642194403075,1.98080558335603));
#248412=CARTESIAN_POINT('Ctrl Pts',(-2.9327007832531,1.33623656599427,1.98218123526536));
#248413=CARTESIAN_POINT('Ctrl Pts',(-2.93766430631603,1.32528882834039,
1.98292167889361));
#248414=CARTESIAN_POINT('Ctrl Pts',(-2.95144387796549,1.29443826601513,
1.98499308316205));
#248415=CARTESIAN_POINT('Ctrl Pts',(-2.96011988237994,1.27447311827945,
1.98631597109495));
#248416=CARTESIAN_POINT('Ctrl Pts',(-3.02005944895654,1.13262585127357,
1.99560099711645));
#248417=CARTESIAN_POINT('Ctrl Pts',(-3.06398752244789,1.00776425100688,
2.00318596802975));
#248418=CARTESIAN_POINT('Ctrl Pts',(-3.13893747152918,0.743888673340769,
2.01868324416095));
#248419=CARTESIAN_POINT('Ctrl Pts',(-3.16867440487929,0.604815865426179,
2.02656402916567));
#248420=CARTESIAN_POINT('Ctrl Pts',(-3.20464311655925,0.357722153633178,
2.04064324728881));
#248421=CARTESIAN_POINT('Ctrl Pts',(-3.21480116470452,0.250506898475419,
2.04677590744531));
#248422=CARTESIAN_POINT('Ctrl Pts',(-3.22167868485758,0.0956520733148445,
2.05581484351066));
#248423=CARTESIAN_POINT('Ctrl Pts',(-3.2227367334429,0.0482752566797369,
2.05860409443329));
#248424=CARTESIAN_POINT('Ctrl Pts',(-3.2227499586742,0.000595948182032424,
2.06144152017187));
#248425=CARTESIAN_POINT('Ctrl Pts',(-3.22275,0.000297973971232206,2.06145925399353));
#248426=CARTESIAN_POINT('Ctrl Pts',(-3.22275,-8.28983494685339E-13,2.06147698899067));
#248427=CARTESIAN_POINT('Origin',(0.,0.,-2.31077344927308));
#248428=CARTESIAN_POINT('',(-3.22275,5.4545833554047E-12,3.55815895351304));
#248429=CARTESIAN_POINT('',(-3.22275,-1.09907859225987E-10,3.31386231834285));
#248430=CARTESIAN_POINT('',(-3.22275,-3.50678552687464E-13,-2.31077344927308));
#248431=CARTESIAN_POINT('',(-3.2227498370861,0.00102472510551524,3.55809228455962));
#248432=CARTESIAN_POINT('Ctrl Pts',(-3.22275,5.4545833554047E-12,3.55815895351304));
#248433=CARTESIAN_POINT('Ctrl Pts',(-3.22275,0.00034157307004431,3.5581367286295));
#248434=CARTESIAN_POINT('Ctrl Pts',(-3.22274994569599,0.000683148107952332,
3.55811450564337));
#248435=CARTESIAN_POINT('Ctrl Pts',(-3.2227498370861,0.0010247251065684,
3.55809228455955));
#248436=CARTESIAN_POINT('Ctrl Pts',(-3.22274983586623,0.00102855442515937,
3.55809203544564));
#248437=CARTESIAN_POINT('Ctrl Pts',(-3.22273820483632,0.037471837150337,
3.55572124147969));
#248438=CARTESIAN_POINT('Ctrl Pts',(-3.22210841499878,0.0739142782399589,
3.55337358624429));
#248439=CARTESIAN_POINT('Ctrl Pts',(-3.22039852623606,0.123826453175173,
3.55019669928976));
#248440=CARTESIAN_POINT('Ctrl Pts',(-3.21985180090162,0.137310060918356,
3.54934232982271));
#248441=CARTESIAN_POINT('Ctrl Pts',(-3.21875217860318,0.160785916127353,
3.5478619901182));
#248442=CARTESIAN_POINT('Ctrl Pts',(-3.2182374079862,0.170779653668331,
3.54723407118625));
#248443=CARTESIAN_POINT('Ctrl Pts',(-3.21713844001681,0.190340995160105,
3.54600965721298));
#248444=CARTESIAN_POINT('Ctrl Pts',(-3.21655808997559,0.19990872924855,
3.54541296667737));
#248445=CARTESIAN_POINT('Ctrl Pts',(-3.21521109565124,0.220588360296694,
3.54412816129711));
#248446=CARTESIAN_POINT('Ctrl Pts',(-3.21442952688872,0.231699028081275,
3.54344087228762));
#248447=CARTESIAN_POINT('Ctrl Pts',(-3.212157952319,0.261763860703516,3.54158871112551));
#248448=CARTESIAN_POINT('Ctrl Pts',(-3.21055777090555,0.280709580645788,
3.54042973636602));
#248449=CARTESIAN_POINT('Ctrl Pts',(-3.2021098880226,0.371176249519088,
3.53493002489401));
#248450=CARTESIAN_POINT('Ctrl Pts',(-3.19303893754264,0.442474294200699,
3.53069849107339));
#248451=CARTESIAN_POINT('Ctrl Pts',(-3.15089964033089,0.703608249011111,
3.5153874968761));
#248452=CARTESIAN_POINT('Ctrl Pts',(-3.10321372094272,0.89067809468383,
3.50476689358768));
#248453=CARTESIAN_POINT('Ctrl Pts',(-2.9801910097107,1.23932235808301,3.48398237337513));
#248454=CARTESIAN_POINT('Ctrl Pts',(-2.90763474381403,1.40110942729422,
3.47388534453785));
#248455=CARTESIAN_POINT('Ctrl Pts',(-2.80553478614379,1.58627831501247,
3.46126581227636));
#248456=CARTESIAN_POINT('Ctrl Pts',(-2.78841865456458,1.6161762278175,3.45919389511154));
#248457=CARTESIAN_POINT('Ctrl Pts',(-2.76057494076108,1.66305339018981,
3.45588757526961));
#248458=CARTESIAN_POINT('Ctrl Pts',(-2.7501619970267,1.68021711219019,3.45466449058606));
#248459=CARTESIAN_POINT('Ctrl Pts',(-2.73024739295164,1.71236135046118,
3.45234966025601));
#248460=CARTESIAN_POINT('Ctrl Pts',(-2.72078104398913,1.72736293584379,
3.45125923462637));
#248461=CARTESIAN_POINT('Ctrl Pts',(-2.69911523808883,1.76107736011302,
3.44878529063712));
#248462=CARTESIAN_POINT('Ctrl Pts',(-2.68684419563857,1.77974289299521,
3.44739915891648));
#248463=CARTESIAN_POINT('Ctrl Pts',(-2.64896457219779,1.83607704426674,
3.44316449279439));
#248464=CARTESIAN_POINT('Ctrl Pts',(-2.62275143509932,1.87333040048548,
3.44029350634888));
#248465=CARTESIAN_POINT('Ctrl Pts',(-2.48152057090043,2.06526678645987,
3.42512004087489));
#248466=CARTESIAN_POINT('Ctrl Pts',(-2.35360178063439,2.20993422866937,
3.41232271326636));
#248467=CARTESIAN_POINT('Ctrl Pts',(-2.09758483754045,2.45187943035928,
3.38856857895729));
#248468=CARTESIAN_POINT('Ctrl Pts',(-1.97364074522804,2.55270835441169,
3.3777155285123));
#248469=CARTESIAN_POINT('Ctrl Pts',(-1.80312920065712,2.67154886197651,
3.36397108369889));
#248470=CARTESIAN_POINT('Ctrl Pts',(-1.76290539056583,2.69826115947316,
3.36080883179749));
#248471=CARTESIAN_POINT('Ctrl Pts',(-1.69410864082025,2.74175303542997,
3.35555193382845));
#248472=CARTESIAN_POINT('Ctrl Pts',(-1.66585034885558,2.75901370155642,
3.35343438149211));
#248473=CARTESIAN_POINT('Ctrl Pts',(-1.62539047440193,2.78287899714211,
3.35046653290972));
#248474=CARTESIAN_POINT('Ctrl Pts',(-1.61340554212683,2.78984449027362,
3.34959524338327));
#248475=CARTESIAN_POINT('Ctrl Pts',(-1.592631734027,2.80173932553383,3.34809899809088));
#248476=CARTESIAN_POINT('Ctrl Pts',(-1.58386409631974,2.80670511879655,
3.34747177838447));
#248477=CARTESIAN_POINT('Ctrl Pts',(-1.56526229419403,2.81712583459774,
3.34615021692128));
#248478=CARTESIAN_POINT('Ctrl Pts',(-1.55542273047473,2.82257048733811,
3.34545650807029));
#248479=CARTESIAN_POINT('Ctrl Pts',(-1.52844038516536,2.83731703153946,
3.34356820367578));
#248480=CARTESIAN_POINT('Ctrl Pts',(-1.51124103858267,2.84651515266133,
3.34237990363718));
#248481=CARTESIAN_POINT('Ctrl Pts',(-1.42456875341322,2.89186001139771,
3.33646306224073));
#248482=CARTESIAN_POINT('Ctrl Pts',(-1.35387262078618,2.92562496231921,
3.33186485165266));
#248483=CARTESIAN_POINT('Ctrl Pts',(-1.08476213433725,3.04230669904457,
3.31494644234621));
#248484=CARTESIAN_POINT('Ctrl Pts',(-0.879441533515686,3.10788230088653,
3.30316354797984));
#248485=CARTESIAN_POINT('Ctrl Pts',(-0.522907704142829,3.18355510868616,
3.28255340940763));
#248486=CARTESIAN_POINT('Ctrl Pts',(-0.374740084232653,3.20437479895645,
3.27395340601488));
#248487=CARTESIAN_POINT('Ctrl Pts',(-0.192449014036389,3.21717115309778,
3.26303687384691));
#248488=CARTESIAN_POINT('Ctrl Pts',(-0.159191599858462,3.21898815812914,
3.26103225874643));
#248489=CARTESIAN_POINT('Ctrl Pts',(-0.106098357815305,3.22106409703047,
3.25780868747769));
#248490=CARTESIAN_POINT('Ctrl Pts',(-0.0862774425607045,3.22165593358697,
3.25660007984606));
#248491=CARTESIAN_POINT('Ctrl Pts',(-0.0486759815078143,3.22243143545234,
3.25429692818853));
#248492=CARTESIAN_POINT('Ctrl Pts',(-0.0308968571526456,3.22265093853157,
3.25320354097748));
#248493=CARTESIAN_POINT('Ctrl Pts',(0.00962817657580653,3.22281588320249,
3.25070093048315));
#248494=CARTESIAN_POINT('Ctrl Pts',(0.0323733190128121,3.22266765968807,
3.24928885104319));
#248495=CARTESIAN_POINT('Ctrl Pts',(0.0918844051583125,3.22164976955488,
3.24557397995792));
#248496=CARTESIAN_POINT('Ctrl Pts',(0.128639545142351,3.22039154001892,
3.24325933036316));
#248497=CARTESIAN_POINT('Ctrl Pts',(0.43190691043073,3.20480992990229,3.22398762914779));
#248498=CARTESIAN_POINT('Ctrl Pts',(0.695673085753161,3.15805911561848,
3.20599016096453));
#248499=CARTESIAN_POINT('Ctrl Pts',(1.10240952090309,3.03249948105887,3.17724350798005));
#248500=CARTESIAN_POINT('Ctrl Pts',(1.25056238363601,2.97446872652255,3.16657749830486));
#248501=CARTESIAN_POINT('Ctrl Pts',(1.41346709145941,2.89632561825077,3.15503484744299));
#248502=CARTESIAN_POINT('Ctrl Pts',(1.43299647288497,2.88671309167331,3.15365444644216));
#248503=CARTESIAN_POINT('Ctrl Pts',(1.46289971728469,2.87161619953125,3.15154767000034));
#248504=CARTESIAN_POINT('Ctrl Pts',(1.47334311449402,2.86627201383727,3.15081320642945));
#248505=CARTESIAN_POINT('Ctrl Pts',(1.49261149654056,2.85627869221506,3.14946084621743));
#248506=CARTESIAN_POINT('Ctrl Pts',(1.50144413164689,2.85164558990546,3.1488420368096));
#248507=CARTESIAN_POINT('Ctrl Pts',(1.52156866650713,2.84096996822715,3.14743452475259));
#248508=CARTESIAN_POINT('Ctrl Pts',(1.53284619509809,2.83490107803413,3.14664747500901));
#248509=CARTESIAN_POINT('Ctrl Pts',(1.56769098308754,2.81588097551683,3.14422004275143));
#248510=CARTESIAN_POINT('Ctrl Pts',(1.59113318352275,2.80270155115572,3.14259317913196));
#248511=CARTESIAN_POINT('Ctrl Pts',(1.80403676723555,2.67947277931232,3.12784969511117));
#248512=CARTESIAN_POINT('Ctrl Pts',(1.9820041024881,2.55064866409071,3.11573089069606));
#248513=CARTESIAN_POINT('Ctrl Pts',(2.27814421780201,2.28642939986175,3.09349983088599));
#248514=CARTESIAN_POINT('Ctrl Pts',(2.40072549248626,2.15736160707306,3.08348084110783));
#248515=CARTESIAN_POINT('Ctrl Pts',(2.54574313657052,1.97691786424192,3.06985437633003));
#248516=CARTESIAN_POINT('Ctrl Pts',(2.57839055992683,1.93414425145221,3.06665114727982));
#248517=CARTESIAN_POINT('Ctrl Pts',(2.62393296537588,1.87127268127357,3.06196919740733));
#248518=CARTESIAN_POINT('Ctrl Pts',(2.63770034035068,1.85181600663214,3.06052384425123));
#248519=CARTESIAN_POINT('Ctrl Pts',(2.66144103184456,1.81746265306636,3.05797711547961));
#248520=CARTESIAN_POINT('Ctrl Pts',(2.67150833638669,1.80263197840953,3.05687934713849));
#248521=CARTESIAN_POINT('Ctrl Pts',(2.69215892592693,1.77165755238502,3.05458968550711));
#248522=CARTESIAN_POINT('Ctrl Pts',(2.70272190866169,1.75550118886462,3.05339709414926));
#248523=CARTESIAN_POINT('Ctrl Pts',(2.72979398434849,1.71327019695115,3.05028367826437));
#248524=CARTESIAN_POINT('Ctrl Pts',(2.74607450114559,1.68705207189909,3.04835457554762));
#248525=CARTESIAN_POINT('Ctrl Pts',(2.81393116932687,1.5741905120779,3.04006392425001));
#248526=CARTESIAN_POINT('Ctrl Pts',(2.86179773004745,1.48539377569277,3.0335722389042));
#248527=CARTESIAN_POINT('Ctrl Pts',(2.99595093446929,1.20588892317464,3.01323692386304));
#248528=CARTESIAN_POINT('Ctrl Pts',(3.06789238929154,1.00891577297083,2.99900515589237));
#248529=CARTESIAN_POINT('Ctrl Pts',(3.15103602008227,0.687200149257676,
2.97662867142827));
#248530=CARTESIAN_POINT('Ctrl Pts',(3.1749871855883,0.566333859810984,2.96841794070674));
#248531=CARTESIAN_POINT('Ctrl Pts',(3.19586231268883,0.416389820650886,
2.95868158424196));
#248532=CARTESIAN_POINT('Ctrl Pts',(3.19939131884632,0.38834484471867,2.95687982261189));
#248533=CARTESIAN_POINT('Ctrl Pts',(3.20400601091198,0.347321830891428,
2.95427589144665));
#248534=CARTESIAN_POINT('Ctrl Pts',(3.20538263977297,0.334378705055904,
2.95345891125379));
#248535=CARTESIAN_POINT('Ctrl Pts',(3.20767555737348,0.311503690749481,
2.95202353350335));
#248536=CARTESIAN_POINT('Ctrl Pts',(3.20862420551826,0.30157544265629,2.95140339779013));
#248537=CARTESIAN_POINT('Ctrl Pts',(3.21058883698534,0.279954668556267,
2.9500591909348));
#248538=CARTESIAN_POINT('Ctrl Pts',(3.21158705443249,0.268260877584965,
2.94933609668564));
#248539=CARTESIAN_POINT('Ctrl Pts',(3.21420783812306,0.235444895199184,
2.94731727043798));
#248540=CARTESIAN_POINT('Ctrl Pts',(3.21568608858832,0.214311359288031,
2.94602918755814));
#248541=CARTESIAN_POINT('Ctrl Pts',(3.22414844386557,0.0733792936525302,
2.93751054944187));
#248542=CARTESIAN_POINT('Ctrl Pts',(3.2246457926928,-0.0467273835608476,
2.93059136498316));
#248543=CARTESIAN_POINT('Ctrl Pts',(3.21579418261589,-0.21773281124742,
2.92088397833321));
#248544=CARTESIAN_POINT('Ctrl Pts',(3.21192856197228,-0.268802707770167,
2.91800357849531));
#248545=CARTESIAN_POINT('Ctrl Pts',(3.19343181518326,-0.454305345317533,
2.90754732518912));
#248546=CARTESIAN_POINT('Ctrl Pts',(3.17156195260599,-0.587872414287476,
2.90002477438403));
#248547=CARTESIAN_POINT('Ctrl Pts',(3.12145068564085,-0.806609428056208,
2.88728179814289));
#248548=CARTESIAN_POINT('Ctrl Pts',(3.09793332186683,-0.892681731611156,
2.88215640094006));
#248549=CARTESIAN_POINT('Ctrl Pts',(3.05234085060794,-1.03588933200876,
2.87334870506628));
#248550=CARTESIAN_POINT('Ctrl Pts',(3.03215261074513,-1.09357268218618,
2.86972236067306));
#248551=CARTESIAN_POINT('Ctrl Pts',(3.00140161624102,-1.17402399740174,
2.86453547998867));
#248552=CARTESIAN_POINT('Ctrl Pts',(2.99219348922953,-1.19729782332667,
2.86301946792215));
#248553=CARTESIAN_POINT('Ctrl Pts',(2.97585308277802,-1.23723253664806,
2.86039026907377));
#248554=CARTESIAN_POINT('Ctrl Pts',(2.96884954929545,-1.25394507564014,
2.85928142864144));
#248555=CARTESIAN_POINT('Ctrl Pts',(2.95426178019234,-1.28794851116944,
2.85700748722554));
#248556=CARTESIAN_POINT('Ctrl Pts',(2.94666579932208,-1.30523357158907,
2.85584202290379));
#248557=CARTESIAN_POINT('Ctrl Pts',(2.9270682821886,-1.34878567520039,2.85288076208835));
#248558=CARTESIAN_POINT('Ctrl Pts',(2.91486494312401,-1.37495956414327,
2.85107814981408));
#248559=CARTESIAN_POINT('Ctrl Pts',(2.86629731419576,-1.47557476667705,
2.84405746363688));
#248560=CARTESIAN_POINT('Ctrl Pts',(2.8274221226308,-1.54876187959743,2.83875414919275));
#248561=CARTESIAN_POINT('Ctrl Pts',(2.67273414190372,-1.81470541655516,
2.81873425374766));
#248562=CARTESIAN_POINT('Ctrl Pts',(2.53967868150552,-1.99666549417463,
2.803463033712));
#248563=CARTESIAN_POINT('Ctrl Pts',(2.32431186708538,-2.23448457818065,
2.78183730636758));
#248564=CARTESIAN_POINT('Ctrl Pts',(2.2566689232045,-2.30277974467909,2.7754038205973));
#248565=CARTESIAN_POINT('Ctrl Pts',(2.15958146972077,-2.39240993042038,
2.7667481715331));
#248566=CARTESIAN_POINT('Ctrl Pts',(2.13268125929044,-2.41642054758717,
2.76440685510545));
#248567=CARTESIAN_POINT('Ctrl Pts',(2.08525641111725,-2.45734204409144,
2.76038478612001));
#248568=CARTESIAN_POINT('Ctrl Pts',(2.06491525222595,-2.47445940115774,
2.75869224757462));
#248569=CARTESIAN_POINT('Ctrl Pts',(2.03454596640609,-2.49938023755613,
2.75621587841797));
#248570=CARTESIAN_POINT('Ctrl Pts',(2.02468032253591,-2.50737880375097,
2.75541914863242));
#248571=CARTESIAN_POINT('Ctrl Pts',(2.00774602050674,-2.52094315911444,
2.75406509516637));
#248572=CARTESIAN_POINT('Ctrl Pts',(2.00070103443402,-2.52653792212658,
2.75350575306733));
#248573=CARTESIAN_POINT('Ctrl Pts',(1.98454794107962,-2.53925593830009,
2.75223236105411));
#248574=CARTESIAN_POINT('Ctrl Pts',(1.97542484678221,-2.54635974185872,
2.75151967042854));
#248575=CARTESIAN_POINT('Ctrl Pts',(1.95009258142763,-2.56586692007177,
2.74955803571339));
#248576=CARTESIAN_POINT('Ctrl Pts',(1.93380320903282,-2.5781658838638,2.74831606767961));
#248577=CARTESIAN_POINT('Ctrl Pts',(1.83863505924553,-2.64861120169602,
2.74116483858797));
#248578=CARTESIAN_POINT('Ctrl Pts',(1.75724649293034,-2.70329588197189,
2.73546181601185));
#248579=CARTESIAN_POINT('Ctrl Pts',(1.53256202557386,-2.83981730948932,
2.72043723687877));
#248580=CARTESIAN_POINT('Ctrl Pts',(1.38527071204616,-2.9145047442422,2.71131554183506));
#248581=CARTESIAN_POINT('Ctrl Pts',(1.0705417756412,-3.04482176041822,2.69216110362256));
#248582=CARTESIAN_POINT('Ctrl Pts',(0.902971123622289,-3.09864996758937,
2.68213411828887));
#248583=CARTESIAN_POINT('Ctrl Pts',(0.698353142185645,-3.14636365309048,
2.66959437576612));
#248584=CARTESIAN_POINT('Ctrl Pts',(0.664723905270156,-3.15363969763416,
2.6675250051704));
#248585=CARTESIAN_POINT('Ctrl Pts',(0.611307864430769,-3.16430448979699,
2.66422181693925));
#248586=CARTESIAN_POINT('Ctrl Pts',(0.591594260856632,-3.16804930700748,
2.66299927997776));
#248587=CARTESIAN_POINT('Ctrl Pts',(0.554388869425165,-3.174757510376,2.66068490786022));
#248588=CARTESIAN_POINT('Ctrl Pts',(0.536905017613769,-3.17776104363946,
2.65959438665336));
#248589=CARTESIAN_POINT('Ctrl Pts',(0.497337561215314,-3.18422243762676,
2.65711943665369));
#248590=CARTESIAN_POINT('Ctrl Pts',(0.475241167969115,-3.18759517101655,
2.65573238589707));
#248591=CARTESIAN_POINT('Ctrl Pts',(0.409446430128924,-3.19693858378569,
2.65158686358277));
#248592=CARTESIAN_POINT('Ctrl Pts',(0.365660089473951,-3.20224219572318,
2.64880780033021));
#248593=CARTESIAN_POINT('Ctrl Pts',(0.10027185813783,-3.22887336654518,
2.63183484668577));
#248594=CARTESIAN_POINT('Ctrl Pts',(-0.122908437967073,-3.22808618412978,
2.61695712750408));
#248595=CARTESIAN_POINT('Ctrl Pts',(-0.48094219470975,-3.18962847467594,
2.59262365338703));
#248596=CARTESIAN_POINT('Ctrl Pts',(-0.61662219192827,-3.16619891788591,
2.58330775181483));
#248597=CARTESIAN_POINT('Ctrl Pts',(-0.793751734870082,-3.12378989679679,
2.57129422204483));
#248598=CARTESIAN_POINT('Ctrl Pts',(-0.836890628882467,-3.11251017509812,
2.56838101615001));
#248599=CARTESIAN_POINT('Ctrl Pts',(-0.909806294157113,-3.09181888516357,
2.56349350448069));
#248600=CARTESIAN_POINT('Ctrl Pts',(-0.939705018092214,-3.08286330483247,
2.56150001261691));
#248601=CARTESIAN_POINT('Ctrl Pts',(-0.982383558607825,-3.06940115554044,
2.55867429339445));
#248602=CARTESIAN_POINT('Ctrl Pts',(-0.995271420015805,-3.06524643798228,
2.557823617158));
#248603=CARTESIAN_POINT('Ctrl Pts',(-1.0176607305634,-3.05787259784906,
2.5563508265253));
#248604=CARTESIAN_POINT('Ctrl Pts',(-1.02717390512542,-3.0546901588129,
2.55572664750061));
#248605=CARTESIAN_POINT('Ctrl Pts',(-1.04747672608429,-3.04779268919275,
2.55439810189948));
#248606=CARTESIAN_POINT('Ctrl Pts',(-1.05826163582326,-3.04406473114278,
2.55369448788541));
#248607=CARTESIAN_POINT('Ctrl Pts',(-1.08764943832201,-3.033731356943,2.55178240636846));
#248608=CARTESIAN_POINT('Ctrl Pts',(-1.10621213648137,-3.02701205809077,
2.55058035387507));
#248609=CARTESIAN_POINT('Ctrl Pts',(-1.20492380877698,-2.99025121530015,
2.54421281295866));
#248610=CARTESIAN_POINT('Ctrl Pts',(-1.28392059334139,-2.95719363660581,
2.53920388534461));
#248611=CARTESIAN_POINT('Ctrl Pts',(-1.51895211333019,-2.84764358494459,
2.52430183747064));
#248612=CARTESIAN_POINT('Ctrl Pts',(-1.67020713366898,-2.76164872483479,
2.51469961725588));
#248613=CARTESIAN_POINT('Ctrl Pts',(-1.96281191971226,-2.56241793403974,
2.49480930804273));
#248614=CARTESIAN_POINT('Ctrl Pts',(-2.10303002708986,-2.4486465011688,
2.48453813131786));
#248615=CARTESIAN_POINT('Ctrl Pts',(-2.2579082061274,-2.29981782158523,
2.4717201379051));
#248616=CARTESIAN_POINT('Ctrl Pts',(-2.2824352725212,-2.2754780967696,2.46964212293087));
#248617=CARTESIAN_POINT('Ctrl Pts',(-2.32060166867222,-2.23636521497344,
2.46632829842681));
#248618=CARTESIAN_POINT('Ctrl Pts',(-2.33450265728251,-2.22185030869405,
2.46510389631652));
#248619=CARTESIAN_POINT('Ctrl Pts',(-2.36041359797178,-2.19428342817489,
2.46278794889375));
#248620=CARTESIAN_POINT('Ctrl Pts',(-2.37245337679163,-2.18126043190607,
2.46169773806644));
#248621=CARTESIAN_POINT('Ctrl Pts',(-2.39938992298103,-2.15163728723446,
2.4592261534708));
#248622=CARTESIAN_POINT('Ctrl Pts',(-2.41422296463741,-2.13498066865706,
2.45784218669277));
#248623=CARTESIAN_POINT('Ctrl Pts',(-2.45870132023615,-2.08397788262185,
2.45362096846656));
#248624=CARTESIAN_POINT('Ctrl Pts',(-2.48779432700483,-2.04915959609886,
2.45076147385152));
#248625=CARTESIAN_POINT('Ctrl Pts',(-2.63794060419737,-1.86155381978938,
2.43546293057711));
#248626=CARTESIAN_POINT('Ctrl Pts',(-2.74566309043722,-1.69865422440675,
2.42251617183928));
#248627=CARTESIAN_POINT('Ctrl Pts',(-2.91289611353815,-1.38785392708609,
2.3987111821227));
#248628=CARTESIAN_POINT('Ctrl Pts',(-2.97745277950062,-1.24333428675556,
2.38796211958973));
#248629=CARTESIAN_POINT('Ctrl Pts',(-3.05544361208147,-1.02737493749487,
2.37278034444477));
#248630=CARTESIAN_POINT('Ctrl Pts',(-3.07749691403045,-0.95929625738058,
2.36811743229979));
#248631=CARTESIAN_POINT('Ctrl Pts',(-3.10231684408046,-0.872972897974947,
2.3624037469124));
#248632=CARTESIAN_POINT('Ctrl Pts',(-3.10721698217725,-0.85536784092586,
2.36124873170681));
#248633=CARTESIAN_POINT('Ctrl Pts',(-3.11482024736893,-0.827123239765063,
2.35941310431767));
#248634=CARTESIAN_POINT('Ctrl Pts',(-3.11761914442909,-0.81651019946153,
2.35872727497787));
#248635=CARTESIAN_POINT('Ctrl Pts',(-3.1228806622513,-0.796137698523732,
2.35741854861118));
#248636=CARTESIAN_POINT('Ctrl Pts',(-3.12535184403775,-0.786380772181157,
2.3567951999368));
#248637=CARTESIAN_POINT('Ctrl Pts',(-3.13070829353867,-0.764807870739081,
2.35542425001323));
#248638=CARTESIAN_POINT('Ctrl Pts',(-3.13357248809667,-0.752986700465426,
2.35467782873675));
#248639=CARTESIAN_POINT('Ctrl Pts',(-3.14349140876524,-0.711012162798436,
2.35204355768091));
#248640=CARTESIAN_POINT('Ctrl Pts',(-3.15017862076739,-0.680772611206659,
2.35017517905102));
#248641=CARTESIAN_POINT('Ctrl Pts',(-3.20032911924268,-0.437404332589009,
2.33533964358688));
#248642=CARTESIAN_POINT('Ctrl Pts',(-3.22255453540802,-0.220443682782572,
2.32331999856126));
#248643=CARTESIAN_POINT('Ctrl Pts',(-3.22274957214941,-0.00191754697872536,
2.3110756989822));
#248644=CARTESIAN_POINT('Ctrl Pts',(-3.22275000000004,-0.000958768568118341,
2.3110219753754));
#248645=CARTESIAN_POINT('Ctrl Pts',(-3.22275,1.20843135519762E-10,2.31096825019553));
#248646=CARTESIAN_POINT('Ctrl Pts',(-3.22275,-8.28983494685339E-13,2.06147698899067));
#248647=CARTESIAN_POINT('Ctrl Pts',(-3.22274999999999,-0.0339972115249406,
2.06350045582317));
#248648=CARTESIAN_POINT('Ctrl Pts',(-3.22221203950403,-0.0679913131819596,
2.06553925904328));
#248649=CARTESIAN_POINT('Ctrl Pts',(-3.22043179503059,-0.124227760372896,
2.06894080846313));
#248650=CARTESIAN_POINT('Ctrl Pts',(-3.21949650969314,-0.146477536901708,
2.0702940719618));
#248651=CARTESIAN_POINT('Ctrl Pts',(-3.21738344095369,-0.186785377642087,
2.07275993161626));
#248652=CARTESIAN_POINT('Ctrl Pts',(-3.21628400070987,-0.204846745826508,
2.07387005087609));
#248653=CARTESIAN_POINT('Ctrl Pts',(-3.21358425686546,-0.243787334517675,
2.07627512342972));
#248654=CARTESIAN_POINT('Ctrl Pts',(-3.21193244198802,-0.26466204057638,
2.07757163061838));
#248655=CARTESIAN_POINT('Ctrl Pts',(-3.20678265582034,-0.322560899965624,
2.08118841681156));
#248656=CARTESIAN_POINT('Ctrl Pts',(-3.20284716525184,-0.359541913790397,
2.08352214890238));
#248657=CARTESIAN_POINT('Ctrl Pts',(-3.17322558534967,-0.5985102625577,
2.09876131070165));
#248658=CARTESIAN_POINT('Ctrl Pts',(-3.12908986305313,-0.797713385329973,
2.11224486322262));
#248659=CARTESIAN_POINT('Ctrl Pts',(-2.99914551331924,-1.19964385980282,
2.14071567900263));
#248660=CARTESIAN_POINT('Ctrl Pts',(-2.91077521656446,-1.40050675599089,
2.15566473164271));
#248661=CARTESIAN_POINT('Ctrl Pts',(-2.78920641741812,-1.61468099612505,
2.17148927341377));
#248662=CARTESIAN_POINT('Ctrl Pts',(-2.77538784506512,-1.63831913305582,
2.17323345583134));
#248663=CARTESIAN_POINT('Ctrl Pts',(-2.75455631395967,-1.6729335186778,
2.17578084657559));
#248664=CARTESIAN_POINT('Ctrl Pts',(-2.74777577437603,-1.68404731288453,
2.17659771413546));
#248665=CARTESIAN_POINT('Ctrl Pts',(-2.73557430817447,-1.7037765007393,
2.17804554150918));
#248666=CARTESIAN_POINT('Ctrl Pts',(-2.73017971346998,-1.71240763275635,
2.17867812660426));
#248667=CARTESIAN_POINT('Ctrl Pts',(-2.71820344872484,-1.73136870282536,
2.18006598769917));
#248668=CARTESIAN_POINT('Ctrl Pts',(-2.71160371612674,-1.74168678923196,
2.1808200798644));
#248669=CARTESIAN_POINT('Ctrl Pts',(-2.69217991172997,-1.77167612156242,
2.18300925680772));
#248670=CARTESIAN_POINT('Ctrl Pts',(-2.67919918337484,-1.7912455902901,
2.18443453910911));
#248671=CARTESIAN_POINT('Ctrl Pts',(-2.64885696131784,-1.8359210047047,
2.18768504944634));
#248672=CARTESIAN_POINT('Ctrl Pts',(-2.63135017996808,-1.86092597959875,
2.18950194148782));
#248673=CARTESIAN_POINT('Ctrl Pts',(-2.5704963333159,-1.94526742986716,
2.19563570470074));
#248674=CARTESIAN_POINT('Ctrl Pts',(-2.52547446985483,-2.00337134908094,
2.19987086709616));
#248675=CARTESIAN_POINT('Ctrl Pts',(-2.39031516647057,-2.16599799259079,
2.21190962411294));
#248676=CARTESIAN_POINT('Ctrl Pts',(-2.29540182003195,-2.26633772133248,
2.21957536104972));
#248677=CARTESIAN_POINT('Ctrl Pts',(-2.05578107840721,-2.48911188604598,
2.23793647238236));
#248678=CARTESIAN_POINT('Ctrl Pts',(-1.9061574350839,-2.60546837937968,
2.2486805173335));
#248679=CARTESIAN_POINT('Ctrl Pts',(-1.71756047742832,-2.72715017459533,
2.2620630584129));
#248680=CARTESIAN_POINT('Ctrl Pts',(-1.6876061982865,-2.7457871807857,2.26418312372979));
#248681=CARTESIAN_POINT('Ctrl Pts',(-1.63956900594751,-2.77459204583927,
2.26757767800525));
#248682=CARTESIAN_POINT('Ctrl Pts',(-1.62168296709077,-2.78508381729775,
2.26884043323253));
#248683=CARTESIAN_POINT('Ctrl Pts',(-1.588132153922,-2.80433161965916,2.2712075798081));
#248684=CARTESIAN_POINT('Ctrl Pts',(-1.57249301099894,-2.81313086813159,
2.27231036831007));
#248685=CARTESIAN_POINT('Ctrl Pts',(-1.53710673728504,-2.83265341241917,
2.27480463908018));
#248686=CARTESIAN_POINT('Ctrl Pts',(-1.51731945614875,-2.84330162031279,
2.27619870795483));
#248687=CARTESIAN_POINT('Ctrl Pts',(-1.45784640883252,-2.87450847234073,
2.28038757177748));
#248688=CARTESIAN_POINT('Ctrl Pts',(-1.41784395180717,-2.8944487073069,
2.28320359355855));
#248689=CARTESIAN_POINT('Ctrl Pts',(-1.22417047088155,-2.98601187386396,
2.29683642588812));
#248690=CARTESIAN_POINT('Ctrl Pts',(-1.06544228436468,-3.04625647769654,
2.30802652857114));
#248691=CARTESIAN_POINT('Ctrl Pts',(-0.726255394145973,-3.1452292423351,
2.33176844904113));
#248692=CARTESIAN_POINT('Ctrl Pts',(-0.545694585095951,-3.18152997631991,
2.34431360247577));
#248693=CARTESIAN_POINT('Ctrl Pts',(-0.293218791259436,-3.21015193640287,
2.36111259404778));
#248694=CARTESIAN_POINT('Ctrl Pts',(-0.223169519390601,-3.21578133873182,
2.36569274733126));
#248695=CARTESIAN_POINT('Ctrl Pts',(-0.133920771989147,-3.22002284727679,
2.37138169220627));
#248696=CARTESIAN_POINT('Ctrl Pts',(-0.114846186987461,-3.22075958497019,
2.37258904283301));
#248697=CARTESIAN_POINT('Ctrl Pts',(-0.0844608778842142,-3.22166289881622,
2.37449758551501));
#248698=CARTESIAN_POINT('Ctrl Pts',(-0.07315420465038,-3.22193946947361,
2.37520452576081));
#248699=CARTESIAN_POINT('Ctrl Pts',(-0.0514673560231443,-3.22235572710195,
2.37655394969274));
#248700=CARTESIAN_POINT('Ctrl Pts',(-0.0410877128160776,-3.22250479020141,
2.37719690160708));
#248701=CARTESIAN_POINT('Ctrl Pts',(-0.0160513173086691,-3.22274335593215,
2.37874106916979));
#248702=CARTESIAN_POINT('Ctrl Pts',(-0.00139412330314588,-3.2227830299668,
2.37963957861804));
#248703=CARTESIAN_POINT('Ctrl Pts',(0.0501838199945576,-3.22257076037367,
2.3827836196372));
#248704=CARTESIAN_POINT('Ctrl Pts',(0.0871009188320858,-3.22178435192632,
2.38500194341372));
#248705=CARTESIAN_POINT('Ctrl Pts',(0.179674846434587,-3.21821985137548,
2.39050227532089));
#248706=CARTESIAN_POINT('Ctrl Pts',(0.235289657990019,-3.21463240364879,
2.39375007957079));
#248707=CARTESIAN_POINT('Ctrl Pts',(0.504586891057592,-3.19023440326406,
2.40931872998733));
#248708=CARTESIAN_POINT('Ctrl Pts',(0.71592571992699,-3.14954977598937,
2.42108682620467));
#248709=CARTESIAN_POINT('Ctrl Pts',(1.05898053129865,-3.04716506466833,
2.44135583743441));
#248710=CARTESIAN_POINT('Ctrl Pts',(1.19340190003298,-2.9970718712757,2.44961095275508));
#248711=CARTESIAN_POINT('Ctrl Pts',(1.35536145635372,-2.92408849102193,
2.46021483728581));
#248712=CARTESIAN_POINT('Ctrl Pts',(1.38645912946501,-2.90947231088525,
2.46228170572547));
#248713=CARTESIAN_POINT('Ctrl Pts',(1.43558260532636,-2.88541744135682,
2.46559898352912));
#248714=CARTESIAN_POINT('Ctrl Pts',(1.45376349272485,-2.87630021130383,
2.46683833165537));
#248715=CARTESIAN_POINT('Ctrl Pts',(1.48802369245221,-2.85871182824981,
2.46919642596796));
#248716=CARTESIAN_POINT('Ctrl Pts',(1.50412007560849,-2.85027553109285,
2.47031392294028));
#248717=CARTESIAN_POINT('Ctrl Pts',(1.54057490840569,-2.8307743440377,2.47286716260956));
#248718=CARTESIAN_POINT('Ctrl Pts',(1.56088692555879,-2.81962522267304,
2.47430583092269));
#248719=CARTESIAN_POINT('Ctrl Pts',(1.62322425619025,-2.78452870317254,
2.47877183664026));
#248720=CARTESIAN_POINT('Ctrl Pts',(1.66483047305611,-2.75985437622065,
2.48182479159486));
#248721=CARTESIAN_POINT('Ctrl Pts',(1.7607120434375,-2.70003516873833,2.48903446976324));
#248722=CARTESIAN_POINT('Ctrl Pts',(1.81451490788503,-2.66417558895296,
2.49321531438081));
#248723=CARTESIAN_POINT('Ctrl Pts',(2.0164143960751,-2.52065584478898,2.50942666581588));
#248724=CARTESIAN_POINT('Ctrl Pts',(2.15630676687972,-2.40207456011241,
2.52180052860347));
#248725=CARTESIAN_POINT('Ctrl Pts',(2.30467916522628,-2.25284754000171,
2.53601445098197));
#248726=CARTESIAN_POINT('Ctrl Pts',(2.32374682863003,-2.23317459837365,
2.53786352740111));
#248727=CARTESIAN_POINT('Ctrl Pts',(2.43689292444735,-2.11341840971826,
2.54896320770817));
#248728=CARTESIAN_POINT('Ctrl Pts',(2.52475522660024,-2.00763627908183,
2.55812820082239));
#248729=CARTESIAN_POINT('Ctrl Pts',(2.61846289356527,-1.87889514845465,
2.56830392637445));
#248730=CARTESIAN_POINT('Ctrl Pts',(2.63114077578863,-1.86109999237588,
2.56968998637514));
#248731=CARTESIAN_POINT('Ctrl Pts',(2.65052238328633,-1.83330128183385,
2.57182197569998));
#248732=CARTESIAN_POINT('Ctrl Pts',(2.65735241253575,-1.82338713956691,
2.57257586790359));
#248733=CARTESIAN_POINT('Ctrl Pts',(2.66986541922957,-1.80500421361638,
2.57396150634533));
#248734=CARTESIAN_POINT('Ctrl Pts',(2.67556380224138,-1.79654666295264,
2.57459423093243));
#248735=CARTESIAN_POINT('Ctrl Pts',(2.68859873259164,-1.77700061388987,
2.57604569339867));
#248736=CARTESIAN_POINT('Ctrl Pts',(2.69590690768322,-1.76589362251439,
2.57686257192101));
#248737=CARTESIAN_POINT('Ctrl Pts',(2.7188568685721,-1.73053963930116,2.57943881716627));
#248738=CARTESIAN_POINT('Ctrl Pts',(2.73424233037289,-1.70612693639275,
2.58118239465844));
#248739=CARTESIAN_POINT('Ctrl Pts',(2.81520117897665,-1.57375779140271,
2.59046617722703));
#248740=CARTESIAN_POINT('Ctrl Pts',(2.87471929866967,-1.46221294221823,
2.59769046703219));
#248741=CARTESIAN_POINT('Ctrl Pts',(3.01904123741079,-1.14865197939621,
2.61716800091635));
#248742=CARTESIAN_POINT('Ctrl Pts',(3.09005199176125,-0.941057169957835,
2.62921374744402));
#248743=CARTESIAN_POINT('Ctrl Pts',(3.1595318075088,-0.64137342489453,2.64697391288844));
#248744=CARTESIAN_POINT('Ctrl Pts',(3.17600067870114,-0.554092780345073,
2.652182324925));
#248745=CARTESIAN_POINT('Ctrl Pts',(3.19317466451042,-0.436633626085735,
2.65929646023212));
#248746=CARTESIAN_POINT('Ctrl Pts',(3.19709186897456,-0.406960504697855,
2.66110236644904));
#248747=CARTESIAN_POINT('Ctrl Pts',(3.20286470411744,-0.357982101182787,
2.66409940041464));
#248748=CARTESIAN_POINT('Ctrl Pts',(3.20496042372282,-0.338706590640208,
2.6652830031103));
#248749=CARTESIAN_POINT('Ctrl Pts',(3.2087144316238,-0.30101671723573,2.66760586713654));
#248750=CARTESIAN_POINT('Ctrl Pts',(3.21038844297154,-0.282604654140058,
2.66874459033441));
#248751=CARTESIAN_POINT('Ctrl Pts',(3.21398232187494,-0.238910145150559,
2.67145679301039));
#248752=CARTESIAN_POINT('Ctrl Pts',(3.21576240228028,-0.213617734340076,
2.67303455120055));
#248753=CARTESIAN_POINT('Ctrl Pts',(3.22081270796597,-0.127332995099941,
2.67844489826843));
#248754=CARTESIAN_POINT('Ctrl Pts',(3.22264724878694,-0.0662729042080321,
2.68232125166998));
#248755=CARTESIAN_POINT('Ctrl Pts',(3.22288888114103,0.0834610978155122,
2.69194855098586));
#248756=CARTESIAN_POINT('Ctrl Pts',(3.2193731253348,0.172084415841955,2.69775199704938));
#248757=CARTESIAN_POINT('Ctrl Pts',(3.20127563992011,0.395291039741049,
2.71260789526754));
#248758=CARTESIAN_POINT('Ctrl Pts',(3.18186249727505,0.529309173606279,
2.72175356688097));
#248759=CARTESIAN_POINT('Ctrl Pts',(3.14384997502572,0.710500450187193,
2.73426146210632));
#248760=CARTESIAN_POINT('Ctrl Pts',(3.13248147094975,0.75905435352147,2.73762660675216));
#248761=CARTESIAN_POINT('Ctrl Pts',(3.08976581720199,0.924133316236075,
2.74908182365362));
#248762=CARTESIAN_POINT('Ctrl Pts',(3.05300161350705,1.03916421854592,2.75709106547839));
#248763=CARTESIAN_POINT('Ctrl Pts',(3.00218702352582,1.1719439044718,2.76617262429214));
#248764=CARTESIAN_POINT('Ctrl Pts',(2.99430479183625,1.19193888688421,2.76753560223551));
#248765=CARTESIAN_POINT('Ctrl Pts',(2.98172580224073,1.22293574185562,2.76963971354062));
#248766=CARTESIAN_POINT('Ctrl Pts',(2.97716698273,1.23399244570938,2.77038849644178));
#248767=CARTESIAN_POINT('Ctrl Pts',(2.96864024868737,1.25435038281447,2.7717635769591));
#248768=CARTESIAN_POINT('Ctrl Pts',(2.96469008596543,1.26365838217377,2.7723908508708));
#248769=CARTESIAN_POINT('Ctrl Pts',(2.95542156122623,1.28521565208063,2.77384043587277));
#248770=CARTESIAN_POINT('Ctrl Pts',(2.95007080783506,1.29745062338559,2.77466080282308));
#248771=CARTESIAN_POINT('Ctrl Pts',(2.93278997367838,1.33630514092619,2.77725960559082));
#248772=CARTESIAN_POINT('Ctrl Pts',(2.92057410786756,1.36279693028146,2.77902186013557));
#248773=CARTESIAN_POINT('Ctrl Pts',(2.85225312513648,1.50582083661421,2.78850239256062));
#248774=CARTESIAN_POINT('Ctrl Pts',(2.78952604380372,1.61907244460509,2.79588986640193));
#248775=CARTESIAN_POINT('Ctrl Pts',(2.59824043710923,1.92014257282073,2.81600137455967));
#248776=CARTESIAN_POINT('Ctrl Pts',(2.45637092190247,2.09858048985633,2.82851403657614));
#248777=CARTESIAN_POINT('Ctrl Pts',(2.24130872105471,2.31709629455826,2.84629415794579));
#248778=CARTESIAN_POINT('Ctrl Pts',(2.1836487816645,2.37151355884884,2.85095993644486));
#248779=CARTESIAN_POINT('Ctrl Pts',(2.10240051528213,2.44271527088062,2.85744155644524));
#248780=CARTESIAN_POINT('Ctrl Pts',(2.08050364850787,2.46139194544846,2.85917958194086));
#248781=CARTESIAN_POINT('Ctrl Pts',(2.04509837914269,2.49078044643053,2.86197751725359));
#248782=CARTESIAN_POINT('Ctrl Pts',(2.03174876338672,2.50168174580004,2.86302975170819));
#248783=CARTESIAN_POINT('Ctrl Pts',(2.00397955546707,2.52398920538355,2.86521332371793));
#248784=CARTESIAN_POINT('Ctrl Pts',(1.98954854180354,2.53538007907261,2.8663452126846));
#248785=CARTESIAN_POINT('Ctrl Pts',(1.95548045170669,2.56180117512994,2.86901109167864));
#248786=CARTESIAN_POINT('Ctrl Pts',(1.9357664901031,2.57672992366248,2.87054896567277));
#248787=CARTESIAN_POINT('Ctrl Pts',(1.86987923366042,2.62544136156591,2.87567426263755));
#248788=CARTESIAN_POINT('Ctrl Pts',(1.82298036366683,2.65821982215202,2.87929943821583));
#248789=CARTESIAN_POINT('Ctrl Pts',(1.54499861383155,2.84168918926618,2.90066598035169));
#248790=CARTESIAN_POINT('Ctrl Pts',(1.29622887312025,2.96343710384678,2.91945317482165));
#248791=CARTESIAN_POINT('Ctrl Pts',(0.917406062564434,3.09191198306876,
2.94634487035921));
#248792=CARTESIAN_POINT('Ctrl Pts',(0.797524700869486,3.12498228565185,
2.95460152209426));
#248793=CARTESIAN_POINT('Ctrl Pts',(0.654917886440115,3.15557696975978,
2.96391921129273));
#248794=CARTESIAN_POINT('Ctrl Pts',(0.633768059640023,3.15989264918445,
2.96528821019354));
#248795=CARTESIAN_POINT('Ctrl Pts',(0.600813912900344,3.1662728456083,2.96739961088764));
#248796=CARTESIAN_POINT('Ctrl Pts',(0.589039171830073,3.1684844887648,2.96814974308773));
#248797=CARTESIAN_POINT('Ctrl Pts',(0.56721110938089,3.17245855518935,2.96953206798627));
#248798=CARTESIAN_POINT('Ctrl Pts',(0.557161684310083,3.1742388990652,2.97016519869005));
#248799=CARTESIAN_POINT('Ctrl Pts',(0.533917474638405,3.17824302480967,
2.97162221876054));
#248800=CARTESIAN_POINT('Ctrl Pts',(0.520717121387442,3.18043240590058,
2.97244419523691));
#248801=CARTESIAN_POINT('Ctrl Pts',(0.478551650934126,3.18715631706283,
2.97505348921033));
#248802=CARTESIAN_POINT('Ctrl Pts',(0.449537258497794,3.19137798771895,
2.97682444093907));
#248803=CARTESIAN_POINT('Ctrl Pts',(0.290824799000282,3.21226352504861,
2.9863978198183));
#248804=CARTESIAN_POINT('Ctrl Pts',(0.160249238486313,3.22141944336741,
2.99386228963523));
#248805=CARTESIAN_POINT('Ctrl Pts',(-0.201932682346517,3.22473114139172,
3.0142765075678));
#248806=CARTESIAN_POINT('Ctrl Pts',(-0.432874271934596,3.20191883937146,
3.02701362313365));
#248807=CARTESIAN_POINT('Ctrl Pts',(-0.732692588004195,3.13924968093901,
3.04481592581066));
#248808=CARTESIAN_POINT('Ctrl Pts',(-0.805443235294792,3.12137580793723,
3.04923216854582));
#248809=CARTESIAN_POINT('Ctrl Pts',(-0.904602174981984,3.09331629866866,
3.05541884910837));
#248810=CARTESIAN_POINT('Ctrl Pts',(-0.931600459116803,3.08529274582015,
3.05712058502792));
#248811=CARTESIAN_POINT('Ctrl Pts',(-0.974836141146514,3.07182440961313,
3.05987517390189));
#248812=CARTESIAN_POINT('Ctrl Pts',(-0.991141707227044,3.06660215942896,
3.06092079666553));
#248813=CARTESIAN_POINT('Ctrl Pts',(-1.02493659301173,3.05548084573216,
3.06310243972369));
#248814=CARTESIAN_POINT('Ctrl Pts',(-1.04241835771957,3.04956097880955,
3.06423910615555));
#248815=CARTESIAN_POINT('Ctrl Pts',(-1.08361806953387,3.03521382682813,
3.06693761132399));
#248816=CARTESIAN_POINT('Ctrl Pts',(-1.10728976813531,3.0266582904924,3.06850361164821));
#248817=CARTESIAN_POINT('Ctrl Pts',(-1.18696588005761,2.99680157364479,
3.07382857306545));
#248818=CARTESIAN_POINT('Ctrl Pts',(-1.24247298768127,2.97421717228008,
3.07762944811582));
#248819=CARTESIAN_POINT('Ctrl Pts',(-1.37633851405468,2.91534939283921,
3.08702561863897));
#248820=CARTESIAN_POINT('Ctrl Pts',(-1.45392749616563,2.87744029339153,
3.09267015117679));
#248821=CARTESIAN_POINT('Ctrl Pts',(-1.65292457708602,2.77010778244356,
3.10765223492287));
#248822=CARTESIAN_POINT('Ctrl Pts',(-1.77149902601348,2.69581971125369,
3.11710175042262));
#248823=CARTESIAN_POINT('Ctrl Pts',(-1.92620082787275,2.58427250263613,
3.12998689256025));
#248824=CARTESIAN_POINT('Ctrl Pts',(-1.96682015103134,2.55349419912518,
3.1334256893051));
#248825=CARTESIAN_POINT('Ctrl Pts',(-2.09988849963314,2.44760515118789,
3.14484649812147));
#248826=CARTESIAN_POINT('Ctrl Pts',(-2.18891122441195,2.36832770096022,
3.15274871311623));
#248827=CARTESIAN_POINT('Ctrl Pts',(-2.28855250021586,2.26916398108028,
3.16172802000536));
#248828=CARTESIAN_POINT('Ctrl Pts',(-2.30360624163768,2.25388022296778,
3.16308840732691));
#248829=CARTESIAN_POINT('Ctrl Pts',(-2.32680722797041,2.22984943442775,
3.16518939216665));
#248830=CARTESIAN_POINT('Ctrl Pts',(-2.33506001915892,2.22120577478212,
3.16593760428103));
#248831=CARTESIAN_POINT('Ctrl Pts',(-2.35020755822701,2.20516309330068,
3.16731218757228));
#248832=CARTESIAN_POINT('Ctrl Pts',(-2.35711560724773,2.19777748020672,
3.16793952892136));
#248833=CARTESIAN_POINT('Ctrl Pts',(-2.3730737587362,2.18055432505028,3.16938997954952));
#248834=CARTESIAN_POINT('Ctrl Pts',(-2.38209754649554,2.17069286689037,
3.17021113640701));
#248835=CARTESIAN_POINT('Ctrl Pts',(-2.40952288441563,2.14034467465717,
3.17271087619193));
#248836=CARTESIAN_POINT('Ctrl Pts',(-2.42772394154997,2.11967743611935,
3.17437551696114));
#248837=CARTESIAN_POINT('Ctrl Pts',(-2.46429409611218,2.07706307621035,
3.17773798555687));
#248838=CARTESIAN_POINT('Ctrl Pts',(-2.48264022498827,2.055099519232,3.17943441010173));
#248839=CARTESIAN_POINT('Ctrl Pts',(-2.55368115274164,1.96771105110766,
3.18605476403195));
#248840=CARTESIAN_POINT('Ctrl Pts',(-2.60410494920358,1.90047714699355,
3.19086854400065));
#248841=CARTESIAN_POINT('Ctrl Pts',(-2.75168855990418,1.68677141260038,
3.20558003108914));
#248842=CARTESIAN_POINT('Ctrl Pts',(-2.83954078084347,1.53427429700553,
3.2152819860626));
#248843=CARTESIAN_POINT('Ctrl Pts',(-2.97363591010511,1.25011626080743,
3.23309495820934));
#248844=CARTESIAN_POINT('Ctrl Pts',(-3.02460349094454,1.12119072346685,
3.24108577169568));
#248845=CARTESIAN_POINT('Ctrl Pts',(-3.07757795773426,0.956970377384393,
3.25138829511855));
#248846=CARTESIAN_POINT('Ctrl Pts',(-3.08752267553488,0.924381947709918,
3.25343814919994));
#248847=CARTESIAN_POINT('Ctrl Pts',(-3.10255856068715,0.872157716926107,
3.25673451070762));
#248848=CARTESIAN_POINT('Ctrl Pts',(-3.10798441527301,0.852620402694395,
3.25797020377834));
#248849=CARTESIAN_POINT('Ctrl Pts',(-3.11792604297628,0.815466401802598,
3.26032543997177));
#248850=CARTESIAN_POINT('Ctrl Pts',(-3.12247778331461,0.797860096333169,
3.26144377656268));
#248851=CARTESIAN_POINT('Ctrl Pts',(-3.13251598505542,0.757629910652897,
3.26400470276786));
#248852=CARTESIAN_POINT('Ctrl Pts',(-3.13790675601796,0.734983417154233,
3.26545028405356));
#248853=CARTESIAN_POINT('Ctrl Pts',(-3.14864067099042,0.687618332342686,
3.26848261829641));
#248854=CARTESIAN_POINT('Ctrl Pts',(-3.15393913338513,0.662891341770996,
3.27007067762439));
#248855=CARTESIAN_POINT('Ctrl Pts',(-3.17155560542189,0.575680814400231,
3.27569021929638));
#248856=CARTESIAN_POINT('Ctrl Pts',(-3.18231140337217,0.512900186247806,
3.27976932644396));
#248857=CARTESIAN_POINT('Ctrl Pts',(-3.21221017864354,0.300798516452359,
3.29366493800713));
#248858=CARTESIAN_POINT('Ctrl Pts',(-3.22275000000513,0.150482448427344,
3.30371299133942));
#248859=CARTESIAN_POINT('Ctrl Pts',(-3.22275,-1.09908401824121E-10,3.31386231834285));
#248860=CARTESIAN_POINT('Origin',(0.,0.,-2.31077344927308));
#248861=CARTESIAN_POINT('',(-3.22275,1.54108685473619E-11,4.8132072728278));
#248862=CARTESIAN_POINT('',(-3.22275,-5.68635386092821E-12,4.56684192677376));
#248863=CARTESIAN_POINT('',(-3.22275,-3.50678552687464E-13,-2.31077344927308));
#248864=CARTESIAN_POINT('Ctrl Pts',(-3.22275,1.54108685473619E-11,4.8132072728278));
#248865=CARTESIAN_POINT('Ctrl Pts',(-3.22275,0.000690567994428604,4.81316239703151));
#248866=CARTESIAN_POINT('Ctrl Pts',(-3.22274977823664,0.00138113766044703,
4.81311751533792));
#248867=CARTESIAN_POINT('Ctrl Pts',(-3.2226605004907,0.140262159044363,
4.80409011264835));
#248868=CARTESIAN_POINT('Ctrl Pts',(-3.21368351261808,0.27829100368279,
4.79487241388675));
#248869=CARTESIAN_POINT('Ctrl Pts',(-3.1674056525901,0.634410425249026,
4.7706669772349));
#248870=CARTESIAN_POINT('Ctrl Pts',(-3.11647497344357,0.85001845992052,
4.75556697697216));
#248871=CARTESIAN_POINT('Ctrl Pts',(-3.03586907207272,1.08176304537931,
4.73980542849057));
#248872=CARTESIAN_POINT('Ctrl Pts',(-3.02759590809255,1.10470602731961,
4.73825086306142));
#248873=CARTESIAN_POINT('Ctrl Pts',(-3.01471685791979,1.13919011761568,
4.73592546964963));
#248874=CARTESIAN_POINT('Ctrl Pts',(-3.01030356728095,1.15080159106129,
4.73514439261771));
#248875=CARTESIAN_POINT('Ctrl Pts',(-3.00217046066613,1.171833029223,4.73373354037896));
#248876=CARTESIAN_POINT('Ctrl Pts',(-2.99847316706655,1.1812615291399,4.73310247713628));
#248877=CARTESIAN_POINT('Ctrl Pts',(-2.99072294959577,1.20075455960624,
4.73180095649328));
#248878=CARTESIAN_POINT('Ctrl Pts',(-2.98666356283178,1.21081627183805,
4.73113088529037));
#248879=CARTESIAN_POINT('Ctrl Pts',(-2.97584802131803,1.23723862725734,
4.72937534939798));
#248880=CARTESIAN_POINT('Ctrl Pts',(-2.96900765545248,1.25356469354103,
4.7282947702736));
#248881=CARTESIAN_POINT('Ctrl Pts',(-2.9365510525626,1.32927343023507,4.7232994683895));
#248882=CARTESIAN_POINT('Ctrl Pts',(-2.90928385373234,1.38793682143816,
4.71947381850408));
#248883=CARTESIAN_POINT('Ctrl Pts',(-2.82129697694418,1.56322772417038,
4.70806455249339));
#248884=CARTESIAN_POINT('Ctrl Pts',(-2.75518928374001,1.67700154164072,
4.70068638843717));
#248885=CARTESIAN_POINT('Ctrl Pts',(-2.55411474746019,1.97891437521934,
4.68037250045424));
#248886=CARTESIAN_POINT('Ctrl Pts',(-2.40558491573292,2.15702398560324,
4.6674819508797));
#248887=CARTESIAN_POINT('Ctrl Pts',(-2.20783201637952,2.34808596728322,
4.65119385748321));
#248888=CARTESIAN_POINT('Ctrl Pts',(-2.17576837761097,2.37782707893554,
4.64857865538862));
#248889=CARTESIAN_POINT('Ctrl Pts',(-2.12647410084897,2.42171874186909,
4.64459000623963));
#248890=CARTESIAN_POINT('Ctrl Pts',(-2.1096847765466,2.43635873214634,4.64323690542819));
#248891=CARTESIAN_POINT('Ctrl Pts',(-2.07925984564375,2.46233842424964,
4.64079372705171));
#248892=CARTESIAN_POINT('Ctrl Pts',(-2.06567974502613,2.4737419413753,4.63970631849662));
#248893=CARTESIAN_POINT('Ctrl Pts',(-2.03649545634545,2.49784075902408,
4.63737560663253));
#248894=CARTESIAN_POINT('Ctrl Pts',(-2.02086518862018,2.51050314906165,
4.63613104467078));
#248895=CARTESIAN_POINT('Ctrl Pts',(-1.97800071552304,2.54456882255352,
4.63272736493463));
#248896=CARTESIAN_POINT('Ctrl Pts',(-1.95053896367669,2.5656802071458,4.63055689590759));
#248897=CARTESIAN_POINT('Ctrl Pts',(-1.77581248757799,2.69557557184392,
4.6168055557308));
#248898=CARTESIAN_POINT('Ctrl Pts',(-1.61986456113914,2.79207046534781,
4.60475980484986));
#248899=CARTESIAN_POINT('Ctrl Pts',(-1.29710609886835,2.95560475306769,
4.58045774751439));
#248900=CARTESIAN_POINT('Ctrl Pts',(-1.13117222935722,3.0230007942635,4.56825844311235));
#248901=CARTESIAN_POINT('Ctrl Pts',(-0.885661793636314,3.09965616099004,
4.55119386632549));
#248902=CARTESIAN_POINT('Ctrl Pts',(-0.809984226825709,3.12028728543631,
4.54606546551623));
#248903=CARTESIAN_POINT('Ctrl Pts',(-0.714625775851233,3.14257986400173,
4.53982601086925));
#248904=CARTESIAN_POINT('Ctrl Pts',(-0.695587550801185,3.14684861467757,
4.53859127708239));
#248905=CARTESIAN_POINT('Ctrl Pts',(-0.665515142244039,3.15330519374782,
4.53665942173493));
#248906=CARTESIAN_POINT('Ctrl Pts',(-0.654506605945997,3.1556085247063,
4.53595612503024));
#248907=CARTESIAN_POINT('Ctrl Pts',(-0.633613069160272,3.15986606745569,
4.53462897602693));
#248908=CARTESIAN_POINT('Ctrl Pts',(-0.623730975216488,3.16183155123511,
4.53400454704237));
#248909=CARTESIAN_POINT('Ctrl Pts',(-0.60023447167596,3.16639040629807,
4.53252737451355));
#248910=CARTESIAN_POINT('Ctrl Pts',(-0.586612313987692,3.16894235277619,
4.53167694341117));
#248911=CARTESIAN_POINT('Ctrl Pts',(-0.540409303260744,3.17728979012759,
4.52881137511865));
#248912=CARTESIAN_POINT('Ctrl Pts',(-0.507754658317553,3.18267152300163,
4.52681783360016));
#248913=CARTESIAN_POINT('Ctrl Pts',(-0.427306241158793,3.19466027120379,
4.52197159205195));
#248914=CARTESIAN_POINT('Ctrl Pts',(-0.37943495423911,3.20069905499044,
4.51914390818901));
#248915=CARTESIAN_POINT('Ctrl Pts',(-0.172964482540289,3.22204672008978,
4.50712077764098));
#248916=CARTESIAN_POINT('Ctrl Pts',(-0.0134779655086782,3.22665874384267,
4.49826165749148));
#248917=CARTESIAN_POINT('Ctrl Pts',(0.338597384937704,3.21072476377755,
4.47852350317213));
#248918=CARTESIAN_POINT('Ctrl Pts',(0.530294766143791,3.18467867287266,
4.46763950924912));
#248919=CARTESIAN_POINT('Ctrl Pts',(0.762859269670118,3.13149071901396,
4.45351997451963));
#248920=CARTESIAN_POINT('Ctrl Pts',(0.806998630757631,3.1204072319042,4.45079995783708));
#248921=CARTESIAN_POINT('Ctrl Pts',(0.872424323048787,3.1024977000688,4.44670104947028));
#248922=CARTESIAN_POINT('Ctrl Pts',(0.893899394664907,3.09637853178865,
4.44534474940476));
#248923=CARTESIAN_POINT('Ctrl Pts',(0.93231617608023,3.0849989858915,4.44289809215583));
#248924=CARTESIAN_POINT('Ctrl Pts',(0.949281459488707,3.07982091785816,
4.44181043628652));
#248925=CARTESIAN_POINT('Ctrl Pts',(0.985359680890468,3.06848286436239,
4.43948169617216));
#248926=CARTESIAN_POINT('Ctrl Pts',(1.00445945053403,3.06228378385553,4.43823937612253));
#248927=CARTESIAN_POINT('Ctrl Pts',(1.05618859071846,3.04495839913953,4.4348482877582));
#248928=CARTESIAN_POINT('Ctrl Pts',(1.08869864047589,3.03348662677468,4.4326883096396));
#248929=CARTESIAN_POINT('Ctrl Pts',(1.28769317474859,2.95965685832944,4.41928434688513));
#248930=CARTESIAN_POINT('Ctrl Pts',(1.44894035199903,2.88414229997025,4.40760373495105));
#248931=CARTESIAN_POINT('Ctrl Pts',(1.74966899155727,2.71169953788741,4.38434374968966));
#248932=CARTESIAN_POINT('Ctrl Pts',(1.88938172783716,2.61627448081681,4.37282773664565));
#248933=CARTESIAN_POINT('Ctrl Pts',(2.09287919526187,2.45244706062507,4.35540623341453));
#248934=CARTESIAN_POINT('Ctrl Pts',(2.16227479770724,2.39148714067206,4.34933659006795));
#248935=CARTESIAN_POINT('Ctrl Pts',(2.24349880105755,2.3137060667886,4.34216383688442));
#248936=CARTESIAN_POINT('Ctrl Pts',(2.25790476232465,2.2996497049434,4.3408889361582));
#248937=CARTESIAN_POINT('Ctrl Pts',(2.28033268491936,2.27735210701625,4.33890113643941));
#248938=CARTESIAN_POINT('Ctrl Pts',(2.28844356620972,2.26920158360797,4.33818164207182));
#248939=CARTESIAN_POINT('Ctrl Pts',(2.3028299637214,2.25458928595253,4.33690464165469));
#248940=CARTESIAN_POINT('Ctrl Pts',(2.30912205422518,2.24814457525594,4.33634587086138));
#248941=CARTESIAN_POINT('Ctrl Pts',(2.32428686557893,2.23248109260962,4.33499840201047));
#248942=CARTESIAN_POINT('Ctrl Pts',(2.33313180715137,2.22323576024087,4.3342118245637));
#248943=CARTESIAN_POINT('Ctrl Pts',(2.36052369220078,2.19426039902338,4.33177286612426));
#248944=CARTESIAN_POINT('Ctrl Pts',(2.37887770684384,2.17434858389916,4.3301342834055));
#248945=CARTESIAN_POINT('Ctrl Pts',(2.49995216385011,2.03962942739909,4.31927664954797));
#248946=CARTESIAN_POINT('Ctrl Pts',(2.59458971937978,1.91780191177089,4.31054635744549));
#248947=CARTESIAN_POINT('Ctrl Pts',(2.82571527688974,1.5716729242753,4.28717711353406));
#248948=CARTESIAN_POINT('Ctrl Pts',(2.94412309129382,1.33676830086213,4.27269642663068));
#248949=CARTESIAN_POINT('Ctrl Pts',(3.04540417142833,1.05499961822504,4.25492419516252));
#248950=CARTESIAN_POINT('Ctrl Pts',(3.05741830944528,1.01965870419453,4.25269042137498));
#248951=CARTESIAN_POINT('Ctrl Pts',(3.07581025127226,0.962306364750547,
4.2490537951437));
#248952=CARTESIAN_POINT('Ctrl Pts',(3.08257204072811,0.940421083207358,
4.24766340421612));
#248953=CARTESIAN_POINT('Ctrl Pts',(3.09417244658499,0.901405146210326,
4.24517910884337));
#248954=CARTESIAN_POINT('Ctrl Pts',(3.09910355544604,0.884302832478413,
4.24408825045355));
#248955=CARTESIAN_POINT('Ctrl Pts',(3.10920452552743,0.848147685150697,
4.24177775919991));
#248956=CARTESIAN_POINT('Ctrl Pts',(3.11434147631253,0.82908649656522,4.24055711661903));
#248957=CARTESIAN_POINT('Ctrl Pts',(3.12757050911031,0.778140327182126,
4.23728731682261));
#248958=CARTESIAN_POINT('Ctrl Pts',(3.13534990122858,0.746177276044712,
4.23522827390119));
#248959=CARTESIAN_POINT('Ctrl Pts',(3.17405105953332,0.57586014262635,4.22421281309114));
#248960=CARTESIAN_POINT('Ctrl Pts',(3.19630386467259,0.43571479544884,4.21498619646364));
#248961=CARTESIAN_POINT('Ctrl Pts',(3.22804715399094,0.0898865294022592,
4.19189120079028));
#248962=CARTESIAN_POINT('Ctrl Pts',(3.22720906692133,-0.116116688744731,
4.17783530903838));
#248963=CARTESIAN_POINT('Ctrl Pts',(3.19736082628502,-0.414641859135027,
4.15781471954808));
#248964=CARTESIAN_POINT('Ctrl Pts',(3.18383042564079,-0.508203961729918,
4.15159800826799));
#248965=CARTESIAN_POINT('Ctrl Pts',(3.16243262716317,-0.620924234743594,
4.14427928744899));
#248966=CARTESIAN_POINT('Ctrl Pts',(3.15847148530748,-0.640769031093299,
4.14299735836021));
#248967=CARTESIAN_POINT('Ctrl Pts',(3.15196168916056,-0.671854039468318,
4.14100103493579));
#248968=CARTESIAN_POINT('Ctrl Pts',(3.1495392902683,-0.683119761778857,
4.14027995601536));
#248969=CARTESIAN_POINT('Ctrl Pts',(3.14511673039782,-0.703163825544851,
4.13900162105003));
#248970=CARTESIAN_POINT('Ctrl Pts',(3.1431401996556,-0.711946838740806,
4.13844308379712));
#248971=CARTESIAN_POINT('Ctrl Pts',(3.13827371066269,-0.733156491907248,
4.13709807216114));
#248972=CARTESIAN_POINT('Ctrl Pts',(3.13534673768895,-0.745574390530345,
4.1363136966152));
#248973=CARTESIAN_POINT('Ctrl Pts',(3.12602289816131,-0.784105343049968,
4.13388863232516));
#248974=CARTESIAN_POINT('Ctrl Pts',(3.11937279059531,-0.81015668126598,
4.13226151784306));
#248975=CARTESIAN_POINT('Ctrl Pts',(3.08367829222681,-0.943026484081717,
4.12401269905845));
#248976=CARTESIAN_POINT('Ctrl Pts',(3.04946766739934,-1.04839039574007,
4.11763635580063));
#248977=CARTESIAN_POINT('Ctrl Pts',(2.93841270899015,-1.3386022806623,4.10001800264333));
#248978=CARTESIAN_POINT('Ctrl Pts',(2.84969162408951,-1.51834950968589,
4.08901526744249));
#248979=CARTESIAN_POINT('Ctrl Pts',(2.68140884346065,-1.79188052064752,
4.07071042606615));
#248980=CARTESIAN_POINT('Ctrl Pts',(2.61217920809448,-1.89137633446193,
4.06368226062735));
#248981=CARTESIAN_POINT('Ctrl Pts',(2.51742844492292,-2.0123950267043,4.05449490904032));
#248982=CARTESIAN_POINT('Ctrl Pts',(2.49694965633281,-2.03774925259271,
4.05253241725571));
#248983=CARTESIAN_POINT('Ctrl Pts',(2.46349666298485,-2.0779049261223,4.0493606310607));
#248984=CARTESIAN_POINT('Ctrl Pts',(2.45076495477575,-2.09290606583203,
4.04816109696694));
#248985=CARTESIAN_POINT('Ctrl Pts',(2.42624588859265,-2.12126513932456,
4.04586479850591));
#248986=CARTESIAN_POINT('Ctrl Pts',(2.4144835374957,-2.13464379471166,4.04476908564888));
#248987=CARTESIAN_POINT('Ctrl Pts',(2.38726182284919,-2.16509328522513,
4.04224621205076));
#248988=CARTESIAN_POINT('Ctrl Pts',(2.37172931847406,-2.18209714280004,
4.04081602521338));
#248989=CARTESIAN_POINT('Ctrl Pts',(2.32240846611802,-2.2349412916537,4.0363027764898));
#248990=CARTESIAN_POINT('Ctrl Pts',(2.28798119520261,-2.27017296370971,
4.0331927235781));
#248991=CARTESIAN_POINT('Ctrl Pts',(2.20515780447031,-2.35113335472419,
4.025799766236));
#248992=CARTESIAN_POINT('Ctrl Pts',(2.1561265653091,-2.39617742591035,4.02149054162935));
#248993=CARTESIAN_POINT('Ctrl Pts',(1.95762645206896,-2.56750778236424,
4.00430970400565));
#248994=CARTESIAN_POINT('Ctrl Pts',(1.79819173677338,-2.68158357456211,
3.99104299975597));
#248995=CARTESIAN_POINT('Ctrl Pts',(1.50011919802168,-2.85625973403065,
3.9677294947056));
#248996=CARTESIAN_POINT('Ctrl Pts',(1.36567745801429,-2.92292864280902,
3.95769365067794));
#248997=CARTESIAN_POINT('Ctrl Pts',(1.20709336681111,-2.98822856146334,
3.94673594966196));
#248998=CARTESIAN_POINT('Ctrl Pts',(1.18703302523894,-2.99625382548308,
3.94536550986887));
#248999=CARTESIAN_POINT('Ctrl Pts',(1.15586600776289,-3.00836022987959,
3.94326212538279));
#249000=CARTESIAN_POINT('Ctrl Pts',(1.14481542801763,-3.01258280329858,
3.9425213309765));
#249001=CARTESIAN_POINT('Ctrl Pts',(1.12441553618103,-3.02024941439748,
3.94116327831991));
#249002=CARTESIAN_POINT('Ctrl Pts',(1.11507342917202,-3.0237109773978,3.94054504139871));
#249003=CARTESIAN_POINT('Ctrl Pts',(1.09361132009983,-3.03155041006686,
3.93913303462625));
#249004=CARTESIAN_POINT('Ctrl Pts',(1.0814809733793,-3.03589896496896,3.93834097599436));
#249005=CARTESIAN_POINT('Ctrl Pts',(1.04332208484769,-3.04932064072571,
3.9358672142036));
#249006=CARTESIAN_POINT('Ctrl Pts',(1.01720229144661,-3.05813291974347,
3.93419987860793));
#249007=CARTESIAN_POINT('Ctrl Pts',(0.879937177610846,-3.10249000179777,
3.92555722796821));
#249008=CARTESIAN_POINT('Ctrl Pts',(0.767024392593477,-3.13231744855377,
3.91885398987802));
#249009=CARTESIAN_POINT('Ctrl Pts',(0.450893821526948,-3.19770132804359,
3.90058755528953));
#249010=CARTESIAN_POINT('Ctrl Pts',(0.245519604976746,-3.21998761580007,
3.8892506482196));
#249011=CARTESIAN_POINT('Ctrl Pts',(-0.0702298625905273,-3.22385028649462,
3.87117857572261));
#249012=CARTESIAN_POINT('Ctrl Pts',(-0.179869213562804,-3.21959414531582,
3.86479186766123));
#249013=CARTESIAN_POINT('Ctrl Pts',(-0.32068080529009,-3.20691263436101,
3.85633439956107));
#249014=CARTESIAN_POINT('Ctrl Pts',(-0.35224558676475,-3.20359918879381,
3.85442219145808));
#249015=CARTESIAN_POINT('Ctrl Pts',(-0.403108358139404,-3.19749920023712,
3.85131219601143));
#249016=CARTESIAN_POINT('Ctrl Pts',(-0.422439455182285,-3.19500271748781,
3.85012348529319));
#249017=CARTESIAN_POINT('Ctrl Pts',(-0.459440728398727,-3.18988257843508,
3.84783480497384));
#249018=CARTESIAN_POINT('Ctrl Pts',(-0.477114111880822,-3.18728705188233,
3.8467357574827));
#249019=CARTESIAN_POINT('Ctrl Pts',(-0.517891603781801,-3.18095168336399,
3.84418595620492));
#249020=CARTESIAN_POINT('Ctrl Pts',(-0.540978149547474,-3.17710684756747,
3.84273195176244));
#249021=CARTESIAN_POINT('Ctrl Pts',(-0.614565084351167,-3.16402636186574,
3.83806313169127));
#249022=CARTESIAN_POINT('Ctrl Pts',(-0.664885498255447,-3.15383573671152,
3.83481860418387));
#249023=CARTESIAN_POINT('Ctrl Pts',(-0.909829856169486,-3.09810840731017,
3.81876253460645));
#249024=CARTESIAN_POINT('Ctrl Pts',(-1.10014525829515,-3.03574118243091,
3.8054303967669));
#249025=CARTESIAN_POINT('Ctrl Pts',(-1.46544386169624,-2.8771451393537,
3.77853679144732));
#249026=CARTESIAN_POINT('Ctrl Pts',(-1.63978132717997,-2.7814778529991,
3.76504129729913));
#249027=CARTESIAN_POINT('Ctrl Pts',(-1.82796989647494,-2.65432949786062,
3.75042940106515));
#249028=CARTESIAN_POINT('Ctrl Pts',(-1.85150443732313,-2.6379671101803,
3.74860179108884));
#249029=CARTESIAN_POINT('Ctrl Pts',(-1.88535122127449,-2.61375898366427,
3.74597657856255));
#249030=CARTESIAN_POINT('Ctrl Pts',(-1.89583868920558,-2.60616210741316,
3.74516360999163));
#249031=CARTESIAN_POINT('Ctrl Pts',(-1.91403499494291,-2.592813163306,3.74375427508686));
#249032=CARTESIAN_POINT('Ctrl Pts',(-1.92176426896241,-2.58708951625951,
3.7431560295348));
#249033=CARTESIAN_POINT('Ctrl Pts',(-1.92964008205009,-2.58120258064856,
3.74254689519827));
#249034=CARTESIAN_POINT('Ctrl Pts',(-1.92981204715722,-2.58107401506582,
3.74253359520822));
#249035=CARTESIAN_POINT('Ctrl Pts',(-1.93014307082761,-2.5808264815925,
3.74250799382814));
#249036=CARTESIAN_POINT('Ctrl Pts',(-1.93030213125146,-2.58070751617441,
3.74249569226481));
#249037=CARTESIAN_POINT('Ctrl Pts',(-1.93060867059499,-2.58047820325032,
3.74247198517327));
#249038=CARTESIAN_POINT('Ctrl Pts',(-1.93075615105184,-2.58036785780673,
3.74246057950191));
#249039=CARTESIAN_POINT('Ctrl Pts',(-1.93104067778801,-2.58015493576096,
3.74243857539119));
#249040=CARTESIAN_POINT('Ctrl Pts',(-1.93117772534017,-2.58005236089379,
3.74242797683323));
#249041=CARTESIAN_POINT('Ctrl Pts',(-1.9314423851412,-2.57985424022249,
3.7424075096412));
#249042=CARTESIAN_POINT('Ctrl Pts',(-1.93156999846312,-2.57975869587662,
3.74239764090726));
#249043=CARTESIAN_POINT('Ctrl Pts',(-1.93181666384316,-2.57957398845649,
3.74237856572067));
#249044=CARTESIAN_POINT('Ctrl Pts',(-1.93193571682413,-2.57948482660447,
3.74236935918244));
#249045=CARTESIAN_POINT('Ctrl Pts',(-1.93216602998031,-2.57931231424507,
3.74235154891883));
#249046=CARTESIAN_POINT('Ctrl Pts',(-1.93227729093776,-2.5792289647785,
3.74234294512095));
#249047=CARTESIAN_POINT('Ctrl Pts',(-1.93249269862829,-2.57906757359814,
3.7423262878275));
#249048=CARTESIAN_POINT('Ctrl Pts',(-1.93259684602564,-2.57898953277612,
3.74231823427034));
#249049=CARTESIAN_POINT('Ctrl Pts',(-1.93279862825931,-2.57883831210621,
3.74230263090213));
#249050=CARTESIAN_POINT('Ctrl Pts',(-1.93289626366706,-2.57876513302196,
3.74229508103816));
#249051=CARTESIAN_POINT('Ctrl Pts',(-1.93308555742652,-2.5786232379493,
3.74228044362118));
#249052=CARTESIAN_POINT('Ctrl Pts',(-1.93317721627542,-2.57855452261471,
3.74227335602225));
#249053=CARTESIAN_POINT('Ctrl Pts',(-1.9333550352852,-2.57842119942322,
3.74225960612276));
#249054=CARTESIAN_POINT('Ctrl Pts',(-1.93344119586268,-2.57835659214137,
3.74225294378355));
#249055=CARTESIAN_POINT('Ctrl Pts',(-1.93360844709125,-2.57823116615093,
3.74224001123042));
#249056=CARTESIAN_POINT('Ctrl Pts',(-1.93368953808833,-2.57817034795266,
3.74223374098417));
#249057=CARTESIAN_POINT('Ctrl Pts',(-1.93384703561819,-2.57805221329086,
3.742221562795));
#249058=CARTESIAN_POINT('Ctrl Pts',(-1.93392344246848,-2.57799489725911,
3.7422156548227));
#249059=CARTESIAN_POINT('Ctrl Pts',(-1.93407191933086,-2.57788350812713,
3.74220417428767));
#249060=CARTESIAN_POINT('Ctrl Pts',(-1.93414398962734,-2.5778294353984,
3.74219860169874));
#249061=CARTESIAN_POINT('Ctrl Pts',(-1.93428410775566,-2.57772429872202,
3.74218776761005));
#249062=CARTESIAN_POINT('Ctrl Pts',(-1.93435215584104,-2.57767323509617,
3.742182506087));
#249063=CARTESIAN_POINT('Ctrl Pts',(-1.93448451466634,-2.57757390417457,
3.74217227207351));
#249064=CARTESIAN_POINT('Ctrl Pts',(-1.93454882560649,-2.57752563717805,
3.74216729956437));
#249065=CARTESIAN_POINT('Ctrl Pts',(-1.93467396924573,-2.57743170637144,
3.7421576235352));
#249066=CARTESIAN_POINT('Ctrl Pts',(-1.93473480215083,-2.57738604280232,
3.74215291999642));
#249067=CARTESIAN_POINT('Ctrl Pts',(-1.93489158965743,-2.57726834325985,
3.74214079740648));
#249068=CARTESIAN_POINT('Ctrl Pts',(-1.93498754185828,-2.5771963040773,
3.74213337857657));
#249069=CARTESIAN_POINT('Ctrl Pts',(-1.93517842235295,-2.57705297777379,
3.7421186202012));
#249070=CARTESIAN_POINT('Ctrl Pts',(-1.93527335074042,-2.57698169075902,
3.74211128064726));
#249071=CARTESIAN_POINT('Ctrl Pts',(-1.93546222742072,-2.57683983641469,
3.7420966774322));
#249072=CARTESIAN_POINT('Ctrl Pts',(-1.9355561757973,-2.57676926918942,
3.74208941376342));
#249073=CARTESIAN_POINT('Ctrl Pts',(-1.93574313466924,-2.57662882321356,
3.74207495905099));
#249074=CARTESIAN_POINT('Ctrl Pts',(-1.93583614521817,-2.5765589445811,
3.74206776800208));
#249075=CARTESIAN_POINT('Ctrl Pts',(-1.93602126902772,-2.57641984576439,
3.74205345538718));
#249076=CARTESIAN_POINT('Ctrl Pts',(-1.9361133823625,-2.57635062567445,
3.74204633381442));
#249077=CARTESIAN_POINT('Ctrl Pts',(-1.9362967508696,-2.57621281498715,
3.74203215712333));
#249078=CARTESIAN_POINT('Ctrl Pts',(-1.93638800612883,-2.57614422446659,
3.7420251019973));
#249079=CARTESIAN_POINT('Ctrl Pts',(-1.93656969629851,-2.57600764491864,
3.74201105527285));
#249080=CARTESIAN_POINT('Ctrl Pts',(-1.93666013126483,-2.57593965598387,
3.74200406366918));
#249081=CARTESIAN_POINT('Ctrl Pts',(-1.93684021731373,-2.57580425259338,
3.74199014116712));
#249082=CARTESIAN_POINT('Ctrl Pts',(-1.93692986845239,-2.57573683822301,
3.74198321026352));
#249083=CARTESIAN_POINT('Ctrl Pts',(-1.9371084221011,-2.57560255782986,
3.74196940643301));
#249084=CARTESIAN_POINT('Ctrl Pts',(-1.93719732465869,-2.57553569189207,
3.74196253350159));
#249085=CARTESIAN_POINT('Ctrl Pts',(-1.93737441518375,-2.5754024831218,
3.74194884298113));
#249086=CARTESIAN_POINT('Ctrl Pts',(-1.93746260322022,-2.5753361403517,
3.74194202538596));
#249087=CARTESIAN_POINT('Ctrl Pts',(-1.93763829770002,-2.57520395343339,
3.74192844298436));
#249088=CARTESIAN_POINT('Ctrl Pts',(-1.93772580419423,-2.57513810935504,
3.74192167817326));
#249089=CARTESIAN_POINT('Ctrl Pts',(-1.93790016753006,-2.57500689610809,
3.74190819886802));
#249090=CARTESIAN_POINT('Ctrl Pts',(-1.93798702441897,-2.57494152700619,
3.74190148436952));
#249091=CARTESIAN_POINT('Ctrl Pts',(-1.93816011949252,-2.57481124072426,
3.74188810329459));
#249092=CARTESIAN_POINT('Ctrl Pts',(-1.9382463577253,-2.5747463236047,3.74188143671377));
#249093=CARTESIAN_POINT('Ctrl Pts',(-1.93841824553793,-2.57461691895322,
3.74186814914879));
#249094=CARTESIAN_POINT('Ctrl Pts',(-1.93850389515173,-2.57455243148708,
3.74186152816138));
#249095=CARTESIAN_POINT('Ctrl Pts',(-1.93867463484646,-2.5744238644888,
3.74184832952996));
#249096=CARTESIAN_POINT('Ctrl Pts',(-1.93875972497793,-2.57435978500482,
3.74184175188147));
#249097=CARTESIAN_POINT('Ctrl Pts',(-1.93892937407035,-2.57423201286794,
3.74182863773333));
#249098=CARTESIAN_POINT('Ctrl Pts',(-1.93901393305621,-2.57416832027761,
3.74182210123122));
#249099=CARTESIAN_POINT('Ctrl Pts',(-1.93918254737945,-2.57404130143913,
3.74180906724641));
#249100=CARTESIAN_POINT('Ctrl Pts',(-1.93926660275728,-2.57397797523712,
3.74180256976008));
#249101=CARTESIAN_POINT('Ctrl Pts',(-1.93943423665176,-2.57385166922161,
3.74178961173432));
#249102=CARTESIAN_POINT('Ctrl Pts',(-1.93951781521416,-2.57378868944572,
3.74178315119087));
#249103=CARTESIAN_POINT('Ctrl Pts',(-1.93968452161611,-2.57366305680027,
3.74177026502867));
#249104=CARTESIAN_POINT('Ctrl Pts',(-1.93976764947724,-2.57360040398217,
3.7417638394078));
#249105=CARTESIAN_POINT('Ctrl Pts',(-1.93993347992707,-2.57347540627158,
3.74175102112182));
#249106=CARTESIAN_POINT('Ctrl Pts',(-1.94001618253987,-2.57341306142447,
3.74174462845443));
#249107=CARTESIAN_POINT('Ctrl Pts',(-1.95027320703567,-2.56568009224111,
3.74095179588585));
#249108=CARTESIAN_POINT('Ctrl Pts',(-1.96040214740219,-2.55794905164122,
3.740169485119));
#249109=CARTESIAN_POINT('Ctrl Pts',(-1.98232492229874,-2.54100951188826,
3.73847698664242));
#249110=CARTESIAN_POINT('Ctrl Pts',(-1.99410107452955,-2.53177849749452,
3.7375682885136));
#249111=CARTESIAN_POINT('Ctrl Pts',(-2.02614295980632,-2.5062994495726,
3.73509573287671));
#249112=CARTESIAN_POINT('Ctrl Pts',(-2.04627763834667,-2.48988757536617,
3.73354193731715));
#249113=CARTESIAN_POINT('Ctrl Pts',(-2.11083510416449,-2.43595436224979,
3.7285516884782));
#249114=CARTESIAN_POINT('Ctrl Pts',(-2.15444326778432,-2.39747229949171,
3.72516769384942));
#249115=CARTESIAN_POINT('Ctrl Pts',(-2.3736802563351,-2.19319070549532,
3.70794450351096));
#249116=CARTESIAN_POINT('Ctrl Pts',(-2.53131077380543,-2.00920901385574,
3.69478215764833));
#249117=CARTESIAN_POINT('Ctrl Pts',(-2.73260364437299,-1.71250854976627,
3.67431769978638));
#249118=CARTESIAN_POINT('Ctrl Pts',(-2.79296659593321,-1.6121853664318,
3.66751967072787));
#249119=CARTESIAN_POINT('Ctrl Pts',(-2.86287577304075,-1.48023826858379,
3.65859186079497));
#249120=CARTESIAN_POINT('Ctrl Pts',(-2.87758227114909,-1.45144176009658,
3.65664451816991));
#249121=CARTESIAN_POINT('Ctrl Pts',(-2.90051238110816,-1.40482398859129,
3.65349135175389));
#249122=CARTESIAN_POINT('Ctrl Pts',(-2.9090110357424,-1.38713996389784,
3.6522950801908));
#249123=CARTESIAN_POINT('Ctrl Pts',(-2.92492272876894,-1.3532414496271,
3.65000114570518));
#249124=CARTESIAN_POINT('Ctrl Pts',(-2.93236374783051,-1.33704084475036,
3.64890449575432));
#249125=CARTESIAN_POINT('Ctrl Pts',(-2.94915274531775,-1.29967343674534,
3.64637384111156));
#249126=CARTESIAN_POINT('Ctrl Pts',(-2.95840785386545,-1.27846622291077,
3.6449367453212));
#249127=CARTESIAN_POINT('Ctrl Pts',(-2.98688090940351,-1.21125775843862,
3.64037874505704));
#249128=CARTESIAN_POINT('Ctrl Pts',(-3.00525952572255,-1.16491101204488,
3.63723008067478));
#249129=CARTESIAN_POINT('Ctrl Pts',(-3.04602452355081,-1.0547169422649,
3.62972746585643));
#249130=CARTESIAN_POINT('Ctrl Pts',(-3.0674893965274,-0.990555910421785,
3.62534611747546));
#249131=CARTESIAN_POINT('Ctrl Pts',(-3.17700624829429,-0.625379425581347,
3.60034898457542));
#249132=CARTESIAN_POINT('Ctrl Pts',(-3.22274999999998,-0.313514198417957,
3.57855815143349));
#249133=CARTESIAN_POINT('Ctrl Pts',(-3.22275000000001,5.45539308172138E-12,
3.55815895351304));
#249134=CARTESIAN_POINT('',(-3.22274864161822,-0.00290502672063927,3.31405834319998));
#249135=CARTESIAN_POINT('Ctrl Pts',(-3.22275,-1.09907859225987E-10,3.31386231834285));
#249136=CARTESIAN_POINT('Ctrl Pts',(-3.22274999999997,-0.000968490989623499,
3.31392763845649));
#249137=CARTESIAN_POINT('Ctrl Pts',(-3.2227495634281,-0.00193698879745099,
3.31399296222398));
#249138=CARTESIAN_POINT('Ctrl Pts',(-3.22274869026566,-0.00290549324082802,
3.31405828957594));
#249139=CARTESIAN_POINT('Ctrl Pts',(-3.22274869068103,-0.00290503247812938,
3.31405825849667));
#249140=CARTESIAN_POINT('Ctrl Pts',(-3.22258761851836,-0.181593258945338,
3.32611109786505));
#249141=CARTESIAN_POINT('Ctrl Pts',(-3.2075656848062,-0.359970542783448,
3.3382714130059));
#249142=CARTESIAN_POINT('Ctrl Pts',(-3.17038612993277,-0.58032053983041,
3.35289451087542));
#249143=CARTESIAN_POINT('Ctrl Pts',(-3.16202199513422,-0.624289576077566,
3.35579099359991));
#249144=CARTESIAN_POINT('Ctrl Pts',(-3.14968992747057,-0.682486647066304,
3.35958398381453));
#249145=CARTESIAN_POINT('Ctrl Pts',(-3.14653663874808,-0.696880091531935,
3.3605187318783));
#249146=CARTESIAN_POINT('Ctrl Pts',(-3.14035122602267,-0.724215721059071,
3.36228696280049));
#249147=CARTESIAN_POINT('Ctrl Pts',(-3.1373375379251,-0.737161733242957,
3.36312138138069));
#249148=CARTESIAN_POINT('Ctrl Pts',(-3.13187021135824,-0.760006934933148,
3.36458807094616));
#249149=CARTESIAN_POINT('Ctrl Pts',(-3.12944957440491,-0.769913587886718,
3.36522214200679));
#249150=CARTESIAN_POINT('Ctrl Pts',(-3.12406810772593,-0.791492908465782,
3.36659899933795));
#249151=CARTESIAN_POINT('Ctrl Pts',(-3.12108885234614,-0.803160601878099,
3.36734074139752));
#249152=CARTESIAN_POINT('Ctrl Pts',(-3.11251711429248,-0.835962123428764,
3.36941907630098));
#249153=CARTESIAN_POINT('Ctrl Pts',(-3.10677478208397,-0.857056573775631,
3.37074751336503));
#249154=CARTESIAN_POINT('Ctrl Pts',(-3.06307135267211,-1.01138715118845,
3.38041777166932));
#249155=CARTESIAN_POINT('Ctrl Pts',(-3.0167642134933,-1.14212638645514,
3.38834497992889));
#249156=CARTESIAN_POINT('Ctrl Pts',(-2.90670168098247,-1.3989417334166,
3.40410568710466));
#249157=CARTESIAN_POINT('Ctrl Pts',(-2.84279789623171,-1.52461578898582,
3.41192093412923));
#249158=CARTESIAN_POINT('Ctrl Pts',(-2.70687462735731,-1.7534698508819,
3.42694560328845));
#249159=CARTESIAN_POINT('Ctrl Pts',(-2.63664456965658,-1.857398204448,3.43411334015358));
#249160=CARTESIAN_POINT('Ctrl Pts',(-2.5283266573769,-1.99912408497023,
3.44461522283098));
#249161=CARTESIAN_POINT('Ctrl Pts',(-2.49507281278966,-2.040476409855,3.44777417822137));
#249162=CARTESIAN_POINT('Ctrl Pts',(-2.44658730863064,-2.09781161618541,
3.45230172126968));
#249163=CARTESIAN_POINT('Ctrl Pts',(-2.4321880251138,-2.11448916043558,
3.45363701974798));
#249164=CARTESIAN_POINT('Ctrl Pts',(-2.41718554830607,-2.13150932850677,
3.45501923999838));
#249165=CARTESIAN_POINT('Ctrl Pts',(-2.41675181778127,-2.1320010890478,
3.45505919313904));
#249166=CARTESIAN_POINT('Ctrl Pts',(-2.4040970867804,-2.14634010801313,
3.456224661956));
#249167=CARTESIAN_POINT('Ctrl Pts',(-2.39175763122639,-2.1600819598472,
3.45735502630952));
#249168=CARTESIAN_POINT('Ctrl Pts',(-2.36776411413128,-2.18634471794267,
3.45954180278764));
#249169=CARTESIAN_POINT('Ctrl Pts',(-2.35612711985948,-2.19888042036685,
3.46059747584587));
#249170=CARTESIAN_POINT('Ctrl Pts',(-2.32512917242755,-2.23174369750116,
3.46339698933537));
#249171=CARTESIAN_POINT('Ctrl Pts',(-2.30560179198641,-2.25191160955721,
3.46514790553473));
#249172=CARTESIAN_POINT('Ctrl Pts',(-2.2334675682802,-2.32449012109322,
3.47157197551704));
#249173=CARTESIAN_POINT('Ctrl Pts',(-2.17932023313647,-2.37533020833573,
3.4763118632669));
#249174=CARTESIAN_POINT('Ctrl Pts',(-1.94818039897605,-2.57779193513913,
3.49622360391479));
#249175=CARTESIAN_POINT('Ctrl Pts',(-1.75677362054549,-2.7118513369829,
3.51203717013012));
#249176=CARTESIAN_POINT('Ctrl Pts',(-1.43860511811695,-2.886773796846,3.53651160904171));
#249177=CARTESIAN_POINT('Ctrl Pts',(-1.32088234220945,-2.94250296581392,
3.5452098624625));
#249178=CARTESIAN_POINT('Ctrl Pts',(-1.17295553786098,-3.00185750510564,
3.55546970617373));
#249179=CARTESIAN_POINT('Ctrl Pts',(-1.14566030407205,-3.01238041755164,
3.55733566420366));
#249180=CARTESIAN_POINT('Ctrl Pts',(-1.10568687833804,-3.02716910613166,
3.56002510312143));
#249181=CARTESIAN_POINT('Ctrl Pts',(-1.09312024735683,-3.03172960692806,
3.5608644291981));
#249182=CARTESIAN_POINT('Ctrl Pts',(-1.07099773541198,-3.03960255384739,
3.56233073521922));
#249183=CARTESIAN_POINT('Ctrl Pts',(-1.06145416635896,-3.04294838882461,
3.56295961296539));
#249184=CARTESIAN_POINT('Ctrl Pts',(-1.04059950484556,-3.05014967247437,
3.56432574466373));
#249185=CARTESIAN_POINT('Ctrl Pts',(-1.02928259329696,-3.05398718197573,
3.56506196608427));
#249186=CARTESIAN_POINT('Ctrl Pts',(-0.997595416466308,-3.06453600388561,
3.56710978015883));
#249187=CARTESIAN_POINT('Ctrl Pts',(-0.977178710676943,-3.07110718748708,
3.56841359075955));
#249188=CARTESIAN_POINT('Ctrl Pts',(-0.843127756837876,-3.11277973351913,
3.57688130232848));
#249189=CARTESIAN_POINT('Ctrl Pts',(-0.727678176750141,-3.14177539103797,
3.58374102801339));
#249190=CARTESIAN_POINT('Ctrl Pts',(-0.561906469245577,-3.1737779272468,
3.59331592299491));
#249191=CARTESIAN_POINT('Ctrl Pts',(-0.51272061806219,-3.18209411387246,
3.5961229863274));
#249192=CARTESIAN_POINT('Ctrl Pts',(-0.331094538621187,-3.20848213571036,
3.60642202858491));
#249193=CARTESIAN_POINT('Ctrl Pts',(-0.197761702633655,-3.21945193153625,
3.61385897174902));
#249194=CARTESIAN_POINT('Ctrl Pts',(0.0265329823053955,-3.22391651701158,
3.62658982575467));
#249195=CARTESIAN_POINT('Ctrl Pts',(0.117232522317018,-3.22189332209526,
3.63179677806883));
#249196=CARTESIAN_POINT('Ctrl Pts',(0.26966701059199,-3.21204770744448,
3.64074346597529));
#249197=CARTESIAN_POINT('Ctrl Pts',(0.331480357297423,-3.20625806875407,
3.64442557175297));
#249198=CARTESIAN_POINT('Ctrl Pts',(0.418405866603907,-3.19557583429122,
3.6496984134265));
#249199=CARTESIAN_POINT('Ctrl Pts',(0.443688137908328,-3.19216371156812,
3.65124336028755));
#249200=CARTESIAN_POINT('Ctrl Pts',(0.487244896755648,-3.18575780427341,
3.65392579050463));
#249201=CARTESIAN_POINT('Ctrl Pts',(0.505539232893881,-3.18290597388686,
3.65505878922268));
#249202=CARTESIAN_POINT('Ctrl Pts',(0.540623668982058,-3.17712669895831,
3.65724424392317));
#249203=CARTESIAN_POINT('Ctrl Pts',(0.557417152099547,-3.17422338747694,
3.65829590568656));
#249204=CARTESIAN_POINT('Ctrl Pts',(0.601474142285977,-3.16624626992806,
3.66106992510736));
#249205=CARTESIAN_POINT('Ctrl Pts',(0.62869610337194,-3.16095360908572,
3.66279911696278));
#249206=CARTESIAN_POINT('Ctrl Pts',(0.726292195445964,-3.14066781475323,
3.66905491504746));
#249207=CARTESIAN_POINT('Ctrl Pts',(0.796223698503015,-3.12367110928172,
3.67364378890512));
#249208=CARTESIAN_POINT('Ctrl Pts',(1.09114595593895,-3.04144383336252,
3.69346037110032));
#249209=CARTESIAN_POINT('Ctrl Pts',(1.30921389121566,-2.95413459175153,
3.70934763233808));
#249210=CARTESIAN_POINT('Ctrl Pts',(1.63211463333146,-2.7820269301989,3.73401782621837));
#249211=CARTESIAN_POINT('Ctrl Pts',(1.74447092614427,-2.71298720568552,
3.74282896584637));
#249212=CARTESIAN_POINT('Ctrl Pts',(1.87636648764199,-2.62034954248813,
3.75320541788491));
#249213=CARTESIAN_POINT('Ctrl Pts',(1.90020749734336,-2.60311246926652,
3.75508219188885));
#249214=CARTESIAN_POINT('Ctrl Pts',(1.93455934672457,-2.57755256265045,
3.75778418749249));
#249215=CARTESIAN_POINT('Ctrl Pts',(1.94525885506979,-2.56948731865943,
3.75862545568758));
#249216=CARTESIAN_POINT('Ctrl Pts',(1.96402063289817,-2.55516040777961,
3.76009961546359));
#249217=CARTESIAN_POINT('Ctrl Pts',(1.97210386002413,-2.54892685873635,
3.76073437511173));
#249218=CARTESIAN_POINT('Ctrl Pts',(1.98959992895737,-2.53530134574946,
3.76210744378303));
#249219=CARTESIAN_POINT('Ctrl Pts',(1.99900132194905,-2.52789527403994,
3.76284475938736));
#249220=CARTESIAN_POINT('Ctrl Pts',(2.02519857895498,-2.50702049601065,
3.76489861194788));
#249221=CARTESIAN_POINT('Ctrl Pts',(2.04190139578684,-2.49343534058479,
3.766207293532));
#249222=CARTESIAN_POINT('Ctrl Pts',(2.1523989195752,-2.40170768686351,3.77486896071459));
#249223=CARTESIAN_POINT('Ctrl Pts',(2.24183467364514,-2.31844876802866,
3.78190118549108));
#249224=CARTESIAN_POINT('Ctrl Pts',(2.51784361053033,-2.03055559610329,
3.80449762916262));
#249225=CARTESIAN_POINT('Ctrl Pts',(2.68281541239459,-1.80698468355226,
3.81959781185925));
#249226=CARTESIAN_POINT('Ctrl Pts',(2.84545308860876,-1.51423200287893,
3.83925770746937));
#249227=CARTESIAN_POINT('Ctrl Pts',(2.87232123957701,-1.46262500951657,
3.84271427900689));
#249228=CARTESIAN_POINT('Ctrl Pts',(2.90866799389909,-1.38794360297326,
3.84771846754082));
#249229=CARTESIAN_POINT('Ctrl Pts',(2.91929924156062,-1.3654408918766,3.8492265349319));
#249230=CARTESIAN_POINT('Ctrl Pts',(2.93733953851354,-1.32608179785532,
3.85186573935885));
#249231=CARTESIAN_POINT('Ctrl Pts',(2.94486682151639,-1.30928067300504,
3.85299278802608));
#249232=CARTESIAN_POINT('Ctrl Pts',(2.95914430496461,-1.27666680322901,
3.8551818693089));
#249233=CARTESIAN_POINT('Ctrl Pts',(2.96591274351086,-1.26086269031789,
3.85624323749));
#249234=CARTESIAN_POINT('Ctrl Pts',(2.98358387527426,-1.21867138891481,
3.85907861770062));
#249235=CARTESIAN_POINT('Ctrl Pts',(2.99426272608619,-1.1921926600421,3.86086004957385));
#249236=CARTESIAN_POINT('Ctrl Pts',(3.03265669395756,-1.0932218176259,3.86752771323817));
#249237=CARTESIAN_POINT('Ctrl Pts',(3.0581004840827,-1.01988252977222,3.87248744408377));
#249238=CARTESIAN_POINT('Ctrl Pts',(3.14803808095682,-0.726887060380422,
3.89238217693537));
#249239=CARTESIAN_POINT('Ctrl Pts',(3.19169549707302,-0.501561128582362,
3.90791777694789));
#249240=CARTESIAN_POINT('Ctrl Pts',(3.22214313978351,-0.144146217813104,
3.93209659249631));
#249241=CARTESIAN_POINT('Ctrl Pts',(3.22533558531727,-0.0141813625976974,
3.94077795065607));
#249242=CARTESIAN_POINT('Ctrl Pts',(3.2196262867641,0.144838821149949,3.95102032454814));
#249243=CARTESIAN_POINT('Ctrl Pts',(3.21818037448073,0.174031391206086,
3.95288465255639));
#249244=CARTESIAN_POINT('Ctrl Pts',(3.21549487345626,0.216538371257538,
3.95557219708008));
#249245=CARTESIAN_POINT('Ctrl Pts',(3.21456930682533,0.229870254080964,
3.95641122858429));
#249246=CARTESIAN_POINT('Ctrl Pts',(3.21279077863745,0.253371472397949,
3.95788294239884));
#249247=CARTESIAN_POINT('Ctrl Pts',(3.21197241286599,0.263543011996047,
3.95851747058732));
#249248=CARTESIAN_POINT('Ctrl Pts',(3.21008725766431,0.28565916454671,3.95989174627766));
#249249=CARTESIAN_POINT('Ctrl Pts',(3.20900210540162,0.297601845251194,
3.96063048398925));
#249250=CARTESIAN_POINT('Ctrl Pts',(3.20577227384963,0.331073672103552,
3.96269219115687));
#249251=CARTESIAN_POINT('Ctrl Pts',(3.20347737998515,0.352588118114054,
3.96400720942522));
#249252=CARTESIAN_POINT('Ctrl Pts',(3.18631328445752,0.499460203484161,
3.97292473857919));
#249253=CARTESIAN_POINT('Ctrl Pts',(3.16430474959837,0.623887282667455,
3.98018395824887));
#249254=CARTESIAN_POINT('Ctrl Pts',(3.12572180288597,0.785876225434057,
3.98960699699214));
#249255=CARTESIAN_POINT('Ctrl Pts',(3.11566099216859,0.824860531917362,
3.99187238185345));
#249256=CARTESIAN_POINT('Ctrl Pts',(3.07050841732539,0.987187325712524,
4.00132965224258));
#249257=CARTESIAN_POINT('Ctrl Pts',(3.02880182205437,1.10856652322391,4.00846565804865));
#249258=CARTESIAN_POINT('Ctrl Pts',(2.94374932019487,1.31510796677328,4.02111742234584));
#249259=CARTESIAN_POINT('Ctrl Pts',(2.9036471798791,1.40142792335283,4.02656855459159));
#249260=CARTESIAN_POINT('Ctrl Pts',(2.83017864655181,1.54283207426288,4.03589029913804));
#249261=CARTESIAN_POINT('Ctrl Pts',(2.79887414384019,1.59891985170751,4.0396963632809));
#249262=CARTESIAN_POINT('Ctrl Pts',(2.75265381972605,1.67621069236225,4.04511630841779));
#249263=CARTESIAN_POINT('Ctrl Pts',(2.73912514644251,1.69822810884001,4.04668077209535));
#249264=CARTESIAN_POINT('Ctrl Pts',(2.71542011612938,1.73578689268357,4.04938626454634));
#249265=CARTESIAN_POINT('Ctrl Pts',(2.70537134539315,1.75140754963326,4.05052259614647));
#249266=CARTESIAN_POINT('Ctrl Pts',(2.68463832335715,1.78303250057773,4.05284637424434));
#249267=CARTESIAN_POINT('Ctrl Pts',(2.67394464892622,1.79902968692595,4.05403413957572));
#249268=CARTESIAN_POINT('Ctrl Pts',(2.64664722279766,1.83908413165214,4.05703979586312));
#249269=CARTESIAN_POINT('Ctrl Pts',(2.62985850252061,1.86301264955017,4.05886458225399));
#249270=CARTESIAN_POINT('Ctrl Pts',(2.5643690305434,1.95370360165604,4.06589542607785));
#249271=CARTESIAN_POINT('Ctrl Pts',(2.51343599267419,2.01880753224785,4.0711857437557));
#249272=CARTESIAN_POINT('Ctrl Pts',(2.31518342580373,2.25307361224488,4.09115599368582));
#249273=CARTESIAN_POINT('Ctrl Pts',(2.1528438931671,2.40866265623148,4.10638606810754));
#249274=CARTESIAN_POINT('Ctrl Pts',(1.87438348094797,2.62473801120903,4.13013800245248));
#249275=CARTESIAN_POINT('Ctrl Pts',(1.76845590861693,2.69724541236611,4.13870571364588));
#249276=CARTESIAN_POINT('Ctrl Pts',(1.63356640435371,2.77820493240319,4.14883048942756));
#249277=CARTESIAN_POINT('Ctrl Pts',(1.60845064939524,2.79282088350849,4.15068379712695));
#249278=CARTESIAN_POINT('Ctrl Pts',(1.57152663327977,2.81364520896418,4.1533585364995));
#249279=CARTESIAN_POINT('Ctrl Pts',(1.55987282512971,2.82012271098336,4.15419557934603));
#249280=CARTESIAN_POINT('Ctrl Pts',(1.53923161332175,2.83142855717502,4.15566512384545));
#249281=CARTESIAN_POINT('Ctrl Pts',(1.53026105521298,2.83628678847731,4.15629945163804));
#249282=CARTESIAN_POINT('Ctrl Pts',(1.5106768143253,2.84677316222275,4.1576748248232));
#249283=CARTESIAN_POINT('Ctrl Pts',(1.500054615212,2.8523846228353,4.15841484569766));
#249284=CARTESIAN_POINT('Ctrl Pts',(1.47012954832996,2.86797993950919,4.16048364994763));
#249285=CARTESIAN_POINT('Ctrl Pts',(1.45075632379681,2.87782834251036,4.16180439509308));
#249286=CARTESIAN_POINT('Ctrl Pts',(1.31448240496268,2.94537745419819,4.17097561327199));
#249287=CARTESIAN_POINT('Ctrl Pts',(1.19426117756273,2.99614088933111,4.17845965620575));
#249288=CARTESIAN_POINT('Ctrl Pts',(1.03795467223725,3.05123194903325,4.18782729734363));
#249289=CARTESIAN_POINT('Ctrl Pts',(1.0044352525925,3.06242978480467,4.18981547561764));
#249290=CARTESIAN_POINT('Ctrl Pts',(0.79672592656325,3.12804204972523,4.20204298889468));
#249291=CARTESIAN_POINT('Ctrl Pts',(0.618367565812259,3.16812842197894,
4.21216609266073));
#249292=CARTESIAN_POINT('Ctrl Pts',(0.373633902622566,3.20166846709655,
4.22638682641243));
#249293=CARTESIAN_POINT('Ctrl Pts',(0.30944357503122,3.20850856646885,4.23014430814276));
#249294=CARTESIAN_POINT('Ctrl Pts',(0.196924432245244,3.21709062899586,
4.23681041436933));
#249295=CARTESIAN_POINT('Ctrl Pts',(0.148680569706699,3.21968089616628,
4.23969393387703));
#249296=CARTESIAN_POINT('Ctrl Pts',(0.0772502364507711,3.22190724980168,
4.24400911363017));
#249297=CARTESIAN_POINT('Ctrl Pts',(0.0540953414206763,3.22237917952252,
4.24541501224381));
#249298=CARTESIAN_POINT('Ctrl Pts',(0.0127666227477288,3.22277594610537,
4.24793788484352));
#249299=CARTESIAN_POINT('Ctrl Pts',(-0.00540542899463652,3.22279669629168,
4.24905183987339));
#249300=CARTESIAN_POINT('Ctrl Pts',(-0.0439211589359999,3.22251492250118,
4.25142316143626));
#249301=CARTESIAN_POINT('Ctrl Pts',(-0.0642636733894452,3.2221734348334,
4.25268168829634));
#249302=CARTESIAN_POINT('Ctrl Pts',(-0.11897980296284,3.22073657265357,
4.25608377926682));
#249303=CARTESIAN_POINT('Ctrl Pts',(-0.153340612515038,3.21928358097877,
4.25823829551716));
#249304=CARTESIAN_POINT('Ctrl Pts',(-0.331267306303314,3.20890475411463,
4.26949217876983));
#249305=CARTESIAN_POINT('Ctrl Pts',(-0.474123230275399,3.19092546846574,
4.27886761240281));
#249306=CARTESIAN_POINT('Ctrl Pts',(-0.825550386026511,3.1225739203204,
4.30270267862349));
#249307=CARTESIAN_POINT('Ctrl Pts',(-1.03120205845841,3.06081981913464,
4.31737070010911));
#249308=CARTESIAN_POINT('Ctrl Pts',(-1.2806586297594,2.95789276537326,4.33529758416999));
#249309=CARTESIAN_POINT('Ctrl Pts',(-1.33155958004648,2.9353306257068,4.33896001561896));
#249310=CARTESIAN_POINT('Ctrl Pts',(-1.41518458863889,2.89564006871776,
4.34495681337516));
#249311=CARTESIAN_POINT('Ctrl Pts',(-1.44824367123161,2.87924805485308,
4.34732205716297));
#249312=CARTESIAN_POINT('Ctrl Pts',(-1.49402926897528,2.85555752970776,
4.3505828395644));
#249313=CARTESIAN_POINT('Ctrl Pts',(-1.50699724391859,2.84873508559692,
4.35150468966395));
#249314=CARTESIAN_POINT('Ctrl Pts',(-1.52907109990915,2.83692912604252,
4.3530703367325));
#249315=CARTESIAN_POINT('Ctrl Pts',(-1.53820017455359,2.83198967685502,
4.35371679795972));
#249316=CARTESIAN_POINT('Ctrl Pts',(-1.55722679397468,2.82157583506806,
4.35506175391373));
#249317=CARTESIAN_POINT('Ctrl Pts',(-1.56711957091571,2.81609334724797,
4.35575973878881));
#249318=CARTESIAN_POINT('Ctrl Pts',(-1.59363408340467,2.80121625321076,
4.35762747759854));
#249319=CARTESIAN_POINT('Ctrl Pts',(-1.6102018186385,2.79172567282342,4.3587913627164));
#249320=CARTESIAN_POINT('Ctrl Pts',(-1.6873870038303,2.74659555779403,4.36420332729992));
#249321=CARTESIAN_POINT('Ctrl Pts',(-1.74691621291337,2.70912298014112,
4.36834744718454));
#249322=CARTESIAN_POINT('Ctrl Pts',(-1.95743452296027,2.56677802068385,
4.38306993538948));
#249323=CARTESIAN_POINT('Ctrl Pts',(-2.10061645113594,2.4509832340051,4.39322917830641));
#249324=CARTESIAN_POINT('Ctrl Pts',(-2.35537711849186,2.20613992392381,
4.41306932536024));
#249325=CARTESIAN_POINT('Ctrl Pts',(-2.46813008134808,2.07922578135291,
4.42269629312879));
#249326=CARTESIAN_POINT('Ctrl Pts',(-2.59733263870874,1.90839673616246,
4.43538035161858));
#249327=CARTESIAN_POINT('Ctrl Pts',(-2.62354652751897,1.87219610807684,
4.43805283002688));
#249328=CARTESIAN_POINT('Ctrl Pts',(-2.6617951365915,1.81699451594448,4.44211180378256));
#249329=CARTESIAN_POINT('Ctrl Pts',(-2.67439824756349,1.79839272530539,
4.44347688312329));
#249330=CARTESIAN_POINT('Ctrl Pts',(-2.69671424327869,1.76470162291268,
4.44594522887242));
#249331=CARTESIAN_POINT('Ctrl Pts',(-2.7064976412232,1.74965997424406,4.44704581215187));
#249332=CARTESIAN_POINT('Ctrl Pts',(-2.72731435251805,1.71706257874903,
4.44942827260592));
#249333=CARTESIAN_POINT('Ctrl Pts',(-2.73830481955926,1.69948055596741,
4.45071165978634));
#249334=CARTESIAN_POINT('Ctrl Pts',(-2.76753242025832,1.65170400498327,
4.45419530692381));
#249335=CARTESIAN_POINT('Ctrl Pts',(-2.78544430834579,1.62131479521157,
4.45640716230311));
#249336=CARTESIAN_POINT('Ctrl Pts',(-2.89644519416116,1.42572090910679,
4.47062296771631));
#249337=CARTESIAN_POINT('Ctrl Pts',(-2.97528437985863,1.2528914377389,4.48312576397147));
#249338=CARTESIAN_POINT('Ctrl Pts',(-3.08472684356091,0.943312849939473,
4.50520661615248));
#249339=CARTESIAN_POINT('Ctrl Pts',(-3.12248378576721,0.809613366588782,
4.5146391280033));
#249340=CARTESIAN_POINT('Ctrl Pts',(-3.16670361284636,0.602817580847188,
4.52879943928522));
#249341=CARTESIAN_POINT('Ctrl Pts',(-3.17949457738736,0.531240317593413,
4.533622811106));
#249342=CARTESIAN_POINT('Ctrl Pts',(-3.19620428997651,0.415187721105826,
4.54126079824792));
#249343=CARTESIAN_POINT('Ctrl Pts',(-3.20163915569329,0.370958047490449,
4.5441293755178));
#249344=CARTESIAN_POINT('Ctrl Pts',(-3.20775123873508,0.31096221751003,
4.54795087873103));
#249345=CARTESIAN_POINT('Ctrl Pts',(-3.20923234664428,0.295285080916615,
4.54894303851876));
#249346=CARTESIAN_POINT('Ctrl Pts',(-3.21151684438641,0.269052339403136,
4.55059181280767));
#249347=CARTESIAN_POINT('Ctrl Pts',(-3.21238322835734,0.258502626483601,
4.5512517961673));
#249348=CARTESIAN_POINT('Ctrl Pts',(-3.21403958164885,0.237037730192024,
4.55258810099946));
#249349=CARTESIAN_POINT('Ctrl Pts',(-3.21482595969784,0.226122477987101,
4.55326422556669));
#249350=CARTESIAN_POINT('Ctrl Pts',(-3.216720162461,0.197819389555422,4.55500906190687));
#249351=CARTESIAN_POINT('Ctrl Pts',(-3.21774262859818,0.180425944328434,
4.55607318094827));
#249352=CARTESIAN_POINT('Ctrl Pts',(-3.22134701236618,0.109263957526231,
4.56039658077629));
#249353=CARTESIAN_POINT('Ctrl Pts',(-3.22272281160825,0.055440052023331,
4.56359609952793));
#249354=CARTESIAN_POINT('Ctrl Pts',(-3.22274986700139,0.00106910844232826,
4.56677934809673));
#249355=CARTESIAN_POINT('Ctrl Pts',(-3.22275,0.000534553557451239,4.56681063984618));
#249356=CARTESIAN_POINT('Ctrl Pts',(-3.22275,-5.68635386092821E-12,4.56684192677376));
#249357=CARTESIAN_POINT('Origin',(0.,0.,-2.31077344927308));
#249358=CARTESIAN_POINT('',(-3.22275,2.79355756999193E-11,6.06189028282397));
#249359=CARTESIAN_POINT('',(-3.22275,-2.46480457644168E-12,5.81181920673623));
#249360=CARTESIAN_POINT('',(-3.22275,-3.50678552687464E-13,-2.31077344927308));
#249361=CARTESIAN_POINT('Ctrl Pts',(-3.22275,2.79355756999193E-11,6.06189028282397));
#249362=CARTESIAN_POINT('Ctrl Pts',(-3.22275000000001,0.0971439062167578,
6.05639764174954));
#249363=CARTESIAN_POINT('Ctrl Pts',(-3.21835769004865,0.194235148630419,
6.05084379826759));
#249364=CARTESIAN_POINT('Ctrl Pts',(-3.20472638919507,0.344593473675672,
6.04202940771024));
#249365=CARTESIAN_POINT('Ctrl Pts',(-3.19852309806985,0.398077144571545,
6.03885214157138));
#249366=CARTESIAN_POINT('Ctrl Pts',(-3.1876269961524,0.475106281598435,
6.03420238934845));
#249367=CARTESIAN_POINT('Ctrl Pts',(-3.18400608468515,0.498795601701799,
6.0327623053316));
#249368=CARTESIAN_POINT('Ctrl Pts',(-3.17722759346265,0.540056507391252,
6.03023526324292));
#249369=CARTESIAN_POINT('Ctrl Pts',(-3.17418754280275,0.55764651468537,
6.02915197650542));
#249370=CARTESIAN_POINT('Ctrl Pts',(-3.16777503594112,0.592997197078166,
6.02696239177531));
#249371=CARTESIAN_POINT('Ctrl Pts',(-3.16439895900502,0.610756548486171,
6.02585601635352));
#249372=CARTESIAN_POINT('Ctrl Pts',(-3.15717657953903,0.647080379400539,
6.02357961015912));
#249373=CARTESIAN_POINT('Ctrl Pts',(-3.15331552150017,0.665641171598705,
6.02240915101558));
#249374=CARTESIAN_POINT('Ctrl Pts',(-3.14308221678452,0.712746158379625,
6.01941970057964));
#249375=CARTESIAN_POINT('Ctrl Pts',(-3.1364848619716,0.741239184400215,
6.01759362975829));
#249376=CARTESIAN_POINT('Ctrl Pts',(-3.10894354816324,0.853227667488226,
6.01034407868926));
#249377=CARTESIAN_POINT('Ctrl Pts',(-3.08504720881984,0.935953502695616,
6.00482796140598));
#249378=CARTESIAN_POINT('Ctrl Pts',(-3.01394369164409,1.14961455198215,
5.99015310451358));
#249379=CARTESIAN_POINT('Ctrl Pts',(-2.96152040992606,1.27861669171392,
5.98085402507507));
#249380=CARTESIAN_POINT('Ctrl Pts',(-2.81517426253864,1.58103505802602,
5.95818929454772));
#249381=CARTESIAN_POINT('Ctrl Pts',(-2.71335254836097,1.75002994144372,
5.94477250312231));
#249382=CARTESIAN_POINT('Ctrl Pts',(-2.57398103533259,1.93964318749871,
5.92950945192888));
#249383=CARTESIAN_POINT('Ctrl Pts',(-2.55067047406933,1.97019656274585,
5.92704399569452));
#249384=CARTESIAN_POINT('Ctrl Pts',(-2.51769906959785,2.0118461163637,5.92368286930112));
#249385=CARTESIAN_POINT('Ctrl Pts',(-2.50850138080828,2.02330280548462,
5.92275828544569));
#249386=CARTESIAN_POINT('Ctrl Pts',(-2.49277583554952,2.0426185531503,5.921199988243));
#249387=CARTESIAN_POINT('Ctrl Pts',(-2.48628842772258,2.05051012805239,
5.92056349321495));
#249388=CARTESIAN_POINT('Ctrl Pts',(-2.47279894742059,2.06676119274584,
5.9192532999467));
#249389=CARTESIAN_POINT('Ctrl Pts',(-2.4657918311181,2.07511616926612,5.91857996992352));
#249390=CARTESIAN_POINT('Ctrl Pts',(-2.44713893692753,2.09712916608329,
5.91680614744469));
#249391=CARTESIAN_POINT('Ctrl Pts',(-2.43542105252485,2.1107259524534,5.91571072632346));
#249392=CARTESIAN_POINT('Ctrl Pts',(-2.38357656002721,2.16987685124993,
5.91094257518709));
#249393=CARTESIAN_POINT('Ctrl Pts',(-2.34227848795306,2.21439275537493,
5.90734705232182));
#249394=CARTESIAN_POINT('Ctrl Pts',(-2.11983076971391,2.44098123475763,
5.88884163618523));
#249395=CARTESIAN_POINT('Ctrl Pts',(-1.91864515468566,2.60209437306891,
5.87489853219412));
#249396=CARTESIAN_POINT('Ctrl Pts',(-1.62697310071655,2.78326393949472,
5.85537604714825));
#249397=CARTESIAN_POINT('Ctrl Pts',(-1.5516915859894,2.82592486619816,5.85039897227247));
#249398=CARTESIAN_POINT('Ctrl Pts',(-1.42164298618653,2.89285696704888,
5.84182066465821));
#249399=CARTESIAN_POINT('Ctrl Pts',(-1.36774915383201,2.91872434411009,
5.83827143641693));
#249400=CARTESIAN_POINT('Ctrl Pts',(-1.2905040740226,2.95319027506277,5.8331762201799));
#249401=CARTESIAN_POINT('Ctrl Pts',(-1.26772293920817,2.96304101604838,
5.83167260134459));
#249402=CARTESIAN_POINT('Ctrl Pts',(-1.22815013764021,2.97961269954699,
5.82905800533204));
#249403=CARTESIAN_POINT('Ctrl Pts',(-1.21141127560663,2.98645731601754,
5.82795124311025));
#249404=CARTESIAN_POINT('Ctrl Pts',(-1.17702019134184,3.00018332130682,
5.82567525303668));
#249405=CARTESIAN_POINT('Ctrl Pts',(-1.15936314847231,3.0070506410691,5.82450560728564));
#249406=CARTESIAN_POINT('Ctrl Pts',(-1.114353071075,3.02410096497071,5.8215207410963));
#249407=CARTESIAN_POINT('Ctrl Pts',(-1.08692081823974,3.03406863121012,
5.81969848424239));
#249408=CARTESIAN_POINT('Ctrl Pts',(-0.978572046449844,3.07177981569216,
5.81248714930083));
#249409=CARTESIAN_POINT('Ctrl Pts',(-0.896705627207794,3.09666778101928,
5.80700669511644));
#249410=CARTESIAN_POINT('Ctrl Pts',(-0.576719859925738,3.1801926708841,
5.7854601668821));
#249411=CARTESIAN_POINT('Ctrl Pts',(-0.333213222596353,3.21483640274297,
5.76872145949128));
#249412=CARTESIAN_POINT('Ctrl Pts',(-0.00823055482417009,3.2237317534507,
5.74689592256636));
#249413=CARTESIAN_POINT('Ctrl Pts',(0.0717770033805431,3.22294333701456,
5.741572124074));
#249414=CARTESIAN_POINT('Ctrl Pts',(0.198983382920385,3.21694980825102,
5.73326108779646));
#249415=CARTESIAN_POINT('Ctrl Pts',(0.246238107501246,3.21367823278527,
5.73020770460111));
#249416=CARTESIAN_POINT('Ctrl Pts',(0.30923286513669,3.20791913449751,5.72619741036557));
#249417=CARTESIAN_POINT('Ctrl Pts',(0.325048959733889,3.20635514817282,
5.7251956307641));
#249418=CARTESIAN_POINT('Ctrl Pts',(0.351250121256505,3.20356835941545,
5.72354522066061));
#249419=CARTESIAN_POINT('Ctrl Pts',(0.361641787519611,3.20241192025137,
5.72289304113583));
#249420=CARTESIAN_POINT('Ctrl Pts',(0.381270438432944,3.20013077774537,
5.72166590571767));
#249421=CARTESIAN_POINT('Ctrl Pts',(0.390508479323459,3.1990166105531,5.72109035541206));
#249422=CARTESIAN_POINT('Ctrl Pts',(0.414909645911928,3.19596639683822,
5.71957506421613));
#249423=CARTESIAN_POINT('Ctrl Pts',(0.430064253467761,3.19396242669063,
5.71863903895045));
#249424=CARTESIAN_POINT('Ctrl Pts',(0.484273714673252,3.18640120542509,
5.71530709812945));
#249425=CARTESIAN_POINT('Ctrl Pts',(0.523241677843993,3.18023460297524,
5.71294231862377));
#249426=CARTESIAN_POINT('Ctrl Pts',(0.855790231150312,3.12133108050151,
5.69294712328959));
#249427=CARTESIAN_POINT('Ctrl Pts',(1.14087829997956,3.02878305876367,5.67692873706354));
#249428=CARTESIAN_POINT('Ctrl Pts',(1.47938557329845,2.86419752252249,5.65543508441461));
#249429=CARTESIAN_POINT('Ctrl Pts',(1.54831037321241,2.82753301316698,5.65092489527404));
#249430=CARTESIAN_POINT('Ctrl Pts',(1.66381646441471,2.76059918357091,5.6430748589695));
#249431=CARTESIAN_POINT('Ctrl Pts',(1.71107156347548,2.73156121021883,5.63977561027405));
#249432=CARTESIAN_POINT('Ctrl Pts',(1.77776566987291,2.68816821282045,5.63497863747436));
#249433=CARTESIAN_POINT('Ctrl Pts',(1.79783063193502,2.67479047554919,5.63351667040417));
#249434=CARTESIAN_POINT('Ctrl Pts',(1.83258020517745,2.65105454504744,5.63095074031175));
#249435=CARTESIAN_POINT('Ctrl Pts',(1.84733199064832,2.64079626346014,5.62985055630425));
#249436=CARTESIAN_POINT('Ctrl Pts',(1.87576327492936,2.62067055729023,5.62770852546819));
#249437=CARTESIAN_POINT('Ctrl Pts',(1.88945263307856,2.61081802576101,5.62666726973743));
#249438=CARTESIAN_POINT('Ctrl Pts',(1.92582300737283,2.58420560538922,5.62387389126816));
#249439=CARTESIAN_POINT('Ctrl Pts',(1.94836202727434,2.56725499254312,5.62211445798598));
#249440=CARTESIAN_POINT('Ctrl Pts',(2.0321883242572,2.50247315947323,5.61546154747821));
#249441=CARTESIAN_POINT('Ctrl Pts',(2.09195667854685,2.45272846463051,5.6104938275079));
#249442=CARTESIAN_POINT('Ctrl Pts',(2.32082772858264,2.2477857843588,5.5905523536666));
#249443=CARTESIAN_POINT('Ctrl Pts',(2.47493294911913,2.07688806171453,5.57497270600437));
#249444=CARTESIAN_POINT('Ctrl Pts',(2.66671539386692,1.81224509674283,5.55293830591617));
#249445=CARTESIAN_POINT('Ctrl Pts',(2.72026571003837,1.73082639200155,5.54641318598829));
#249446=CARTESIAN_POINT('Ctrl Pts',(2.78863272048446,1.61584878560609,5.53764812663343));
#249447=CARTESIAN_POINT('Ctrl Pts',(2.80668727878983,1.58428106368615,5.53528619597426));
#249448=CARTESIAN_POINT('Ctrl Pts',(2.83709319752367,1.52896555439585,5.53123248140996));
#249449=CARTESIAN_POINT('Ctrl Pts',(2.8496899513464,1.50535735498699,5.52952867347749));
#249450=CARTESIAN_POINT('Ctrl Pts',(2.86784563221889,1.47028607203132,5.52703909975039));
#249451=CARTESIAN_POINT('Ctrl Pts',(2.87363263419062,1.4589431792616,5.52624024303432));
#249452=CARTESIAN_POINT('Ctrl Pts',(2.88339486346415,1.43952513771686,5.52488382457752));
#249453=CARTESIAN_POINT('Ctrl Pts',(2.88740367902103,1.4314672759165,5.52432422460227));
#249454=CARTESIAN_POINT('Ctrl Pts',(2.89647549953428,1.41303942043793,5.5230519574839));
#249455=CARTESIAN_POINT('Ctrl Pts',(2.90151661164644,1.40265893395652,5.52234063437426));
#249456=CARTESIAN_POINT('Ctrl Pts',(2.91527543874067,1.37393563189173,5.52038648878447));
#249457=CARTESIAN_POINT('Ctrl Pts',(2.92387585708866,1.35553680299991,5.51915055622134));
#249458=CARTESIAN_POINT('Ctrl Pts',(2.97212181874132,1.24972853076145,5.51212615090402));
#249459=CARTESIAN_POINT('Ctrl Pts',(3.00802443578682,1.16065584407663,5.50653539555241));
#249460=CARTESIAN_POINT('Ctrl Pts',(3.09512928251753,0.91321290959359,5.49153124631669));
#249461=CARTESIAN_POINT('Ctrl Pts',(3.13813163177877,0.752274796544907,
5.48233145616816));
#249462=CARTESIAN_POINT('Ctrl Pts',(3.20075301547494,0.415249867864579,
5.46305839222876));
#249463=CARTESIAN_POINT('Ctrl Pts',(3.21868172541316,0.239435604094995,
5.45299272507181));
#249464=CARTESIAN_POINT('Ctrl Pts',(3.22280678134039,0.0286260828562297,
5.44040892091165));
#249465=CARTESIAN_POINT('Ctrl Pts',(3.22292866306092,-0.00580508913796709,
5.43833813674266));
#249466=CARTESIAN_POINT('Ctrl Pts',(3.22224832831783,-0.060300309013837,
5.435033209645));
#249467=CARTESIAN_POINT('Ctrl Pts',(3.22181029250909,-0.0803668309714191,
5.43381036808096));
#249468=CARTESIAN_POINT('Ctrl Pts',(3.22063206192379,-0.118158217237558,
5.43149574030741));
#249469=CARTESIAN_POINT('Ctrl Pts',(3.21993289525594,-0.135883673867505,
5.430405271413));
#249470=CARTESIAN_POINT('Ctrl Pts',(3.21802247348689,-0.175920961738625,
5.42793087797457));
#249471=CARTESIAN_POINT('Ctrl Pts',(3.21672544716932,-0.198227601916761,
5.42654433623924));
#249472=CARTESIAN_POINT('Ctrl Pts',(3.21218146026364,-0.2644796865809,5.42240179883741));
#249473=CARTESIAN_POINT('Ctrl Pts',(3.20826515402188,-0.308372557199517,
5.41962525535792));
#249474=CARTESIAN_POINT('Ctrl Pts',(3.17900973163127,-0.574489429845016,
5.40258919301438));
#249475=CARTESIAN_POINT('Ctrl Pts',(3.13149616089561,-0.793625607532219,
5.38763866823074));
#249476=CARTESIAN_POINT('Ctrl Pts',(3.0189929642407,-1.13600795425366,5.36328415443066));
#249477=CARTESIAN_POINT('Ctrl Pts',(2.96805344355116,-1.26312891608525,
5.35401976750253));
#249478=CARTESIAN_POINT('Ctrl Pts',(2.89006211484203,-1.42675654995869,
5.34206489196169));
#249479=CARTESIAN_POINT('Ctrl Pts',(2.87010830429375,-1.46648285979311,
5.33916064733501));
#249480=CARTESIAN_POINT('Ctrl Pts',(2.83478907769937,-1.53331603239556,
5.33428650827851));
#249481=CARTESIAN_POINT('Ctrl Pts',(2.81984116193708,-1.56063549761402,
5.33229755608761));
#249482=CARTESIAN_POINT('Ctrl Pts',(2.79783396918563,-1.59950794464164,
5.329477058876));
#249483=CARTESIAN_POINT('Ctrl Pts',(2.79109472819697,-1.61123890764236,
5.32862715521531));
#249484=CARTESIAN_POINT('Ctrl Pts',(2.77923093741058,-1.63159233616332,
5.32715523962301));
#249485=CARTESIAN_POINT('Ctrl Pts',(2.77413971131905,-1.64023383316495,
5.32653117048161));
#249486=CARTESIAN_POINT('Ctrl Pts',(2.76316664932994,-1.6586615035197,5.32520234431484));
#249487=CARTESIAN_POINT('Ctrl Pts',(2.75727308277397,-1.66844031104205,
5.32449834449039));
#249488=CARTESIAN_POINT('Ctrl Pts',(2.74103312238073,-1.69506513316945,
5.32258413749414));
#249489=CARTESIAN_POINT('Ctrl Pts',(2.73058330791917,-1.71184789812527,
5.32138036918034));
#249490=CARTESIAN_POINT('Ctrl Pts',(2.67380929480595,-1.80118612094496,
5.31498180608123));
#249491=CARTESIAN_POINT('Ctrl Pts',(2.62474260682964,-1.87196593272686,
5.30994540535129));
#249492=CARTESIAN_POINT('Ctrl Pts',(2.46850262364561,-2.07910197953422,
5.29503855472475));
#249493=CARTESIAN_POINT('Ctrl Pts',(2.3531074906982,-2.2088597368398,5.28545514332235));
#249494=CARTESIAN_POINT('Ctrl Pts',(2.11748060354611,-2.43427919741146,
5.26713218780895));
#249495=CARTESIAN_POINT('Ctrl Pts',(1.99977777712679,-2.53186128681745,
5.2584521400424));
#249496=CARTESIAN_POINT('Ctrl Pts',(1.83384457428873,-2.6506167674389,5.24642251134698));
#249497=CARTESIAN_POINT('Ctrl Pts',(1.7913740865185,-2.67950249484282,5.24336144593831));
#249498=CARTESIAN_POINT('Ctrl Pts',(1.72856868626863,-2.72005804967191,
5.23885029439212));
#249499=CARTESIAN_POINT('Ctrl Pts',(1.70876680282965,-2.73254121032327,
5.23743019046927));
#249500=CARTESIAN_POINT('Ctrl Pts',(1.67361683542561,-2.75416835965136,
5.23491237297281));
#249501=CARTESIAN_POINT('Ctrl Pts',(1.65832526729757,-2.76340260419168,
5.23381800771791));
#249502=CARTESIAN_POINT('Ctrl Pts',(1.62619096076716,-2.78244503567971,
5.23151991162237));
#249503=CARTESIAN_POINT('Ctrl Pts',(1.60933447755556,-2.79222848820446,
5.23031534640659));
#249504=CARTESIAN_POINT('Ctrl Pts',(1.56480497491848,-2.81753610676699,
5.22713517377398));
#249505=CARTESIAN_POINT('Ctrl Pts',(1.53699016362341,-2.83280522532898,
5.22515061533734));
#249506=CARTESIAN_POINT('Ctrl Pts',(1.41213305569642,-2.89896612021009,
5.21624786635569));
#249507=CARTESIAN_POINT('Ctrl Pts',(1.31276740728948,-2.94529483229652,
5.20917431766811));
#249508=CARTESIAN_POINT('Ctrl Pts',(1.02009870960136,-3.06399459087948,
5.1883861726227));
#249509=CARTESIAN_POINT('Ctrl Pts',(0.821961912734697,-3.12298411213479,
5.17433696990364));
#249510=CARTESIAN_POINT('Ctrl Pts',(0.505095442632602,-3.18505950591686,
5.15261992758744));
#249511=CARTESIAN_POINT('Ctrl Pts',(0.389474168807351,-3.20125606041612,
5.14485634674332));
#249512=CARTESIAN_POINT('Ctrl Pts',(0.245758873802969,-3.21348404348153,
5.13558633325421));
#249513=CARTESIAN_POINT('Ctrl Pts',(0.218268081635785,-3.21546828358876,
5.13383032118401));
#249514=CARTESIAN_POINT('Ctrl Pts',(0.17789165435825,-3.21786235695231,
5.13127971098141));
#249515=CARTESIAN_POINT('Ctrl Pts',(0.165024403638235,-3.21854789437368,
5.13047111714878));
#249516=CARTESIAN_POINT('Ctrl Pts',(0.142201486829234,-3.21962661750934,
5.1290448237995));
#249517=CARTESIAN_POINT('Ctrl Pts',(0.132247700875389,-3.22005083396614,
5.12842546784221));
#249518=CARTESIAN_POINT('Ctrl Pts',(0.110470102880129,-3.2208778104986,
5.12707633947649));
#249519=CARTESIAN_POINT('Ctrl Pts',(0.0986459234983415,-3.22126163262434,
5.1263476067731));
#249520=CARTESIAN_POINT('Ctrl Pts',(0.0652201645634567,-3.22216243703899,
5.12429755996702));
#249521=CARTESIAN_POINT('Ctrl Pts',(0.0436146792168579,-3.22252730898203,
5.12298427427346));
#249522=CARTESIAN_POINT('Ctrl Pts',(-0.128407510517826,-3.22370198768397,
5.11261041285779));
#249523=CARTESIAN_POINT('Ctrl Pts',(-0.278728315887484,-3.21419734408733,
5.10404273106163));
#249524=CARTESIAN_POINT('Ctrl Pts',(-0.538304385539554,-3.17942838175692,
5.08930817921019));
#249525=CARTESIAN_POINT('Ctrl Pts',(-0.647916398784636,-3.15891453081912,
5.08310554866025));
#249526=CARTESIAN_POINT('Ctrl Pts',(-0.911529947639595,-3.09527850836576,
5.06785394724913));
#249527=CARTESIAN_POINT('Ctrl Pts',(-1.06379585760533,-3.04630371197736,
5.05874952423793));
#249528=CARTESIAN_POINT('Ctrl Pts',(-1.25173551391868,-2.9700393512815,
5.04672525391651));
#249529=CARTESIAN_POINT('Ctrl Pts',(-1.29134591953172,-2.95303250908413,
5.04414562203884));
#249530=CARTESIAN_POINT('Ctrl Pts',(-1.35051464403786,-2.92621013528758,
5.04021744453096));
#249531=CARTESIAN_POINT('Ctrl Pts',(-1.37033453844909,-2.91698110658641,
5.03888874432115));
#249532=CARTESIAN_POINT('Ctrl Pts',(-1.40602851323281,-2.89991632853603,
5.03647174572506));
#249533=CARTESIAN_POINT('Ctrl Pts',(-1.42193496711033,-2.89215003452836,
5.03538586981074));
#249534=CARTESIAN_POINT('Ctrl Pts',(-1.45603824759524,-2.87514983107137,
5.03303840603439));
#249535=CARTESIAN_POINT('Ctrl Pts',(-1.47421289180194,-2.86587338324543,
5.03177537427398));
#249536=CARTESIAN_POINT('Ctrl Pts',(-1.5233633008965,-2.84019546471198,
5.0283263410484));
#249537=CARTESIAN_POINT('Ctrl Pts',(-1.55416085345914,-2.82346062684813,
5.02612875141087));
#249538=CARTESIAN_POINT('Ctrl Pts',(-1.75359579012857,-2.71083958814724,
5.01165289847587));
#249539=CARTESIAN_POINT('Ctrl Pts',(-1.91352809934512,-2.60041101784718,
4.99884925699455));
#249540=CARTESIAN_POINT('Ctrl Pts',(-2.17041628043224,-2.3864452124865,
4.97634924471806));
#249541=CARTESIAN_POINT('Ctrl Pts',(-2.27230413910459,-2.28964227671207,
4.96680451949895));
#249542=CARTESIAN_POINT('Ctrl Pts',(-2.41477596487089,-2.13537321047692,
4.95275942543722));
#249543=CARTESIAN_POINT('Ctrl Pts',(-2.46033075838091,-2.08272307233226,
4.94814748105809));
#249544=CARTESIAN_POINT('Ctrl Pts',(-2.5312517595283,-1.99517823331353,
4.94081555129679));
#249545=CARTESIAN_POINT('Ctrl Pts',(-2.55768462403771,-1.96117858101826,
4.9380456394262));
#249546=CARTESIAN_POINT('Ctrl Pts',(-2.59260140394756,-1.91435913495794,
4.93434612644114));
#249547=CARTESIAN_POINT('Ctrl Pts',(-2.60168555146636,-1.90199507107719,
4.93337974689889));
#249548=CARTESIAN_POINT('Ctrl Pts',(-2.61674467326198,-1.88118893866705,
4.9317718130144));
#249549=CARTESIAN_POINT('Ctrl Pts',(-2.62276785853029,-1.8727822292678,
4.93112706489592));
#249550=CARTESIAN_POINT('Ctrl Pts',(-2.6349409214599,-1.8556180662377,4.92982091626052));
#249551=CARTESIAN_POINT('Ctrl Pts',(-2.64108781855827,-1.84685874114237,
4.92915970903332));
#249552=CARTESIAN_POINT('Ctrl Pts',(-2.65690012660457,-1.82408581749953,
4.92745404017584));
#249553=CARTESIAN_POINT('Ctrl Pts',(-2.66649847475332,-1.81002576372841,
4.92641397058985));
#249554=CARTESIAN_POINT('Ctrl Pts',(-2.70515279896411,-1.75242847133306,
4.92220316468132));
#249555=CARTESIAN_POINT('Ctrl Pts',(-2.73325910103646,-1.70826010341974,
4.91908914207751));
#249556=CARTESIAN_POINT('Ctrl Pts',(-2.7970137943147,-1.60246583913932,
4.91184933080062));
#249557=CARTESIAN_POINT('Ctrl Pts',(-2.83172159206399,-1.54030413864414,
4.90776428554631));
#249558=CARTESIAN_POINT('Ctrl Pts',(-2.88898980517162,-1.42924705378697,
4.90067045549339));
#249559=CARTESIAN_POINT('Ctrl Pts',(-2.91243587073341,-1.38084277020505,
4.89764395388316));
#249560=CARTESIAN_POINT('Ctrl Pts',(-2.98947793491511,-1.21108772028001,
4.88718524297691));
#249561=CARTESIAN_POINT('Ctrl Pts',(-3.03678605519984,-1.08703335179264,
4.8798063148235));
#249562=CARTESIAN_POINT('Ctrl Pts',(-3.10372140507184,-0.872633161128614,
4.86706760128167));
#249563=CARTESIAN_POINT('Ctrl Pts',(-3.12735642633569,-0.783718857501115,
4.86178997584171));
#249564=CARTESIAN_POINT('Ctrl Pts',(-3.16060406632569,-0.632929793834891,
4.8527478125322));
#249565=CARTESIAN_POINT('Ctrl Pts',(-3.17227534908156,-0.571564993537487,
4.84904344805756));
#249566=CARTESIAN_POINT('Ctrl Pts',(-3.18614905038585,-0.484983211031298,
4.84376398047287));
#249567=CARTESIAN_POINT('Ctrl Pts',(-3.18984915378901,-0.46001826843165,
4.84223563735827));
#249568=CARTESIAN_POINT('Ctrl Pts',(-3.19570655636985,-0.417021427437538,
4.8395918562448));
#249569=CARTESIAN_POINT('Ctrl Pts',(-3.19800538377502,-0.399009786401751,
4.83848089609451));
#249570=CARTESIAN_POINT('Ctrl Pts',(-3.20237656818334,-0.362292753544884,
4.83620872598666));
#249571=CARTESIAN_POINT('Ctrl Pts',(-3.20443752531751,-0.343586737613318,
4.83504720546761));
#249572=CARTESIAN_POINT('Ctrl Pts',(-3.20921609760914,-0.296423313247933,
4.8321083042675));
#249573=CARTESIAN_POINT('Ctrl Pts',(-3.21171908225268,-0.26794625309277,
4.83032431487426));
#249574=CARTESIAN_POINT('Ctrl Pts',(-3.21977934084448,-0.159758967577081,
4.82350895342058));
#249575=CARTESIAN_POINT('Ctrl Pts',(-3.22274999999999,-0.0798906883009946,
4.81839888084207));
#249576=CARTESIAN_POINT('Ctrl Pts',(-3.22275,1.54108685473619E-11,4.8132072728278));
#249577=CARTESIAN_POINT('',(-3.22274964543185,0.00151174366742828,5.81173083705462));
#249578=CARTESIAN_POINT('Ctrl Pts',(-3.22275,-5.68635386092821E-12,4.56684192677376));
#249579=CARTESIAN_POINT('Ctrl Pts',(-3.22274999999983,-0.0986548522817535,
4.57261610439067));
#249580=CARTESIAN_POINT('Ctrl Pts',(-3.21821994880484,-0.197264624384204,
4.57822708228791));
#249581=CARTESIAN_POINT('Ctrl Pts',(-3.1874477793893,-0.531435454229501,
4.59713258198355));
#249582=CARTESIAN_POINT('Ctrl Pts',(-3.13977764501502,-0.764224446223105,
4.6101742616043));
#249583=CARTESIAN_POINT('Ctrl Pts',(-3.04579227124887,-1.05548448265948,
4.62801654316085));
#249584=CARTESIAN_POINT('Ctrl Pts',(-3.0224487473042,-1.12058048520465,
4.63210282731022));
#249585=CARTESIAN_POINT('Ctrl Pts',(-2.98699269771024,-1.210263470703,4.63789754195369));
#249586=CARTESIAN_POINT('Ctrl Pts',(-2.9766322919091,-1.23552546483991,
4.63954841037038));
#249587=CARTESIAN_POINT('Ctrl Pts',(-2.95931572495307,-1.27626637121178,
4.64224252286054));
#249588=CARTESIAN_POINT('Ctrl Pts',(-2.95255596121336,-1.29182765454154,
4.64327914526764));
#249589=CARTESIAN_POINT('Ctrl Pts',(-2.93813676120055,-1.32431685700455,
4.6454597334517));
#249590=CARTESIAN_POINT('Ctrl Pts',(-2.93045319390485,-1.34123332078802,
4.64660448749106));
#249591=CARTESIAN_POINT('Ctrl Pts',(-2.91172027884689,-1.38154698397642,
4.6493554975104));
#249592=CARTESIAN_POINT('Ctrl Pts',(-2.90053472055626,-1.4048791136317,
4.65096636457358));
#249593=CARTESIAN_POINT('Ctrl Pts',(-2.86051444481726,-1.48584228917728,
4.6566230257277));
#249594=CARTESIAN_POINT('Ctrl Pts',(-2.83023471730324,-1.54273805336361,
4.6607181566678));
#249595=CARTESIAN_POINT('Ctrl Pts',(-2.75084742999899,-1.68169425877717,
4.67102731209234));
#249596=CARTESIAN_POINT('Ctrl Pts',(-2.699756844677,-1.76254575610088,4.67730417275568));
#249597=CARTESIAN_POINT('Ctrl Pts',(-2.59561775987218,-1.91217284840742,
4.68943590561957));
#249598=CARTESIAN_POINT('Ctrl Pts',(-2.54323284231886,-1.98131325789362,
4.69527064384686));
#249599=CARTESIAN_POINT('Ctrl Pts',(-2.36379596519379,-2.19928493189945,
4.71433461028405));
#249600=CARTESIAN_POINT('Ctrl Pts',(-2.22596393652188,-2.33869232057012,
4.72763054210887));
#249601=CARTESIAN_POINT('Ctrl Pts',(-2.05396595891868,-2.48358541314899,
4.74210669012912));
#249602=CARTESIAN_POINT('Ctrl Pts',(-2.03134540196986,-2.50212083245402,
4.74397208068401));
#249603=CARTESIAN_POINT('Ctrl Pts',(-1.9981325307271,-2.52858831009139,
4.74665190185437));
#249604=CARTESIAN_POINT('Ctrl Pts',(-1.98773941758833,-2.53676653916622,
4.74748225626082));
#249605=CARTESIAN_POINT('Ctrl Pts',(-1.96923158348602,-2.55114657155005,
4.74894598192547));
#249606=CARTESIAN_POINT('Ctrl Pts',(-1.96113733146996,-2.5573740899968,
4.749581102196));
#249607=CARTESIAN_POINT('Ctrl Pts',(-1.94352117302168,-2.5707947031525,
4.75095241475063));
#249608=CARTESIAN_POINT('Ctrl Pts',(-1.93398881160816,-2.57797347597473,
4.75168763781905));
#249609=CARTESIAN_POINT('Ctrl Pts',(-1.90678980646376,-2.59822113849531,
4.7537668842568));
#249610=CARTESIAN_POINT('Ctrl Pts',(-1.88902869700136,-2.61116278545878,
4.75510255170106));
#249611=CARTESIAN_POINT('Ctrl Pts',(-1.74764691782975,-2.71198305772239,
4.76557345018828));
#249612=CARTESIAN_POINT('Ctrl Pts',(-1.61807922520001,-2.79122781553408,
4.7742090443557));
#249613=CARTESIAN_POINT('Ctrl Pts',(-1.25666895854297,-2.97861127104595,
4.79711204509908));
#249614=CARTESIAN_POINT('Ctrl Pts',(-1.01679197724353,-3.06878931060516,
4.81118230517882));
#249615=CARTESIAN_POINT('Ctrl Pts',(-0.723089568302622,-3.14093514632293,
4.82900213805161));
#249616=CARTESIAN_POINT('Ctrl Pts',(-0.677150533653468,-3.15115834927157,
4.83180274421321));
#249617=CARTESIAN_POINT('Ctrl Pts',(-0.608159023441252,-3.1649333242609,
4.83603668765029));
#249618=CARTESIAN_POINT('Ctrl Pts',(-0.585263951846832,-3.1692469781298,
4.8374462798628));
#249619=CARTESIAN_POINT('Ctrl Pts',(-0.545527596141718,-3.1762884318237,
4.83990150631911));
#249620=CARTESIAN_POINT('Ctrl Pts',(-0.528707513479019,-3.17913147071711,
4.8409434879517));
#249621=CARTESIAN_POINT('Ctrl Pts',(-0.493598013269676,-3.18477957099909,
4.84312446549881));
#249622=CARTESIAN_POINT('Ctrl Pts',(-0.475305465807736,-3.18756091803992,
4.84426416302737));
#249623=CARTESIAN_POINT('Ctrl Pts',(-0.431808150409862,-3.19379185858663,
4.84698266841423));
#249624=CARTESIAN_POINT('Ctrl Pts',(-0.406584789288867,-3.19710079053359,
4.84856580851949));
#249625=CARTESIAN_POINT('Ctrl Pts',(-0.320144133022171,-3.20740106643206,
4.8540154782244));
#249626=CARTESIAN_POINT('Ctrl Pts',(-0.25876992512015,-3.21293497728788,
4.85792663711149));
#249627=CARTESIAN_POINT('Ctrl Pts',(-0.107697943617962,-3.22220009985294,
4.86766118228952));
#249628=CARTESIAN_POINT('Ctrl Pts',(-0.0179342315945053,-3.22394920783809,
4.8735386221631));
#249629=CARTESIAN_POINT('Ctrl Pts',(0.20566406224828,-3.2189678156127,4.88838322270597));
#249630=CARTESIAN_POINT('Ctrl Pts',(0.339226372805878,-3.2076429925882,
4.89743703731633));
#249631=CARTESIAN_POINT('Ctrl Pts',(0.522019698413308,-3.18059767929463,
4.90992088736739));
#249632=CARTESIAN_POINT('Ctrl Pts',(0.572167344919531,-3.17196009208536,
4.91335452123766));
#249633=CARTESIAN_POINT('Ctrl Pts',(0.739085122151661,-3.13912222685998,
4.92477963265236));
#249634=CARTESIAN_POINT('Ctrl Pts',(0.854725246695212,-3.10962790397464,
4.93269122995297));
#249635=CARTESIAN_POINT('Ctrl Pts',(0.988937721559243,-3.06734087691087,
4.94167950875389));
#249636=CARTESIAN_POINT('Ctrl Pts',(1.00933661333444,-3.06068906130979,
4.94304012647017));
#249637=CARTESIAN_POINT('Ctrl Pts',(1.04099305994269,-3.05001538442492,
4.94514139160854));
#249638=CARTESIAN_POINT('Ctrl Pts',(1.05229683266794,-3.04613390754304,
4.94588965667127));
#249639=CARTESIAN_POINT('Ctrl Pts',(1.07312526507173,-3.03885208568645,
4.94726428848358));
#249640=CARTESIAN_POINT('Ctrl Pts',(1.08265557460268,-3.03546977313781,
4.94789162594917));
#249641=CARTESIAN_POINT('Ctrl Pts',(1.10474481101625,-3.02751302259283,
4.94934200589844));
#249642=CARTESIAN_POINT('Ctrl Pts',(1.11729137056544,-3.02290525937947,
4.95016309667502));
#249643=CARTESIAN_POINT('Ctrl Pts',(1.15719014689239,-3.00796996291873,
4.95276662445287));
#249644=CARTESIAN_POINT('Ctrl Pts',(1.1844314777628,-2.99734791817495,4.95453279709229));
#249645=CARTESIAN_POINT('Ctrl Pts',(1.33196630639441,-2.93749497376177,
4.96405509436756));
#249646=CARTESIAN_POINT('Ctrl Pts',(1.44935388104242,-2.88138703051498,
4.97147720478038));
#249647=CARTESIAN_POINT('Ctrl Pts',(1.76344910931434,-2.70719065798654,
4.99172455820149));
#249648=CARTESIAN_POINT('Ctrl Pts',(1.95142015441589,-2.57499328518299,
5.00433781408325));
#249649=CARTESIAN_POINT('Ctrl Pts',(2.18191565297002,-2.37304355976495,
5.02212711194031));
#249650=CARTESIAN_POINT('Ctrl Pts',(2.23819578024565,-2.32003662484254,
5.02668038924848));
#249651=CARTESIAN_POINT('Ctrl Pts',(2.31254852651237,-2.2447827261485,5.03302920142302));
#249652=CARTESIAN_POINT('Ctrl Pts',(2.3323133519876,-2.22424021291845,5.03475110338649));
#249653=CARTESIAN_POINT('Ctrl Pts',(2.36355175806603,-2.19089843447372,
5.03752975887448));
#249654=CARTESIAN_POINT('Ctrl Pts',(2.37520024316876,-2.17826459603496,
5.03857903593065));
#249655=CARTESIAN_POINT('Ctrl Pts',(2.39912121389744,-2.15190011114326,
5.0407616339254));
#249656=CARTESIAN_POINT('Ctrl Pts',(2.41137813631746,-2.13815624985995,
5.04189554772472));
#249657=CARTESIAN_POINT('Ctrl Pts',(2.43994189858018,-2.10556929171489,
5.04457545757187));
#249658=CARTESIAN_POINT('Ctrl Pts',(2.45614912647858,-2.08664082287587,
5.04612545695101));
#249659=CARTESIAN_POINT('Ctrl Pts',(2.50957948737611,-2.02275431701971,
5.05133610861066));
#249660=CARTESIAN_POINT('Ctrl Pts',(2.54579881618331,-1.97697544632534,
5.05503626474707));
#249661=CARTESIAN_POINT('Ctrl Pts',(2.63061851811143,-1.86357055267236,
5.06412722885367));
#249662=CARTESIAN_POINT('Ctrl Pts',(2.677877823063,-1.7949979277509,5.0695631503027));
#249663=CARTESIAN_POINT('Ctrl Pts',(2.79876149765712,-1.60418136286022,
5.08450793902741));
#249664=CARTESIAN_POINT('Ctrl Pts',(2.86700823601016,-1.47875724061629,
5.09414606886764));
#249665=CARTESIAN_POINT('Ctrl Pts',(2.93988252757465,-1.32068045758809,
5.10590682926379));
#249666=CARTESIAN_POINT('Ctrl Pts',(2.95262741918425,-1.29193556039143,
5.10803004659204));
#249667=CARTESIAN_POINT('Ctrl Pts',(3.01993157016601,-1.1339370967351,5.11960469937688));
#249668=CARTESIAN_POINT('Ctrl Pts',(3.06643258941631,-1.0013987429798,5.12897375333015));
#249669=CARTESIAN_POINT('Ctrl Pts',(3.11002964776455,-0.845169598859093,
5.13933921764393));
#249670=CARTESIAN_POINT('Ctrl Pts',(3.11569481421617,-0.824040014475264,
5.14072698807235));
#249671=CARTESIAN_POINT('Ctrl Pts',(3.12414517777828,-0.791188692737247,
5.1428610512909));
#249672=CARTESIAN_POINT('Ctrl Pts',(3.127080420288,-0.779506699964299,5.1436153300966));
#249673=CARTESIAN_POINT('Ctrl Pts',(3.13237975052589,-0.757904121151732,
5.14500132908464));
#249674=CARTESIAN_POINT('Ctrl Pts',(3.13476226856351,-0.747988691117952,
5.14563403158122));
#249675=CARTESIAN_POINT('Ctrl Pts',(3.1401408294909,-0.725127361562234,
5.14708499968029));
#249676=CARTESIAN_POINT('Ctrl Pts',(3.14310391515902,-0.712174074424841,
5.1479014109949));
#249677=CARTESIAN_POINT('Ctrl Pts',(3.15223761637016,-0.671077966968531,
5.15047458706594));
#249678=CARTESIAN_POINT('Ctrl Pts',(3.15811119056082,-0.642869710461523,
5.15221561626061));
#249679=CARTESIAN_POINT('Ctrl Pts',(3.18761479197423,-0.49099859935512,
5.16147266265394));
#249680=CARTESIAN_POINT('Ctrl Pts',(3.20436365043623,-0.366097940569403,
5.16867477164358));
#249681=CARTESIAN_POINT('Ctrl Pts',(3.23000982107142,-0.023429972332404,
5.18806682828025));
#249682=CARTESIAN_POINT('Ctrl Pts',(3.22421853766283,0.194745799613003,
5.20004993365799));
#249683=CARTESIAN_POINT('Ctrl Pts',(3.1849946506127,0.500046321840096,5.21780988683606));
#249684=CARTESIAN_POINT('Ctrl Pts',(3.16976963971649,0.588893543495585,
5.22309327479103));
#249685=CARTESIAN_POINT('Ctrl Pts',(3.14452649461475,0.706381613134253,
5.23029401617538));
#249686=CARTESIAN_POINT('Ctrl Pts',(3.13779854853652,0.735691535770736,
5.23210827704359));
#249687=CARTESIAN_POINT('Ctrl Pts',(3.12605255217834,0.783766616708003,
5.2351155357479));
#249688=CARTESIAN_POINT('Ctrl Pts',(3.12127317579946,0.802588565138288,
5.23630090366181));
#249689=CARTESIAN_POINT('Ctrl Pts',(3.11161604578071,0.83922844546739,5.23862454266085));
#249690=CARTESIAN_POINT('Ctrl Pts',(3.10675460987071,0.857049923684429,
5.23976225052994));
#249691=CARTESIAN_POINT('Ctrl Pts',(3.0948824950718,0.899143001297471,5.24246767327893));
#249692=CARTESIAN_POINT('Ctrl Pts',(3.08773917394485,0.923375617485213,
5.24403960868963));
#249693=CARTESIAN_POINT('Ctrl Pts',(3.06252403059443,1.00534793012647,5.2494074775207));
#249694=CARTESIAN_POINT('Ctrl Pts',(3.04311240170282,1.06265894243753,5.25324624886556));
#249695=CARTESIAN_POINT('Ctrl Pts',(2.99170991578357,1.20143445084811,5.26275819533515));
#249696=CARTESIAN_POINT('Ctrl Pts',(2.95799303033413,1.28220440569085,5.2684822262022));
#249697=CARTESIAN_POINT('Ctrl Pts',(2.86297702889624,1.48605714776504,5.28339406667683));
#249698=CARTESIAN_POINT('Ctrl Pts',(2.79701461540177,1.60676966191795,5.29268404150515));
#249699=CARTESIAN_POINT('Ctrl Pts',(2.69665350019406,1.76542045184021,5.3053670955559));
#249700=CARTESIAN_POINT('Ctrl Pts',(2.66876065923517,1.80730908883245,5.30876307807839));
#249701=CARTESIAN_POINT('Ctrl Pts',(2.5710322324836,1.94687587081247,5.32020785079583));
#249702=CARTESIAN_POINT('Ctrl Pts',(2.49671682779944,2.04130922351024,5.32817621373671));
#249703=CARTESIAN_POINT('Ctrl Pts',(2.40309379623298,2.14749132587736,5.33721873895071));
#249704=CARTESIAN_POINT('Ctrl Pts',(2.38872931195625,2.16345813902699,5.33858073642223));
#249705=CARTESIAN_POINT('Ctrl Pts',(2.36612094801712,2.1880887023567,5.34068366941165));
#249706=CARTESIAN_POINT('Ctrl Pts',(2.35798693959434,2.19685186423434,5.34143224111474));
#249707=CARTESIAN_POINT('Ctrl Pts',(2.34288365398304,2.21294283777586,5.34280714009197));
#249708=CARTESIAN_POINT('Ctrl Pts',(2.33592861352483,2.22028316562009,5.34343444137163));
#249709=CARTESIAN_POINT('Ctrl Pts',(2.31970535949034,2.23724452317044,5.34488435856982));
#249710=CARTESIAN_POINT('Ctrl Pts',(2.31041175465772,2.24684079313815,5.34570502720339));
#249711=CARTESIAN_POINT('Ctrl Pts',(2.28061590662946,2.27722663938834,5.34830580716778));
#249712=CARTESIAN_POINT('Ctrl Pts',(2.25989007520149,2.2977961316083,5.35006970237861));
#249713=CARTESIAN_POINT('Ctrl Pts',(2.14566639873494,2.40811746070337,5.3595677286241));
#249714=CARTESIAN_POINT('Ctrl Pts',(2.0470897425368,2.4924575156919,5.36696971130355));
#249715=CARTESIAN_POINT('Ctrl Pts',(1.76174468179251,2.70821051542694,5.38713805184988));
#249716=CARTESIAN_POINT('Ctrl Pts',(1.56571590589933,2.82607137389018,5.39969277030554));
#249717=CARTESIAN_POINT('Ctrl Pts',(1.28776582640211,2.95532212385702,5.41747655410687));
#249718=CARTESIAN_POINT('Ctrl Pts',(1.21546495466953,2.98578519071791,5.42209514006862));
#249719=CARTESIAN_POINT('Ctrl Pts',(1.11532367101914,3.02373814846748,5.42852107775098));
#249720=CARTESIAN_POINT('Ctrl Pts',(1.088384884437,3.03353878254591,5.43025238272244));
#249721=CARTESIAN_POINT('Ctrl Pts',(1.04506596019011,3.04864740791368,5.43304227436132));
#249722=CARTESIAN_POINT('Ctrl Pts',(1.02876743151095,3.0541858870987,5.43409326871958));
#249723=CARTESIAN_POINT('Ctrl Pts',(0.994959743864795,3.06537291817463,
5.43627640215543));
#249724=CARTESIAN_POINT('Ctrl Pts',(0.977445056584141,3.0710026308408,5.43740910977572));
#249725=CARTESIAN_POINT('Ctrl Pts',(0.936202809504896,3.0838704938522,5.44008072817259));
#249726=CARTESIAN_POINT('Ctrl Pts',(0.912438237352037,3.09098517170136,
5.44162357184136));
#249727=CARTESIAN_POINT('Ctrl Pts',(0.833147204859636,3.11372937993529,
5.44678374970276));
#249728=CARTESIAN_POINT('Ctrl Pts',(0.777286033555698,3.12814172631091,
5.45043954755075));
#249729=CARTESIAN_POINT('Ctrl Pts',(0.45179222761321,3.20286335457135,5.47186930920237));
#249730=CARTESIAN_POINT('Ctrl Pts',(0.175712982882834,3.22978721300955,
5.49069059745284));
#249731=CARTESIAN_POINT('Ctrl Pts',(-0.223488210381403,3.21735125815338,
5.51753527790441));
#249732=CARTESIAN_POINT('Ctrl Pts',(-0.346321751064119,3.20645654334309,
5.52572010544602));
#249733=CARTESIAN_POINT('Ctrl Pts',(-0.489569334430889,3.18542056153159,
5.53496928938033));
#249734=CARTESIAN_POINT('Ctrl Pts',(-0.510866757840209,3.18207440206927,
5.53633654523143));
#249735=CARTESIAN_POINT('Ctrl Pts',(-0.543939505403389,3.17653754248131,
5.53844583333215));
#249736=CARTESIAN_POINT('Ctrl Pts',(-0.555738473941731,3.17449455876358,
5.53919557261394));
#249737=CARTESIAN_POINT('Ctrl Pts',(-0.577573332897452,3.17058839764178,
5.54057754690301));
#249738=CARTESIAN_POINT('Ctrl Pts',(-0.587611823457463,3.16874329835069,
5.54121071576184));
#249739=CARTESIAN_POINT('Ctrl Pts',(-0.610798530618598,3.16436754845529,
5.5426682997573));
#249740=CARTESIAN_POINT('Ctrl Pts',(-0.623939920735859,3.16180262138462,
5.54349079647664));
#249741=CARTESIAN_POINT('Ctrl Pts',(-0.665850878985013,3.15335099223102,
5.54610348977568));
#249742=CARTESIAN_POINT('Ctrl Pts',(-0.694557004318693,3.14715277304657,
5.54787726054944));
#249743=CARTESIAN_POINT('Ctrl Pts',(-0.851055991525991,3.11111584521567,
5.55748089215516));
#249744=CARTESIAN_POINT('Ctrl Pts',(-0.977032370339452,3.0738823889067,
5.5649704477637));
#249745=CARTESIAN_POINT('Ctrl Pts',(-1.31914727261272,2.9495989910338,5.58548337473681));
#249746=CARTESIAN_POINT('Ctrl Pts',(-1.52863264446049,2.84667567401028,
5.59829380447683));
#249747=CARTESIAN_POINT('Ctrl Pts',(-1.78728078892754,2.68274969186606,
5.61610460417383));
#249748=CARTESIAN_POINT('Ctrl Pts',(-1.84798740328848,2.64129890409673,
5.62044041103311));
#249749=CARTESIAN_POINT('Ctrl Pts',(-1.929759157357,2.58126498251226,5.62653174224741));
#249750=CARTESIAN_POINT('Ctrl Pts',(-1.95208033463764,2.56442617525084,
5.62822137530027));
#249751=CARTESIAN_POINT('Ctrl Pts',(-1.98768248800329,2.53683419900508,
5.63096154460233));
#249752=CARTESIAN_POINT('Ctrl Pts',(-2.00110226476565,2.52626188960205,
5.63200499709723));
#249753=CARTESIAN_POINT('Ctrl Pts',(-2.02817974734219,2.50457869520352,
5.63413237427724));
#249754=CARTESIAN_POINT('Ctrl Pts',(-2.04183171393983,2.49346160198148,
5.63521652427954));
#249755=CARTESIAN_POINT('Ctrl Pts',(-2.05592572867899,2.48179117602389,
5.63634804668832));
#249756=CARTESIAN_POINT('Ctrl Pts',(-2.05645961919156,2.48134880213718,
5.63639092792553));
#249757=CARTESIAN_POINT('Ctrl Pts',(-2.05751398644129,2.48047459480543,
5.63647564945486));
#249758=CARTESIAN_POINT('Ctrl Pts',(-2.05803447010627,2.48004276973805,
5.63651748940746));
#249759=CARTESIAN_POINT('Ctrl Pts',(-2.07560033262908,2.46545971856123,
5.63793014360183));
#249760=CARTESIAN_POINT('Ctrl Pts',(-2.09249912789394,2.45113355928242,
5.63930800904221));
#249761=CARTESIAN_POINT('Ctrl Pts',(-2.12944719994724,2.41914982744088,
5.64236312059056));
#249762=CARTESIAN_POINT('Ctrl Pts',(-2.14942715861677,2.40141501756703,
5.64404346983437));
#249763=CARTESIAN_POINT('Ctrl Pts',(-2.20301905089817,2.35264057939362,
5.64862894439861));
#249764=CARTESIAN_POINT('Ctrl Pts',(-2.23619326181725,2.32113118938754,
5.65155312275996));
#249765=CARTESIAN_POINT('Ctrl Pts',(-2.34107084796557,2.21718114079909,
5.66108082364586));
#249766=CARTESIAN_POINT('Ctrl Pts',(-2.41000737934355,2.14204721799929,
5.66779023663637));
#249767=CARTESIAN_POINT('Ctrl Pts',(-2.59930495367726,1.91500672674728,
5.68751308391195));
#249768=CARTESIAN_POINT('Ctrl Pts',(-2.70967525685434,1.7553612804268,5.70074453258324));
#249769=CARTESIAN_POINT('Ctrl Pts',(-2.85045144406285,1.5065025851044,5.71980994815918));
#249770=CARTESIAN_POINT('Ctrl Pts',(-2.89239878430832,1.42430890419627,
5.72587402046414));
#249771=CARTESIAN_POINT('Ctrl Pts',(-2.93925027477849,1.32187046831723,
5.73306008565515));
#249772=CARTESIAN_POINT('Ctrl Pts',(-2.94755896109007,1.30323824867788,
5.73435250557192));
#249773=CARTESIAN_POINT('Ctrl Pts',(-2.96035928985006,1.27378477368088,
5.7363711785142));
#249774=CARTESIAN_POINT('Ctrl Pts',(-2.96496965461113,1.26301612497903,
5.73710415575155));
#249775=CARTESIAN_POINT('Ctrl Pts',(-2.97350527290124,1.24277475207837,
5.73847206897431));
#249776=CARTESIAN_POINT('Ctrl Pts',(-2.97744404391373,1.23330842068044,
5.73910775648999));
#249777=CARTESIAN_POINT('Ctrl Pts',(-2.98658176180141,1.21104815793461,
5.74059333302139));
#249778=CARTESIAN_POINT('Ctrl Pts',(-2.99174373961122,1.19823940560914,
5.74144103847204));
#249779=CARTESIAN_POINT('Ctrl Pts',(-3.00849642592024,1.15588666161436,
5.74422187761295));
#249780=CARTESIAN_POINT('Ctrl Pts',(-3.01973346614564,1.12620365916316,
5.74613547777468));
#249781=CARTESIAN_POINT('Ctrl Pts',(-3.04595736486575,1.05371610609848,
5.75073430074019));
#249782=CARTESIAN_POINT('Ctrl Pts',(-3.06048306520564,1.01075105372816,
5.7533980440949));
#249783=CARTESIAN_POINT('Ctrl Pts',(-3.116332203421,0.833296619679835,5.76420082616484));
#249784=CARTESIAN_POINT('Ctrl Pts',(-3.14973700107303,0.696470863367105,
5.7720715455626));
#249785=CARTESIAN_POINT('Ctrl Pts',(-3.20638562499776,0.374172004119983,
5.79039355616449));
#249786=CARTESIAN_POINT('Ctrl Pts',(-3.22266215886783,0.188016439694972,
5.80082974578902));
#249787=CARTESIAN_POINT('Ctrl Pts',(-3.22274964543185,0.00151174366742828,
5.81173083705462));
#249788=CARTESIAN_POINT('Ctrl Pts',(-3.22274964711574,0.00150814964619596,
5.81173104712312));
#249789=CARTESIAN_POINT('Ctrl Pts',(-3.22274988237226,0.00100543239060466,
5.81176043066946));
#249790=CARTESIAN_POINT('Ctrl Pts',(-3.22275,0.000502715827386431,5.81178981720521));
#249791=CARTESIAN_POINT('Ctrl Pts',(-3.22275,-2.46480457644168E-12,5.81181920673623));
#249792=CARTESIAN_POINT('Origin',(0.,0.,-2.31077344927308));
#249793=CARTESIAN_POINT('',(-3.22275,-3.49632484551545E-13,7.3077847617826));
#249794=CARTESIAN_POINT('',(-3.22275,-1.40828092660302E-10,7.06317491433944));
#249795=CARTESIAN_POINT('',(-3.22275,-3.50678552687464E-13,-2.31077344927308));
#249796=CARTESIAN_POINT('',(-3.22274894051683,-0.00261321596174632,6.06203802249303));
#249797=CARTESIAN_POINT('Ctrl Pts',(-3.22275,-3.49632484551545E-13,7.3077847617826));
#249798=CARTESIAN_POINT('Ctrl Pts',(-3.22275,9.92968828600041E-6,7.30778413912117));
#249799=CARTESIAN_POINT('Ctrl Pts',(-3.22274999995411,1.98593771586289E-5,
7.30778351646216));
#249800=CARTESIAN_POINT('Ctrl Pts',(-3.22274990056665,0.0107721578420478,
7.3071092768844));
#249801=CARTESIAN_POINT('Ctrl Pts',(-3.22269609007642,0.0215146429154826,
7.30643851249414));
#249802=CARTESIAN_POINT('Ctrl Pts',(-3.22248534667233,0.0425687601278631,
7.30512975584816));
#249803=CARTESIAN_POINT('Ctrl Pts',(-3.22233263290866,0.05288019896246,
7.30449156074315));
#249804=CARTESIAN_POINT('Ctrl Pts',(-3.22183246382275,0.0783840571584081,
7.30291957959404));
#249805=CARTESIAN_POINT('Ctrl Pts',(-3.22142703847561,0.0935753280267247,
7.3019889396206));
#249806=CARTESIAN_POINT('Ctrl Pts',(-3.2194973597628,0.150720687044368,
7.29850770247362));
#249807=CARTESIAN_POINT('Ctrl Pts',(-3.21726078129448,0.192648416198304,
7.2959932056103));
#249808=CARTESIAN_POINT('Ctrl Pts',(-3.19470635481189,0.501763836330129,
7.27767028645722));
#249809=CARTESIAN_POINT('Ctrl Pts',(-3.14195334462456,0.765557875235954,
7.26314887218175));
#249810=CARTESIAN_POINT('Ctrl Pts',(-3.01261116089885,1.15329797079758,
7.23999119463465));
#249811=CARTESIAN_POINT('Ctrl Pts',(-2.95938772438528,1.28372113674657,
7.23187654620352));
#249812=CARTESIAN_POINT('Ctrl Pts',(-2.88304488375447,1.44059337587614,
7.2214584885312));
#249813=CARTESIAN_POINT('Ctrl Pts',(-2.86779777632045,1.47071168550149,
7.21942734060435));
#249814=CARTESIAN_POINT('Ctrl Pts',(-2.84280250890804,1.51821886732769,
7.21617114624924));
#249815=CARTESIAN_POINT('Ctrl Pts',(-2.83336102759058,1.53576687472613,
7.21495682616968));
#249816=CARTESIAN_POINT('Ctrl Pts',(-2.8151968950943,1.56878918455843,7.21264916746556));
#249817=CARTESIAN_POINT('Ctrl Pts',(-2.80650782780787,1.58428117967987,
7.21155705069021));
#249818=CARTESIAN_POINT('Ctrl Pts',(-2.7864839183745,1.61930068689068,7.20906624926801));
#249819=CARTESIAN_POINT('Ctrl Pts',(-2.77507112898384,1.63878233140046,
7.20766480808503));
#249820=CARTESIAN_POINT('Ctrl Pts',(-2.73936717251082,1.69828644288028,
7.20333461920212));
#249821=CARTESIAN_POINT('Ctrl Pts',(-2.71440871702244,1.73789939254625,
7.20038191083833));
#249822=CARTESIAN_POINT('Ctrl Pts',(-2.65427213999663,1.82888831123676,
7.19343125108904));
#249823=CARTESIAN_POINT('Ctrl Pts',(-2.61845129760521,1.87981516253603,
7.1894110801307));
#249824=CARTESIAN_POINT('Ctrl Pts',(-2.47841145631802,2.06713630457029,
7.17413037868015));
#249825=CARTESIAN_POINT('Ctrl Pts',(-2.36483468976505,2.19616078423416,
7.16256598829609));
#249826=CARTESIAN_POINT('Ctrl Pts',(-2.11987614033175,2.43329319902482,
7.13952174865675));
#249827=CARTESIAN_POINT('Ctrl Pts',(-1.98910914412167,2.54130781750367,
7.12808166467081));
#249828=CARTESIAN_POINT('Ctrl Pts',(-1.82629320997995,2.65549264062458,
7.11527317150592));
#249829=CARTESIAN_POINT('Ctrl Pts',(-1.80190493580973,2.67210156926538,
7.11339000053754));
#249830=CARTESIAN_POINT('Ctrl Pts',(-1.7661898598399,2.69571289996707,7.11068705902997));
#249831=CARTESIAN_POINT('Ctrl Pts',(-1.75504309604228,2.70298324181404,
7.10985108337329));
#249832=CARTESIAN_POINT('Ctrl Pts',(-1.73541542073565,2.71561254776196,
7.10839281845152));
#249833=CARTESIAN_POINT('Ctrl Pts',(-1.72695404252774,2.72100127482593,
7.10776862235713));
#249834=CARTESIAN_POINT('Ctrl Pts',(-1.70881537198541,2.73243440164455,
7.10644014792023));
#249835=CARTESIAN_POINT('Ctrl Pts',(-1.69913102574339,2.73846699841989,
7.10573662116968));
#249836=CARTESIAN_POINT('Ctrl Pts',(-1.67216217331049,2.75506835966679,
7.10379277510277));
#249837=CARTESIAN_POINT('Ctrl Pts',(-1.65480941242268,2.76552596376837,
7.10255938456042));
#249838=CARTESIAN_POINT('Ctrl Pts',(-1.5472301140943,2.82898322281394,7.09501193895917));
#249839=CARTESIAN_POINT('Ctrl Pts',(-1.45455628333657,2.8777313163928,7.0889354577235));
#249840=CARTESIAN_POINT('Ctrl Pts',(-1.23334877869778,2.98066762276816,
7.07502347487843));
#249841=CARTESIAN_POINT('Ctrl Pts',(-1.10334893106829,3.03119653588395,
7.06728303828353));
#249842=CARTESIAN_POINT('Ctrl Pts',(-0.7855903423067,3.13154274737149,7.04859510706689));
#249843=CARTESIAN_POINT('Ctrl Pts',(-0.595828782214898,3.17311950542628,
7.03759860876347));
#249844=CARTESIAN_POINT('Ctrl Pts',(-0.368973638569646,3.20174743709907,
7.02396100487141));
#249845=CARTESIAN_POINT('Ctrl Pts',(-0.334386019773027,3.20554426680463,
7.02186954228853));
#249846=CARTESIAN_POINT('Ctrl Pts',(-0.279484994904434,3.21067278565784,
7.01852742441718));
#249847=CARTESIAN_POINT('Ctrl Pts',(-0.259208212426221,3.21237337061352,
7.01728826463294));
#249848=CARTESIAN_POINT('Ctrl Pts',(-0.221259469102199,3.21519444553711,
7.0149595723535));
#249849=CARTESIAN_POINT('Ctrl Pts',(-0.203591666941271,3.216361529545,7.01387153568127));
#249850=CARTESIAN_POINT('Ctrl Pts',(-0.164011700420257,3.21864864491948,
7.01142504293399));
#249851=CARTESIAN_POINT('Ctrl Pts',(-0.142096074098543,3.21969060705654,
7.01006421003083));
#249852=CARTESIAN_POINT('Ctrl Pts',(-0.0767056934237409,3.2221306218554,
7.00598459602022));
#249853=CARTESIAN_POINT('Ctrl Pts',(-0.0332128620819631,3.22287233988978,
7.0032457069895));
#249854=CARTESIAN_POINT('Ctrl Pts',(0.173149674675503,3.22221407476818,
6.99012421587993));
#249855=CARTESIAN_POINT('Ctrl Pts',(0.335723127776088,3.20934904401457,
6.97939698001102));
#249856=CARTESIAN_POINT('Ctrl Pts',(0.664433778654918,3.1580841704323,6.95707273266367));
#249857=CARTESIAN_POINT('Ctrl Pts',(0.82992438424521,3.11868449703209,6.94549285844709));
#249858=CARTESIAN_POINT('Ctrl Pts',(1.07813899885514,3.03842356006187,6.92810418100185));
#249859=CARTESIAN_POINT('Ctrl Pts',(1.16352308682281,3.00676212580583,6.92212285788626));
#249860=CARTESIAN_POINT('Ctrl Pts',(1.26595478943538,2.96376085570955,6.9150379533545));
#249861=CARTESIAN_POINT('Ctrl Pts',(1.28437806163169,2.9558235705828,6.91376738323969));
#249862=CARTESIAN_POINT('Ctrl Pts',(1.31322965751872,2.94307276339479,6.91178483703123));
#249863=CARTESIAN_POINT('Ctrl Pts',(1.32370807210394,2.9383747843607,6.91106632028839));
#249864=CARTESIAN_POINT('Ctrl Pts',(1.34236283952437,2.92989091031711,6.90979013728379));
#249865=CARTESIAN_POINT('Ctrl Pts',(1.35054847642814,2.92612671538305,6.90923121645568));
#249866=CARTESIAN_POINT('Ctrl Pts',(1.37034119335466,2.9169242130583,6.90788220507077));
#249867=CARTESIAN_POINT('Ctrl Pts',(1.38193174731057,2.91145092858595,6.90709424875949));
#249868=CARTESIAN_POINT('Ctrl Pts',(1.41801548519087,2.89414745477862,6.90464656426738));
#249869=CARTESIAN_POINT('Ctrl Pts',(1.44239244008304,2.88207591237268,6.90300077599895));
#249870=CARTESIAN_POINT('Ctrl Pts',(1.56763469040185,2.81806841600179,6.89457076032574));
#249871=CARTESIAN_POINT('Ctrl Pts',(1.6658685108344,2.76113658404077,6.88804401156089));
#249872=CARTESIAN_POINT('Ctrl Pts',(1.76545001935222,2.69617011079135,6.88130898670823));
#249873=CARTESIAN_POINT('Ctrl Pts',(1.76998950273728,2.69319219470912,6.88100170212606));
#249874=CARTESIAN_POINT('Ctrl Pts',(1.94779231388993,2.57590925209789,6.86895475172678));
#249875=CARTESIAN_POINT('Ctrl Pts',(2.1096127577566,2.44514584111433,6.85753718341984));
#249876=CARTESIAN_POINT('Ctrl Pts',(2.33393448848163,2.22492020141764,6.83952796465508));
#249877=CARTESIAN_POINT('Ctrl Pts',(2.40636218236888,2.14637785044955,6.83330355665445));
#249878=CARTESIAN_POINT('Ctrl Pts',(2.49501186551378,2.04010624454021,6.82502407177305));
#249879=CARTESIAN_POINT('Ctrl Pts',(2.51491065990404,2.01552523288682,6.82311849188951));
#249880=CARTESIAN_POINT('Ctrl Pts',(2.54646872729053,1.97534644067041,6.82001663800918));
#249881=CARTESIAN_POINT('Ctrl Pts',(2.55835430474045,1.95992851027221,6.81882935200126));
#249882=CARTESIAN_POINT('Ctrl Pts',(2.58088100562111,1.93015288007785,6.81654162384857));
#249883=CARTESIAN_POINT('Ctrl Pts',(2.59154384516465,1.91581246053714,6.81544208642551));
#249884=CARTESIAN_POINT('Ctrl Pts',(2.61592592647397,1.88244504047772,6.81288848908343));
#249885=CARTESIAN_POINT('Ctrl Pts',(2.62955766319016,1.86335563778055,6.81143114692731));
#249886=CARTESIAN_POINT('Ctrl Pts',(2.6725251758865,1.80177489167004,6.8067402298617));
#249887=CARTESIAN_POINT('Ctrl Pts',(2.70104747157817,1.75872841634368,6.80347654566614));
#249888=CARTESIAN_POINT('Ctrl Pts',(2.87746594039411,1.47805386410286,6.78228333501577));
#249889=CARTESIAN_POINT('Ctrl Pts',(2.9948852858588,1.22272705100825,6.76324518793915));
#249890=CARTESIAN_POINT('Ctrl Pts',(3.11616109469286,0.83208319320178,6.73571935017519));
#249891=CARTESIAN_POINT('Ctrl Pts',(3.14702579791309,0.706440375824682,
6.72711694127453));
#249892=CARTESIAN_POINT('Ctrl Pts',(3.17411031207386,0.558211110288434,
6.71749158113461));
#249893=CARTESIAN_POINT('Ctrl Pts',(3.17774866245485,0.537112103405677,
6.71613379105527));
#249894=CARTESIAN_POINT('Ctrl Pts',(3.18306361112129,0.504343656094835,
6.71404567417669));
#249895=CARTESIAN_POINT('Ctrl Pts',(3.18488682955874,0.492699065371516,
6.71330766891566));
#249896=CARTESIAN_POINT('Ctrl Pts',(3.18813397148161,0.471188598342148,
6.71195214400059));
#249897=CARTESIAN_POINT('Ctrl Pts',(3.18957602125016,0.461326049453632,
6.71133367462751));
#249898=CARTESIAN_POINT('Ctrl Pts',(3.192785759684,0.438639067559258,6.70991784316439));
#249899=CARTESIAN_POINT('Ctrl Pts',(3.19452195983252,0.425810521480139,
6.70912222901144));
#249900=CARTESIAN_POINT('Ctrl Pts',(3.1997537213394,0.385319467081328,6.70662572376869));
#249901=CARTESIAN_POINT('Ctrl Pts',(3.20296772631286,0.357621071460053,
6.70493957857703));
#249902=CARTESIAN_POINT('Ctrl Pts',(3.21806136541277,0.210940404891598,
6.69610811044508));
#249903=CARTESIAN_POINT('Ctrl Pts',(3.22367294941302,0.0913959533191167,
6.68924816963208));
#249904=CARTESIAN_POINT('Ctrl Pts',(3.22007552636798,-0.319790651449177,
6.66600197014875));
#249905=CARTESIAN_POINT('Ctrl Pts',(3.17796370029111,-0.609667990583178,
6.65008176197737));
#249906=CARTESIAN_POINT('Ctrl Pts',(3.08548983642161,-0.931527342351729,
6.63023873720678));
#249907=CARTESIAN_POINT('Ctrl Pts',(3.07270221924298,-0.972877961567803,
6.62764986328819));
#249908=CARTESIAN_POINT('Ctrl Pts',(3.05210698965571,-1.03501331324056,
6.62369354040752));
#249909=CARTESIAN_POINT('Ctrl Pts',(3.0449106851032,-1.05599645685755,6.62234593721242));
#249910=CARTESIAN_POINT('Ctrl Pts',(3.03157556804165,-1.09360930455246,
6.61990871314423));
#249911=CARTESIAN_POINT('Ctrl Pts',(3.02551503695888,-1.11026594886001,
6.61882170576858));
#249912=CARTESIAN_POINT('Ctrl Pts',(3.01226223381168,-1.14577525113013,
6.61648749010996));
#249913=CARTESIAN_POINT('Ctrl Pts',(3.00502971663756,-1.16461198004802,
6.6152389831758));
#249914=CARTESIAN_POINT('Ctrl Pts',(2.98479607243098,-1.21586587592183,
6.61181312038411));
#249915=CARTESIAN_POINT('Ctrl Pts',(2.971444383829,-1.248140834654,6.60962416222343));
#249916=CARTESIAN_POINT('Ctrl Pts',(2.88047405663126,-1.45830566659103,
6.59515644053076));
#249917=CARTESIAN_POINT('Ctrl Pts',(2.78745774375217,-1.629062067312,6.58235105442465));
#249918=CARTESIAN_POINT('Ctrl Pts',(2.56991516257729,-1.9546564267444,6.55600107273));
#249919=CARTESIAN_POINT('Ctrl Pts',(2.44529027770861,-2.10848423433274,
6.54250614681055));
#249920=CARTESIAN_POINT('Ctrl Pts',(2.27049269015021,-2.28774326783346,
6.52610215632516));
#249921=CARTESIAN_POINT('Ctrl Pts',(2.23269861233805,-2.32464275490054,
6.52268600639115));
#249922=CARTESIAN_POINT('Ctrl Pts',(2.18150253628502,-2.37222594434649,
6.51824718474363));
#249923=CARTESIAN_POINT('Ctrl Pts',(2.16890013718429,-2.38375365157204,
6.51716910344834));
#249924=CARTESIAN_POINT('Ctrl Pts',(2.14824446049359,-2.40234844809482,
6.51542651682457));
#249925=CARTESIAN_POINT('Ctrl Pts',(2.14024671933528,-2.40947635727887,
6.51475766014646));
#249926=CARTESIAN_POINT('Ctrl Pts',(2.12446539479925,-2.42340073387847,
6.51344958346601));
#249927=CARTESIAN_POINT('Ctrl Pts',(2.11668444445044,-2.43019984718989,
6.51281018557082));
#249928=CARTESIAN_POINT('Ctrl Pts',(2.09730245005747,-2.4469724236332,6.51123079472882));
#249929=CARTESIAN_POINT('Ctrl Pts',(2.0856626534697,-2.4569010819002,6.51029401486487));
#249930=CARTESIAN_POINT('Ctrl Pts',(2.04124141690142,-2.49424886762088,
6.50676119509746));
#249931=CARTESIAN_POINT('Ctrl Pts',(2.00798491934538,-2.52109914332094,
6.50420265035953));
#249932=CARTESIAN_POINT('Ctrl Pts',(1.91978253991394,-2.58945804374075,
6.4976096477115));
#249933=CARTESIAN_POINT('Ctrl Pts',(1.86402174777053,-2.62988250526622,
6.49363002391463));
#249934=CARTESIAN_POINT('Ctrl Pts',(1.69026934368923,-2.74754132208565,
6.48165256698351));
#249935=CARTESIAN_POINT('Ctrl Pts',(1.56846774853541,-2.81884826405065,
6.47382015761052));
#249936=CARTESIAN_POINT('Ctrl Pts',(1.26794867288633,-2.96925468139527,
6.45497577567945));
#249937=CARTESIAN_POINT('Ctrl Pts',(1.08596934518146,-3.04053035076556,
6.44391673140866));
#249938=CARTESIAN_POINT('Ctrl Pts',(0.865283068253194,-3.10461138461063,
6.43021044176989));
#249939=CARTESIAN_POINT('Ctrl Pts',(0.831736859943135,-3.11376625543214,
6.42812029691482));
#249940=CARTESIAN_POINT('Ctrl Pts',(0.778340758447474,-3.12741379707448,
6.42477981277982));
#249941=CARTESIAN_POINT('Ctrl Pts',(0.758584589860587,-3.13226448198665,
6.42354094962034));
#249942=CARTESIAN_POINT('Ctrl Pts',(0.721548928330557,-3.14098682522939,
6.42121252058057));
#249943=CARTESIAN_POINT('Ctrl Pts',(0.704280808700624,-3.14490375290543,
6.42012444732169));
#249944=CARTESIAN_POINT('Ctrl Pts',(0.665538857599904,-3.15335650824511,
6.41767748441787));
#249945=CARTESIAN_POINT('Ctrl Pts',(0.644049365521355,-3.15781563995248,
6.41631621384987));
#249946=CARTESIAN_POINT('Ctrl Pts',(0.579804714302836,-3.17046353891684,
6.41223394590117));
#249947=CARTESIAN_POINT('Ctrl Pts',(0.536928788786448,-3.17800562289104,
6.40949280155574));
#249948=CARTESIAN_POINT('Ctrl Pts',(0.332690613915168,-3.20968113667216,
6.39635087698163));
#249949=CARTESIAN_POINT('Ctrl Pts',(0.169822668895752,-3.22240332598583,
6.38560421312784));
#249950=CARTESIAN_POINT('Ctrl Pts',(-0.163756445318266,-3.22309801782482,
6.36321845845729));
#249951=CARTESIAN_POINT('Ctrl Pts',(-0.333981225130233,-3.20992729097151,
6.35159596295352));
#249952=CARTESIAN_POINT('Ctrl Pts',(-0.591409786316228,-3.16930252761697,
6.33422929634166));
#249953=CARTESIAN_POINT('Ctrl Pts',(-0.679834515013803,-3.15151900362662,
6.32830692119331));
#249954=CARTESIAN_POINT('Ctrl Pts',(-0.786842538724266,-3.12528349678802,
6.32128072960539));
#249955=CARTESIAN_POINT('Ctrl Pts',(-0.806236439989325,-3.12033667501667,
6.32001309632444));
#249956=CARTESIAN_POINT('Ctrl Pts',(-0.836673498853508,-3.11227033587859,
6.31803411347751));
#249957=CARTESIAN_POINT('Ctrl Pts',(-0.847747872473475,-3.1092720597373,
6.31731626027007));
#249958=CARTESIAN_POINT('Ctrl Pts',(-0.867492042521257,-3.10381319180374,
6.31604062939932));
#249959=CARTESIAN_POINT('Ctrl Pts',(-0.87616757975041,-3.10137536392791,
6.31548160408613));
#249960=CARTESIAN_POINT('Ctrl Pts',(-0.897173176305563,-3.0953776096944,
6.31413153394572));
#249961=CARTESIAN_POINT('Ctrl Pts',(-0.909492338238396,-3.09178038587292,
6.31334263270765));
#249962=CARTESIAN_POINT('Ctrl Pts',(-0.947933725905005,-3.08030576599116,
6.31088895709953));
#249963=CARTESIAN_POINT('Ctrl Pts',(-0.973978348481327,-3.072169957538,
6.30923822031145));
#249964=CARTESIAN_POINT('Ctrl Pts',(-1.10846881845805,-3.0282755845197,
6.3007597119694));
#249965=CARTESIAN_POINT('Ctrl Pts',(-1.21507163760882,-2.98709928602528,
6.29419271233494));
#249966=CARTESIAN_POINT('Ctrl Pts',(-1.57902898757241,-2.82379915637499,
6.27160206127704));
#249967=CARTESIAN_POINT('Ctrl Pts',(-1.82218061619398,-2.67335576162192,
6.25607856667965));
#249968=CARTESIAN_POINT('Ctrl Pts',(-2.07896240590237,-2.46297905215695,
6.23652182583848));
#249969=CARTESIAN_POINT('Ctrl Pts',(-2.11485067051489,-2.43223288429633,
6.23370983321367));
#249970=CARTESIAN_POINT('Ctrl Pts',(-2.16915404099555,-2.38359939847418,
6.22932278716067));
#249971=CARTESIAN_POINT('Ctrl Pts',(-2.18805400213912,-2.36626181391754,
6.22777019616485));
#249972=CARTESIAN_POINT('Ctrl Pts',(-2.21990009643659,-2.33634050805216,
6.22510866133825));
#249973=CARTESIAN_POINT('Ctrl Pts',(-2.23295128327971,-2.32387003800486,
6.22400455008015));
#249974=CARTESIAN_POINT('Ctrl Pts',(-2.25781587823742,-2.29970894364226,
6.22187479444982));
#249975=CARTESIAN_POINT('Ctrl Pts',(-2.26964499380194,-2.28803526004887,
6.22084990319165));
#249976=CARTESIAN_POINT('Ctrl Pts',(-2.29731962633682,-2.26029847227512,
6.21842408318191));
#249977=CARTESIAN_POINT('Ctrl Pts',(-2.31308762715854,-2.24415958370711,
6.21701983521302));
#249978=CARTESIAN_POINT('Ctrl Pts',(-2.36871986864714,-2.18600955240233,
6.21198481231834));
#249979=CARTESIAN_POINT('Ctrl Pts',(-2.40761768514765,-2.1430930856171,
6.20831358679803));
#249980=CARTESIAN_POINT('Ctrl Pts',(-2.49971248225722,-2.0358104658504,
6.19923828357681));
#249981=CARTESIAN_POINT('Ctrl Pts',(-2.55160298927834,-1.97038247925033,
6.19378772811086));
#249982=CARTESIAN_POINT('Ctrl Pts',(-2.6928149508659,-1.77738533314449,
6.1779649041189));
#249983=CARTESIAN_POINT('Ctrl Pts',(-2.77550933578156,-1.64526389469577,
6.16742353444825));
#249984=CARTESIAN_POINT('Ctrl Pts',(-2.91730192578725,-1.37739019448851,
6.14695400670735));
#249985=CARTESIAN_POINT('Ctrl Pts',(-2.9772592161,-1.24249337954665,6.1370493421721));
#249986=CARTESIAN_POINT('Ctrl Pts',(-3.03795118879321,-1.07603586388396,
6.12563939903445));
#249987=CARTESIAN_POINT('Ctrl Pts',(-3.047744226582,-1.04797704146004,6.12374313096452));
#249988=CARTESIAN_POINT('Ctrl Pts',(-3.06130523570215,-1.00732338702539,
6.1210384806562));
#249989=CARTESIAN_POINT('Ctrl Pts',(-3.06538617129397,-0.994835557741038,
6.12021345088048));
#249990=CARTESIAN_POINT('Ctrl Pts',(-3.0724417050406,-0.972789659871621,
6.11876753570489));
#249991=CARTESIAN_POINT('Ctrl Pts',(-3.07544830106975,-0.963242186992404,
6.11814484719697));
#249992=CARTESIAN_POINT('Ctrl Pts',(-3.08181666335691,-0.942685581572961,
6.11681175580627));
#249993=CARTESIAN_POINT('Ctrl Pts',(-3.0851639741898,-0.931672321204153,
6.11610217561669));
#249994=CARTESIAN_POINT('Ctrl Pts',(-3.09437385812005,-0.900776150222252,
6.11412387401025));
#249995=CARTESIAN_POINT('Ctrl Pts',(-3.10010382781171,-0.880853877806726,
6.11286248755346));
#249996=CARTESIAN_POINT('Ctrl Pts',(-3.13669814305368,-0.74883873285409,
6.10458936781926));
#249997=CARTESIAN_POINT('Ctrl Pts',(-3.16167282775681,-0.635189267223042,
6.09787156647126));
#249998=CARTESIAN_POINT('Ctrl Pts',(-3.20846359115117,-0.34924018308778,
6.08142006333233));
#249999=CARTESIAN_POINT('Ctrl Pts',(-3.22260828707642,-0.176074090493909,
6.07184374685539));
#250000=CARTESIAN_POINT('Ctrl Pts',(-3.22274894051683,-0.00261321596174632,
6.06203802249303));
#250001=CARTESIAN_POINT('Ctrl Pts',(-3.22274894300508,-0.00261014551656878,
6.06203784892107));
#250002=CARTESIAN_POINT('Ctrl Pts',(-3.22274964767178,-0.00174009292913683,
6.06198866493141));
#250003=CARTESIAN_POINT('Ctrl Pts',(-3.22275,-0.000870044343129958,6.06193947624883));
#250004=CARTESIAN_POINT('Ctrl Pts',(-3.22275,2.79355756999193E-11,6.06189028282397));
#250005=CARTESIAN_POINT('Ctrl Pts',(-3.22275,-2.46480457644168E-12,5.81181920673623));
#250006=CARTESIAN_POINT('Ctrl Pts',(-3.22274999999997,-0.0434837801921187,
5.81436133457606));
#250007=CARTESIAN_POINT('Ctrl Pts',(-3.22186992859092,-0.0869620681209187,
5.81692596223994));
#250008=CARTESIAN_POINT('Ctrl Pts',(-3.21876213012256,-0.16370143329292,
5.8215013348071));
#250009=CARTESIAN_POINT('Ctrl Pts',(-3.21689761344425,-0.196970637444475,
5.8235011317141));
#250010=CARTESIAN_POINT('Ctrl Pts',(-3.2132447692424,-0.247978130235755,
5.82659471663913));
#250011=CARTESIAN_POINT('Ctrl Pts',(-3.21182452403085,-0.265741053369173,
5.82767716406584));
#250012=CARTESIAN_POINT('Ctrl Pts',(-3.20872449272806,-0.300845860292135,
5.82982699177066));
#250013=CARTESIAN_POINT('Ctrl Pts',(-3.2070512404925,-0.318187718373057,
5.8308941344599));
#250014=CARTESIAN_POINT('Ctrl Pts',(-3.20318487296555,-0.355123861307938,
5.83317832567699));
#250015=CARTESIAN_POINT('Ctrl Pts',(-3.20095239888262,-0.3747132236896,
5.83439656018849));
#250016=CARTESIAN_POINT('Ctrl Pts',(-3.19469099110278,-0.425507934445638,
5.83757361289999));
#250017=CARTESIAN_POINT('Ctrl Pts',(-3.19038463378829,-0.456676370873758,
5.83954099701342));
#250018=CARTESIAN_POINT('Ctrl Pts',(-3.16995062350541,-0.590129144996906,
5.84804415735175));
#250019=CARTESIAN_POINT('Ctrl Pts',(-3.14935635711355,-0.691657541877878,
5.85471705432241));
#250020=CARTESIAN_POINT('Ctrl Pts',(-3.07551957797401,-0.982890686845009,
5.87444655537153));
#250021=CARTESIAN_POINT('Ctrl Pts',(-3.00973527357927,-1.16892070316436,
5.88781763692185));
#250022=CARTESIAN_POINT('Ctrl Pts',(-2.87312121358051,-1.46565190533348,
5.90983649590704));
#250023=CARTESIAN_POINT('Ctrl Pts',(-2.81176894529414,-1.58016537397906,
5.91851154516345));
#250024=CARTESIAN_POINT('Ctrl Pts',(-2.72834464461649,-1.71554850246875,
5.92874739559476));
#250025=CARTESIAN_POINT('Ctrl Pts',(-2.71267934469497,-1.74021322663474,
5.93061111494307));
#250026=CARTESIAN_POINT('Ctrl Pts',(-2.68936369435831,-1.77584318601964,
5.93329795252256));
#250027=CARTESIAN_POINT('Ctrl Pts',(-2.68197760228885,-1.78697852738216,
5.93413687445286));
#250028=CARTESIAN_POINT('Ctrl Pts',(-2.6688803407211,-1.80645994943347,
5.93560273587624));
#250029=CARTESIAN_POINT('Ctrl Pts',(-2.66319886825772,-1.8148255067094,
5.9362315691915));
#250030=CARTESIAN_POINT('Ctrl Pts',(-2.65071542092706,-1.83302160717609,
5.93759791271207));
#250031=CARTESIAN_POINT('Ctrl Pts',(-2.64389805461189,-1.84284116040986,
5.93833438745232));
#250032=CARTESIAN_POINT('Ctrl Pts',(-2.62468625090145,-1.87018727170844,
5.94038359910477));
#250033=CARTESIAN_POINT('Ctrl Pts',(-2.61217086321912,-1.88762861389349,
5.94168853702127));
#250034=CARTESIAN_POINT('Ctrl Pts',(-2.52875214648964,-2.00146157631271,
5.95020111930038));
#250035=CARTESIAN_POINT('Ctrl Pts',(-2.45269395925307,-2.09397572825346,
5.95710078863815));
#250036=CARTESIAN_POINT('Ctrl Pts',(-2.33744502524973,-2.2192389766148,
5.96675188708547));
#250037=CARTESIAN_POINT('Ctrl Pts',(-2.30236158104117,-2.25561570424696,
5.96959502134017));
#250038=CARTESIAN_POINT('Ctrl Pts',(-2.17101005743024,-2.38555024846243,
5.97996112729002));
#250039=CARTESIAN_POINT('Ctrl Pts',(-2.06977974434252,-2.47389280448074,
5.98743089631052));
#250040=CARTESIAN_POINT('Ctrl Pts',(-1.8923612162319,-2.61019110226427,
6.00013383179475));
#250041=CARTESIAN_POINT('Ctrl Pts',(-1.81914719874243,-2.66173447535921,
6.00527579280438));
#250042=CARTESIAN_POINT('Ctrl Pts',(-1.69217285180737,-2.74343765765416,
6.01412222473061));
#250043=CARTESIAN_POINT('Ctrl Pts',(-1.6395200852128,-2.77522473155901,
6.01777084062713));
#250044=CARTESIAN_POINT('Ctrl Pts',(-1.56386350641135,-2.81799480037799,
6.02300387363359));
#250045=CARTESIAN_POINT('Ctrl Pts',(-1.54158762781295,-2.83024226723834,
6.0245434576738));
#250046=CARTESIAN_POINT('Ctrl Pts',(-1.50285447117774,-2.85094514736221,
6.02721957242242));
#250047=CARTESIAN_POINT('Ctrl Pts',(-1.48646476326562,-2.85952483467569,
6.02835167654317));
#250048=CARTESIAN_POINT('Ctrl Pts',(-1.45481789801272,-2.87574574470078,
6.03053753385242));
#250049=CARTESIAN_POINT('Ctrl Pts',(-1.43957210356486,-2.88340785278103,
6.03159051117639));
#250050=CARTESIAN_POINT('Ctrl Pts',(-1.39928962963657,-2.90325358030089,
6.03437291778503));
#250051=CARTESIAN_POINT('Ctrl Pts',(-1.37415507793311,-2.91523422103812,
6.03610926048347));
#250052=CARTESIAN_POINT('Ctrl Pts',(-1.28283947035231,-2.95731742446838,
6.04242001402605));
#250053=CARTESIAN_POINT('Ctrl Pts',(-1.21580365689693,-2.98550223324129,
6.04705813285214));
#250054=CARTESIAN_POINT('Ctrl Pts',(-0.929681320955207,-3.09456566158678,
6.06688466627563));
#250055=CARTESIAN_POINT('Ctrl Pts',(-0.703115906473292,-3.15376672359909,
6.08272465723729));
#250056=CARTESIAN_POINT('Ctrl Pts',(-0.342117300404767,-3.20723589531851,
6.107328791496));
#250057=CARTESIAN_POINT('Ctrl Pts',(-0.210979787273408,-3.21852454018246,
6.11612254515036));
#250058=CARTESIAN_POINT('Ctrl Pts',(-0.0501263333765563,-3.22249418519377,
6.12648104944104));
#250059=CARTESIAN_POINT('Ctrl Pts',(-0.0207340267677778,-3.22281734861643,
6.12835616498684));
#250060=CARTESIAN_POINT('Ctrl Pts',(0.0220534536508843,-3.22270237541045,
6.1310562359189));
#250061=CARTESIAN_POINT('Ctrl Pts',(0.0354470871757176,-3.22258288862273,
6.13189720693695));
#250062=CARTESIAN_POINT('Ctrl Pts',(0.0590457762746158,-3.22222521613324,
6.13337104162845));
#250063=CARTESIAN_POINT('Ctrl Pts',(0.0692509535850956,-3.22202204563668,
6.13400577041875));
#250064=CARTESIAN_POINT('Ctrl Pts',(0.0914227474266566,-3.22147524398119,
6.1353789986524));
#250065=CARTESIAN_POINT('Ctrl Pts',(0.103388550565497,-3.22111342311192,
6.13611650251022));
#250066=CARTESIAN_POINT('Ctrl Pts',(0.136881351187679,-3.21991384258314,
6.13817139368808));
#250067=CARTESIAN_POINT('Ctrl Pts',(0.158402803307684,-3.21892688114299,
6.13948091300208));
#250068=CARTESIAN_POINT('Ctrl Pts',(0.302342682603505,-3.21087873596547,
6.1481759156007));
#250069=CARTESIAN_POINT('Ctrl Pts',(0.424295494991865,-3.19705070855505,
6.15523774563957));
#250070=CARTESIAN_POINT('Ctrl Pts',(0.592610254043079,-3.16816145914844,
6.16491185220941));
#250071=CARTESIAN_POINT('Ctrl Pts',(0.639857846724015,-3.15895806007848,
6.16761914093297));
#250072=CARTESIAN_POINT('Ctrl Pts',(0.83250807587018,-3.11693181681067,
6.17868123678252));
#250073=CARTESIAN_POINT('Ctrl Pts',(0.975753039941638,-3.07509970124007,
6.18697016357154));
#250074=CARTESIAN_POINT('Ctrl Pts',(1.19105815897809,-2.99565850149194,
6.20005808361595));
#250075=CARTESIAN_POINT('Ctrl Pts',(1.26545890642882,-2.96499610419253,
6.20470069680824));
#250076=CARTESIAN_POINT('Ctrl Pts',(1.39041368338942,-2.9079387641284,6.2127707496896));
#250077=CARTESIAN_POINT('Ctrl Pts',(1.44155796667899,-2.88292700501812,
6.21615496389612));
#250078=CARTESIAN_POINT('Ctrl Pts',(1.51388736643585,-2.84514880851099,
6.22107267326997));
#250079=CARTESIAN_POINT('Ctrl Pts',(1.53563136380337,-2.83347189218761,
6.22256852240006));
#250080=CARTESIAN_POINT('Ctrl Pts',(1.5733280835242,-2.81266671094163,6.22519352312719));
#250081=CARTESIAN_POINT('Ctrl Pts',(1.58934100165527,-2.80364948662779,
6.22631871622271));
#250082=CARTESIAN_POINT('Ctrl Pts',(1.62023165496409,-2.7859045998588,6.22850948314495));
#250083=CARTESIAN_POINT('Ctrl Pts',(1.63511819422471,-2.77719346245137,
6.22957443754758));
#250084=CARTESIAN_POINT('Ctrl Pts',(1.67471534581362,-2.75359371328175,
6.23243222437584));
#250085=CARTESIAN_POINT('Ctrl Pts',(1.69929672151833,-2.73849235774925,
6.2342326941016));
#250086=CARTESIAN_POINT('Ctrl Pts',(1.79107630691541,-2.68039681418366,
6.24105714501779));
#250087=CARTESIAN_POINT('Ctrl Pts',(1.85686860321058,-2.6352454634842,6.24615917039027));
#250088=CARTESIAN_POINT('Ctrl Pts',(2.10309270887033,-2.45246740354339,
6.26608576567545));
#250089=CARTESIAN_POINT('Ctrl Pts',(2.27046339344333,-2.29838367772893,
6.28148897922877));
#250090=CARTESIAN_POINT('Ctrl Pts',(2.50553693557324,-2.03103084639467,
6.30548281140622));
#250091=CARTESIAN_POINT('Ctrl Pts',(2.58492722075026,-1.92897875492472,
6.31411501697992));
#250092=CARTESIAN_POINT('Ctrl Pts',(2.67446859591214,-1.79838404641024,
6.32430655114676));
#250093=CARTESIAN_POINT('Ctrl Pts',(2.69062783703285,-1.77411652035588,
6.32616612690197));
#250094=CARTESIAN_POINT('Ctrl Pts',(2.71370402399587,-1.73842062268418,
6.3288481505682));
#250095=CARTESIAN_POINT('Ctrl Pts',(2.72088228435699,-1.72716397614703,
6.32968632543366));
#250096=CARTESIAN_POINT('Ctrl Pts',(2.73337396831992,-1.70730388290779,
6.33115136684133));
#250097=CARTESIAN_POINT('Ctrl Pts',(2.73871712178513,-1.69871961658833,
6.33178011983613));
#250098=CARTESIAN_POINT('Ctrl Pts',(2.75029307720659,-1.67992518684091,
6.3331468611566));
#250099=CARTESIAN_POINT('Ctrl Pts',(2.75650950877249,-1.66970535800357,
6.33388380856446));
#250100=CARTESIAN_POINT('Ctrl Pts',(2.77374037667783,-1.64101925293855,
6.3359356281472));
#250101=CARTESIAN_POINT('Ctrl Pts',(2.78462734645388,-1.62247664484869,
6.33724266967249));
#250102=CARTESIAN_POINT('Ctrl Pts',(2.8555545724189,-1.4988566951796,6.34583906152488));
#250103=CARTESIAN_POINT('Ctrl Pts',(2.90982722216481,-1.39056649427554,
6.35281327951319));
#250104=CARTESIAN_POINT('Ctrl Pts',(2.97753217432288,-1.23404580301658,
6.36247851978687));
#250105=CARTESIAN_POINT('Ctrl Pts',(2.99613195870388,-1.1881752141994,6.36526278766254));
#250106=CARTESIAN_POINT('Ctrl Pts',(3.06161652968979,-1.01534935859894,
6.37563158174329));
#250107=CARTESIAN_POINT('Ctrl Pts',(3.10154639574376,-0.885911472376493,
6.38316223198478));
#250108=CARTESIAN_POINT('Ctrl Pts',(3.1539661248722,-0.668184252813939,
6.39588272071658));
#250109=CARTESIAN_POINT('Ctrl Pts',(3.17114689989669,-0.581204157903485,
6.40097651612725));
#250110=CARTESIAN_POINT('Ctrl Pts',(3.19407378258385,-0.433288461617131,
6.40974853126948));
#250111=CARTESIAN_POINT('Ctrl Pts',(3.20170944303909,-0.372695793936298,
6.41337219167467));
#250112=CARTESIAN_POINT('Ctrl Pts',(3.21007288546623,-0.28669213038376,
6.41857554178521));
#250113=CARTESIAN_POINT('Ctrl Pts',(3.2122288153374,-0.261431233461784,
6.42011110406467));
#250114=CARTESIAN_POINT('Ctrl Pts',(3.21544114280908,-0.217709942757812,
6.42278248875917));
#250115=CARTESIAN_POINT('Ctrl Pts',(3.21663713654521,-0.199260813090744,
6.42391392802023));
#250116=CARTESIAN_POINT('Ctrl Pts',(3.21876213748401,-0.161443011757707,
6.42624221872893));
#250117=CARTESIAN_POINT('Ctrl Pts',(3.21967520556881,-0.142074235520886,
6.42743951729091));
#250118=CARTESIAN_POINT('Ctrl Pts',(3.22155310608351,-0.0927859004338243,
6.4304991420596));
#250119=CARTESIAN_POINT('Ctrl Pts',(3.22227593910218,-0.0628594839236813,
6.43236887683812));
#250120=CARTESIAN_POINT('Ctrl Pts',(3.22348939228392,0.0558977309461934,
6.43983834612798));
#250121=CARTESIAN_POINT('Ctrl Pts',(3.22072405111211,0.144715592496733,
6.44553668549827));
#250122=CARTESIAN_POINT('Ctrl Pts',(3.19845322814192,0.45155282828387,6.46561259437435));
#250123=CARTESIAN_POINT('Ctrl Pts',(3.16042462564723,0.667607318405048,
6.48048139666669));
#250124=CARTESIAN_POINT('Ctrl Pts',(3.06640012289486,0.999629187325682,
6.50372882837039));
#250125=CARTESIAN_POINT('Ctrl Pts',(3.02487108279783,1.11903039912414,6.51216134606523));
#250126=CARTESIAN_POINT('Ctrl Pts',(2.96537368340655,1.26234264883259,6.5221459944541));
#250127=CARTESIAN_POINT('Ctrl Pts',(2.95395289252483,1.2888415288211,6.52398604136861));
#250128=CARTESIAN_POINT('Ctrl Pts',(2.93675162662851,1.32732219459556,6.5266453600994));
#250129=CARTESIAN_POINT('Ctrl Pts',(2.93125076900897,1.33942646994399,6.52747999941842));
#250130=CARTESIAN_POINT('Ctrl Pts',(2.9213982755777,1.36075482119124,6.52894692900998));
#250131=CARTESIAN_POINT('Ctrl Pts',(2.91707756644868,1.36999271855508,6.52958102155058));
#250132=CARTESIAN_POINT('Ctrl Pts',(2.90756054367352,1.39009143299319,6.53095775282469));
#250133=CARTESIAN_POINT('Ctrl Pts',(2.90234716864195,1.40094376427632,6.53169934901541));
#250134=CARTESIAN_POINT('Ctrl Pts',(2.88750137806793,1.43140866704053,6.53377687735812));
#250135=CARTESIAN_POINT('Ctrl Pts',(2.87772995098887,1.45095326189195,6.53510466369191));
#250136=CARTESIAN_POINT('Ctrl Pts',(2.8050358134513,1.59273080602215,6.54471045131479));
#250137=CARTESIAN_POINT('Ctrl Pts',(2.73454022203084,1.71094005118563,6.55258027867703));
#250138=CARTESIAN_POINT('Ctrl Pts',(2.63740694746517,1.85239410447137,6.56226186750096));
#250139=CARTESIAN_POINT('Ctrl Pts',(2.61766799416713,1.88018446980692,6.56417729415332));
#250140=CARTESIAN_POINT('Ctrl Pts',(2.51324224686741,2.02237200984046,6.57407284824353));
#250141=CARTESIAN_POINT('Ctrl Pts',(2.42148669302438,2.1313789139507,6.58199212384508));
#250142=CARTESIAN_POINT('Ctrl Pts',(2.26491028046179,2.2941840468394,6.59485350485533));
#250143=CARTESIAN_POINT('Ctrl Pts',(2.20467428323837,2.35212859985901,6.59966780867515));
#250144=CARTESIAN_POINT('Ctrl Pts',(2.09853868242801,2.44656442915691,6.6080060323586));
#250145=CARTESIAN_POINT('Ctrl Pts',(2.05377039497085,2.48426420610363,6.6114825839729));
#250146=CARTESIAN_POINT('Ctrl Pts',(1.98849235441949,2.53626455946217,6.61651062712068));
#250147=CARTESIAN_POINT('Ctrl Pts',(1.96880277933712,2.55157898606136,6.61802203505817));
#250148=CARTESIAN_POINT('Ctrl Pts',(1.93426822706409,2.57780202176966,6.6206651339773));
#250149=CARTESIAN_POINT('Ctrl Pts',(1.91950364424909,2.58881489786488,6.62179270097019));
#250150=CARTESIAN_POINT('Ctrl Pts',(1.89078881511507,2.60985254332799,6.6239813667044));
#250151=CARTESIAN_POINT('Ctrl Pts',(1.87685119808133,2.6198935481183,6.62504178889267));
#250152=CARTESIAN_POINT('Ctrl Pts',(1.83960097242881,2.64627973721825,6.62787123654757));
#250153=CARTESIAN_POINT('Ctrl Pts',(1.81615131161926,2.66242793628292,6.62964762460616));
#250154=CARTESIAN_POINT('Ctrl Pts',(1.72846374160248,2.72111493460486,6.63627439661543));
#250155=CARTESIAN_POINT('Ctrl Pts',(1.66292479284379,2.76165402253906,6.64119711894708));
#250156=CARTESIAN_POINT('Ctrl Pts',(1.39669269527074,2.91341701566903,6.661083732319));
#250157=CARTESIAN_POINT('Ctrl Pts',(1.18584232505115,3.00541212417166,6.67665399107499));
#250158=CARTESIAN_POINT('Ctrl Pts',(0.842986879369213,3.11326285673778,
6.70088123684733));
#250159=CARTESIAN_POINT('Ctrl Pts',(0.716662166643344,3.14474705712447,
6.70957543827166));
#250160=CARTESIAN_POINT('Ctrl Pts',(0.560017428313409,3.1738546442395,6.71983109103602));
#250161=CARTESIAN_POINT('Ctrl Pts',(0.531192211306453,3.17880603292495,
6.72169665743349));
#250162=CARTESIAN_POINT('Ctrl Pts',(0.489098777384011,3.18544794750114,
6.72438564046118));
#250163=CARTESIAN_POINT('Ctrl Pts',(0.475881989485765,3.18744922893152,
6.72522489505407));
#250164=CARTESIAN_POINT('Ctrl Pts',(0.452644766912786,3.19082004305697,
6.72669112185593));
#250165=CARTESIAN_POINT('Ctrl Pts',(0.442629839432663,3.19222472065259,
6.72731999116825));
#250166=CARTESIAN_POINT('Ctrl Pts',(0.420765931408192,3.19518644250604,
6.72868615860354));
#250167=CARTESIAN_POINT('Ctrl Pts',(0.408914770192005,3.19672474459167,
6.7294224236821));
#250168=CARTESIAN_POINT('Ctrl Pts',(0.375768312520601,3.20083986628428,
6.73147047887866));
#250169=CARTESIAN_POINT('Ctrl Pts',(0.354455018187135,3.20327010568336,
6.73277448401887));
#250170=CARTESIAN_POINT('Ctrl Pts',(0.214699744145634,3.21779365496335,
6.74124993639423));
#250171=CARTESIAN_POINT('Ctrl Pts',(0.095676831531037,3.22352974226774,
6.74811655439362));
#250172=CARTESIAN_POINT('Ctrl Pts',(-0.0742990084174624,3.22229543520331,
6.75775616151764));
#250173=CARTESIAN_POINT('Ctrl Pts',(-0.125181119712875,3.22072011832756,
6.76062021632438));
#250174=CARTESIAN_POINT('Ctrl Pts',(-0.309122202453196,3.21065945419343,
6.77095613217079));
#250175=CARTESIAN_POINT('Ctrl Pts',(-0.441658104199968,3.19512565755485,
6.77837530234735));
#250176=CARTESIAN_POINT('Ctrl Pts',(-0.706553295066735,3.14727825321421,
6.79365419546302));
#250177=CARTESIAN_POINT('Ctrl Pts',(-0.838583848678587,3.11469886899691,
6.80150519680006));
#250178=CARTESIAN_POINT('Ctrl Pts',(-0.99963117863456,3.06397520352493,
6.81159575059794));
#250179=CARTESIAN_POINT('Ctrl Pts',(-1.03095153974753,3.05357910386917,
6.81358256137524));
#250180=CARTESIAN_POINT('Ctrl Pts',(-1.08103224392659,3.03609761094416,
6.8168014344336));
#250181=CARTESIAN_POINT('Ctrl Pts',(-1.09989619576528,3.0293147320911,6.81802357708241));
#250182=CARTESIAN_POINT('Ctrl Pts',(-1.1357992252247,3.01602558107791,6.82036875067955));
#250183=CARTESIAN_POINT('Ctrl Pts',(-1.15284880043982,3.00954976824428,
6.82149073693595));
#250184=CARTESIAN_POINT('Ctrl Pts',(-1.19157149238932,2.99446468648838,
6.82405839361698));
#250185=CARTESIAN_POINT('Ctrl Pts',(-1.21320777545681,2.98576426199977,
6.82550705510592));
#250186=CARTESIAN_POINT('Ctrl Pts',(-1.27975267672658,2.95816237099969,
6.83000689416161));
#250187=CARTESIAN_POINT('Ctrl Pts',(-1.32432685217871,2.93847741255057,
6.83308406440381));
#250188=CARTESIAN_POINT('Ctrl Pts',(-1.60257200150501,2.80798118934138,
6.85270280318403));
#250189=CARTESIAN_POINT('Ctrl Pts',(-1.82260555600264,2.67040444290543,
6.87017896088731));
#250190=CARTESIAN_POINT('Ctrl Pts',(-2.1426996812463,2.41211507541641,6.89793681740898));
#250191=CARTESIAN_POINT('Ctrl Pts',(-2.25464277211062,2.3078251317209,6.90817570944262));
#250192=CARTESIAN_POINT('Ctrl Pts',(-2.37375902490236,2.17987829365035,
6.91934544891933));
#250193=CARTESIAN_POINT('Ctrl Pts',(-2.38858076105836,2.16362734600826,
6.92074047507661));
#250194=CARTESIAN_POINT('Ctrl Pts',(-2.41118862081899,2.13832399002285,
6.92287464803779));
#250195=CARTESIAN_POINT('Ctrl Pts',(-2.41909244815879,2.12937826356613,
6.92362198499067));
#250196=CARTESIAN_POINT('Ctrl Pts',(-2.43366557436497,2.11269820921734,
6.92500186392206));
#250197=CARTESIAN_POINT('Ctrl Pts',(-2.44034785531494,2.1049760568126,6.92563531396071));
#250198=CARTESIAN_POINT('Ctrl Pts',(-2.45559576764542,2.0871851196157,6.92708259997092));
#250199=CARTESIAN_POINT('Ctrl Pts',(-2.46413627394468,2.07709526383945,
6.92789463611117));
#250200=CARTESIAN_POINT('Ctrl Pts',(-2.49134864031281,2.04454217871398,
6.93048758337708));
#250201=CARTESIAN_POINT('Ctrl Pts',(-2.50977784328783,2.02187687046959,
6.93225217373322));
#250202=CARTESIAN_POINT('Ctrl Pts',(-2.64744288241673,1.84778510279578,
6.94552671743596));
#250203=CARTESIAN_POINT('Ctrl Pts',(-2.75320160660144,1.68616812097163,
6.95628291647143));
#250204=CARTESIAN_POINT('Ctrl Pts',(-2.91658001159659,1.37969398163169,
6.97572772606296));
#250205=CARTESIAN_POINT('Ctrl Pts',(-2.97936638809607,1.23829175574905,
6.98437688485443));
#250206=CARTESIAN_POINT('Ctrl Pts',(-3.05177592024263,1.03743091348531,
6.99671559524954));
#250207=CARTESIAN_POINT('Ctrl Pts',(-3.07025736679884,0.981385908372844,
7.00016224717586));
#250208=CARTESIAN_POINT('Ctrl Pts',(-3.10013791266096,0.881645225790939,
7.00632636900969));
#250209=CARTESIAN_POINT('Ctrl Pts',(-3.11217687395752,0.838157616008936,
7.00902384680454));
#250210=CARTESIAN_POINT('Ctrl Pts',(-3.12885784199226,0.772576712192959,
7.01311323980674));
#250211=CARTESIAN_POINT('Ctrl Pts',(-3.13418748932593,0.750662982831865,
7.01448324448297));
#250212=CARTESIAN_POINT('Ctrl Pts',(-3.14334528888919,0.711210350097816,
7.01695688879043));
#250213=CARTESIAN_POINT('Ctrl Pts',(-3.14725775490478,0.693691841559114,
7.01805779468869));
#250214=CARTESIAN_POINT('Ctrl Pts',(-3.15536142575268,0.65592630657276,
7.02043686852944));
#250215=CARTESIAN_POINT('Ctrl Pts',(-3.15950451986651,0.635669886135118,
7.02171650808363));
#250216=CARTESIAN_POINT('Ctrl Pts',(-3.17013787019608,0.581007157240908,
7.02517987838766));
#250217=CARTESIAN_POINT('Ctrl Pts',(-3.17626266387758,0.546533410817749,
7.02737497771469));
#250218=CARTESIAN_POINT('Ctrl Pts',(-3.20906871155223,0.342647366588913,
7.04042568250777));
#250219=CARTESIAN_POINT('Ctrl Pts',(-3.22275000000749,0.171449469762571,
7.05168326423443));
#250220=CARTESIAN_POINT('Ctrl Pts',(-3.22275,-1.40828737560383E-10,7.06317491433944));
#250221=CARTESIAN_POINT('Origin',(0.,0.,-2.31077344927308));
#250222=CARTESIAN_POINT('',(-3.22275,6.20733405470152E-11,8.56255098483899));
#250223=CARTESIAN_POINT('',(-3.22275,-3.27109834657983E-12,8.3171463242964));
#250224=CARTESIAN_POINT('',(-3.22275,-3.50678552687464E-13,-2.31077344927308));
#250225=CARTESIAN_POINT('',(-3.22274893538059,0.00261954256402689,8.56237746067257));
#250226=CARTESIAN_POINT('Ctrl Pts',(-3.22275,6.20733405470152E-11,8.56255098483899));
#250227=CARTESIAN_POINT('Ctrl Pts',(-3.22274999999998,0.000873176498947361,
8.56249315116623));
#250228=CARTESIAN_POINT('Ctrl Pts',(-3.22274964513048,0.00174635740424604,
8.56243530976668));
#250229=CARTESIAN_POINT('Ctrl Pts',(-3.22274893538059,0.00261954256399533,
8.56237746067257));
#250230=CARTESIAN_POINT('Ctrl Pts',(-3.22274893830454,0.00261594284377387,
8.56237769915637));
#250231=CARTESIAN_POINT('Ctrl Pts',(-3.22256516576624,0.229017201608468,
8.5473784713664));
#250232=CARTESIAN_POINT('Ctrl Pts',(-3.19852586970591,0.454758449831492,
8.53186200725869));
#250233=CARTESIAN_POINT('Ctrl Pts',(-3.13847030541308,0.734646266102758,
8.51280182570542));
#250234=CARTESIAN_POINT('Ctrl Pts',(-3.12428256145324,0.792817925200208,
8.50885435029793));
#250235=CARTESIAN_POINT('Ctrl Pts',(-3.09826356417928,0.887907324882827,
8.50245878119287));
#250236=CARTESIAN_POINT('Ctrl Pts',(-3.08737267217223,0.925065845381036,
8.4999742227873));
#250237=CARTESIAN_POINT('Ctrl Pts',(-3.07141595910779,0.976083329288819,
8.49659171460607));
#250238=CARTESIAN_POINT('Ctrl Pts',(-3.06692117279408,0.990115750214793,
8.49566438309405));
#250239=CARTESIAN_POINT('Ctrl Pts',(-3.05914486721358,1.01383172322626,
8.49410284435985));
#250240=CARTESIAN_POINT('Ctrl Pts',(-3.05591324766903,1.02353129673551,
8.49346582856823));
#250241=CARTESIAN_POINT('Ctrl Pts',(-3.04914432580199,1.04353007563975,
8.49215601334705));
#250242=CARTESIAN_POINT('Ctrl Pts',(-3.04560091040924,1.05382695020228,
8.49148356987967));
#250243=CARTESIAN_POINT('Ctrl Pts',(-3.03610122267661,1.08098411764399,
8.48971472099901));
#250244=CARTESIAN_POINT('Ctrl Pts',(-3.03005661083684,1.09781340184896,
8.48862333613525));
#250245=CARTESIAN_POINT('Ctrl Pts',(-3.0031036583681,1.17093637874964,8.48389856287013));
#250246=CARTESIAN_POINT('Ctrl Pts',(-2.98076301510413,1.22669328969606,
8.48034066427099));
#250247=CARTESIAN_POINT('Ctrl Pts',(-2.93227833574217,1.33853875066314,
8.47323325481358));
#250248=CARTESIAN_POINT('Ctrl Pts',(-2.90605160932365,1.3945633538104,8.46968862318166));
#250249=CARTESIAN_POINT('Ctrl Pts',(-2.85410152616811,1.49769764104126,
8.4631328011241));
#250250=CARTESIAN_POINT('Ctrl Pts',(-2.82878296611447,1.54498572694711,
8.46011439510555));
#250251=CARTESIAN_POINT('Ctrl Pts',(-2.71816207604229,1.73975099305964,
8.44754788922916));
#250252=CARTESIAN_POINT('Ctrl Pts',(-2.6224193552483,1.88097124489743,8.43809065262141));
#250253=CARTESIAN_POINT('Ctrl Pts',(-2.47206050327171,2.06880894309093,
8.42428928437099));
#250254=CARTESIAN_POINT('Ctrl Pts',(-2.42637608029303,2.12220446545546,
8.42021219203979));
#250255=CARTESIAN_POINT('Ctrl Pts',(-2.34463199771312,2.21165359354654,
8.41306816124801));
#250256=CARTESIAN_POINT('Ctrl Pts',(-2.30939404615842,2.24842379019215,
8.41003308261231));
#250257=CARTESIAN_POINT('Ctrl Pts',(-2.25810576027505,2.2994641785123,8.40566767077397));
#250258=CARTESIAN_POINT('Ctrl Pts',(-2.24276019747075,2.31443379590396,
8.40436789985169));
#250259=CARTESIAN_POINT('Ctrl Pts',(-2.22685433344969,2.32964324857572,
8.40302674155583));
#250260=CARTESIAN_POINT('Ctrl Pts',(-2.2264418559548,2.33003745679979,8.40299196623254));
#250261=CARTESIAN_POINT('Ctrl Pts',(-2.22560068041687,2.33084094805349,
8.40292105650763));
#250262=CARTESIAN_POINT('Ctrl Pts',(-2.22517197412512,2.33125022238333,
8.40288492173852));
#250263=CARTESIAN_POINT('Ctrl Pts',(-2.21174537637508,2.34406115511253,
8.40175336124031));
#250264=CARTESIAN_POINT('Ctrl Pts',(-2.19864433604815,2.3563538299562,8.40065333424121));
#250265=CARTESIAN_POINT('Ctrl Pts',(-2.17304203874568,2.37997699525984,
8.39851114544122));
#250266=CARTESIAN_POINT('Ctrl Pts',(-2.16055321348649,2.39132013638167,
8.39746957088449));
#250267=CARTESIAN_POINT('Ctrl Pts',(-2.12693239443544,2.42137831566538,
8.39467420786597));
#250268=CARTESIAN_POINT('Ctrl Pts',(-2.10564298792965,2.43991431911858,
8.39291308989584));
#250269=CARTESIAN_POINT('Ctrl Pts',(-2.02466899600205,2.50856666164642,
8.38624626848788));
#250270=CARTESIAN_POINT('Ctrl Pts',(-1.96342049994779,2.55678891088787,
8.38126592183347));
#250271=CARTESIAN_POINT('Ctrl Pts',(-1.69597408550167,2.75207489333075,
8.35976864844818));
#250272=CARTESIAN_POINT('Ctrl Pts',(-1.4745876183046,2.87676965641239,8.34248545069205));
#250273=CARTESIAN_POINT('Ctrl Pts',(-1.13960125366551,3.01653503696742,
8.31810947762373));
#250274=CARTESIAN_POINT('Ctrl Pts',(-1.03615871796513,3.05361329749542,
8.31081909360575));
#250275=CARTESIAN_POINT('Ctrl Pts',(-0.905376819231954,3.09307737232661,
8.30204590511184));
#250276=CARTESIAN_POINT('Ctrl Pts',(-0.879640706716284,3.10049466221572,
8.30034047399109));
#250277=CARTESIAN_POINT('Ctrl Pts',(-0.841531127769652,3.11096531417921,
8.29784899932326));
#250278=CARTESIAN_POINT('Ctrl Pts',(-0.829227931784571,3.11426730948811,
8.29704983712732));
#250279=CARTESIAN_POINT('Ctrl Pts',(-0.808198753215153,3.11977777184471,
8.2956930787246));
#250280=CARTESIAN_POINT('Ctrl Pts',(-0.79948270464364,3.12202273890778,
8.29513344143526));
#250281=CARTESIAN_POINT('Ctrl Pts',(-0.779573432645709,3.12706186555746,
8.29386133435046));
#250282=CARTESIAN_POINT('Ctrl Pts',(-0.768374509896765,3.12983246676215,
8.29315020641053));
#250283=CARTESIAN_POINT('Ctrl Pts',(-0.73743456169804,3.13731090041672,
8.29119712794687));
#250284=CARTESIAN_POINT('Ctrl Pts',(-0.717663204729228,3.14189258103911,
8.28996205511375));
#250285=CARTESIAN_POINT('Ctrl Pts',(-0.604437135116019,3.1670062238142,
8.28295629999623));
#250286=CARTESIAN_POINT('Ctrl Pts',(-0.510139426278922,3.1835567998964,
8.2773820935005));
#250287=CARTESIAN_POINT('Ctrl Pts',(-0.212428354284217,3.222237938988,8.26020876644491));
#250288=CARTESIAN_POINT('Ctrl Pts',(-0.00756736986425217,3.2292247309117,
8.24897959781515));
#250289=CARTESIAN_POINT('Ctrl Pts',(0.337816250873611,3.20811778630414,
8.22937079253028));
#250290=CARTESIAN_POINT('Ctrl Pts',(0.478315019225521,3.19019554116657,
8.22120795137853));
#250291=CARTESIAN_POINT('Ctrl Pts',(0.649443765073081,3.15680558133873,
8.21078843376565));
#250292=CARTESIAN_POINT('Ctrl Pts',(0.681616403522962,3.15001549863993,
8.2088088812646));
#250293=CARTESIAN_POINT('Ctrl Pts',(0.732926603091755,3.13836354583708,
8.20561612262152));
#250294=CARTESIAN_POINT('Ctrl Pts',(0.752133643901503,3.13381590177792,
8.20441291332319));
#250295=CARTESIAN_POINT('Ctrl Pts',(0.788579791638005,3.12483220415761,
8.20211388635386));
#250296=CARTESIAN_POINT('Ctrl Pts',(0.805826339366947,3.12042918244698,
8.20101916316113));
#250297=CARTESIAN_POINT('Ctrl Pts',(0.845187310501891,3.11003230265226,
8.1985047311464));
#250298=CARTESIAN_POINT('Ctrl Pts',(0.867275862060893,3.10394507833176,
8.19708206689853));
#250299=CARTESIAN_POINT('Ctrl Pts',(0.92519323358183,3.08731756880291,8.19332036651984));
#250300=CARTESIAN_POINT('Ctrl Pts',(0.960906174000562,3.07638934930804,
8.19096898129311));
#250301=CARTESIAN_POINT('Ctrl Pts',(1.24554923096658,2.98384823064309,8.1719651855904));
#250302=CARTESIAN_POINT('Ctrl Pts',(1.48383287017575,2.872792042607,8.15431647340847));
#250303=CARTESIAN_POINT('Ctrl Pts',(1.83679747051241,2.6525572410114,8.1262134737614));
#250304=CARTESIAN_POINT('Ctrl Pts',(1.96158014791696,2.56165908348011,8.11585010096142));
#250305=CARTESIAN_POINT('Ctrl Pts',(2.10008739437867,2.44468500173641,8.10420347614881));
#250306=CARTESIAN_POINT('Ctrl Pts',(2.12056902908312,2.42694023939971,8.10247754245812));
#250307=CARTESIAN_POINT('Ctrl Pts',(2.1503914736593,2.40043701513786,8.0999620742373));
#250308=CARTESIAN_POINT('Ctrl Pts',(2.1599072437576,2.39187835496144,8.09915906859326));
#250309=CARTESIAN_POINT('Ctrl Pts',(2.17603299885462,2.3771998406796,8.09779802278509));
#250310=CARTESIAN_POINT('Ctrl Pts',(2.1826686270984,2.37110867864724,8.09723790571617));
#250311=CARTESIAN_POINT('Ctrl Pts',(2.19771506940251,2.35718013576969,8.09596776166901));
#250312=CARTESIAN_POINT('Ctrl Pts',(2.20610956624229,2.34932550106059,8.0952590495035));
#250313=CARTESIAN_POINT('Ctrl Pts',(2.2290768342929,2.32760363458407,8.09331916685197));
#250314=CARTESIAN_POINT('Ctrl Pts',(2.24356234929104,2.31364436422788,8.09209472366204));
#250315=CARTESIAN_POINT('Ctrl Pts',(2.32364180441999,2.23501474786827,8.08531381867647));
#250316=CARTESIAN_POINT('Ctrl Pts',(2.38657624321483,2.16768519963862,8.0799391816895));
#250317=CARTESIAN_POINT('Ctrl Pts',(2.55659429886864,1.9693977041362,8.06497428472047));
#250318=CARTESIAN_POINT('Ctrl Pts',(2.65637782565291,1.83258384578791,8.05562508019494));
#250319=CARTESIAN_POINT('Ctrl Pts',(2.83011781469167,1.55014863299856,8.03698597571246));
#250320=CARTESIAN_POINT('Ctrl Pts',(2.90466570523152,1.40550224215686,8.02773299834416));
#250321=CARTESIAN_POINT('Ctrl Pts',(2.98491720060174,1.21584331976309,8.015527095778));
#250322=CARTESIAN_POINT('Ctrl Pts',(3.00103828843865,1.17548908819945,8.01292710717728));
#250323=CARTESIAN_POINT('Ctrl Pts',(3.02406078605224,1.11429570602391,8.00897413548107));
#250324=CARTESIAN_POINT('Ctrl Pts',(3.03157364727922,1.09369088083438,8.00764138543358));
#250325=CARTESIAN_POINT('Ctrl Pts',(3.04477057222164,1.05631586973668,8.00522008783156));
#250326=CARTESIAN_POINT('Ctrl Pts',(3.05052788382326,1.03957234693322,8.00413400370949));
#250327=CARTESIAN_POINT('Ctrl Pts',(3.06260652674807,1.00348050258098,8.00178954365318));
#250328=CARTESIAN_POINT('Ctrl Pts',(3.06888308131703,0.984118112705343,
8.0005297560088));
#250329=CARTESIAN_POINT('Ctrl Pts',(3.08539944250445,0.931472192703086,
7.99709830369803));
#250330=CARTESIAN_POINT('Ctrl Pts',(3.0952836527629,0.898080799813092,7.99491524727062));
#250331=CARTESIAN_POINT('Ctrl Pts',(3.15582447554704,0.680673602889096,
7.98065425361863));
#250332=CARTESIAN_POINT('Ctrl Pts',(3.19058205784246,0.492655610007064,
7.96806861545985));
#250333=CARTESIAN_POINT('Ctrl Pts',(3.22158747211894,0.164005740571538,
7.94586418685519));
#250334=CARTESIAN_POINT('Ctrl Pts',(3.22566549115339,0.0246141418466337,
7.93639376924152));
#250335=CARTESIAN_POINT('Ctrl Pts',(3.21813043917037,-0.187143636830151,
7.92220497898741));
#250336=CARTESIAN_POINT('Ctrl Pts',(3.21309907637538,-0.259580103156683,
7.91738859757074));
#250337=CARTESIAN_POINT('Ctrl Pts',(3.20106153988697,-0.375882523598728,
7.90977306584647));
#250338=CARTESIAN_POINT('Ctrl Pts',(3.19558818779224,-0.41988002117325,
7.9069195121529));
#250339=CARTESIAN_POINT('Ctrl Pts',(3.18697665390763,-0.479101156392063,
7.90312789085596));
#250340=CARTESIAN_POINT('Ctrl Pts',(3.18463400508372,-0.494433399686895,
7.90215073406484));
#250341=CARTESIAN_POINT('Ctrl Pts',(3.18053958125119,-0.519993449135298,
7.90052990388033));
#250342=CARTESIAN_POINT('Ctrl Pts',(3.17884895594334,-0.530230647830305,
7.89988292922826));
#250343=CARTESIAN_POINT('Ctrl Pts',(3.17553724394443,-0.54969864684475,
7.8986569867339));
#250344=CARTESIAN_POINT('Ctrl Pts',(3.17392529220638,-0.558930796016713,
7.89807749585145));
#250345=CARTESIAN_POINT('Ctrl Pts',(3.16996867309066,-0.581022401219024,
7.89669504989115));
#250346=CARTESIAN_POINT('Ctrl Pts',(3.16758597705393,-0.593874995594126,
7.895894190184));
#250347=CARTESIAN_POINT('Ctrl Pts',(3.16003092170776,-0.633288517059704,
7.89344784321252));
#250348=CARTESIAN_POINT('Ctrl Pts',(3.15460205239384,-0.659799794096786,
7.89181567171407));
#250349=CARTESIAN_POINT('Ctrl Pts',(3.11302122980016,-0.850594928022836,
7.88014546040248));
#250350=CARTESIAN_POINT('Ctrl Pts',(3.0643854813284,-1.01191287369005,7.87067861793006));
#250351=CARTESIAN_POINT('Ctrl Pts',(2.94087568448125,-1.32931014390101,
7.85159562389091));
#250352=CARTESIAN_POINT('Ctrl Pts',(2.86560173286738,-1.48463403263234,
7.84200574471944));
#250353=CARTESIAN_POINT('Ctrl Pts',(2.74665872677585,-1.68697239439719,
7.82847400958385));
#250354=CARTESIAN_POINT('Ctrl Pts',(2.71348798565185,-1.73982536823445,
7.82483695248746));
#250355=CARTESIAN_POINT('Ctrl Pts',(2.65273468018209,-1.83065982039452,
7.81837551119254));
#250356=CARTESIAN_POINT('Ctrl Pts',(2.62581714089898,-1.86906411626918,
7.81557446231823));
#250357=CARTESIAN_POINT('Ctrl Pts',(2.58470422236186,-1.9250797616251,7.81137728117581));
#250358=CARTESIAN_POINT('Ctrl Pts',(2.57114530557423,-1.94315202275065,
7.81000540378385));
#250359=CARTESIAN_POINT('Ctrl Pts',(2.54658821944538,-1.97517633619724,
7.80754167095056));
#250360=CARTESIAN_POINT('Ctrl Pts',(2.53566249647054,-1.98918294851917,
7.80645267418254));
#250361=CARTESIAN_POINT('Ctrl Pts',(2.51224173273012,-2.01870150403738,
7.80413287002825));
#250362=CARTESIAN_POINT('Ctrl Pts',(2.49971760301111,-2.03418931346044,
7.80290093388389));
#250363=CARTESIAN_POINT('Ctrl Pts',(2.46560861930843,-2.07557907003295,
7.79956803750673));
#250364=CARTESIAN_POINT('Ctrl Pts',(2.44375999127483,-2.1012594573266,7.7974565113822));
#250365=CARTESIAN_POINT('Ctrl Pts',(2.32909537552576,-2.23182607609774,
7.78648955815788));
#250366=CARTESIAN_POINT('Ctrl Pts',(2.22992810613304,-2.33091068841016,
7.77737212337351));
#250367=CARTESIAN_POINT('Ctrl Pts',(1.92280559998955,-2.60019081821858,
7.75021015919382));
#250368=CARTESIAN_POINT('Ctrl Pts',(1.69966223837185,-2.75123888063121,
7.73167041025852));
#250369=CARTESIAN_POINT('Ctrl Pts',(1.43475210289737,-2.88590205155199,
7.71234285873751));
#250370=CARTESIAN_POINT('Ctrl Pts',(1.40894729087121,-2.89858791437247,
7.71048732035853));
#250371=CARTESIAN_POINT('Ctrl Pts',(1.36280734284358,-2.92050890489379,
7.70722181786576));
#250372=CARTESIAN_POINT('Ctrl Pts',(1.34253973305436,-2.92988109763965,
7.70580502995511));
#250373=CARTESIAN_POINT('Ctrl Pts',(1.31136967718072,-2.94390345200097,
7.70365478631454));
#250374=CARTESIAN_POINT('Ctrl Pts',(1.30053670948763,-2.94870518068374,
7.70291273159243));
#250375=CARTESIAN_POINT('Ctrl Pts',(1.28054864398093,-2.95743333908937,
7.70155352696631));
#250376=CARTESIAN_POINT('Ctrl Pts',(1.27140174763619,-2.96137710956607,
7.70093538534946));
#250377=CARTESIAN_POINT('Ctrl Pts',(1.25040405208881,-2.97031524247129,
7.69952506353682));
#250378=CARTESIAN_POINT('Ctrl Pts',(1.23854150904905,-2.9752811424265,7.69873457829612));
#250379=CARTESIAN_POINT('Ctrl Pts',(1.20128938397193,-2.99061422817989,
7.69627083894764));
#250380=CARTESIAN_POINT('Ctrl Pts',(1.17579628695179,-3.00072871976973,
7.69461178726365));
#250381=CARTESIAN_POINT('Ctrl Pts',(0.947302054553337,-3.08802556763735,
7.6799548259521));
#250382=CARTESIAN_POINT('Ctrl Pts',(0.73708469238602,-3.14483933957551,
7.66793500941696));
#250383=CARTESIAN_POINT('Ctrl Pts',(0.345874379720156,-3.20914480737122,
7.64572960314135));
#250384=CARTESIAN_POINT('Ctrl Pts',(0.166922456073278,-3.22340934216191,
7.63563018239052));
#250385=CARTESIAN_POINT('Ctrl Pts',(-0.0661585020297892,-3.22252133387607,
7.62191094516255));
#250386=CARTESIAN_POINT('Ctrl Pts',(-0.120022711545808,-3.22096487825367,
7.61870322054083));
#250387=CARTESIAN_POINT('Ctrl Pts',(-0.1976336307,-3.21677279810791,7.61401588058594));
#250388=CARTESIAN_POINT('Ctrl Pts',(-0.221431339444422,-3.21522229432192,
7.61256974301212));
#250389=CARTESIAN_POINT('Ctrl Pts',(-0.263083982668706,-3.21204385865439,
7.61002211200481));
#250390=CARTESIAN_POINT('Ctrl Pts',(-0.280946811771764,-3.2105307661657,
7.60892423394666));
#250391=CARTESIAN_POINT('Ctrl Pts',(-0.318010105905912,-3.20707959447224,
7.60663481153101));
#250392=CARTESIAN_POINT('Ctrl Pts',(-0.337207603902068,-3.20511793214001,
7.60544257319093));
#250393=CARTESIAN_POINT('Ctrl Pts',(-0.387032350640315,-3.19957408858473,
7.60233112149887));
#250394=CARTESIAN_POINT('Ctrl Pts',(-0.417627294780195,-3.19572460110338,
7.60040364942186));
#250395=CARTESIAN_POINT('Ctrl Pts',(-0.547813944547506,-3.1774429794755,
7.59212741828171));
#250396=CARTESIAN_POINT('Ctrl Pts',(-0.646746739277233,-3.15879078181821,
7.58564906873014));
#250397=CARTESIAN_POINT('Ctrl Pts',(-0.948367520102334,-3.0871610740129,
7.56531700919316));
#250398=CARTESIAN_POINT('Ctrl Pts',(-1.14688361574539,-3.01904074183851,
7.55107334695094));
#250399=CARTESIAN_POINT('Ctrl Pts',(-1.44942736427279,-2.8810498217309,
7.52868036184968));
#250400=CARTESIAN_POINT('Ctrl Pts',(-1.55847771933964,-2.82355105997055,
7.52046520061428));
#250401=CARTESIAN_POINT('Ctrl Pts',(-1.6881879185444,-2.7453484917562,7.51072423907064));
#250402=CARTESIAN_POINT('Ctrl Pts',(-1.7122065529566,-2.73043323205823,
7.50892203436262));
#250403=CARTESIAN_POINT('Ctrl Pts',(-1.74699368568106,-2.70819129066408,
7.50631758802554));
#250404=CARTESIAN_POINT('Ctrl Pts',(-1.75791828770339,-2.70111279142114,
7.50550052772984));
#250405=CARTESIAN_POINT('Ctrl Pts',(-1.77713697606881,-2.68849422562496,
7.50406506262489));
#250406=CARTESIAN_POINT('Ctrl Pts',(-1.78544861135059,-2.68298160602879,
7.50344491888437));
#250407=CARTESIAN_POINT('Ctrl Pts',(-1.80348432908141,-2.67089864113393,
7.50210075601906));
#250408=CARTESIAN_POINT('Ctrl Pts',(-1.81319821691838,-2.66431370387102,
7.50137771320789));
#250409=CARTESIAN_POINT('Ctrl Pts',(-1.84034250979878,-2.64569567535157,
7.49935917425581));
#250410=CARTESIAN_POINT('Ctrl Pts',(-1.85769092364641,-2.6335433631997,
7.49807132375313));
#250411=CARTESIAN_POINT('Ctrl Pts',(-1.97239446501926,-2.55149768216892,
7.48956227679538));
#250412=CARTESIAN_POINT('Ctrl Pts',(-2.06591608850664,-2.47638391009125,
7.48265162962741));
#250413=CARTESIAN_POINT('Ctrl Pts',(-2.19322130822174,-2.36189208385287,
7.47294479453799));
#250414=CARTESIAN_POINT('Ctrl Pts',(-2.23057316056949,-2.32664941076407,
7.47005661380756));
#250415=CARTESIAN_POINT('Ctrl Pts',(-2.36489299881334,-2.19370537026154,
7.4594565106647));
#250416=CARTESIAN_POINT('Ctrl Pts',(-2.45641431549734,-2.09071515613957,
7.45179999133454));
#250417=CARTESIAN_POINT('Ctrl Pts',(-2.62241759286614,-1.87790747457348,
7.43646355931109));
#250418=CARTESIAN_POINT('Ctrl Pts',(-2.69726133190693,-1.76872443507827,
7.42881082168785));
#250419=CARTESIAN_POINT('Ctrl Pts',(-2.78178513447398,-1.62752389156052,
7.41897160363767));
#250420=CARTESIAN_POINT('Ctrl Pts',(-2.79796974717712,-1.59953985023089,
7.41702469080633));
#250421=CARTESIAN_POINT('Ctrl Pts',(-2.82329566761753,-1.55418918515955,
7.41387205278009));
#250422=CARTESIAN_POINT('Ctrl Pts',(-2.83270432016028,-1.53697386387557,
7.41267587394001));
#250423=CARTESIAN_POINT('Ctrl Pts',(-2.85036182149819,-1.50395242309228,
7.41038200615435));
#250424=CARTESIAN_POINT('Ctrl Pts',(-2.85863785754082,-1.48816161208251,
7.40928532908256));
#250425=CARTESIAN_POINT('Ctrl Pts',(-2.87717890656514,-1.45205957018702,
7.40677820029387));
#250426=CARTESIAN_POINT('Ctrl Pts',(-2.8873605582297,-1.43170682062964,
7.40536490933303));
#250427=CARTESIAN_POINT('Ctrl Pts',(-2.91381819758687,-1.3773886733909,
7.40159263321956));
#250428=CARTESIAN_POINT('Ctrl Pts',(-2.92971538825062,-1.34324368561402,
7.39922085862288));
#250429=CARTESIAN_POINT('Ctrl Pts',(-3.05023439663354,-1.0720625973999,
7.38037436783688));
#250430=CARTESIAN_POINT('Ctrl Pts',(-3.12650499082791,-0.823509052567751,
7.36292844953784));
#250431=CARTESIAN_POINT('Ctrl Pts',(-3.19229483663836,-0.456448987694319,
7.33773544373467));
#250432=CARTESIAN_POINT('Ctrl Pts',(-3.20643327838788,-0.34333729478466,
7.33006542802909));
#250433=CARTESIAN_POINT('Ctrl Pts',(-3.21878910424195,-0.170429634894116,
7.31867179497308));
#250434=CARTESIAN_POINT('Ctrl Pts',(-3.2213848981587,-0.111040043629163,
7.31481799965721));
#250435=CARTESIAN_POINT('Ctrl Pts',(-3.22261223720652,-0.034407617749416,
7.30994969608496));
#250436=CARTESIAN_POINT('Ctrl Pts',(-3.22275,-0.017204164504275,7.30886358410991));
#250437=CARTESIAN_POINT('Ctrl Pts',(-3.22275,-3.49632484551545E-13,7.3077847617826));
#250438=CARTESIAN_POINT('',(-3.2227498657163,0.000930336277219642,8.31709040082309));
#250439=CARTESIAN_POINT('Ctrl Pts',(-3.22275,-1.40828092660302E-10,7.06317491433944));
#250440=CARTESIAN_POINT('Ctrl Pts',(-3.22274999999996,-0.000953531021211235,
7.06323882613367));
#250441=CARTESIAN_POINT('Ctrl Pts',(-3.22274957684046,-0.00190706973096647,
7.06330274445318));
#250442=CARTESIAN_POINT('Ctrl Pts',(-3.22252667574421,-0.253025888032566,
7.08013750826466));
#250443=CARTESIAN_POINT('Ctrl Pts',(-3.19317800943748,-0.502316457797773,
7.09734588176947));
#250444=CARTESIAN_POINT('Ctrl Pts',(-3.12848874678906,-0.774299356712258,
7.11534388989034));
#250445=CARTESIAN_POINT('Ctrl Pts',(-3.12129716478292,-0.802798530885497,
7.11721890539666));
#250446=CARTESIAN_POINT('Ctrl Pts',(-3.11029875201956,-0.843999306421481,
7.11990987998768));
#250447=CARTESIAN_POINT('Ctrl Pts',(-3.10680207164883,-0.856781219402947,
7.12074194229381));
#250448=CARTESIAN_POINT('Ctrl Pts',(-3.10047035227186,-0.879377910673626,
7.12220755478895));
#250449=CARTESIAN_POINT('Ctrl Pts',(-3.09766735274477,-0.889201269152986,
7.12284287059426));
#250450=CARTESIAN_POINT('Ctrl Pts',(-3.09149385174459,-0.910453342516979,
7.12421328294044));
#250451=CARTESIAN_POINT('Ctrl Pts',(-3.08810664465587,-0.921876827985553,
7.12494742284139));
#250452=CARTESIAN_POINT('Ctrl Pts',(-3.0783171371103,-0.954232837354177,
7.12702042462482));
#250453=CARTESIAN_POINT('Ctrl Pts',(-3.07176468743532,-0.975119720127279,
7.12835100955111));
#250454=CARTESIAN_POINT('Ctrl Pts',(-3.01956137922603,-1.13577529114735,
7.13853817107374));
#250455=CARTESIAN_POINT('Ctrl Pts',(-2.96460066690011,-1.27235597560013,
7.14692538665781));
#250456=CARTESIAN_POINT('Ctrl Pts',(-2.79473371201036,-1.62310125157332,
7.16887031409096));
#250457=CARTESIAN_POINT('Ctrl Pts',(-2.66465457994802,-1.82882605445227,
7.18222979907216));
#250458=CARTESIAN_POINT('Ctrl Pts',(-2.47306894240764,-2.06737950812083,
7.20012497136034));
#250459=CARTESIAN_POINT('Ctrl Pts',(-2.43196980713013,-2.11557323232554,
7.20387671620316));
#250460=CARTESIAN_POINT('Ctrl Pts',(-2.37177528277691,-2.1820851722432,
7.20927231248871));
#250461=CARTESIAN_POINT('Ctrl Pts',(-2.35383183267888,-2.20142892953185,
7.21086886501484));
#250462=CARTESIAN_POINT('Ctrl Pts',(-2.32291506054037,-2.23394829102413,
7.21360118899848));
#250463=CARTESIAN_POINT('Ctrl Pts',(-2.31006198716238,-2.247236734024,7.21473181114377));
#250464=CARTESIAN_POINT('Ctrl Pts',(-2.28372809017572,-2.27399797588429,
7.2170380665918));
#250465=CARTESIAN_POINT('Ctrl Pts',(-2.27024067857951,-2.28746322830508,
7.2182139641804));
#250466=CARTESIAN_POINT('Ctrl Pts',(-2.23640142187085,-2.32065280846793,
7.22115166885254));
#250467=CARTESIAN_POINT('Ctrl Pts',(-2.21590762943885,-2.34022949159859,
7.22291974101126));
#250468=CARTESIAN_POINT('Ctrl Pts',(-2.1345712645501,-2.41589965578216,
7.22989594846167));
#250469=CARTESIAN_POINT('Ctrl Pts',(-2.07183995967479,-2.46990745824362,
7.23518948900365));
#250470=CARTESIAN_POINT('Ctrl Pts',(-1.89821176174216,-2.6081182311143,
7.24962050550192));
#250471=CARTESIAN_POINT('Ctrl Pts',(-1.78382851108215,-2.68764540471774,
7.25890820220459));
#250472=CARTESIAN_POINT('Ctrl Pts',(-1.4784990665978,-2.87183437263658,
7.28294502815948));
#250473=CARTESIAN_POINT('Ctrl Pts',(-1.2814257099444,-2.9650215208448,7.29779139859344));
#250474=CARTESIAN_POINT('Ctrl Pts',(-1.05051036632447,-3.04685139884914,
7.31353556825694));
#250475=CARTESIAN_POINT('Ctrl Pts',(-1.02444351974757,-3.05571449371794,
7.31528959362654));
#250476=CARTESIAN_POINT('Ctrl Pts',(-0.985858828249833,-3.06828456802298,
7.31784856597426));
#250477=CARTESIAN_POINT('Ctrl Pts',(-0.973427648319938,-3.07225103902177,
7.31866734137015));
#250478=CARTESIAN_POINT('Ctrl Pts',(-0.951255076351548,-3.07917764757313,
7.32011722518384));
#250479=CARTESIAN_POINT('Ctrl Pts',(-0.941523369377431,-3.08216725036393,
7.320749977743));
#250480=CARTESIAN_POINT('Ctrl Pts',(-0.920074233389323,-3.08864540227538,
7.32213662497717));
#250481=CARTESIAN_POINT('Ctrl Pts',(-0.908350998171864,-3.09211343441985,
7.32288935143317));
#250482=CARTESIAN_POINT('Ctrl Pts',(-0.874158532188023,-3.10201719657204,
7.32507054937929));
#250483=CARTESIAN_POINT('Ctrl Pts',(-0.851638166658515,-3.10827545939235,
7.32648932645618));
#250484=CARTESIAN_POINT('Ctrl Pts',(-0.799733764438047,-3.12209286827458,
7.32972262549627));
#250485=CARTESIAN_POINT('Ctrl Pts',(-0.770306742007576,-3.12948328439213,
7.3315289356792));
#250486=CARTESIAN_POINT('Ctrl Pts',(-0.669920195412353,-3.15319290622601,
7.33761364473023));
#250487=CARTESIAN_POINT('Ctrl Pts',(-0.598510540842762,-3.16752347483356,
7.34181174390286));
#250488=CARTESIAN_POINT('Ctrl Pts',(-0.389881453923603,-3.2020829695681,
7.35385548295524));
#250489=CARTESIAN_POINT('Ctrl Pts',(-0.25176649684484,-3.21589161607035,
7.36155891000548));
#250490=CARTESIAN_POINT('Ctrl Pts',(0.0762458684478214,-3.22741904230161,
7.37997732319351));
#250491=CARTESIAN_POINT('Ctrl Pts',(0.265874385737307,-3.21735072640884,
7.39074018283069));
#250492=CARTESIAN_POINT('Ctrl Pts',(0.488429866184755,-3.18571782468613,
7.4041434806085));
#250493=CARTESIAN_POINT('Ctrl Pts',(0.523267593151709,-3.18018123271999,
7.40626331180025));
#250494=CARTESIAN_POINT('Ctrl Pts',(0.578427575455487,-3.17048403462823,
7.40965752330677));
#250495=CARTESIAN_POINT('Ctrl Pts',(0.598813211306928,-3.1666970459578,
7.410920172178));
#250496=CARTESIAN_POINT('Ctrl Pts',(0.636769659202039,-3.15926635933357,
7.41328713759469));
#250497=CARTESIAN_POINT('Ctrl Pts',(0.65434940807425,-3.15567209319773,
7.41438985162708));
#250498=CARTESIAN_POINT('Ctrl Pts',(0.6938733381964,-3.14724676745014,7.41688397564538));
#250499=CARTESIAN_POINT('Ctrl Pts',(0.715798677445564,-3.14233267453331,
7.4182779722957));
#250500=CARTESIAN_POINT('Ctrl Pts',(0.781176479613671,-3.1269599133044,
7.42246668111982));
#250501=CARTESIAN_POINT('Ctrl Pts',(0.824463200142806,-3.11582655244611,
7.42528262080311));
#250502=CARTESIAN_POINT('Ctrl Pts',(1.03077672987471,-3.05816248832955,
7.43891504761489));
#250503=CARTESIAN_POINT('Ctrl Pts',(1.19017244796175,-2.99972224575463,
7.45010483838697));
#250504=CARTESIAN_POINT('Ctrl Pts',(1.51127630516548,-2.85235859203769,
7.47384509830776));
#250505=CARTESIAN_POINT('Ctrl Pts',(1.67147305428396,-2.76153673095869,
7.48638887995182));
#250506=CARTESIAN_POINT('Ctrl Pts',(1.88103229076042,-2.61778116730715,
7.50319070730147));
#250507=CARTESIAN_POINT('Ctrl Pts',(1.93769720796257,-2.57611952190976,
7.50777470461426));
#250508=CARTESIAN_POINT('Ctrl Pts',(2.00796130262482,-2.52082793241392,
7.51346757119507));
#250509=CARTESIAN_POINT('Ctrl Pts',(2.02285998857198,-2.508888113294,7.51467517446767));
#250510=CARTESIAN_POINT('Ctrl Pts',(2.0464144284822,-2.48966533167798,7.51658397811625));
#250511=CARTESIAN_POINT('Ctrl Pts',(2.05513921155751,-2.48246818853482,
7.51729093068752));
#250512=CARTESIAN_POINT('Ctrl Pts',(2.07179820249049,-2.46857803388579,
7.51864031065389));
#250513=CARTESIAN_POINT('Ctrl Pts',(2.07973815675831,-2.46189246370422,
7.51928320698627));
#250514=CARTESIAN_POINT('Ctrl Pts',(2.09880883259322,-2.4456765443024,7.52082709621985));
#250515=CARTESIAN_POINT('Ctrl Pts',(2.10990727635468,-2.43610828559084,
7.52172538501965));
#250516=CARTESIAN_POINT('Ctrl Pts',(2.14872163446305,-2.40218117126878,
7.52486783570805));
#250517=CARTESIAN_POINT('Ctrl Pts',(2.17608519410062,-2.37742140323437,
7.52708482535148));
#250518=CARTESIAN_POINT('Ctrl Pts',(2.24365136050259,-2.31414031090584,
7.53258111318452));
#250519=CARTESIAN_POINT('Ctrl Pts',(2.28329325135337,-2.27503612817723,
7.53582627075722));
#250520=CARTESIAN_POINT('Ctrl Pts',(2.47047641003316,-2.08056794131524,
7.55136765110232));
#250521=CARTESIAN_POINT('Ctrl Pts',(2.60329314780584,-1.91177701701462,
7.56311296168481));
#250522=CARTESIAN_POINT('Ctrl Pts',(2.79560838319224,-1.60977108245903,
7.58338124441627));
#250523=CARTESIAN_POINT('Ctrl Pts',(2.8646252263604,-1.4834772091751,7.59166208358882));
#250524=CARTESIAN_POINT('Ctrl Pts',(2.93941389977534,-1.32179651252657,
7.60229532830778));
#250525=CARTESIAN_POINT('Ctrl Pts',(2.95335009669646,-1.29035776648659,
7.60436383352325));
#250526=CARTESIAN_POINT('Ctrl Pts',(2.97472618599645,-1.23997402839485,
7.60768312632876));
#250527=CARTESIAN_POINT('Ctrl Pts',(2.98249453471051,-1.22117066533209,
7.60892282881088));
#250528=CARTESIAN_POINT('Ctrl Pts',(2.99686358167087,-1.18543513607,7.61128120822325));
#250529=CARTESIAN_POINT('Ctrl Pts',(3.00350013180096,-1.16851817528474,
7.61239863186569));
#250530=CARTESIAN_POINT('Ctrl Pts',(3.01826877967523,-1.12991483776668,
7.61495115998175));
#250531=CARTESIAN_POINT('Ctrl Pts',(3.02631080756419,-1.10819529799116,
7.61638918387486));
#250532=CARTESIAN_POINT('Ctrl Pts',(3.05040461772171,-1.04090513018184,
7.62085109799654));
#250533=CARTESIAN_POINT('Ctrl Pts',(3.06566568951295,-0.995060450743638,
7.62390053770755));
#250534=CARTESIAN_POINT('Ctrl Pts',(3.09889604482007,-0.887202190439704,
7.63110036182815));
#250535=CARTESIAN_POINT('Ctrl Pts',(3.11604338271559,-0.824958890782594,
7.63527477672648));
#250536=CARTESIAN_POINT('Ctrl Pts',(3.17448469572475,-0.584881724674091,
7.65144422524452));
#250537=CARTESIAN_POINT('Ctrl Pts',(3.20250882890306,-0.404184540027611,
7.66378062337057));
#250538=CARTESIAN_POINT('Ctrl Pts',(3.21744807614554,-0.187933170835252,
7.67842265555932));
#250539=CARTESIAN_POINT('Ctrl Pts',(3.21926391396761,-0.153723414628061,
7.68073442698605));
#250540=CARTESIAN_POINT('Ctrl Pts',(3.22540421270944,0.011770606368995,
7.69188158034767));
#250541=CARTESIAN_POINT('Ctrl Pts',(3.22224543175025,0.143221596182795,
7.70063001977925));
#250542=CARTESIAN_POINT('Ctrl Pts',(3.20922025119336,0.295797348931664,
7.71041462621891));
#250543=CARTESIAN_POINT('Ctrl Pts',(3.20715065436056,0.317451463312989,
7.71179443564843));
#250544=CARTESIAN_POINT('Ctrl Pts',(3.20359748639591,0.351034366725555,
7.71391888795789));
#250545=CARTESIAN_POINT('Ctrl Pts',(3.2022662042726,0.36297816636175,7.71467140810044));
#250546=CARTESIAN_POINT('Ctrl Pts',(3.19968137894554,0.385046360134685,
7.71605583801941));
#250547=CARTESIAN_POINT('Ctrl Pts',(3.19844657043142,0.39517232479427,7.71668871137639));
#250548=CARTESIAN_POINT('Ctrl Pts',(3.19548774346559,0.418513120822464,
7.71814219877517));
#250549=CARTESIAN_POINT('Ctrl Pts',(3.19372981958098,0.43172329659818,7.71896093402771));
#250550=CARTESIAN_POINT('Ctrl Pts',(3.18788332209423,0.473666283547361,
7.72154915400199));
#250551=CARTESIAN_POINT('Ctrl Pts',(3.18348843220928,0.502355807066949,
7.72330264217801));
#250552=CARTESIAN_POINT('Ctrl Pts',(3.15763268848809,0.65714003809271,7.73269038443449));
#250553=CARTESIAN_POINT('Ctrl Pts',(3.12906495024704,0.781944007393687,
7.74000090212326));
#250554=CARTESIAN_POINT('Ctrl Pts',(3.03045907033571,1.11906415631442,7.75981227087039));
#250555=CARTESIAN_POINT('Ctrl Pts',(2.94566356999454,1.32629213034917,7.77210337978645));
#250556=CARTESIAN_POINT('Ctrl Pts',(2.80057662288507,1.59683788075037,7.78986826591017));
#250557=CARTESIAN_POINT('Ctrl Pts',(2.75817217270412,1.66901324411107,7.79478618283662));
#250558=CARTESIAN_POINT('Ctrl Pts',(2.69716364558812,1.76416772331911,7.8015639503566));
#250559=CARTESIAN_POINT('Ctrl Pts',(2.68098103807282,1.7886643271088,7.80333615005662));
#250560=CARTESIAN_POINT('Ctrl Pts',(2.65362672810704,1.82886687516966,7.80629205124987));
#250561=CARTESIAN_POINT('Ctrl Pts',(2.64264457704182,1.8447001039809,7.80746864681965));
#250562=CARTESIAN_POINT('Ctrl Pts',(2.62080866357975,1.87558627476477,7.80978894519906));
#250563=CARTESIAN_POINT('Ctrl Pts',(2.60996555108171,1.89064584854694,7.81093221371985));
#250564=CARTESIAN_POINT('Ctrl Pts',(2.58376827185787,1.9263753654588,7.81367377419666));
#250565=CARTESIAN_POINT('Ctrl Pts',(2.56829544621929,1.94695633516277,7.81527659596907));
#250566=CARTESIAN_POINT('Ctrl Pts',(2.51374689442721,2.01773148391793,7.82087250912876));
#250567=CARTESIAN_POINT('Ctrl Pts',(2.4734350008627,2.06694997067148,7.82491352971956));
#250568=CARTESIAN_POINT('Ctrl Pts',(2.37009912950556,2.18576244655493,7.83505232600325));
#250569=CARTESIAN_POINT('Ctrl Pts',(2.30544310935422,2.25385379931654,7.84121025381088));
#250570=CARTESIAN_POINT('Ctrl Pts',(2.09233171637936,2.45951143799465,7.86090430607929));
#250571=CARTESIAN_POINT('Ctrl Pts',(1.93385504188494,2.58597116265882,7.87472963515643));
#250572=CARTESIAN_POINT('Ctrl Pts',(1.68386946247264,2.7495460470864,7.89467715365666));
#250573=CARTESIAN_POINT('Ctrl Pts',(1.60082542433281,2.79871064388989,7.90102822078808));
#250574=CARTESIAN_POINT('Ctrl Pts',(1.49750579643703,2.85377271521622,7.90849892163109));
#250575=CARTESIAN_POINT('Ctrl Pts',(1.47922464601704,2.86329125617286,7.90980490324973));
#250576=CARTESIAN_POINT('Ctrl Pts',(1.45036934892486,2.87796536499773,7.91184002374966));
#250577=CARTESIAN_POINT('Ctrl Pts',(1.4398564929783,2.88323935534855,7.91257606088977));
#250578=CARTESIAN_POINT('Ctrl Pts',(1.42105597551721,2.892542547139,7.91388239035409));
#250579=CARTESIAN_POINT('Ctrl Pts',(1.41277984433935,2.89659379039281,7.9144540016309));
#250580=CARTESIAN_POINT('Ctrl Pts',(1.3926808113147,2.9063258180604,7.91583399916982));
#250581=CARTESIAN_POINT('Ctrl Pts',(1.38084046441022,2.91196999100449,7.91664015324996));
#250582=CARTESIAN_POINT('Ctrl Pts',(1.34371569676275,2.92938963344834,7.91914760981549));
#250583=CARTESIAN_POINT('Ctrl Pts',(1.31831194088421,2.94090959437336,7.9208342912058));
#250584=CARTESIAN_POINT('Ctrl Pts',(1.18520068270418,2.99920067592472,7.92953755341671));
#250585=CARTESIAN_POINT('Ctrl Pts',(1.07513550448367,3.04039379387161,7.93628017357476));
#250586=CARTESIAN_POINT('Ctrl Pts',(0.765188682659938,3.13745040137833,
7.95465491746747));
#250587=CARTESIAN_POINT('Ctrl Pts',(0.561806150291263,3.18017034454195,
7.96606317156575));
#250588=CARTESIAN_POINT('Ctrl Pts',(0.249979193514176,3.21480150336395,
7.98403903669595));
#250589=CARTESIAN_POINT('Ctrl Pts',(0.143722608692009,3.22130080726887,
7.99024087744728));
#250590=CARTESIAN_POINT('Ctrl Pts',(0.00533877931180301,3.22290453713602,
7.99851876314798));
#250591=CARTESIAN_POINT('Ctrl Pts',(-0.026671224341357,3.22279858102165,
8.00044724962345));
#250592=CARTESIAN_POINT('Ctrl Pts',(-0.0785034403496282,3.22185476535973,
8.00359448381885));
#250593=CARTESIAN_POINT('Ctrl Pts',(-0.0983292668588446,3.22131064122808,
8.00480411159918));
#250594=CARTESIAN_POINT('Ctrl Pts',(-0.136436719884786,3.21991265318188,
8.00714086505246));
#250595=CARTESIAN_POINT('Ctrl Pts',(-0.154718616741983,3.21908598837162,
8.00826710166205));
#250596=CARTESIAN_POINT('Ctrl Pts',(-0.197129678575149,3.21680614185889,
8.01089226172787));
#250597=CARTESIAN_POINT('Ctrl Pts',(-0.22125126416158,3.21523711286866,
8.01239472401419));
#250598=CARTESIAN_POINT('Ctrl Pts',(-0.299132884207038,3.20929061968452,
8.01727714353183));
#250599=CARTESIAN_POINT('Ctrl Pts',(-0.352799033073016,3.20383505348674,
8.02069010004052));
#250600=CARTESIAN_POINT('Ctrl Pts',(-0.574938912025167,3.17560403984677,
8.03502657847184));
#250601=CARTESIAN_POINT('Ctrl Pts',(-0.741595117827573,3.14086590443657,
8.04630413137959));
#250602=CARTESIAN_POINT('Ctrl Pts',(-1.10451230971558,3.03471649314292,
8.07176760297457));
#250603=CARTESIAN_POINT('Ctrl Pts',(-1.29818488725824,2.95705522506851,
8.08598731440934));
#250604=CARTESIAN_POINT('Ctrl Pts',(-1.51762072480884,2.84331914133104,
8.10203333711949));
#250605=CARTESIAN_POINT('Ctrl Pts',(-1.55189513614819,2.82475807771813,
8.1045363500097));
#250606=CARTESIAN_POINT('Ctrl Pts',(-1.59923252330628,2.79800108208885,
8.10798014180331));
#250607=CARTESIAN_POINT('Ctrl Pts',(-1.6125847848581,2.7903270511897,8.10895002319282));
#250608=CARTESIAN_POINT('Ctrl Pts',(-1.63487157423647,2.77730461163928,
8.11056571734811));
#250609=CARTESIAN_POINT('Ctrl Pts',(-1.64383601835097,2.77200813954035,
8.11121472862217));
#250610=CARTESIAN_POINT('Ctrl Pts',(-1.66223068520974,2.76101938291241,
8.11254443670403));
#250611=CARTESIAN_POINT('Ctrl Pts',(-1.67165763788342,2.75532205627298,
8.1132248038879));
#250612=CARTESIAN_POINT('Ctrl Pts',(-1.69619746179007,2.74031872619947,
8.11499356254984));
#250613=CARTESIAN_POINT('Ctrl Pts',(-1.71126322378803,2.73093587657025,
8.11607712205303));
#250614=CARTESIAN_POINT('Ctrl Pts',(-1.77904317078882,2.68794184081215,
8.12094499398641));
#250615=CARTESIAN_POINT('Ctrl Pts',(-1.83085350028505,2.65292339059457,
8.12464672371816));
#250616=CARTESIAN_POINT('Ctrl Pts',(-1.98159942387934,2.54451335474954,
8.13546178023975));
#250617=CARTESIAN_POINT('Ctrl Pts',(-2.07738621806542,2.46693230739397,
8.14239587285383));
#250618=CARTESIAN_POINT('Ctrl Pts',(-2.34756303679599,2.22118324286179,
8.16286947326698));
#250619=CARTESIAN_POINT('Ctrl Pts',(-2.5076863413829,2.03867691820129,8.17631869411077));
#250620=CARTESIAN_POINT('Ctrl Pts',(-2.66840353093015,1.80756694530306,
8.19299932844885));
#250621=CARTESIAN_POINT('Ctrl Pts',(-2.69034180387487,1.7747496851045,8.19535857054753));
#250622=CARTESIAN_POINT('Ctrl Pts',(-2.72438899974833,1.72173633918532,
8.19915977865434));
#250623=CARTESIAN_POINT('Ctrl Pts',(-2.73688931883192,1.70179559739131,
8.20058738564981));
#250624=CARTESIAN_POINT('Ctrl Pts',(-2.75870241643252,1.66613692289908,
8.20313731398124));
#250625=CARTESIAN_POINT('Ctrl Pts',(-2.7681021378251,1.65047320528892,8.204256415402));
#250626=CARTESIAN_POINT('Ctrl Pts',(-2.78748208481103,1.61754714210972,
8.20660717254968));
#250627=CARTESIAN_POINT('Ctrl Pts',(-2.79743626019383,1.60027043712824,
8.20783970293279));
#250628=CARTESIAN_POINT('Ctrl Pts',(-2.8231929920192,1.55459166685591,8.21109655724054));
#250629=CARTESIAN_POINT('Ctrl Pts',(-2.83872700187022,1.52604154813008,
8.21313026720772));
#250630=CARTESIAN_POINT('Ctrl Pts',(-2.91338552114394,1.38374019643407,
8.22326073650538));
#250631=CARTESIAN_POINT('Ctrl Pts',(-2.96611117523795,1.26677925994366,
8.23157495481695));
#250632=CARTESIAN_POINT('Ctrl Pts',(-3.10551114465178,0.900751112335599,
8.25751308038769));
#250633=CARTESIAN_POINT('Ctrl Pts',(-3.1687325277635,0.643951241439419,
8.2756831860355));
#250634=CARTESIAN_POINT('Ctrl Pts',(-3.20664551714391,0.326632590981115,
8.29666089333697));
#250635=CARTESIAN_POINT('Ctrl Pts',(-3.21184552326581,0.270764653685991,
8.30029561595211));
#250636=CARTESIAN_POINT('Ctrl Pts',(-3.21676311648958,0.197142798860358,
8.30498476996007));
#250637=CARTESIAN_POINT('Ctrl Pts',(-3.21779639937825,0.179489820271894,
8.30610153431829));
#250638=CARTESIAN_POINT('Ctrl Pts',(-3.2192367304144,0.150842437076011,
8.30790055094247));
#250639=CARTESIAN_POINT('Ctrl Pts',(-3.21973285729915,0.13985314914494,
8.30858749710112));
#250640=CARTESIAN_POINT('Ctrl Pts',(-3.220556688238,0.119266076445391,8.30986820628513));
#250641=CARTESIAN_POINT('Ctrl Pts',(-3.22089777452835,0.109669083833807,
8.31046268952154));
#250642=CARTESIAN_POINT('Ctrl Pts',(-3.22152144770192,0.0895935262464321,
8.31170120631046));
#250643=CARTESIAN_POINT('Ctrl Pts',(-3.22179581953792,0.0791147401977138,
8.31234479286206));
#250644=CARTESIAN_POINT('Ctrl Pts',(-3.22249972328521,0.0460703270001148,
8.31436576064609));
#250645=CARTESIAN_POINT('Ctrl Pts',(-3.22274335007289,0.0235009802904541,
8.31573350607326));
#250646=CARTESIAN_POINT('Ctrl Pts',(-3.2227498657163,0.000930336277219642,
8.31709040082309));
#250647=CARTESIAN_POINT('Ctrl Pts',(-3.22274986493329,0.000933044715058097,
8.31709023799804));
#250648=CARTESIAN_POINT('Ctrl Pts',(-3.22274995497795,0.000622029195259805,
8.31710893554152));
#250649=CARTESIAN_POINT('Ctrl Pts',(-3.22275,0.000311014285896028,8.31712763097307));
#250650=CARTESIAN_POINT('Ctrl Pts',(-3.22275,-3.27109834657983E-12,8.3171463242964));
#250651=CARTESIAN_POINT('Origin',(0.,0.,-2.31077344927308));
#250652=CARTESIAN_POINT('',(-3.22275,1.94885615773067E-11,9.8126895994942));
#250653=CARTESIAN_POINT('',(-3.22275,-1.85372951893938E-11,9.562284768011));
#250654=CARTESIAN_POINT('',(-3.22275,-3.50678552687464E-13,-2.31077344927308));
#250655=CARTESIAN_POINT('Ctrl Pts',(-3.22275,1.94885615773067E-11,9.8126895994942));
#250656=CARTESIAN_POINT('Ctrl Pts',(-3.22275000000001,0.0988455592422595,
9.80700803712948));
#250657=CARTESIAN_POINT('Ctrl Pts',(-3.2182025068033,0.197631261900894,
9.80122982269705));
#250658=CARTESIAN_POINT('Ctrl Pts',(-3.20630297517147,0.326621490038495,
9.79347359146827));
#250659=CARTESIAN_POINT('Ctrl Pts',(-3.20304561883108,0.357154073828275,
9.79162224555709));
#250660=CARTESIAN_POINT('Ctrl Pts',(-3.19703483776758,0.406764205710066,
9.78858696404115));
#250661=CARTESIAN_POINT('Ctrl Pts',(-3.19454561689965,0.425872222001901,
9.78741130405184));
#250662=CARTESIAN_POINT('Ctrl Pts',(-3.18940869268016,0.462721833992583,
9.78513084305691));
#250663=CARTESIAN_POINT('Ctrl Pts',(-3.18678392163908,0.48046594140659,
9.78402680124839));
#250664=CARTESIAN_POINT('Ctrl Pts',(-3.18031406131337,0.521816097999275,
9.78143971545899));
#250665=CARTESIAN_POINT('Ctrl Pts',(-3.1763540817414,0.545402848367702,
9.77995311094355));
#250666=CARTESIAN_POINT('Ctrl Pts',(-3.16254898397611,0.622372957546348,
9.77506519345983));
#250667=CARTESIAN_POINT('Ctrl Pts',(-3.15161804072738,0.67554965144936,
9.77163010674489));
#250668=CARTESIAN_POINT('Ctrl Pts',(-3.09780676148598,0.907465109565107,
9.75638515759688));
#250669=CARTESIAN_POINT('Ctrl Pts',(-3.04102895179079,1.08260123155504,
9.74415192581572));
#250670=CARTESIAN_POINT('Ctrl Pts',(-2.88757695506529,1.4466001183839,9.7175019958554));
#250671=CARTESIAN_POINT('Ctrl Pts',(-2.78655674024109,1.63274813349019,
9.70309232820139));
#250672=CARTESIAN_POINT('Ctrl Pts',(-2.65236925050841,1.8308017671199,9.68771144179242));
#250673=CARTESIAN_POINT('Ctrl Pts',(-2.63640136263731,1.85372212793734,
9.68593126357213));
#250674=CARTESIAN_POINT('Ctrl Pts',(-2.61267422313975,1.88685326473907,
9.68336113089466));
#250675=CARTESIAN_POINT('Ctrl Pts',(-2.60514931133334,1.8972292738479,9.68255666878094));
#250676=CARTESIAN_POINT('Ctrl Pts',(-2.59165831078906,1.91560023568649,
9.68113356184292));
#250677=CARTESIAN_POINT('Ctrl Pts',(-2.58571675236563,1.92361273352193,
9.6805133096404));
#250678=CARTESIAN_POINT('Ctrl Pts',(-2.57271125440297,1.94098217466305,
9.67916975010088));
#250679=CARTESIAN_POINT('Ctrl Pts',(-2.56563339080009,1.95032825824069,
9.67844741117817));
#250680=CARTESIAN_POINT('Ctrl Pts',(-2.54529170059245,1.97688641270331,
9.67639584299928));
#250681=CARTESIAN_POINT('Ctrl Pts',(-2.53190430697451,1.9940036028236,9.67507484700015));
#250682=CARTESIAN_POINT('Ctrl Pts',(-2.42077112882318,2.13317504015373,
9.6643329567526));
#250683=CARTESIAN_POINT('Ctrl Pts',(-2.31442123982545,2.24811813168069,
9.65544607699868));
#250684=CARTESIAN_POINT('Ctrl Pts',(-2.00270714973908,2.53934651246845,
9.631469873342));
#250685=CARTESIAN_POINT('Ctrl Pts',(-1.78289263874554,2.69822140564367,
9.61657741837827));
#250686=CARTESIAN_POINT('Ctrl Pts',(-1.51392323977047,2.84525516848052,
9.59836858928018));
#250687=CARTESIAN_POINT('Ctrl Pts',(-1.48171570208415,2.86215984359172,
9.5961905311965));
#250688=CARTESIAN_POINT('Ctrl Pts',(-1.42901915174892,2.88869067889221,
9.59262689870506));
#250689=CARTESIAN_POINT('Ctrl Pts',(-1.40870222749015,2.89865271611693,
9.59125296878732));
#250690=CARTESIAN_POINT('Ctrl Pts',(-1.37224796508273,2.91605362973353,
9.5887869699881));
#250691=CARTESIAN_POINT('Ctrl Pts',(-1.35615069564134,2.92357461338874,
9.58769778052999));
#250692=CARTESIAN_POINT('Ctrl Pts',(-1.32189634464499,2.9392351941097,9.58537907583011));
#250693=CARTESIAN_POINT('Ctrl Pts',(-1.30372448298975,2.94734048195089,
9.58414844544484));
#250694=CARTESIAN_POINT('Ctrl Pts',(-1.2546483645017,2.96868749125039,9.58082285331471));
#250695=CARTESIAN_POINT('Ctrl Pts',(-1.22361068629477,2.98161444375182,
9.57871740537086));
#250696=CARTESIAN_POINT('Ctrl Pts',(-1.0474640628348,3.05176458483243,9.56675218123542));
#250697=CARTESIAN_POINT('Ctrl Pts',(-0.898572803182584,3.09887122066553,
9.55656164640332));
#250698=CARTESIAN_POINT('Ctrl Pts',(-0.55731968604107,3.18017025270206,
9.53314049461768));
#250699=CARTESIAN_POINT('Ctrl Pts',(-0.364067801303678,3.20804289941476,
9.51982352382647));
#250700=CARTESIAN_POINT('Ctrl Pts',(-0.0796188710241167,3.22302294678228,
9.50084331376008));
#250701=CARTESIAN_POINT('Ctrl Pts',(0.0104157261899073,3.22398984660574,
9.49493146995976));
#250702=CARTESIAN_POINT('Ctrl Pts',(0.120376080726387,3.22056320967653,
9.48791577458799));
#250703=CARTESIAN_POINT('Ctrl Pts',(0.14036637062032,3.21975389072774,9.48664867002654));
#250704=CARTESIAN_POINT('Ctrl Pts',(0.171805118165219,3.21818771143488,
9.48467032874919));
#250705=CARTESIAN_POINT('Ctrl Pts',(0.183258915773735,3.21755579965851,
9.48395259504536));
#250706=CARTESIAN_POINT('Ctrl Pts',(0.203704893531968,3.21631825166988,
9.48267706338429));
#250707=CARTESIAN_POINT('Ctrl Pts',(0.212697958220273,3.21573605268973,
9.48211801902361));
#250708=CARTESIAN_POINT('Ctrl Pts',(0.234494493502573,3.2142331372408,9.48076775717731));
#250709=CARTESIAN_POINT('Ctrl Pts',(0.247295051528603,3.21327364200759,
9.47997868497144));
#250710=CARTESIAN_POINT('Ctrl Pts',(0.28729954156046,3.21003454195876,9.47752392439355));
#250711=CARTESIAN_POINT('Ctrl Pts',(0.314481222292297,3.20748569112191,
9.47587229132811));
#250712=CARTESIAN_POINT('Ctrl Pts',(0.455304734749,3.19247308035518,9.46738497841751));
#250713=CARTESIAN_POINT('Ctrl Pts',(0.568267527192083,3.17431313740642,
9.46081067071436));
#250714=CARTESIAN_POINT('Ctrl Pts',(0.879128161140997,3.10720712283164,
9.44280178780318));
#250715=CARTESIAN_POINT('Ctrl Pts',(1.0736954260329,3.04545269958723,9.43159872471844));
#250716=CARTESIAN_POINT('Ctrl Pts',(1.36628520308246,2.92103375962386,9.41343258892693));
#250717=CARTESIAN_POINT('Ctrl Pts',(1.46897386430393,2.87076389857998,9.4067876065458));
#250718=CARTESIAN_POINT('Ctrl Pts',(1.59676178100323,2.79955286305026,9.39803890016618));
#250719=CARTESIAN_POINT('Ctrl Pts',(1.62451852171566,2.78353801489366,9.39610858633339));
#250720=CARTESIAN_POINT('Ctrl Pts',(1.66882380695965,2.75708671819037,9.39297634651653));
#250721=CARTESIAN_POINT('Ctrl Pts',(1.68552459252708,2.74690860644417,9.39178374103354));
#250722=CARTESIAN_POINT('Ctrl Pts',(1.71728367895618,2.72715469715855,9.38949239513758));
#250723=CARTESIAN_POINT('Ctrl Pts',(1.73235715279015,2.71760457962975,9.38839462392593));
#250724=CARTESIAN_POINT('Ctrl Pts',(1.76689871767813,2.69531588841356,9.38585488886143));
#250725=CARTESIAN_POINT('Ctrl Pts',(1.78630954568023,2.68249081614156,9.38440975817567));
#250726=CARTESIAN_POINT('Ctrl Pts',(1.84745482341426,2.64113309571356,9.37979932842482));
#250727=CARTESIAN_POINT('Ctrl Pts',(1.88865594263913,2.61182917206897,9.37660535448691));
#250728=CARTESIAN_POINT('Ctrl Pts',(2.15473551380437,2.41299388028354,9.35538504743334));
#250729=CARTESIAN_POINT('Ctrl Pts',(2.35722230946593,2.21559744462313,9.33622980504371));
#250730=CARTESIAN_POINT('Ctrl Pts',(2.6113610568486,1.89303621417104,9.30859599707018));
#250731=CARTESIAN_POINT('Ctrl Pts',(2.68511740468086,1.78688112523138,9.30000155340758));
#250732=CARTESIAN_POINT('Ctrl Pts',(2.76344644622969,1.65829416762707,9.29038373695233));
#250733=CARTESIAN_POINT('Ctrl Pts',(2.77440078311683,1.6399012649188,9.28902611191978));
#250734=CARTESIAN_POINT('Ctrl Pts',(2.79110082028487,1.61121465780451,9.28693819432081));
#250735=CARTESIAN_POINT('Ctrl Pts',(2.79697446770584,1.60099665825581,9.28620022551655));
#250736=CARTESIAN_POINT('Ctrl Pts',(2.80771206017983,1.58207771734311,9.28484473344258));
#250737=CARTESIAN_POINT('Ctrl Pts',(2.81259173033896,1.57338637306132,9.28422626083309));
#250738=CARTESIAN_POINT('Ctrl Pts',(2.82371655406337,1.55335442880377,9.28281037849427));
#250739=CARTESIAN_POINT('Ctrl Pts',(2.82993377498239,1.54199870350698,9.28201471718869));
#250740=CARTESIAN_POINT('Ctrl Pts',(2.84932674839883,1.50606516650349,9.27951790942258));
#250741=CARTESIAN_POINT('Ctrl Pts',(2.8622524014073,1.48135293336928,9.27783151392644));
#250742=CARTESIAN_POINT('Ctrl Pts',(2.92891205126769,1.34977711604699,9.26899751263772));
#250743=CARTESIAN_POINT('Ctrl Pts',(2.97699165276299,1.24014131050492,9.26213546966041));
#250744=CARTESIAN_POINT('Ctrl Pts',(3.12091495578911,0.854985203175454,
9.23889148732172));
#250745=CARTESIAN_POINT('Ctrl Pts',(3.18543006684272,0.569333836528587,
9.2229749702295));
#250746=CARTESIAN_POINT('Ctrl Pts',(3.21440612881801,0.235765640543175,
9.2031355070566));
#250747=CARTESIAN_POINT('Ctrl Pts',(3.21728332597761,0.19256150800319,9.20054563537087));
#250748=CARTESIAN_POINT('Ctrl Pts',(3.22031710669064,0.127151578323691,
9.19658808703209));
#250749=CARTESIAN_POINT('Ctrl Pts',(3.22111611723109,0.104979584072407,
9.19524027500394));
#250750=CARTESIAN_POINT('Ctrl Pts',(3.22214153330588,0.0650821452169431,
9.19280282531749));
#250751=CARTESIAN_POINT('Ctrl Pts',(3.22245074365331,0.0473595958562845,
9.19171580326542));
#250752=CARTESIAN_POINT('Ctrl Pts',(3.22279926085774,0.00946147154036004,
9.18938172343155));
#250753=CARTESIAN_POINT('Ctrl Pts',(3.22279533689981,-0.0107136497997664,
9.18813336853537));
#250754=CARTESIAN_POINT('Ctrl Pts',(3.2222673539085,-0.0658007884909828,
9.18470836132474));
#250755=CARTESIAN_POINT('Ctrl Pts',(3.22136537290233,-0.100705637038769,
9.18252011643383));
#250756=CARTESIAN_POINT('Ctrl Pts',(3.2117510543864,-0.329023317061161,
9.16808338118603));
#250757=CARTESIAN_POINT('Ctrl Pts',(3.18619300942496,-0.521299454672617,
9.15531103800266));
#250758=CARTESIAN_POINT('Ctrl Pts',(3.10020748318422,-0.901953506429309,
9.12905298927459));
#250759=CARTESIAN_POINT('Ctrl Pts',(3.03939388735818,-1.08944745710421,
9.11561729865114));
#250760=CARTESIAN_POINT('Ctrl Pts',(2.94061627282881,-1.31977246839704,
9.09918724606191));
#250761=CARTESIAN_POINT('Ctrl Pts',(2.91812834531447,-1.36877724630226,
9.09569826990591));
#250762=CARTESIAN_POINT('Ctrl Pts',(2.88685322128073,-1.43265213382302,
9.09118074014602));
#250763=CARTESIAN_POINT('Ctrl Pts',(2.87916244551326,-1.44804602840178,
9.09009437824143));
#250764=CARTESIAN_POINT('Ctrl Pts',(2.86647125687722,-1.47294788337783,
9.08834177604551));
#250765=CARTESIAN_POINT('Ctrl Pts',(2.86154607134036,-1.482493515369,9.08767109393355));
#250766=CARTESIAN_POINT('Ctrl Pts',(2.85179849271435,-1.50115598242906,
9.08636236779632));
#250767=CARTESIAN_POINT('Ctrl Pts',(2.84697992768021,-1.51027455176945,
9.08572412199129));
#250768=CARTESIAN_POINT('Ctrl Pts',(2.83495133138678,-1.53277511922437,
9.08415182683004));
#250769=CARTESIAN_POINT('Ctrl Pts',(2.82769012541347,-1.54612974648939,
9.08322092638036));
#250770=CARTESIAN_POINT('Ctrl Pts',(2.80000523153786,-1.59619965811925,
9.07973751520617));
#250771=CARTESIAN_POINT('Ctrl Pts',(2.7789578252253,-1.63256743313165,9.07722116301177));
#250772=CARTESIAN_POINT('Ctrl Pts',(2.61844777940571,-1.89780864678177,
9.05889344588966));
#250773=CARTESIAN_POINT('Ctrl Pts',(2.45161721041623,-2.10892236171782,
9.04436922798549));
#250774=CARTESIAN_POINT('Ctrl Pts',(2.16031459842974,-2.39560806092738,
9.02121276734335));
#250775=CARTESIAN_POINT('Ctrl Pts',(2.05373667529267,-2.48758040434914,
9.01310302402228));
#250776=CARTESIAN_POINT('Ctrl Pts',(1.9145618044599,-2.5926260471843,9.00269055170905));
#250777=CARTESIAN_POINT('Ctrl Pts',(1.88730554256204,-2.61253409242558,
9.00065971133069));
#250778=CARTESIAN_POINT('Ctrl Pts',(1.8434692722266,-2.64350820527525,8.997403895119));
#250779=CARTESIAN_POINT('Ctrl Pts',(1.82709016275755,-2.65485519352223,
8.99618964122244));
#250780=CARTESIAN_POINT('Ctrl Pts',(1.79591293049383,-2.67602873991179,
8.99388203552029));
#250781=CARTESIAN_POINT('Ctrl Pts',(1.78113668263124,-2.68588629108383,
8.99278990481542));
#250782=CARTESIAN_POINT('Ctrl Pts',(1.7473930736956,-2.70799646845851,8.99029897044064));
#250783=CARTESIAN_POINT('Ctrl Pts',(1.72837707138401,-2.72017280425203,
8.98889740911024));
#250784=CARTESIAN_POINT('Ctrl Pts',(1.66953696502145,-2.75698324441747,
8.98456646529523));
#250785=CARTESIAN_POINT('Ctrl Pts',(1.62930407134655,-2.78094914807715,
8.98161311002642));
#250786=CARTESIAN_POINT('Ctrl Pts',(1.53438466208592,-2.83472378560857,
8.97466064660419));
#250787=CARTESIAN_POINT('Ctrl Pts',(1.47932916877494,-2.86384001592262,
8.97063930294934));
#250788=CARTESIAN_POINT('Ctrl Pts',(1.26940216781119,-2.96719143655235,
8.95535136796648));
#250789=CARTESIAN_POINT('Ctrl Pts',(1.10953435010655,-3.03059892613544,
8.94378059685818));
#250790=CARTESIAN_POINT('Ctrl Pts',(0.78364615359253,-3.13059771829394,
8.92073970149784));
#250791=CARTESIAN_POINT('Ctrl Pts',(0.61822635421217,-3.16742000636907,
8.90930940428953));
#250792=CARTESIAN_POINT('Ctrl Pts',(0.421443125242144,-3.1952111645793,
8.8965090809936));
#250793=CARTESIAN_POINT('Ctrl Pts',(0.392161672726725,-3.19893701994791,
8.89462520268363));
#250794=CARTESIAN_POINT('Ctrl Pts',(0.34960680670148,-3.20375869795211,
8.89192143689016));
#250795=CARTESIAN_POINT('Ctrl Pts',(0.336372174169736,-3.20517526648536,
8.89108533109125));
#250796=CARTESIAN_POINT('Ctrl Pts',(0.313147726848543,-3.20751565837872,
8.88962691855068));
#250797=CARTESIAN_POINT('Ctrl Pts',(0.303161803515259,-3.20847489143776,
8.88900270374776));
#250798=CARTESIAN_POINT('Ctrl Pts',(0.281810321414084,-3.21042530690025,
8.88767428063474));
#250799=CARTESIAN_POINT('Ctrl Pts',(0.270443838352012,-3.21140278507544,
8.88697082309523));
#250800=CARTESIAN_POINT('Ctrl Pts',(0.238883840169156,-3.21394808520337,
8.88502736996646));
#250801=CARTESIAN_POINT('Ctrl Pts',(0.218679992692779,-3.21538596309506,
8.88379429857825));
#250802=CARTESIAN_POINT('Ctrl Pts',(0.0941414129397493,-3.2230698803466,
8.87625435804898));
#250803=CARTESIAN_POINT('Ctrl Pts',(-0.0104428233843836,-3.22442822891139,
8.87018451309583));
#250804=CARTESIAN_POINT('Ctrl Pts',(-0.254242440037465,-3.21572922430982,
8.8562735944833));
#250805=CARTESIAN_POINT('Ctrl Pts',(-0.393102184261726,-3.20172249912519,
8.84852820910064));
#250806=CARTESIAN_POINT('Ctrl Pts',(-0.722358174207838,-3.14676076159942,
8.82980753313708));
#250807=CARTESIAN_POINT('Ctrl Pts',(-0.910781150226642,-3.09747790689216,
8.81878266189032));
#250808=CARTESIAN_POINT('Ctrl Pts',(-1.12610154609363,-3.01980237023165,
8.80512743496005));
#250809=CARTESIAN_POINT('Ctrl Pts',(-1.15840694355028,-3.00755785698603,
8.803050513481));
#250810=CARTESIAN_POINT('Ctrl Pts',(-1.2093654099812,-2.98730056211288,
8.79972642472518));
#250811=CARTESIAN_POINT('Ctrl Pts',(-1.22815089588314,-2.97962660263139,
8.79849053983609));
#250812=CARTESIAN_POINT('Ctrl Pts',(-1.26319482297544,-2.96492328905652,
8.79616473913879));
#250813=CARTESIAN_POINT('Ctrl Pts',(-1.2794702817088,-2.95793628215516,
8.79507628372482));
#250814=CARTESIAN_POINT('Ctrl Pts',(-1.31584634632222,-2.9419637500749,
8.79262452842622));
#250815=CARTESIAN_POINT('Ctrl Pts',(-1.33591397401606,-2.93290574850897,
8.79125880597551));
#250816=CARTESIAN_POINT('Ctrl Pts',(-1.39570241887021,-2.90517788830226,
8.78714948688398));
#250817=CARTESIAN_POINT('Ctrl Pts',(-1.43513499622488,-2.88590211980396,
8.78438534319579));
#250818=CARTESIAN_POINT('Ctrl Pts',(-1.62181230664434,-2.78987672371328,
8.77103362329734));
#250819=CARTESIAN_POINT('Ctrl Pts',(-1.76335348165384,-2.70263908910153,
8.76008718118141));
#250820=CARTESIAN_POINT('Ctrl Pts',(-2.04025760024486,-2.50092939574657,
8.73708279213534));
#250821=CARTESIAN_POINT('Ctrl Pts',(-2.17419872257642,-2.3854054667584,
8.72503644765051));
#250822=CARTESIAN_POINT('Ctrl Pts',(-2.35516790057287,-2.20135181210443,
8.7078897104694));
#250823=CARTESIAN_POINT('Ctrl Pts',(-2.41011128877512,-2.14105849970406,
8.70255022770479));
#250824=CARTESIAN_POINT('Ctrl Pts',(-2.47543153566638,-2.06367272137655,
8.69609636158663));
#250825=CARTESIAN_POINT('Ctrl Pts',(-2.48801230048514,-2.04848754599388,
8.69484816260357));
#250826=CARTESIAN_POINT('Ctrl Pts',(-2.50757727759952,-2.0244261584238,
8.69290008276931));
#250827=CARTESIAN_POINT('Ctrl Pts',(-2.51465533488637,-2.01562735390928,
8.69219385878548));
#250828=CARTESIAN_POINT('Ctrl Pts',(-2.52795288216346,-1.99891796688255,
8.69086458490445));
#250829=CARTESIAN_POINT('Ctrl Pts',(-2.53418156634888,-1.99101547050132,
8.69024092574083));
#250830=CARTESIAN_POINT('Ctrl Pts',(-2.54884423566778,-1.97223227140974,
8.68877013154336));
#250831=CARTESIAN_POINT('Ctrl Pts',(-2.55724566051497,-1.96132651988827,
8.6879252516452));
#250832=CARTESIAN_POINT('Ctrl Pts',(-2.5852673501108,-1.92446586541293,
8.68509875281145));
#250833=CARTESIAN_POINT('Ctrl Pts',(-2.60456506827781,-1.89826687421996,
8.68313794025373));
#250834=CARTESIAN_POINT('Ctrl Pts',(-2.65084850258132,-1.83339655539997,
8.6783873752143));
#250835=CARTESIAN_POINT('Ctrl Pts',(-2.6773891907197,-1.79441585518096,
8.67562136957392));
#250836=CARTESIAN_POINT('Ctrl Pts',(-2.80953723011168,-1.59086464485736,
8.66155105530988));
#250837=CARTESIAN_POINT('Ctrl Pts',(-2.90086905856561,-1.41750451604792,
8.65077551218534));
#250838=CARTESIAN_POINT('Ctrl Pts',(-3.02605127227559,-1.11632761566876,
8.63244068732546));
#250839=CARTESIAN_POINT('Ctrl Pts',(-3.06879636522613,-0.992803350138108,
8.62502417564863));
#250840=CARTESIAN_POINT('Ctrl Pts',(-3.12108012090744,-0.805630830402293,
8.6136601090384));
#250841=CARTESIAN_POINT('Ctrl Pts',(-3.13640548974017,-0.743735142676799,
8.60988353157016));
#250842=CARTESIAN_POINT('Ctrl Pts',(-3.15540890375623,-0.65589238963739,
8.60447763747915));
#250843=CARTESIAN_POINT('Ctrl Pts',(-3.16062239090892,-0.630290582089017,
8.60289668357907));
#250844=CARTESIAN_POINT('Ctrl Pts',(-3.16892724074735,-0.586810678611111,
8.60020135028748));
#250845=CARTESIAN_POINT('Ctrl Pts',(-3.17218001604058,-0.568964458058292,
8.59909211439376));
#250846=CARTESIAN_POINT('Ctrl Pts',(-3.17812852830832,-0.534690320336822,
8.59695577067443));
#250847=CARTESIAN_POINT('Ctrl Pts',(-3.1808479853168,-0.518267073010762,
8.5959294495332));
#250848=CARTESIAN_POINT('Ctrl Pts',(-3.18627083675221,-0.483865905355045,
8.59377385388674));
#250849=CARTESIAN_POINT('Ctrl Pts',(-3.18894958269097,-0.465884746456411,
8.59264384253899));
#250850=CARTESIAN_POINT('Ctrl Pts',(-3.19493046185517,-0.423266769116533,
8.58995741252176));
#250851=CARTESIAN_POINT('Ctrl Pts',(-3.19809993621978,-0.398612790540039,
8.58839692174112));
#250852=CARTESIAN_POINT('Ctrl Pts',(-3.21548428706028,-0.249794168388317,
8.57893716533452));
#250853=CARTESIAN_POINT('Ctrl Pts',(-3.22275000000241,-0.124942616104005,
8.57082639181437));
#250854=CARTESIAN_POINT('Ctrl Pts',(-3.22275,6.20740264745123E-11,8.56255098483899));
#250855=CARTESIAN_POINT('Ctrl Pts',(-3.22275,-3.27265992083881E-12,8.3171463242964));
#250856=CARTESIAN_POINT('Ctrl Pts',(-3.22274999999986,-0.138871712641594,
8.32549312351733));
#250857=CARTESIAN_POINT('Ctrl Pts',(-3.21377374162208,-0.277619577087055,
8.33342285303866));
#250858=CARTESIAN_POINT('Ctrl Pts',(-3.18241204635537,-0.51891533647005,
8.34713443980879));
#250859=CARTESIAN_POINT('Ctrl Pts',(-3.16393047941058,-0.621742613134248,
8.35295178595872));
#250860=CARTESIAN_POINT('Ctrl Pts',(-3.10222418486365,-0.88959353889187,
8.3683833070302));
#250861=CARTESIAN_POINT('Ctrl Pts',(-3.05084565312801,-1.05237991766055,
8.3780599905183));
#250862=CARTESIAN_POINT('Ctrl Pts',(-2.97001384318958,-1.25185574018367,
8.3908048922322));
#250863=CARTESIAN_POINT('Ctrl Pts',(-2.95232359297695,-1.29302364002687,
8.39348395222062));
#250864=CARTESIAN_POINT('Ctrl Pts',(-2.92447309013411,-1.35428230193386,
8.39755093625097));
#250865=CARTESIAN_POINT('Ctrl Pts',(-2.91495078667706,-1.37465824124986,
8.39891731461877));
#250866=CARTESIAN_POINT('Ctrl Pts',(-2.89744882457046,-1.41110945661461,
8.40138705532542));
#250867=CARTESIAN_POINT('Ctrl Pts',(-2.88954662220992,-1.42722103656994,
8.4024877211873));
#250868=CARTESIAN_POINT('Ctrl Pts',(-2.87223178632144,-1.46179047554909,
8.40486927612088));
#250869=CARTESIAN_POINT('Ctrl Pts',(-2.86277492496354,-1.48022516056698,
8.40615166499027));
#250870=CARTESIAN_POINT('Ctrl Pts',(-2.83677128042319,-1.52973383510967,
8.40962990804915));
#250871=CARTESIAN_POINT('Ctrl Pts',(-2.81989237745962,-1.56062927275954,
8.41183729701543));
#250872=CARTESIAN_POINT('Ctrl Pts',(-2.70479377398057,-1.76334219900991,
8.42657146642839));
#250873=CARTESIAN_POINT('Ctrl Pts',(-2.59144755426381,-1.92604808273369,
8.43964553354388));
#250874=CARTESIAN_POINT('Ctrl Pts',(-2.37086820140168,-2.18767938900173,
8.46268540361899));
#250875=CARTESIAN_POINT('Ctrl Pts',(-2.27050682223379,-2.29167114989787,
8.47249946178378));
#250876=CARTESIAN_POINT('Ctrl Pts',(-2.11610965271627,-2.43151964924748,
8.48639746402007));
#250877=CARTESIAN_POINT('Ctrl Pts',(-2.06743783135525,-2.47303651449886,
8.49062397353537));
#250878=CARTESIAN_POINT('Ctrl Pts',(-1.9958492479982,-2.53050953568307,
8.49658856510336));
#250879=CARTESIAN_POINT('Ctrl Pts',(-1.97391263024284,-2.54765809455641,
8.49838377559063));
#250880=CARTESIAN_POINT('Ctrl Pts',(-1.93919333930804,-2.57408157973627,
8.50117118052213));
#250881=CARTESIAN_POINT('Ctrl Pts',(-1.92656052298175,-2.58355014658103,
8.50217444640652));
#250882=CARTESIAN_POINT('Ctrl Pts',(-1.90307564949418,-2.60088451189204,
8.50401865294826));
#250883=CARTESIAN_POINT('Ctrl Pts',(-1.89224317655639,-2.6087761397484,
8.50486119682657));
#250884=CARTESIAN_POINT('Ctrl Pts',(-1.88125997720383,-2.61667316956632,
8.5057070612078));
#250885=CARTESIAN_POINT('Ctrl Pts',(-1.88115837905766,-2.61674621067049,
8.50571488500447));
#250886=CARTESIAN_POINT('Ctrl Pts',(-1.88095510584785,-2.61689233021979,
8.50573053707531));
#250887=CARTESIAN_POINT('Ctrl Pts',(-1.88085343078481,-2.61696540865241,
8.50573836534846));
#250888=CARTESIAN_POINT('Ctrl Pts',(-1.88064997299479,-2.6171116249185,
8.50575402873597));
#250889=CARTESIAN_POINT('Ctrl Pts',(-1.88054819025442,-2.61718476274406,
8.50576186384995));
#250890=CARTESIAN_POINT('Ctrl Pts',(-1.88034448587217,-2.61733112018699,
8.50577754331885));
#250891=CARTESIAN_POINT('Ctrl Pts',(-1.88024256422565,-2.61740433978461,
8.50578538767228));
#250892=CARTESIAN_POINT('Ctrl Pts',(-1.88003855027385,-2.61755088351372,
8.50580108805802));
#250893=CARTESIAN_POINT('Ctrl Pts',(-1.8799364579533,-2.61762420762746,
8.50580894408921));
#250894=CARTESIAN_POINT('Ctrl Pts',(-1.87973207033225,-2.61777098351325,
8.50582467030998));
#250895=CARTESIAN_POINT('Ctrl Pts',(-1.87962977500507,-2.61784443526996,
8.50583254049885));
#250896=CARTESIAN_POINT('Ctrl Pts',(-1.8794730214717,-2.61795697607002,
8.50584459935918));
#250897=CARTESIAN_POINT('Ctrl Pts',(-1.87941856637409,-2.61799606939392,
8.50584878831658));
#250898=CARTESIAN_POINT('Ctrl Pts',(-1.87930846282484,-2.6180751075451,
8.50585725761032));
#250899=CARTESIAN_POINT('Ctrl Pts',(-1.87925281430645,-2.61811505230645,
8.50586153794263));
#250900=CARTESIAN_POINT('Ctrl Pts',(-1.87914026225081,-2.61819583725013,
8.5058701947013));
#250901=CARTESIAN_POINT('Ctrl Pts',(-1.87908335866791,-2.61823667734283,
8.50587457112132));
#250902=CARTESIAN_POINT('Ctrl Pts',(-1.87896823077708,-2.61831929973529,
8.50588342507882));
#250903=CARTESIAN_POINT('Ctrl Pts',(-1.87891000638037,-2.61836108196703,
8.50588790261249));
#250904=CARTESIAN_POINT('Ctrl Pts',(-1.87879216671046,-2.61844563857855,
8.50589696415966));
#250905=CARTESIAN_POINT('Ctrl Pts',(-1.87873255136201,-2.61848841287038,
8.5059015481675));
#250906=CARTESIAN_POINT('Ctrl Pts',(-1.87861185478983,-2.61857500698266,
8.50591082839499));
#250907=CARTESIAN_POINT('Ctrl Pts',(-1.8785507735042,-2.61861882669431,
8.50591552460705));
#250908=CARTESIAN_POINT('Ctrl Pts',(-1.87842706478953,-2.61870756876487,
8.50592503537669));
#250909=CARTESIAN_POINT('Ctrl Pts',(-1.87836443730723,-2.61875249099637,
8.505929849925));
#250910=CARTESIAN_POINT('Ctrl Pts',(-1.87823755018696,-2.61884349929906,
8.5059396039387));
#250911=CARTESIAN_POINT('Ctrl Pts',(-1.87817329047198,-2.61888958524618,
8.50594454339554));
#250912=CARTESIAN_POINT('Ctrl Pts',(-1.87804304656839,-2.61898298664363,
8.50595455427835));
#250913=CARTESIAN_POINT('Ctrl Pts',(-1.87797706227456,-2.61903030197501,
8.50595962569673));
#250914=CARTESIAN_POINT('Ctrl Pts',(-1.87784326992688,-2.61912623274476,
8.50596990808571));
#250915=CARTESIAN_POINT('Ctrl Pts',(-1.87777546178851,-2.61917484803255,
8.50597511904576));
#250916=CARTESIAN_POINT('Ctrl Pts',(-1.86962271773971,-2.62501950776203,
8.50660160724154));
#250917=CARTESIAN_POINT('Ctrl Pts',(-1.86151092387614,-2.63077813827006,
8.50722035290794));
#250918=CARTESIAN_POINT('Ctrl Pts',(-1.8437088079843,-2.64329243981024,
8.50856813551125));
#250919=CARTESIAN_POINT('Ctrl Pts',(-1.83400789964211,-2.65003247626621,
8.50929613689761));
#250920=CARTESIAN_POINT('Ctrl Pts',(-1.80709417885046,-2.66851312479392,
8.51129877312448));
#250921=CARTESIAN_POINT('Ctrl Pts',(-1.78980390595036,-2.68014061158269,
8.5125661645145));
#250922=CARTESIAN_POINT('Ctrl Pts',(-1.68904982004112,-2.7464865415766,
8.5198487605171));
#250923=CARTESIAN_POINT('Ctrl Pts',(-1.60318514528748,-2.79747722929399,
8.52565123682874));
#250924=CARTESIAN_POINT('Ctrl Pts',(-1.34061496909161,-2.93733638041824,
8.542638889234));
#250925=CARTESIAN_POINT('Ctrl Pts',(-1.15796184088172,-3.01402109964819,
8.55350967576711));
#250926=CARTESIAN_POINT('Ctrl Pts',(-0.87942278267192,-3.10187685626967,
8.57005774984639));
#250927=CARTESIAN_POINT('Ctrl Pts',(-0.788218928751897,-3.12629710050875,
8.57546709884884));
#250928=CARTESIAN_POINT('Ctrl Pts',(-0.633729432688189,-3.16047185636143,
8.58472483727696));
#250929=CARTESIAN_POINT('Ctrl Pts',(-0.570986416323133,-3.17240745468482,
8.58850989625081));
#250930=CARTESIAN_POINT('Ctrl Pts',(-0.482469479632645,-3.18653505882122,
8.59390494078081));
#250931=CARTESIAN_POINT('Ctrl Pts',(-0.456958492874086,-3.1902933026789,
8.59546613383067));
#250932=CARTESIAN_POINT('Ctrl Pts',(-0.413009018921934,-3.19622992382427,
8.59816775333666));
#250933=CARTESIAN_POINT('Ctrl Pts',(-0.394591515719277,-3.19855587553381,
8.59930351837891));
#250934=CARTESIAN_POINT('Ctrl Pts',(-0.357028783342164,-3.20297032209822,
8.60162773880666));
#250935=CARTESIAN_POINT('Ctrl Pts',(-0.337882899964659,-3.20504657639043,
8.60281652714158));
#250936=CARTESIAN_POINT('Ctrl Pts',(-0.289557429898766,-3.20984935875167,
8.60582799756248));
#250937=CARTESIAN_POINT('Ctrl Pts',(-0.260357601587371,-3.21234964474769,
8.6076576298247));
#250938=CARTESIAN_POINT('Ctrl Pts',(-0.14809568101732,-3.22042160633596,
8.61473217281969));
#250939=CARTESIAN_POINT('Ctrl Pts',(-0.0648693395975112,-3.2231719832213,
8.62006270525894));
#250940=CARTESIAN_POINT('Ctrl Pts',(0.242083126850591,-3.2214228157288,
8.64004278411705));
#250941=CARTESIAN_POINT('Ctrl Pts',(0.46504091812718,-3.19685533736955,
8.65523650750677));
#250942=CARTESIAN_POINT('Ctrl Pts',(0.808754587174836,-3.12224744308685,
8.67893766195811));
#250943=CARTESIAN_POINT('Ctrl Pts',(0.932167789778479,-3.08764996819362,
8.68749180547232));
#250944=CARTESIAN_POINT('Ctrl Pts',(1.08064628823913,-3.03630766924657,
8.69760252965113));
#250945=CARTESIAN_POINT('Ctrl Pts',(1.10795978861963,-3.02644773689932,
8.69945451380098));
#250946=CARTESIAN_POINT('Ctrl Pts',(1.14761205852608,-3.0115248271853,8.70212771450214));
#250947=CARTESIAN_POINT('Ctrl Pts',(1.16005776957652,-3.00675260163004,
8.70296451783457));
#250948=CARTESIAN_POINT('Ctrl Pts',(1.18197591072979,-2.99819188404856,
8.704433801318));
#250949=CARTESIAN_POINT('Ctrl Pts',(1.19146041685937,-2.99443545796566,
8.70506810523149));
#250950=CARTESIAN_POINT('Ctrl Pts',(1.21207751000303,-2.98615640023627,
8.70644361191999));
#250951=CARTESIAN_POINT('Ctrl Pts',(1.22320276642896,-2.98161649778246,
8.70718378839269));
#250952=CARTESIAN_POINT('Ctrl Pts',(1.25438787083266,-2.96868681400308,
8.70925345379271));
#250953=CARTESIAN_POINT('Ctrl Pts',(1.27438898852221,-2.96015592390702,
8.71057489389908));
#250954=CARTESIAN_POINT('Ctrl Pts',(1.41419854510252,-2.89884451377434,
8.71978007405008));
#250955=CARTESIAN_POINT('Ctrl Pts',(1.53079321618765,-2.83900280031649,
8.72729422105979));
#250956=CARTESIAN_POINT('Ctrl Pts',(1.76449308185378,-2.70046054916079,
8.74264812493615));
#250957=CARTESIAN_POINT('Ctrl Pts',(1.88072133441807,-2.62084170723687,
8.75045652086408));
#250958=CARTESIAN_POINT('Ctrl Pts',(2.10978917157012,-2.4408174690713,8.76687559314688));
#250959=CARTESIAN_POINT('Ctrl Pts',(2.22152309911971,-2.33957866938473,
8.77548651030867));
#250960=CARTESIAN_POINT('Ctrl Pts',(2.35503891767824,-2.20038583644537,
8.78692824316239));
#250961=CARTESIAN_POINT('Ctrl Pts',(2.38370996624741,-2.1692931297839,8.78946038801784));
#250962=CARTESIAN_POINT('Ctrl Pts',(2.42634837812063,-2.1211871291642,8.79334826630215));
#250963=CARTESIAN_POINT('Ctrl Pts',(2.44076766996782,-2.10457939584093,
8.79468525959255));
#250964=CARTESIAN_POINT('Ctrl Pts',(2.46559381910714,-2.07538702443204,
8.79702705324854));
#250965=CARTESIAN_POINT('Ctrl Pts',(2.47607722087527,-2.06286833387161,
8.79802868518783));
#250966=CARTESIAN_POINT('Ctrl Pts',(2.49951986638565,-2.03443827579246,
8.80029786556783));
#250967=CARTESIAN_POINT('Ctrl Pts',(2.5124230825974,-2.01848182642884,8.80156760173161));
#250968=CARTESIAN_POINT('Ctrl Pts',(2.54704921480069,-1.97481581898038,
8.80503258032998));
#250969=CARTESIAN_POINT('Ctrl Pts',(2.56847133747548,-1.94687237736057,
8.80723948342038));
#250970=CARTESIAN_POINT('Ctrl Pts',(2.68577887739204,-1.78854744782075,
8.81969007021221));
#250971=CARTESIAN_POINT('Ctrl Pts',(2.77218112189211,-1.6514565233853,8.83028851493101));
#250972=CARTESIAN_POINT('Ctrl Pts',(2.97044599114619,-1.27714379461894,
8.85862020696376));
#250973=CARTESIAN_POINT('Ctrl Pts',(3.06433467069823,-1.0317476905041,8.87666825468886));
#250974=CARTESIAN_POINT('Ctrl Pts',(3.13450705190292,-0.749549442219714,
8.89538209243264));
#250975=CARTESIAN_POINT('Ctrl Pts',(3.1411262463419,-0.72130774545741,8.89723201552028));
#250976=CARTESIAN_POINT('Ctrl Pts',(3.15022833624442,-0.679968011310853,
8.89990282012875));
#250977=CARTESIAN_POINT('Ctrl Pts',(3.15301250855036,-0.666938679584662,
8.90073925047146));
#250978=CARTESIAN_POINT('Ctrl Pts',(3.15778556569586,-0.643903671248034,
8.90220812777865));
#250979=CARTESIAN_POINT('Ctrl Pts',(3.15980784914751,-0.633905342266739,
8.90284239480194));
#250980=CARTESIAN_POINT('Ctrl Pts',(3.1641096133106,-0.612104884364183,
8.90421811050322));
#250981=CARTESIAN_POINT('Ctrl Pts',(3.16637056998124,-0.600299474258282,
8.90495853009412));
#250982=CARTESIAN_POINT('Ctrl Pts',(3.17253916188141,-0.567085875891002,
8.90702954124098));
#250983=CARTESIAN_POINT('Ctrl Pts',(3.17629616734186,-0.545649923993654,
8.90835206741264));
#250984=CARTESIAN_POINT('Ctrl Pts',(3.20127623402628,-0.394112322451382,
8.91761252754723));
#250985=CARTESIAN_POINT('Ctrl Pts',(3.21471887212368,-0.262839283720132,
8.9251756856096));
#250986=CARTESIAN_POINT('Ctrl Pts',(3.22145081768205,-0.0974873599437175,
8.93452603952649));
#250987=CARTESIAN_POINT('Ctrl Pts',(3.22229290629807,-0.0638563153275335,
8.93641852989922));
#250988=CARTESIAN_POINT('Ctrl Pts',(3.22380517304242,0.0974202337625863,
8.94547231077243));
#250989=CARTESIAN_POINT('Ctrl Pts',(3.21741784977303,0.225016397026926,
8.95257536077568));
#250990=CARTESIAN_POINT('Ctrl Pts',(3.19299922949613,0.447311592712934,
8.96523772584299));
#250991=CARTESIAN_POINT('Ctrl Pts',(3.17826077705034,0.542206862520621,
8.97073546687506));
#250992=CARTESIAN_POINT('Ctrl Pts',(3.14655065519546,0.699652108231218,
8.98012852397965));
#250993=CARTESIAN_POINT('Ctrl Pts',(3.13188884131935,0.762604454334836,
8.98395791850103));
#250994=CARTESIAN_POINT('Ctrl Pts',(3.10871385541442,0.850109796472525,
8.98940550770157));
#250995=CARTESIAN_POINT('Ctrl Pts',(3.10178096543433,0.875067588276021,
8.99097358626977));
#250996=CARTESIAN_POINT('Ctrl Pts',(3.08935844405652,0.917783938103222,
8.99368336252657));
#250997=CARTESIAN_POINT('Ctrl Pts',(3.08401457492498,0.935583792083977,
8.9948203234438));
#250998=CARTESIAN_POINT('Ctrl Pts',(3.07283013004021,0.971700649106543,
8.99714363044217));
#250999=CARTESIAN_POINT('Ctrl Pts',(3.06697901139717,0.990013574595633,
8.99833027986354));
#251000=CARTESIAN_POINT('Ctrl Pts',(3.05184546061892,1.03595675992544,9.00132958881494));
#251001=CARTESIAN_POINT('Ctrl Pts',(3.04235152575301,1.06351503462374,9.00314908417564));
#251002=CARTESIAN_POINT('Ctrl Pts',(3.00472615316497,1.16810225889175,9.01013439662061));
#251003=CARTESIAN_POINT('Ctrl Pts',(2.97403416798693,1.24417081105629,9.01538307968314));
#251004=CARTESIAN_POINT('Ctrl Pts',(2.84845398573691,1.5241335877863,9.03534353668843));
#251005=CARTESIAN_POINT('Ctrl Pts',(2.73522166173166,1.71907332218323,9.05061170205248));
#251006=CARTESIAN_POINT('Ctrl Pts',(2.52689865642948,2.00434494549809,9.07441685072121));
#251007=CARTESIAN_POINT('Ctrl Pts',(2.44500779261715,2.10346344091809,9.08299877038743));
#251008=CARTESIAN_POINT('Ctrl Pts',(2.33758508292927,2.21870661871043,9.09313825812359));
#251009=CARTESIAN_POINT('Ctrl Pts',(2.31747059021294,2.23970830213674,9.09499294975559));
#251010=CARTESIAN_POINT('Ctrl Pts',(2.28771959420334,2.26994151535602,9.09766929757518));
#251011=CARTESIAN_POINT('Ctrl Pts',(2.27830626650374,2.27938939091333,9.09850659047124));
#251012=CARTESIAN_POINT('Ctrl Pts',(2.26158905372992,2.29596093016854,9.09997640736427));
#251013=CARTESIAN_POINT('Ctrl Pts',(2.25430964712483,2.30310869597198,9.10061075998425));
#251014=CARTESIAN_POINT('Ctrl Pts',(2.23838656252992,2.31859599887127,9.10198599362348));
#251015=CARTESIAN_POINT('Ctrl Pts',(2.22973011416261,2.32692188051089,9.1027258519865));
#251016=CARTESIAN_POINT('Ctrl Pts',(2.20528936357461,2.35016767810853,9.10479375699021));
#251017=CARTESIAN_POINT('Ctrl Pts',(2.18940016856477,2.36497700872762,9.10611377645315));
#251018=CARTESIAN_POINT('Ctrl Pts',(2.07751830969872,2.46716108282812,9.1152505143857));
#251019=CARTESIAN_POINT('Ctrl Pts',(1.9764623039544,2.54883708027539,9.1227039976922));
#251020=CARTESIAN_POINT('Ctrl Pts',(1.83697665060975,2.64827378911859,9.13238792020146));
#251021=CARTESIAN_POINT('Ctrl Pts',(1.80274724615224,2.67169229682434,9.1347194434662));
#251022=CARTESIAN_POINT('Ctrl Pts',(1.65141396068678,2.77099612686269,9.1448731152008));
#251023=CARTESIAN_POINT('Ctrl Pts',(1.52990537793964,2.83989014209792,9.15263749559056));
#251024=CARTESIAN_POINT('Ctrl Pts',(1.32737900486418,2.93793968981156,9.16543737772343));
#251025=CARTESIAN_POINT('Ctrl Pts',(1.24899283547981,2.97211037649064,9.17035792676415));
#251026=CARTESIAN_POINT('Ctrl Pts',(1.11390527433192,3.02471025492896,9.17886144984751));
#251027=CARTESIAN_POINT('Ctrl Pts',(1.05788150545804,3.04475666516966,9.18239438762166));
#251028=CARTESIAN_POINT('Ctrl Pts',(0.97747792121327,3.07103965888363,9.18748969283881));
#251029=CARTESIAN_POINT('Ctrl Pts',(0.953528564650351,3.07855987357206,
9.18901045006191));
#251030=CARTESIAN_POINT('Ctrl Pts',(0.911832644431462,3.09111938099778,
9.19166447150273));
#251031=CARTESIAN_POINT('Ctrl Pts',(0.894125929603302,3.09628755108062,
9.1927935117546));
#251032=CARTESIAN_POINT('Ctrl Pts',(0.85763663308899,3.10659881186108,9.19512467764991));
#251033=CARTESIAN_POINT('Ctrl Pts',(0.838849882616714,3.11172421984555,
9.1963273194556));
#251034=CARTESIAN_POINT('Ctrl Pts',(0.790689683539448,3.12439547603439,
9.19941702500773));
#251035=CARTESIAN_POINT('Ctrl Pts',(0.761254584397249,3.13169740301161,
9.20131178835742));
#251036=CARTESIAN_POINT('Ctrl Pts',(0.641642722384108,3.15958342444384,
9.20903920692168));
#251037=CARTESIAN_POINT('Ctrl Pts',(0.550709468291767,3.17669469404434,
9.21497947844878));
#251038=CARTESIAN_POINT('Ctrl Pts',(0.195913013091476,3.22776665346799,
9.23840887808661));
#251039=CARTESIAN_POINT('Ctrl Pts',(-0.0710160717257073,3.23292233281573,
9.25667631422829));
#251040=CARTESIAN_POINT('Ctrl Pts',(-0.395495009308637,3.19895941854281,
9.27840397080948));
#251041=CARTESIAN_POINT('Ctrl Pts',(-0.455315691451798,3.19099452952216,
9.28238368066898));
#251042=CARTESIAN_POINT('Ctrl Pts',(-0.553473305392612,3.17510838816105,
9.28883621141655));
#251043=CARTESIAN_POINT('Ctrl Pts',(-0.591951236073455,3.16816035301142,
9.29134569372441));
#251044=CARTESIAN_POINT('Ctrl Pts',(-0.644990451313554,3.15758284491279,
9.29476859539456));
#251045=CARTESIAN_POINT('Ctrl Pts',(-0.659665522997785,3.15454965452598,
9.29571178946506));
#251046=CARTESIAN_POINT('Ctrl Pts',(-0.68452614582728,3.14923013912199,
9.29730244525827));
#251047=CARTESIAN_POINT('Ctrl Pts',(-0.694722624315437,3.14699650470987,
9.29795278337363));
#251048=CARTESIAN_POINT('Ctrl Pts',(-0.715821102949639,3.14226714046142,
9.29929396039003));
#251049=CARTESIAN_POINT('Ctrl Pts',(-0.726721198706648,3.13976415381342,
9.29998439236741));
#251050=CARTESIAN_POINT('Ctrl Pts',(-0.755633066626796,3.13296649930565,
9.30180971577636));
#251051=CARTESIAN_POINT('Ctrl Pts',(-0.773621522782923,3.12857318810004,
9.30293919216496));
#251052=CARTESIAN_POINT('Ctrl Pts',(-0.853585083963955,3.10831186364933,
9.30793636105959));
#251053=CARTESIAN_POINT('Ctrl Pts',(-0.915121499975737,3.0907545927545,
9.31171851506432));
#251054=CARTESIAN_POINT('Ctrl Pts',(-1.15559984020283,3.0143293692113,9.32639266697568));
#251055=CARTESIAN_POINT('Ctrl Pts',(-1.32976740692928,2.94165288655902,
9.33680255997277));
#251056=CARTESIAN_POINT('Ctrl Pts',(-1.64888516008725,2.77432199988384,
9.35702748682802));
#251057=CARTESIAN_POINT('Ctrl Pts',(-1.79451992412909,2.68241944435577,
9.36678407159005));
#251058=CARTESIAN_POINT('Ctrl Pts',(-1.96812510062245,2.55237630252674,
9.37962677292588));
#251059=CARTESIAN_POINT('Ctrl Pts',(-2.00355896184414,2.52465688614686,
9.38231635642619));
#251060=CARTESIAN_POINT('Ctrl Pts',(-2.0558475642037,2.48195805368222,9.38639614566082));
#251061=CARTESIAN_POINT('Ctrl Pts',(-2.07314511300689,2.46752797115906,
9.38776459761015));
#251062=CARTESIAN_POINT('Ctrl Pts',(-2.1039502594539,2.44127691914511,9.39023656874927));
#251063=CARTESIAN_POINT('Ctrl Pts',(-2.11751317425248,2.42952209841076,
9.39133737015744));
#251064=CARTESIAN_POINT('Ctrl Pts',(-2.14650130161633,2.40397129082512,
9.39371749797249));
#251065=CARTESIAN_POINT('Ctrl Pts',(-2.16189316647235,2.39013884743985,
9.39499830800429));
#251066=CARTESIAN_POINT('Ctrl Pts',(-2.20302561553596,2.35245133728751,
9.39846800844348));
#251067=CARTESIAN_POINT('Ctrl Pts',(-2.22851092987276,2.32832300973116,
9.40066833803993));
#251068=CARTESIAN_POINT('Ctrl Pts',(-2.38092814783271,2.17922618415016,
9.41414381981346));
#251069=CARTESIAN_POINT('Ctrl Pts',(-2.49769468477755,2.0443457195269,9.42585513849153));
#251070=CARTESIAN_POINT('Ctrl Pts',(-2.67661259410675,1.79932410080635,
9.44621665294377));
#251071=CARTESIAN_POINT('Ctrl Pts',(-2.74454895905638,1.69389266475163,
9.45472194852874));
#251072=CARTESIAN_POINT('Ctrl Pts',(-2.87078134556872,1.47037228885663,
9.4719984995253));
#251073=CARTESIAN_POINT('Ctrl Pts',(-2.92834112964672,1.35211155607308,
9.48074663081971));
#251074=CARTESIAN_POINT('Ctrl Pts',(-2.98674212113149,1.21076514330352,
9.49051330718898));
#251075=CARTESIAN_POINT('Ctrl Pts',(-2.99476117742538,1.19079229001067,
9.49187779278897));
#251076=CARTESIAN_POINT('Ctrl Pts',(-3.00687969139785,1.15971211395653,
9.49397538874179));
#251077=CARTESIAN_POINT('Ctrl Pts',(-3.01111888049899,1.1486604213875,9.494716268362));
#251078=CARTESIAN_POINT('Ctrl Pts',(-3.01890771861766,1.12801523639184,
9.49609064219623));
#251079=CARTESIAN_POINT('Ctrl Pts',(-3.02247260049738,1.11842816913565,
9.49672497460814));
#251080=CARTESIAN_POINT('Ctrl Pts',(-3.03059204095594,1.09627013175207,
9.49818230757814));
#251081=CARTESIAN_POINT('Ctrl Pts',(-3.03511408276803,1.08368761159811,
9.49900341478691));
#251082=CARTESIAN_POINT('Ctrl Pts',(-3.04954717926666,1.04272862519446,
9.50165653420581));
#251083=CARTESIAN_POINT('Ctrl Pts',(-3.05913990599278,1.01424068399603,
9.50347114763969));
#251084=CARTESIAN_POINT('Ctrl Pts',(-3.1193235302528,0.826883378583062,
9.51523078415365));
#251085=CARTESIAN_POINT('Ctrl Pts',(-3.15792492355337,0.664408295753191,
9.52462007141607));
#251086=CARTESIAN_POINT('Ctrl Pts',(-3.20961605577271,0.335037622274209,
9.5433072965792));
#251087=CARTESIAN_POINT('Ctrl Pts',(-3.22264408328298,0.16866344872347,
9.55258213906997));
#251088=CARTESIAN_POINT('Ctrl Pts',(-3.22274978560362,0.00135739825249329,
9.56220666773146));
#251089=CARTESIAN_POINT('Ctrl Pts',(-3.22275,0.000678697741503386,9.5622457156205));
#251090=CARTESIAN_POINT('Ctrl Pts',(-3.22275,-1.85372951893938E-11,9.562284768011));
#251091=CARTESIAN_POINT('Origin',(0.,0.,-2.31077344927308));
#251092=CARTESIAN_POINT('',(-3.22275,2.40369908895709E-12,11.0578560525147));
#251093=CARTESIAN_POINT('',(-3.22275,-7.2705680572429E-11,10.8125553006127));
#251094=CARTESIAN_POINT('',(-3.22275,-3.50678552687464E-13,-2.31077344927308));
#251095=CARTESIAN_POINT('Ctrl Pts',(-3.22275,2.40444816834717E-12,11.0578560525147));
#251096=CARTESIAN_POINT('Ctrl Pts',(-3.22275000000001,0.129559515672562,
11.0500824638212));
#251097=CARTESIAN_POINT('Ctrl Pts',(-3.21493720991752,0.259019917678811,
11.0426677662696));
#251098=CARTESIAN_POINT('Ctrl Pts',(-3.18771361783945,0.483687132446777,
11.029897752772));
#251099=CARTESIAN_POINT('Ctrl Pts',(-3.17176321528631,0.579128619885433,
11.0245043322675));
#251100=CARTESIAN_POINT('Ctrl Pts',(-3.11552323426711,0.842213631850827,
11.0094280728851));
#251101=CARTESIAN_POINT('Ctrl Pts',(-3.06604976184367,1.00754136211081,
10.9996978770402));
#251102=CARTESIAN_POINT('Ctrl Pts',(-2.98418509968392,1.21804217026348,
10.9864012326541));
#251103=CARTESIAN_POINT('Ctrl Pts',(-2.96352674057112,1.2674763142955,10.9832114858982));
#251104=CARTESIAN_POINT('Ctrl Pts',(-2.93192754731569,1.33808991118212,
10.9785457093997));
#251105=CARTESIAN_POINT('Ctrl Pts',(-2.92196825607857,1.35970041452184,
10.9771027185616));
#251106=CARTESIAN_POINT('Ctrl Pts',(-2.90409116951917,1.39738796538432,
10.9745587105735));
#251107=CARTESIAN_POINT('Ctrl Pts',(-2.89627679837646,1.41351311758217,
10.9734612763886));
#251108=CARTESIAN_POINT('Ctrl Pts',(-2.87975861372052,1.44688670264265,
10.9711709021882));
#251109=CARTESIAN_POINT('Ctrl Pts',(-2.8710333763337,1.46412367298211,10.9699772517989));
#251110=CARTESIAN_POINT('Ctrl Pts',(-2.84793373250783,1.50875716279774,
10.9668579223649));
#251111=CARTESIAN_POINT('Ctrl Pts',(-2.83331912727679,1.53602647687385,
10.9649239062851));
#251112=CARTESIAN_POINT('Ctrl Pts',(-2.76907404225313,1.65186367741078,
10.9565841915675));
#251113=CARTESIAN_POINT('Ctrl Pts',(-2.71567051762071,1.73826199208525,
10.9500464450712));
#251114=CARTESIAN_POINT('Ctrl Pts',(-2.51264845676957,2.03447128423172,
10.9264854137821));
#251115=CARTESIAN_POINT('Ctrl Pts',(-2.34206470399986,2.22871816785953,
10.9087913962321));
#251116=CARTESIAN_POINT('Ctrl Pts',(-2.10590428211393,2.44025078974346,
10.8876853480936));
#251117=CARTESIAN_POINT('Ctrl Pts',(-2.0604974497287,2.47871091541957,10.8837630858007));
#251118=CARTESIAN_POINT('Ctrl Pts',(-1.99345692417629,2.5323788946328,10.8781927051519));
#251119=CARTESIAN_POINT('Ctrl Pts',(-1.97266198190285,2.54861102814899,
10.8764942601736));
#251120=CARTESIAN_POINT('Ctrl Pts',(-1.93963780607322,2.57374267127287,
10.8738457817747));
#251121=CARTESIAN_POINT('Ctrl Pts',(-1.92754166185542,2.5828142244877,10.8728857884457));
#251122=CARTESIAN_POINT('Ctrl Pts',(-1.90500983863986,2.59946560081246,
10.8711168717255));
#251123=CARTESIAN_POINT('Ctrl Pts',(-1.8945916865607,2.60706851644924,10.8703065033178));
#251124=CARTESIAN_POINT('Ctrl Pts',(-1.88403504199095,2.61467579943866,
10.8694931644275));
#251125=CARTESIAN_POINT('Ctrl Pts',(-1.8839421101274,2.61474276006432,10.86948600508));
#251126=CARTESIAN_POINT('Ctrl Pts',(-1.88375602480442,2.6148768259124,10.8694716705297));
#251127=CARTESIAN_POINT('Ctrl Pts',(-1.88366287131279,2.61494393112326,
10.8694644953273));
#251128=CARTESIAN_POINT('Ctrl Pts',(-1.88347631387325,2.61507830682526,
10.8694501268533));
#251129=CARTESIAN_POINT('Ctrl Pts',(-1.88338290991514,2.61514557728422,
10.8694429335841));
#251130=CARTESIAN_POINT('Ctrl Pts',(-1.88319582210173,2.61528030456501,
10.8694285267194));
#251131=CARTESIAN_POINT('Ctrl Pts',(-1.88310213822827,2.6153477613555,10.869421313126));
#251132=CARTESIAN_POINT('Ctrl Pts',(-1.88291446051664,2.61548288281355,
10.8694068633089));
#251133=CARTESIAN_POINT('Ctrl Pts',(-1.88282046665552,2.61555054744818,
10.8693996270874));
#251134=CARTESIAN_POINT('Ctrl Pts',(-1.88263213821211,2.61568610658458,
10.8693851296589));
#251135=CARTESIAN_POINT('Ctrl Pts',(-1.88253780361161,2.6157540010448,10.8693778684549));
#251136=CARTESIAN_POINT('Ctrl Pts',(-1.88234876220566,2.61589004232521,
10.8693633186517));
#251137=CARTESIAN_POINT('Ctrl Pts',(-1.88225405537621,2.61595818910264,
10.8693560300556));
#251138=CARTESIAN_POINT('Ctrl Pts',(-1.88206423726578,2.61609475803781,
10.8693414230015));
#251139=CARTESIAN_POINT('Ctrl Pts',(-1.88196912592922,2.61616318016996,
10.8693341045446));
#251140=CARTESIAN_POINT('Ctrl Pts',(-1.88177846568662,2.61630032343963,
10.8693194352373));
#251141=CARTESIAN_POINT('Ctrl Pts',(-1.88168291675512,2.61636904452413,
10.8693120843908));
#251142=CARTESIAN_POINT('Ctrl Pts',(-1.88149134731724,2.61650680993905,
10.8692973477058));
#251143=CARTESIAN_POINT('Ctrl Pts',(-1.88139532676968,2.61657585422175,
10.8692899618705));
#251144=CARTESIAN_POINT('Ctrl Pts',(-1.88120277914009,2.61671429093594,
10.8692751525385));
#251145=CARTESIAN_POINT('Ctrl Pts',(-1.881106252016,2.61678368331414,10.8692677290453));
#251146=CARTESIAN_POINT('Ctrl Pts',(-1.88091265524343,2.61692284183828,
10.8692528416505));
#251147=CARTESIAN_POINT('Ctrl Pts',(-1.88081558555222,2.61699260792493,
10.8692453777529));
#251148=CARTESIAN_POINT('Ctrl Pts',(-1.88062086655704,2.61713254024876,
10.8692304067201));
#251149=CARTESIAN_POINT('Ctrl Pts',(-1.88052321721424,2.61720270641709,
10.8692228995896));
#251150=CARTESIAN_POINT('Ctrl Pts',(-1.88032730067245,2.61734346609033,
10.8692078391751));
#251151=CARTESIAN_POINT('Ctrl Pts',(-1.88022903341423,2.61741405953397,
10.8692002858949));
#251152=CARTESIAN_POINT('Ctrl Pts',(-1.88007235718182,2.61752659956531,
10.8691882441117));
#251153=CARTESIAN_POINT('Ctrl Pts',(-1.88001395080455,2.61756854971391,
10.8691837553688));
#251154=CARTESIAN_POINT('Ctrl Pts',(-1.87989486991375,2.61765407304937,
10.8691746040579));
#251155=CARTESIAN_POINT('Ctrl Pts',(-1.87983419529939,2.61769764607433,
10.8691699415011));
#251156=CARTESIAN_POINT('Ctrl Pts',(-1.8797104378243,2.6177865150668,10.8691604318536));
#251157=CARTESIAN_POINT('Ctrl Pts',(-1.87964735484877,2.61783181085822,
10.869155584775));
#251158=CARTESIAN_POINT('Ctrl Pts',(-1.87951862837204,2.6179242339366,10.8691456944473));
#251159=CARTESIAN_POINT('Ctrl Pts',(-1.87945298470475,2.61797136105697,
10.8691406512087));
#251160=CARTESIAN_POINT('Ctrl Pts',(-1.87931897094449,2.61806756502409,
10.8691303558859));
#251161=CARTESIAN_POINT('Ctrl Pts',(-1.87925060070609,2.61811664165843,
10.8691251038164));
#251162=CARTESIAN_POINT('Ctrl Pts',(-1.87911095272682,2.61821687366412,
10.8691143770005));
#251163=CARTESIAN_POINT('Ctrl Pts',(-1.87903967482744,2.61826802879724,
10.8691089022706));
#251164=CARTESIAN_POINT('Ctrl Pts',(-1.87889401345825,2.61837255887556,
10.869097715008));
#251165=CARTESIAN_POINT('Ctrl Pts',(-1.878819629823,2.61842593354739,10.8690920024945));
#251166=CARTESIAN_POINT('Ctrl Pts',(-1.87866753983554,2.61853505732013,
10.8690803230856));
#251167=CARTESIAN_POINT('Ctrl Pts',(-1.87858983328096,2.6185908061283,10.8690743562103));
#251168=CARTESIAN_POINT('Ctrl Pts',(-1.87518841643377,2.62103084630225,
10.8688131892507));
#251169=CARTESIAN_POINT('Ctrl Pts',(-1.87186015036279,2.62340882675942,
10.868558416429));
#251170=CARTESIAN_POINT('Ctrl Pts',(-1.86058206347832,2.63143440768492,
10.8676977517389));
#251171=CARTESIAN_POINT('Ctrl Pts',(-1.85261113647786,2.63705226271344,
10.8670939383376));
#251172=CARTESIAN_POINT('Ctrl Pts',(-1.83459453773166,2.64962823242715,
10.8657389134714));
#251173=CARTESIAN_POINT('Ctrl Pts',(-1.82453443193824,2.65656564112859,
10.8649890754729));
#251174=CARTESIAN_POINT('Ctrl Pts',(-1.7903420093807,2.67985874735681,10.8624624968122));
#251175=CARTESIAN_POINT('Ctrl Pts',(-1.7660265561831,2.69594468634451,10.8607025588543));
#251176=CARTESIAN_POINT('Ctrl Pts',(-1.60864653225793,2.79701658045753,
10.8495227339465));
#251177=CARTESIAN_POINT('Ctrl Pts',(-1.46969187544244,2.87246626845974,
10.8406027460142));
#251178=CARTESIAN_POINT('Ctrl Pts',(-1.20045221910409,2.99398231688377,
10.8240342908695));
#251179=CARTESIAN_POINT('Ctrl Pts',(-1.07166350145814,3.04245821673982,
10.8163871953811));
#251180=CARTESIAN_POINT('Ctrl Pts',(-0.856075191112018,3.10821232037135,
10.8035805598983));
#251181=CARTESIAN_POINT('Ctrl Pts',(-0.770964254086266,3.13040909811233,
10.7985249098889));
#251182=CARTESIAN_POINT('Ctrl Pts',(-0.625958286859991,3.16195376934715,
10.7898249647499));
#251183=CARTESIAN_POINT('Ctrl Pts',(-0.566513169271558,3.17314316655377,
10.7862347466975));
#251184=CARTESIAN_POINT('Ctrl Pts',(-0.482170066042086,3.18657357604678,
10.7810907875335));
#251185=CARTESIAN_POINT('Ctrl Pts',(-0.457504918898764,3.19020819449482,
10.7795805542101));
#251186=CARTESIAN_POINT('Ctrl Pts',(-0.414861040399264,3.19598742461422,
10.77695816986));
#251187=CARTESIAN_POINT('Ctrl Pts',(-0.396901607538267,3.19826740504563,
10.7758503038028));
#251188=CARTESIAN_POINT('Ctrl Pts',(-0.360145019859527,3.20261935428669,
10.7735754375195));
#251189=CARTESIAN_POINT('Ctrl Pts',(-0.341346959658448,3.20467742413583,
10.7724080486987));
#251190=CARTESIAN_POINT('Ctrl Pts',(-0.293657577687159,3.20947425100848,
10.7694359175106));
#251191=CARTESIAN_POINT('Ctrl Pts',(-0.264745840222058,3.21198837063366,
10.7676242580571));
#251192=CARTESIAN_POINT('Ctrl Pts',(-0.151965747621098,3.22026253570177,
10.7605171867695));
#251193=CARTESIAN_POINT('Ctrl Pts',(-0.0679248644470271,3.2231302406892,
10.7551337872344));
#251194=CARTESIAN_POINT('Ctrl Pts',(0.239870586383329,3.22159004666573,
10.7350934008747));
#251195=CARTESIAN_POINT('Ctrl Pts',(0.46287007883022,3.197172115212,10.7198935749299));
#251196=CARTESIAN_POINT('Ctrl Pts',(0.818417525960991,3.12024546143878,
10.6953756560294));
#251197=CARTESIAN_POINT('Ctrl Pts',(0.953264652701141,3.08172578692523,
10.6860242228825));
#251198=CARTESIAN_POINT('Ctrl Pts',(1.10536200847474,3.02733403948147,10.6757088239057));
#251199=CARTESIAN_POINT('Ctrl Pts',(1.12546321809909,3.01991873364581,10.6743504962642));
#251200=CARTESIAN_POINT('Ctrl Pts',(1.15638707723655,3.0081593072651,10.67227013515));
#251201=CARTESIAN_POINT('Ctrl Pts',(1.1672621925012,3.00395613718951,10.6715403170101));
#251202=CARTESIAN_POINT('Ctrl Pts',(1.18740757747724,2.99604414032993,10.6701920302247));
#251203=CARTESIAN_POINT('Ctrl Pts',(1.19668346033298,2.99235124024546,10.669572697588));
#251204=CARTESIAN_POINT('Ctrl Pts',(1.21791370270418,2.983784580234,10.6681584381055));
#251205=CARTESIAN_POINT('Ctrl Pts',(1.22985609129761,2.97888204134868,10.6673652264292));
#251206=CARTESIAN_POINT('Ctrl Pts',(1.26706696432384,2.96334446940346,10.6649000314335));
#251207=CARTESIAN_POINT('Ctrl Pts',(1.29223012277711,2.9524583922528,10.6632421724089));
#251208=CARTESIAN_POINT('Ctrl Pts',(1.5121369754719,2.8539721771141,10.6488089694089));
#251209=CARTESIAN_POINT('Ctrl Pts',(1.69789124088129,2.74752704567681,10.6369764680038));
#251210=CARTESIAN_POINT('Ctrl Pts',(2.0240181698143,2.51484562641522,10.6145419210475));
#251211=CARTESIAN_POINT('Ctrl Pts',(2.16650977791634,2.3931827868718,10.6040097190267));
#251212=CARTESIAN_POINT('Ctrl Pts',(2.33320013809648,2.22370549559047,10.5899896064324));
#251213=CARTESIAN_POINT('Ctrl Pts',(2.36789887790087,2.18671980424736,10.5869662548543));
#251214=CARTESIAN_POINT('Ctrl Pts',(2.41724078058268,2.13157385881052,10.5825005146122));
#251215=CARTESIAN_POINT('Ctrl Pts',(2.43258332572874,2.11404787711417,10.5810872403182));
#251216=CARTESIAN_POINT('Ctrl Pts',(2.45934402902874,2.08280173192541,10.5785771793172));
#251217=CARTESIAN_POINT('Ctrl Pts',(2.47084081787816,2.06915000429485,10.5774836712426));
#251218=CARTESIAN_POINT('Ctrl Pts',(2.49468847825476,2.0403502012787,10.5751829787462));
#251219=CARTESIAN_POINT('Ctrl Pts',(2.5070160961159,2.02518389646849,10.5739749211863));
#251220=CARTESIAN_POINT('Ctrl Pts',(2.5391511176897,1.98490605577609,10.5707752881733));
#251221=CARTESIAN_POINT('Ctrl Pts',(2.55872358141808,1.95961066671809,10.5687745618497));
#251222=CARTESIAN_POINT('Ctrl Pts',(2.64594959955199,1.84334491088647,10.5596149134085));
#251223=CARTESIAN_POINT('Ctrl Pts',(2.7091437683332,1.74914405162671,10.5522888671342));
#251224=CARTESIAN_POINT('Ctrl Pts',(2.87193251423436,1.47642925180776,10.5313543279428));
#251225=CARTESIAN_POINT('Ctrl Pts',(2.95970872311629,1.29149212229401,10.5174374203378));
#251226=CARTESIAN_POINT('Ctrl Pts',(3.06883075741024,0.990838920094808,
10.4959340487044));
#251227=CARTESIAN_POINT('Ctrl Pts',(3.10240214701306,0.880107884326185,
10.4882454789333));
#251228=CARTESIAN_POINT('Ctrl Pts',(3.13632429541335,0.741824089946173,
10.4791015506356));
#251229=CARTESIAN_POINT('Ctrl Pts',(3.14237363643059,0.715766094794129,
10.4773982422441));
#251230=CARTESIAN_POINT('Ctrl Pts',(3.15082256759938,0.677197765835653,
10.4749092535776));
#251231=CARTESIAN_POINT('Ctrl Pts',(3.15347341233552,0.664744399741812,
10.4741104909091));
#251232=CARTESIAN_POINT('Ctrl Pts',(3.15787195756625,0.643461931609997,
10.4727541770863));
#251233=CARTESIAN_POINT('Ctrl Pts',(3.15965656219293,0.634640822572474,
10.4721945885743));
#251234=CARTESIAN_POINT('Ctrl Pts',(3.16364526309505,0.61449116804347,10.4709222720665));
#251235=CARTESIAN_POINT('Ctrl Pts',(3.16582548377959,0.60315815680108,10.4702108887756));
#251236=CARTESIAN_POINT('Ctrl Pts',(3.17167504042756,0.571845803454318,
10.4682564141));
#251237=CARTESIAN_POINT('Ctrl Pts',(3.17521650160777,0.551842731757692,
10.4670202164048));
#251238=CARTESIAN_POINT('Ctrl Pts',(3.19442190942959,0.437053503647063,
10.4599900496432));
#251239=CARTESIAN_POINT('Ctrl Pts',(3.20603182205207,0.341629263778248,
10.4543941823359));
#251240=CARTESIAN_POINT('Ctrl Pts',(3.22604325100663,0.0800402408187453,
10.4393890944939));
#251241=CARTESIAN_POINT('Ctrl Pts',(3.22587776478429,-0.0864785839638742,
10.4301928452507));
#251242=CARTESIAN_POINT('Ctrl Pts',(3.19905479949046,-0.428122824957318,
10.4109251680659));
#251243=CARTESIAN_POINT('Ctrl Pts',(3.17083061495106,-0.602547191351914,
10.4008612632071));
#251244=CARTESIAN_POINT('Ctrl Pts',(3.12021418627865,-0.807196605100585,
10.388279466622));
#251245=CARTESIAN_POINT('Ctrl Pts',(3.11141303713501,-0.840483018070908,
10.3862087464774));
#251246=CARTESIAN_POINT('Ctrl Pts',(3.09663971301863,-0.892940588733594,
10.3829038980933));
#251247=CARTESIAN_POINT('Ctrl Pts',(3.09101861743526,-0.912208466166179,
10.3816810702794));
#251248=CARTESIAN_POINT('Ctrl Pts',(3.08009110039021,-0.948404479685862,
10.3793664539743));
#251249=CARTESIAN_POINT('Ctrl Pts',(3.07482414844154,-0.965343814469545,
10.3782759826455));
#251250=CARTESIAN_POINT('Ctrl Pts',(3.06260746957594,-1.0035199690134,10.3758015638254));
#251251=CARTESIAN_POINT('Ctrl Pts',(3.05557623719565,-1.02472955435905,
10.3744149989262));
#251252=CARTESIAN_POINT('Ctrl Pts',(3.03402455467029,-1.08754512388,10.370272325954));
#251253=CARTESIAN_POINT('Ctrl Pts',(3.01887116371246,-1.12892691789836,
10.367495668078));
#251254=CARTESIAN_POINT('Ctrl Pts',(2.9216945364884,-1.37834004650121,10.3504624208976));
#251255=CARTESIAN_POINT('Ctrl Pts',(2.81906256051531,-1.57764868651717,
10.3355151470663));
#251256=CARTESIAN_POINT('Ctrl Pts',(2.62172777414765,-1.87919798964267,
10.3111615725701));
#251257=CARTESIAN_POINT('Ctrl Pts',(2.53958033139242,-1.98881287674083,
10.301894887446));
#251258=CARTESIAN_POINT('Ctrl Pts',(2.42184087033945,-2.12668300612386,
10.2899373943055));
#251259=CARTESIAN_POINT('Ctrl Pts',(2.39227366546494,-2.15988909330625,
10.2870327490336));
#251260=CARTESIAN_POINT('Ctrl Pts',(2.34084151343558,-2.21529870969672,
10.2821580120184));
#251261=CARTESIAN_POINT('Ctrl Pts',(2.31932486032319,-2.23781583720903,
10.2801688567827));
#251262=CARTESIAN_POINT('Ctrl Pts',(2.28799675801897,-2.26966328647004,
10.2773481260236));
#251263=CARTESIAN_POINT('Ctrl Pts',(2.2784483766346,-2.27924847457159,10.2764981878265));
#251264=CARTESIAN_POINT('Ctrl Pts',(2.26171674059134,-2.29583438897668,
10.2750262332787));
#251265=CARTESIAN_POINT('Ctrl Pts',(2.25456074653232,-2.30286213372949,
10.2744021593844));
#251266=CARTESIAN_POINT('Ctrl Pts',(2.23918887936418,-2.31781817038377,
10.2730733464969));
#251267=CARTESIAN_POINT('Ctrl Pts',(2.23096358669727,-2.32573631190899,
10.2723693644935));
#251268=CARTESIAN_POINT('Ctrl Pts',(2.20838220792933,-2.34724441753236,
10.270455254444));
#251269=CARTESIAN_POINT('Ctrl Pts',(2.19394262994782,-2.36074651594631,
10.2692515641771));
#251270=CARTESIAN_POINT('Ctrl Pts',(2.11598168216531,-2.43231274509408,
10.2628544096569));
#251271=CARTESIAN_POINT('Ctrl Pts',(2.05027256359547,-2.48795273277165,
10.2578192561318));
#251272=CARTESIAN_POINT('Ctrl Pts',(1.84571755794919,-2.64754648481533,
10.2429126182326));
#251273=CARTESIAN_POINT('Ctrl Pts',(1.7006369409604,-2.74299392040663,10.233328347952));
#251274=CARTESIAN_POINT('Ctrl Pts',(1.40431094221198,-2.90535521079721,
10.2143422596809));
#251275=CARTESIAN_POINT('Ctrl Pts',(1.25422093900046,-2.97323049176442,
10.2049826725908));
#251276=CARTESIAN_POINT('Ctrl Pts',(1.05853854124332,-3.04426072922567,
10.1926463922301));
#251277=CARTESIAN_POINT('Ctrl Pts',(1.01716378329628,-3.05833366342234,
10.1900319395905));
#251278=CARTESIAN_POINT('Ctrl Pts',(0.954568151810045,-3.07821382147114,
10.1860613584832));
#251279=CARTESIAN_POINT('Ctrl Pts',(0.933552105159202,-3.08465251160618,
10.1847257406609));
#251280=CARTESIAN_POINT('Ctrl Pts',(0.895487776857363,-3.09588966478814,
10.1823013871994));
#251281=CARTESIAN_POINT('Ctrl Pts',(0.87846255451134,-3.10076356656255,
10.1812151439832));
#251282=CARTESIAN_POINT('Ctrl Pts',(0.841818634359222,-3.11092780497337,
10.1788727545809));
#251283=CARTESIAN_POINT('Ctrl Pts',(0.822188421630395,-3.11617338898441,
10.1776152191118));
#251284=CARTESIAN_POINT('Ctrl Pts',(0.76893714291606,-3.12986499718136,
10.1741959590729));
#251285=CARTESIAN_POINT('Ctrl Pts',(0.735228024672672,-3.13795456190473,
10.1720229780966));
#251286=CARTESIAN_POINT('Ctrl Pts',(0.526306521153107,-3.18454072381635,
10.1584984431316));
#251287=CARTESIAN_POINT('Ctrl Pts',(0.348290400572125,-3.20888985430075,
10.1467024106685));
#251288=CARTESIAN_POINT('Ctrl Pts',(0.0436929198071317,-3.22490365054046,
10.1262263081205));
#251289=CARTESIAN_POINT('Ctrl Pts',(-0.0820899289610667,-3.22415462304401,
10.1176942664966));
#251290=CARTESIAN_POINT('Ctrl Pts',(-0.327726135818035,-3.20830587946999,
10.1011263811008));
#251291=CARTESIAN_POINT('Ctrl Pts',(-0.447430289492116,-3.19381316820066,
10.0930982363304));
#251292=CARTESIAN_POINT('Ctrl Pts',(-0.593596385922959,-3.16773480216498,
10.0835519469774));
#251293=CARTESIAN_POINT('Ctrl Pts',(-0.621077384967557,-3.16246161236671,
10.0817686352589));
#251294=CARTESIAN_POINT('Ctrl Pts',(-0.661185426586292,-3.15422247818178,
10.0791861887806));
#251295=CARTESIAN_POINT('Ctrl Pts',(-0.673867993175267,-3.15153733142956,
10.0783725744861));
#251296=CARTESIAN_POINT('Ctrl Pts',(-0.696274348090948,-3.1466520261773,
10.0769408551081));
#251297=CARTESIAN_POINT('Ctrl Pts',(-0.706004553888015,-3.14448318814055,
10.0763210446372));
#251298=CARTESIAN_POINT('Ctrl Pts',(-0.72720402078029,-3.13965451602341,
10.0749749173961));
#251299=CARTESIAN_POINT('Ctrl Pts',(-0.738668887051276,-3.13697696090308,
10.0742496023513));
#251300=CARTESIAN_POINT('Ctrl Pts',(-0.770883027783834,-3.12926712811156,
10.0722185013975));
#251301=CARTESIAN_POINT('Ctrl Pts',(-0.791597755525732,-3.12409129988145,
10.0709205127041));
#251302=CARTESIAN_POINT('Ctrl Pts',(-0.934847582026179,-3.0867822427956,
10.0619908996144));
#251303=CARTESIAN_POINT('Ctrl Pts',(-1.05546026659361,-3.04765079909803,
10.0547067957531));
#251304=CARTESIAN_POINT('Ctrl Pts',(-1.30908287551892,-2.94849491488588,
10.0392999032399));
#251305=CARTESIAN_POINT('Ctrl Pts',(-1.4409503543999,-2.88634433468575,
10.0312281416478));
#251306=CARTESIAN_POINT('Ctrl Pts',(-1.6877552236746,-2.74887951241976,
10.0153116396247));
#251307=CARTESIAN_POINT('Ctrl Pts',(-1.80296991483538,-2.67472439604047,
10.0074985531772));
#251308=CARTESIAN_POINT('Ctrl Pts',(-1.95451730268703,-2.5629331975319,
9.99639704328105));
#251309=CARTESIAN_POINT('Ctrl Pts',(-1.99518045102844,-2.5314065249193,
9.99333072051505));
#251310=CARTESIAN_POINT('Ctrl Pts',(-2.05323296890008,-2.48412975146782,
9.98881324198336));
#251311=CARTESIAN_POINT('Ctrl Pts',(-2.07123376886894,-2.46914091885184,
9.98739219041687));
#251312=CARTESIAN_POINT('Ctrl Pts',(-2.10267298615895,-2.44237651827957,
9.98487329441997));
#251313=CARTESIAN_POINT('Ctrl Pts',(-2.11617999526046,-2.43068281585747,
9.98377880798886));
#251314=CARTESIAN_POINT('Ctrl Pts',(-2.1442116696344,-2.40600362503734,
9.98148106103961));
#251315=CARTESIAN_POINT('Ctrl Pts',(-2.1587171681153,-2.39299755318181,
9.98027697145764));
#251316=CARTESIAN_POINT('Ctrl Pts',(-2.19650898930915,-2.35848900695116,
9.97709944920224));
#251317=CARTESIAN_POINT('Ctrl Pts',(-2.21959712401429,-2.33677355101574,
9.97511709259614));
#251318=CARTESIAN_POINT('Ctrl Pts',(-2.32074258419305,-2.23879002540763,
9.96624484796009));
#251319=CARTESIAN_POINT('Ctrl Pts',(-2.39520908676409,-2.1589339924646,
9.95920095065294));
#251320=CARTESIAN_POINT('Ctrl Pts',(-2.59846943925162,-1.91747763768109,
9.93842971405541));
#251321=CARTESIAN_POINT('Ctrl Pts',(-2.7159618324353,-1.74708386750235,
9.92436463276535));
#251322=CARTESIAN_POINT('Ctrl Pts',(-2.87315530136083,-1.4644993501895,
9.90261469915405));
#251323=CARTESIAN_POINT('Ctrl Pts',(-2.92438204142517,-1.35932867975168,
9.8948350334685));
#251324=CARTESIAN_POINT('Ctrl Pts',(-2.98049777336008,-1.22617762563944,
9.88554819303935));
#251325=CARTESIAN_POINT('Ctrl Pts',(-2.99088472801249,-1.20061950972758,
9.88379050164617));
#251326=CARTESIAN_POINT('Ctrl Pts',(-3.00564195195522,-1.16292741397468,
9.88123793143092));
#251327=CARTESIAN_POINT('Ctrl Pts',(-3.01026933372748,-1.15089628774862,
9.88042902735747));
#251328=CARTESIAN_POINT('Ctrl Pts',(-3.01834520826996,-1.1295171667381,
9.87900239980745));
#251329=CARTESIAN_POINT('Ctrl Pts',(-3.02182268579938,-1.12018056157456,
9.87838301686273));
#251330=CARTESIAN_POINT('Ctrl Pts',(-3.02933335543215,-1.09972580700982,
9.87703407888066));
#251331=CARTESIAN_POINT('Ctrl Pts',(-3.03334868894276,-1.08860147458359,
9.87630556116738));
#251332=CARTESIAN_POINT('Ctrl Pts',(-3.04452129425325,-1.05710634739461,
9.87425670802984));
#251333=CARTESIAN_POINT('Ctrl Pts',(-3.0515353666761,-1.03668495866133,
9.87294438635643));
#251334=CARTESIAN_POINT('Ctrl Pts',(-3.10365722453508,-0.879818686650472,
9.86297600660099));
#251335=CARTESIAN_POINT('Ctrl Pts',(-3.13980374757823,-0.740548013958625,
9.85476901781731));
#251336=CARTESIAN_POINT('Ctrl Pts',(-3.20380124348284,-0.402411361627577,
9.83538110810482));
#251337=CARTESIAN_POINT('Ctrl Pts',(-3.22262044088577,-0.202468119866952,
9.82432452570155));
#251338=CARTESIAN_POINT('Ctrl Pts',(-3.222749777796,-0.00138189335566572,
9.81276902482661));
#251339=CARTESIAN_POINT('Ctrl Pts',(-3.22275,-0.000690945209040148,9.81272931446407));
#251340=CARTESIAN_POINT('Ctrl Pts',(-3.22275,1.94885615773067E-11,9.8126895994942));
#251341=CARTESIAN_POINT('Ctrl Pts',(-3.22275,-1.85372951893938E-11,9.562284768011));
#251342=CARTESIAN_POINT('Ctrl Pts',(-3.22274999999945,-0.0962321027425494,
9.56782198041187));
#251343=CARTESIAN_POINT('Ctrl Pts',(-3.21843979371273,-0.192408777702062,
9.57345181231487));
#251344=CARTESIAN_POINT('Ctrl Pts',(-3.20707792591733,-0.318932905869064,
9.58105853626993));
#251345=CARTESIAN_POINT('Ctrl Pts',(-3.2038820531936,-0.349580766234551,
9.58291653836422));
#251346=CARTESIAN_POINT('Ctrl Pts',(-3.19793787038363,-0.399617562483878,
9.58597732843694));
#251347=CARTESIAN_POINT('Ctrl Pts',(-3.19545139346795,-0.419036018576571,
9.58717192763092));
#251348=CARTESIAN_POINT('Ctrl Pts',(-3.19028530996339,-0.456657074450286,
9.58949996821545));
#251349=CARTESIAN_POINT('Ctrl Pts',(-3.18762643730845,-0.474861786908061,
9.59063271783305));
#251350=CARTESIAN_POINT('Ctrl Pts',(-3.18101618282989,-0.517560782271938,
9.59330462655044));
#251351=CARTESIAN_POINT('Ctrl Pts',(-3.17693756748288,-0.542033907005987,
9.59484772100777));
#251352=CARTESIAN_POINT('Ctrl Pts',(-3.16243381297604,-0.623265631179853,
9.60000966123524));
#251353=CARTESIAN_POINT('Ctrl Pts',(-3.15076730538574,-0.679788479129602,
9.60366700673457));
#251354=CARTESIAN_POINT('Ctrl Pts',(-3.0744917566204,-1.00496895145065,
9.62510002685287));
#251355=CARTESIAN_POINT('Ctrl Pts',(-2.97706596121778,-1.26470985862877,
9.64392310907279));
#251356=CARTESIAN_POINT('Ctrl Pts',(-2.7900972148905,-1.6176032882052,9.67076539476172));
#251357=CARTESIAN_POINT('Ctrl Pts',(-2.7262474916412,-1.72303908715321,
9.67894651569399));
#251358=CARTESIAN_POINT('Ctrl Pts',(-2.64430881096152,-1.84233904030726,
9.68819216376206));
#251359=CARTESIAN_POINT('Ctrl Pts',(-2.6319264157136,-1.85998538353255,
9.68955932979151));
#251360=CARTESIAN_POINT('Ctrl Pts',(-2.61239176967226,-1.88723877097242,
9.69166850935367));
#251361=CARTESIAN_POINT('Ctrl Pts',(-2.60536170788986,-1.89693208067139,
9.69241822870606));
#251362=CARTESIAN_POINT('Ctrl Pts',(-2.59223923766178,-1.91481525942628,
9.69380018551293));
#251363=CARTESIAN_POINT('Ctrl Pts',(-2.58616191181144,-1.92301542185027,
9.69443335660544));
#251364=CARTESIAN_POINT('Ctrl Pts',(-2.57202205498927,-1.94190612223838,
9.69589097047663));
#251365=CARTESIAN_POINT('Ctrl Pts',(-2.56393175221499,-1.95257543349369,
9.69671349454999));
#251366=CARTESIAN_POINT('Ctrl Pts',(-2.53788522016222,-1.98648398678553,
9.69932636638615));
#251367=CARTESIAN_POINT('Ctrl Pts',(-2.51967719653696,-2.00952904473933,
9.7011002851901));
#251368=CARTESIAN_POINT('Ctrl Pts',(-2.41838645004665,-2.13418638149031,
9.71070550690763));
#251369=CARTESIAN_POINT('Ctrl Pts',(-2.32946236532251,-2.23090939190069,
9.71819638101887));
#251370=CARTESIAN_POINT('Ctrl Pts',(-2.06713733959746,-2.4833976731781,
9.7387150502813));
#251371=CARTESIAN_POINT('Ctrl Pts',(-1.88240604270644,-2.6261882417984,
9.75152986706854));
#251372=CARTESIAN_POINT('Ctrl Pts',(-1.62131331104691,-2.78618911293639,
9.76934133879545));
#251373=CARTESIAN_POINT('Ctrl Pts',(-1.55743264850188,-2.82239419473062,
9.77367250458529));
#251374=CARTESIAN_POINT('Ctrl Pts',(-1.46760410592529,-2.86932689611946,
9.77975833009877));
#251375=CARTESIAN_POINT('Ctrl Pts',(-1.44266664334263,-2.88194578898451,
9.78144725880781));
#251376=CARTESIAN_POINT('Ctrl Pts',(-1.40222817996101,-2.90175214026934,
9.78418658944015));
#251377=CARTESIAN_POINT('Ctrl Pts',(-1.38682830694376,-2.90914361657339,
9.78522991609857));
#251378=CARTESIAN_POINT('Ctrl Pts',(-1.35464247041182,-2.92427820924333,
9.78741110559755));
#251379=CARTESIAN_POINT('Ctrl Pts',(-1.33784722831536,-2.93200000664033,
9.78854964927417));
#251380=CARTESIAN_POINT('Ctrl Pts',(-1.29787556437565,-2.94996246959092,
9.79126059027445));
#251381=CARTESIAN_POINT('Ctrl Pts',(-1.27464324029334,-2.96007501666025,
9.79283725521905));
#251382=CARTESIAN_POINT('Ctrl Pts',(-1.19510912032014,-2.99358463031365,
9.79823952638052));
#251383=CARTESIAN_POINT('Ctrl Pts',(-1.13826647228302,-3.01565637750549,
9.80210871915992));
#251384=CARTESIAN_POINT('Ctrl Pts',(-0.997518243332143,-3.06576194884772,
9.81171398015589));
#251385=CARTESIAN_POINT('Ctrl Pts',(-0.913022122182944,-3.09197792081681,
9.81750223093712));
#251386=CARTESIAN_POINT('Ctrl Pts',(-0.696752763617842,-3.14943990624143,
9.83234551167564));
#251387=CARTESIAN_POINT('Ctrl Pts',(-0.563891681021471,-3.1759185617064,
9.84149454060881));
#251388=CARTESIAN_POINT('Ctrl Pts',(-0.381604161391807,-3.20044645960606,
9.85392113059384));
#251389=CARTESIAN_POINT('Ctrl Pts',(-0.333299740472735,-3.20583696873979,
9.85720127972051));
#251390=CARTESIAN_POINT('Ctrl Pts',(-0.163201604872059,-3.2209327587457,
9.86867678295111));
#251391=CARTESIAN_POINT('Ctrl Pts',(-0.040982986919448,-3.22480528078886,
9.87679033448565));
#251392=CARTESIAN_POINT('Ctrl Pts',(0.102695183209003,-3.22118531498955,
9.88597150634783));
#251393=CARTESIAN_POINT('Ctrl Pts',(0.124213765143733,-3.22042732133966,
9.88733703168111));
#251394=CARTESIAN_POINT('Ctrl Pts',(0.157679791043669,-3.21891253141349,
9.88944422854073));
#251395=CARTESIAN_POINT('Ctrl Pts',(0.169632911883861,-3.21830475363847,
9.89019358375382));
#251396=CARTESIAN_POINT('Ctrl Pts',(0.191774043212813,-3.21705524903515,
9.89157522140595));
#251397=CARTESIAN_POINT('Ctrl Pts',(0.20196245435659,-3.21643170761852,
9.89220843358008));
#251398=CARTESIAN_POINT('Ctrl Pts',(0.225516870474322,-3.21487778986251,
9.8936665945339));
#251399=CARTESIAN_POINT('Ctrl Pts',(0.238880217683845,-3.21391246284122,
9.89448961933538));
#251400=CARTESIAN_POINT('Ctrl Pts',(0.281560742246336,-3.21056167478276,
9.89710576086434));
#251401=CARTESIAN_POINT('Ctrl Pts',(0.310852329389705,-3.20785811484842,
9.89888239083612));
#251402=CARTESIAN_POINT('Ctrl Pts',(0.471069344734558,-3.19085511220588,
9.90851677304215));
#251403=CARTESIAN_POINT('Ctrl Pts',(0.601073851334395,-3.16893989396507,
9.91603182619867));
#251404=CARTESIAN_POINT('Ctrl Pts',(0.957418243772569,-3.08614240151789,
9.9366464381391));
#251405=CARTESIAN_POINT('Ctrl Pts',(1.17898751756106,-3.00847290682051,
9.94953274391293));
#251406=CARTESIAN_POINT('Ctrl Pts',(1.45519285522081,-2.87640800732054,
9.96735325773499));
#251407=CARTESIAN_POINT('Ctrl Pts',(1.51913327412975,-2.84315709117237,
9.97160667169849));
#251408=CARTESIAN_POINT('Ctrl Pts',(1.60607639324364,-2.79417358979463,
9.97760019554757));
#251409=CARTESIAN_POINT('Ctrl Pts',(1.63007280461226,-2.78024279694901,
9.97927722934043));
#251410=CARTESIAN_POINT('Ctrl Pts',(1.66851539246745,-2.75725669674366,
9.98200240627509));
#251411=CARTESIAN_POINT('Ctrl Pts',(1.6830751332866,-2.74839338250801,9.98304361699469));
#251412=CARTESIAN_POINT('Ctrl Pts',(1.71330023562836,-2.72966345903398,
9.98522449255018));
#251413=CARTESIAN_POINT('Ctrl Pts',(1.72895222202218,-2.71977655118953,
9.98636487107372));
#251414=CARTESIAN_POINT('Ctrl Pts',(1.76595778086049,-2.69595268222535,
9.98908781307619));
#251415=CARTESIAN_POINT('Ctrl Pts',(1.78723258214847,-2.68189622961948,
9.99067474674864));
#251416=CARTESIAN_POINT('Ctrl Pts',(1.85965327847774,-2.6328028040623,9.99615234777263));
#251417=CARTESIAN_POINT('Ctrl Pts',(1.90995120648743,-2.59654510273198,
10.0000882650041));
#251418=CARTESIAN_POINT('Ctrl Pts',(2.03104674591429,-2.50382937036233,
10.0098993892052));
#251419=CARTESIAN_POINT('Ctrl Pts',(2.10056774832913,-2.44579747409989,
10.0158297760523));
#251420=CARTESIAN_POINT('Ctrl Pts',(2.26588843881952,-2.29554474566585,
10.0306628071818));
#251421=CARTESIAN_POINT('Ctrl Pts',(2.35860075298049,-2.20017619788263,
10.0396473615428));
#251422=CARTESIAN_POINT('Ctrl Pts',(2.4784402047365,-2.06059754898109,10.0520759032181));
#251423=CARTESIAN_POINT('Ctrl Pts',(2.51079736901623,-2.02104547585121,
10.0555239368598));
#251424=CARTESIAN_POINT('Ctrl Pts',(2.61519800545268,-1.88705144390188,
10.066930955144));
#251425=CARTESIAN_POINT('Ctrl Pts',(2.68296800521044,-1.78938876890679,
10.074810322345));
#251426=CARTESIAN_POINT('Ctrl Pts',(2.75642908178534,-1.6699329534434,10.0837677906333));
#251427=CARTESIAN_POINT('Ctrl Pts',(2.76747935558276,-1.65155545622524,
10.0851276238374));
#251428=CARTESIAN_POINT('Ctrl Pts',(2.78440043881926,-1.6227675519306,10.0872279406126));
#251429=CARTESIAN_POINT('Ctrl Pts',(2.79039794329759,-1.61243283890469,
10.087976031288));
#251430=CARTESIAN_POINT('Ctrl Pts',(2.8013653706757,-1.59328964759626,10.0893505113554));
#251431=CARTESIAN_POINT('Ctrl Pts',(2.80635134471072,-1.58449107754594,
10.0899778695918));
#251432=CARTESIAN_POINT('Ctrl Pts',(2.81783266566948,-1.56400619405702,
10.0914285135592));
#251433=CARTESIAN_POINT('Ctrl Pts',(2.8242967988455,-1.55230277758356,10.0922498450617));
#251434=CARTESIAN_POINT('Ctrl Pts',(2.84467436447653,-1.5148601852987,10.0948549406171));
#251435=CARTESIAN_POINT('Ctrl Pts',(2.85831061651877,-1.48897084421152,
10.0966224127509));
#251436=CARTESIAN_POINT('Ctrl Pts',(2.93068903691992,-1.34689579493752,
10.1061585811498));
#251437=CARTESIAN_POINT('Ctrl Pts',(2.98270803498406,-1.22740630954098,
10.1135921944741));
#251438=CARTESIAN_POINT('Ctrl Pts',(3.10614840340232,-0.889244185296949,
10.1338847828737));
#251439=CARTESIAN_POINT('Ctrl Pts',(3.1616257939694,-0.665606777878812,
10.1465315836843));
#251440=CARTESIAN_POINT('Ctrl Pts',(3.20326648867163,-0.362042963571825,
10.1643242298971));
#251441=CARTESIAN_POINT('Ctrl Pts',(3.21096945487758,-0.285771122407251,
10.1688402451533));
#251442=CARTESIAN_POINT('Ctrl Pts',(3.21779166730246,-0.180946760578022,
10.1751450112857));
#251443=CARTESIAN_POINT('Ctrl Pts',(3.21926192066327,-0.152569829133572,
10.1768614879856));
#251444=CARTESIAN_POINT('Ctrl Pts',(3.22101820945468,-0.107023242221201,
10.1796336647172));
#251445=CARTESIAN_POINT('Ctrl Pts',(3.22154260268476,-0.0898639048995677,
10.1806819548268));
#251446=CARTESIAN_POINT('Ctrl Pts',(3.22234553852381,-0.0542799798824783,
10.1828642698148));
#251447=CARTESIAN_POINT('Ctrl Pts',(3.22260320860138,-0.0358555929495794,
10.1839989017341));
#251448=CARTESIAN_POINT('Ctrl Pts',(3.22283799558696,0.00755435606473961,
10.1866837038063));
#251449=CARTESIAN_POINT('Ctrl Pts',(3.22268257216693,0.0325391646398068,
10.1882379188818));
#251450=CARTESIAN_POINT('Ctrl Pts',(3.22118770750078,0.116281926138336,
10.1934784907794));
#251451=CARTESIAN_POINT('Ctrl Pts',(3.21853155920852,0.17500176722095,10.1972049749834));
#251452=CARTESIAN_POINT('Ctrl Pts',(3.20817876671744,0.317445255741478,
10.2063753762966));
#251453=CARTESIAN_POINT('Ctrl Pts',(3.19880899899056,0.401000790314728,
10.2118654601272));
#251454=CARTESIAN_POINT('Ctrl Pts',(3.16488147802437,0.624305322738541,
10.2268152147687));
#251455=CARTESIAN_POINT('Ctrl Pts',(3.13434645275609,0.762954647294478,
10.2363993817619));
#251456=CARTESIAN_POINT('Ctrl Pts',(3.08350989373429,0.937932153507249,
10.2487103600646));
#251457=CARTESIAN_POINT('Ctrl Pts',(3.07150882078722,0.976516056120752,
10.2514381516863));
#251458=CARTESIAN_POINT('Ctrl Pts',(3.01753466588182,1.13919331200442,10.2629743340372));
#251459=CARTESIAN_POINT('Ctrl Pts',(2.96873745874446,1.26090518525626,10.2716979469752));
#251460=CARTESIAN_POINT('Ctrl Pts',(2.90335492570937,1.39897124631875,10.2814590954967));
#251461=CARTESIAN_POINT('Ctrl Pts',(2.89384958243091,1.41852917696301,10.2828384295427));
#251462=CARTESIAN_POINT('Ctrl Pts',(2.87878527280628,1.44874335037549,10.2849623078064));
#251463=CARTESIAN_POINT('Ctrl Pts',(2.87336362367431,1.4594668338615,10.2857147228123));
#251464=CARTESIAN_POINT('Ctrl Pts',(2.86322834589739,1.47923800304823,10.2870990593185));
#251465=CARTESIAN_POINT('Ctrl Pts',(2.85853170312195,1.48829369971653,10.2877319432777));
#251466=CARTESIAN_POINT('Ctrl Pts',(2.8475993285111,1.50912997370945,10.2891855830152));
#251467=CARTESIAN_POINT('Ctrl Pts',(2.84133343360045,1.52089432465362,10.2900044585259));
#251468=CARTESIAN_POINT('Ctrl Pts',(2.82118688531478,1.55816081400135,10.2925935883113));
#251469=CARTESIAN_POINT('Ctrl Pts',(2.80703409473307,1.58351516783993,10.2943478301863));
#251470=CARTESIAN_POINT('Ctrl Pts',(2.72863369319886,1.71961236355655,10.3037435251637));
#251471=CARTESIAN_POINT('Ctrl Pts',(2.6581666231115,1.82665415449185,10.3110606389115));
#251472=CARTESIAN_POINT('Ctrl Pts',(2.44762265656137,2.1083841273469,10.3308976438504));
#251473=CARTESIAN_POINT('Ctrl Pts',(2.29545567808049,2.27310831168819,10.3432076390063));
#251474=CARTESIAN_POINT('Ctrl Pts',(2.06489095450143,2.47573858532714,10.360973302694));
#251475=CARTESIAN_POINT('Ctrl Pts',(2.00021770514078,2.52827681544219,10.365869229625));
#251476=CARTESIAN_POINT('Ctrl Pts',(1.91013539180736,2.59583504141919,10.3726213964921));
#251477=CARTESIAN_POINT('Ctrl Pts',(1.88644681872817,2.61310066631415,10.3743908708388));
#251478=CARTESIAN_POINT('Ctrl Pts',(1.84680928101333,2.64117094607519,10.3773434491204));
#251479=CARTESIAN_POINT('Ctrl Pts',(1.83099277474013,2.65216023661717,10.3785194806386));
#251480=CARTESIAN_POINT('Ctrl Pts',(1.79974013650502,2.67346172342993,10.3808395965237));
#251481=CARTESIAN_POINT('Ctrl Pts',(1.78431150883124,2.68378362807107,10.3819832551557));
#251482=CARTESIAN_POINT('Ctrl Pts',(1.74724349426358,2.70812156638074,10.3847273046824));
#251483=CARTESIAN_POINT('Ctrl Pts',(1.72552366356987,2.72201217329395,10.3863322467823));
#251484=CARTESIAN_POINT('Ctrl Pts',(1.64945934111924,2.76938178499682,10.3919441145624));
#251485=CARTESIAN_POINT('Ctrl Pts',(1.59429155709696,2.80150407909379,10.395999337042));
#251486=CARTESIAN_POINT('Ctrl Pts',(1.45533017296593,2.87698229408727,10.406182735094));
#251487=CARTESIAN_POINT('Ctrl Pts',(1.37052117316731,2.91833552518431,10.4123717589124));
#251488=CARTESIAN_POINT('Ctrl Pts',(1.10179744717344,3.03506733001694,10.4318583370959));
#251489=CARTESIAN_POINT('Ctrl Pts',(0.912650132228294,3.09720115101598,
10.4454288095991));
#251490=CARTESIAN_POINT('Ctrl Pts',(0.62240769885971,3.16362821774711,10.465325395543));
#251491=CARTESIAN_POINT('Ctrl Pts',(0.524845115619453,3.18126958349547,
10.471855945961));
#251492=CARTESIAN_POINT('Ctrl Pts',(0.40605621806227,3.19713405529047,10.4795044810292));
#251493=CARTESIAN_POINT('Ctrl Pts',(0.385469468073379,3.19968141545888,
10.4808190564944));
#251494=CARTESIAN_POINT('Ctrl Pts',(0.353143426595405,3.20336484315521,
10.4828645937358));
#251495=CARTESIAN_POINT('Ctrl Pts',(0.341420445436577,3.2046354999902,10.4836025649908));
#251496=CARTESIAN_POINT('Ctrl Pts',(0.320529454716142,3.20678394100045,
10.4849105199478));
#251497=CARTESIAN_POINT('Ctrl Pts',(0.311364581027744,3.20768677958702,
10.4854818431183));
#251498=CARTESIAN_POINT('Ctrl Pts',(0.289181766969773,3.20977605615368,
10.486858828219));
#251499=CARTESIAN_POINT('Ctrl Pts',(0.276160326290791,3.21092259526601,
10.4876622852308));
#251500=CARTESIAN_POINT('Ctrl Pts',(0.235571560549808,3.21424770024315,
10.49015264114));
#251501=CARTESIAN_POINT('Ctrl Pts',(0.207982153600756,3.21615077026735,
10.49182520212));
#251502=CARTESIAN_POINT('Ctrl Pts',(0.0652600382944481,3.22415117184827,
10.5003887591813));
#251503=CARTESIAN_POINT('Ctrl Pts',(-0.0501256704311403,3.22442277834251,
10.5070154380644));
#251504=CARTESIAN_POINT('Ctrl Pts',(-0.370147389744503,3.20798794312745,
10.5251568717563));
#251505=CARTESIAN_POINT('Ctrl Pts',(-0.573531612139767,3.17793305548913,
10.5364429856697));
#251506=CARTESIAN_POINT('Ctrl Pts',(-0.880106872551583,3.10222074875802,
10.5545082077002));
#251507=CARTESIAN_POINT('Ctrl Pts',(-0.986085538519319,3.070178075699,10.5609495975644));
#251508=CARTESIAN_POINT('Ctrl Pts',(-1.12053779497783,3.02184578307338,
10.5694938388171));
#251509=CARTESIAN_POINT('Ctrl Pts',(-1.15070949953352,3.01048574519325,
10.5714358292591));
#251510=CARTESIAN_POINT('Ctrl Pts',(-1.19920500772803,2.99139101856716,
10.5745996435991));
#251511=CARTESIAN_POINT('Ctrl Pts',(-1.2176369658357,2.98393583519317,10.5758121647751));
#251512=CARTESIAN_POINT('Ctrl Pts',(-1.25288498278775,2.96929808445124,
10.5781507805286));
#251513=CARTESIAN_POINT('Ctrl Pts',(-1.26971125092759,2.96214199727008,
10.5792759494487));
#251514=CARTESIAN_POINT('Ctrl Pts',(-1.30853648615561,2.94523832154223,
10.5818930364675));
#251515=CARTESIAN_POINT('Ctrl Pts',(-1.33048877789817,2.93538686858313,
10.5833884249102));
#251516=CARTESIAN_POINT('Ctrl Pts',(-1.40070799685684,2.90292533188765,
10.5882233716066));
#251517=CARTESIAN_POINT('Ctrl Pts',(-1.44852302056825,2.87936432165036,
10.5915950388468));
#251518=CARTESIAN_POINT('Ctrl Pts',(-1.6288425468457,2.78488296833156,10.6046232451472));
#251519=CARTESIAN_POINT('Ctrl Pts',(-1.75689781451043,2.70591969534315,
10.6145469710705));
#251520=CARTESIAN_POINT('Ctrl Pts',(-2.02020092168454,2.51696763540905,
10.6363009701347));
#251521=CARTESIAN_POINT('Ctrl Pts',(-2.15300324799859,2.40435334144088,
10.6481544889736));
#251522=CARTESIAN_POINT('Ctrl Pts',(-2.33579508348467,2.22200239524783,
10.6653241976289));
#251523=CARTESIAN_POINT('Ctrl Pts',(-2.39315833723716,2.16009929588233,
10.6708546190297));
#251524=CARTESIAN_POINT('Ctrl Pts',(-2.4611460173667,2.08069327405424,10.6775195453369));
#251525=CARTESIAN_POINT('Ctrl Pts',(-2.47411772943321,2.0652519768859,10.6787964530447));
#251526=CARTESIAN_POINT('Ctrl Pts',(-2.49428642011847,2.04078075582713,
10.6807888258874));
#251527=CARTESIAN_POINT('Ctrl Pts',(-2.50158103330588,2.03183246907789,
10.6815109044545));
#251528=CARTESIAN_POINT('Ctrl Pts',(-2.51529060975761,2.01482920752362,
10.6828704846155));
#251529=CARTESIAN_POINT('Ctrl Pts',(-2.52171505660054,2.00678268945641,
10.6835086157571));
#251530=CARTESIAN_POINT('Ctrl Pts',(-2.53686384419113,1.98762145148082,
10.6850160190314));
#251531=CARTESIAN_POINT('Ctrl Pts',(-2.54555381481949,1.97647994960083,
10.6858829055886));
#251532=CARTESIAN_POINT('Ctrl Pts',(-2.5746759340121,1.93863149979293,10.6887968351944));
#251533=CARTESIAN_POINT('Ctrl Pts',(-2.59476401409998,1.91166110162229,
10.6908216864322));
#251534=CARTESIAN_POINT('Ctrl Pts',(-2.64309395920673,1.84460715484574,
10.6957439247588));
#251535=CARTESIAN_POINT('Ctrl Pts',(-2.67085087359908,1.80418328172941,
10.6986156427719));
#251536=CARTESIAN_POINT('Ctrl Pts',(-2.79449639261705,1.61500059957039,
10.7116973580481));
#251537=CARTESIAN_POINT('Ctrl Pts',(-2.87895610419706,1.45912878470321,
10.721493574949));
#251538=CARTESIAN_POINT('Ctrl Pts',(-3.00535912151205,1.1716314202764,10.7391169766518));
#251539=CARTESIAN_POINT('Ctrl Pts',(-3.05246063470123,1.04277684821285,
10.7468691586429));
#251540=CARTESIAN_POINT('Ctrl Pts',(-3.11085676321661,0.844696786475436,
10.7589062817746));
#251541=CARTESIAN_POINT('Ctrl Pts',(-3.12833864452524,0.777456606934578,
10.7630109678197));
#251542=CARTESIAN_POINT('Ctrl Pts',(-3.14965732297129,0.683025983857816,
10.7688275990454));
#251543=CARTESIAN_POINT('Ctrl Pts',(-3.15534085936503,0.65626956232807,
10.7704813878463));
#251544=CARTESIAN_POINT('Ctrl Pts',(-3.16399840365401,0.612796711582066,
10.7731789624255));
#251545=CARTESIAN_POINT('Ctrl Pts',(-3.16718217686836,0.596123099239622,
10.7742160920858));
#251546=CARTESIAN_POINT('Ctrl Pts',(-3.17357310110557,0.561156169897997,
10.776396683289));
#251547=CARTESIAN_POINT('Ctrl Pts',(-3.17675413072964,0.542858770945003,
10.7775409246045));
#251548=CARTESIAN_POINT('Ctrl Pts',(-3.18277267131403,0.50637386823863,
10.7798292443499));
#251549=CARTESIAN_POINT('Ctrl Pts',(-3.18561286102506,0.488187514195531,
10.7809731913038));
#251550=CARTESIAN_POINT('Ctrl Pts',(-3.19193261906208,0.445314739964485,
10.7836780628135));
#251551=CARTESIAN_POINT('Ctrl Pts',(-3.1952817954966,0.420610573029445,
10.7852429840813));
#251552=CARTESIAN_POINT('Ctrl Pts',(-3.21460151418605,0.264521413500904,
10.7951720862643));
#251553=CARTESIAN_POINT('Ctrl Pts',(-3.22275000000299,0.132315334174674,
10.8037745307319));
#251554=CARTESIAN_POINT('Ctrl Pts',(-3.22275,-7.27048976578715E-11,10.8125553006127));
#251555=CARTESIAN_POINT('Origin',(0.,0.,-2.31077344927308));
#251556=CARTESIAN_POINT('',(-3.22275,1.56756299712326E-10,12.3117125106066));
#251557=CARTESIAN_POINT('',(-3.22275,-3.23896726357594E-13,12.0672299157825));
#251558=CARTESIAN_POINT('',(-3.22275,-3.50678552687464E-13,-2.31077344927308));
#251559=CARTESIAN_POINT('',(-3.22274985281522,-0.000974001778823583,11.0579144994549));
#251560=CARTESIAN_POINT('Ctrl Pts',(-3.22275,1.56756299712326E-10,12.3117125106066));
#251561=CARTESIAN_POINT('Ctrl Pts',(-3.22274999999995,0.000963693077442329,
12.3116478163493));
#251562=CARTESIAN_POINT('Ctrl Pts',(-3.22274956776502,0.00192739439762696,
12.3115831158696));
#251563=CARTESIAN_POINT('Ctrl Pts',(-3.2225911459169,0.178522212106079,
12.2997259502982));
#251564=CARTESIAN_POINT('Ctrl Pts',(-3.20807700117422,0.35384475023305,
12.2877455189971));
#251565=CARTESIAN_POINT('Ctrl Pts',(-3.1657934191203,0.608884374812476,
12.2705632833884));
#251566=CARTESIAN_POINT('Ctrl Pts',(-3.14908513252086,0.690111124929629,
12.2651324203364));
#251567=CARTESIAN_POINT('Ctrl Pts',(-3.12452696344479,0.789835988465645,
12.2585863864486));
#251568=CARTESIAN_POINT('Ctrl Pts',(-3.11961505580837,0.809018901392957,
12.2573328889204));
#251569=CARTESIAN_POINT('Ctrl Pts',(-3.1116201763617,0.839086024001066,
12.2553784275076));
#251570=CARTESIAN_POINT('Ctrl Pts',(-3.10865626706594,0.85000099996604,
12.2546710538948));
#251571=CARTESIAN_POINT('Ctrl Pts',(-3.10294828711516,0.870592119491925,
12.2533409293721));
#251572=CARTESIAN_POINT('Ctrl Pts',(-3.10021638921003,0.880271011321753,
12.252717556468));
#251573=CARTESIAN_POINT('Ctrl Pts',(-3.09364747624946,0.903134203437649,
12.2512491943078));
#251574=CARTESIAN_POINT('Ctrl Pts',(-3.08977144978147,0.916306990302155,
12.250406438283));
#251575=CARTESIAN_POINT('Ctrl Pts',(-3.07648864362384,0.960406208132865,
12.2475947796619));
#251576=CARTESIAN_POINT('Ctrl Pts',(-3.06670047045955,0.991216859271332,
12.2456463876615));
#251577=CARTESIAN_POINT('Ctrl Pts',(-3.04162997563112,1.06620314858394,
12.2409319855267));
#251578=CARTESIAN_POINT('Ctrl Pts',(-3.02584673334668,1.11020449752553,
12.2381892520277));
#251579=CARTESIAN_POINT('Ctrl Pts',(-2.95540438051979,1.29391040658139,
12.2267781331871));
#251580=CARTESIAN_POINT('Ctrl Pts',(-2.89198062831041,1.43006053000821,
12.2184125530114));
#251581=CARTESIAN_POINT('Ctrl Pts',(-2.71968753645359,1.74117591139875,
12.198504724398));
#251582=CARTESIAN_POINT('Ctrl Pts',(-2.603103123981,1.91108243737097,12.1869564146417));
#251583=CARTESIAN_POINT('Ctrl Pts',(-2.44216990261269,2.10332121276743,
12.172114452214));
#251584=CARTESIAN_POINT('Ctrl Pts',(-2.41248030602323,2.1373096247501,12.1694166236801));
#251585=CARTESIAN_POINT('Ctrl Pts',(-2.36709696518064,2.18711336859659,
12.1653446596141));
#251586=CARTESIAN_POINT('Ctrl Pts',(-2.35193629140182,2.20340839898983,
12.1639926702756));
#251587=CARTESIAN_POINT('Ctrl Pts',(-2.32439657542084,2.23240061868887,
12.1615506981579));
#251588=CARTESIAN_POINT('Ctrl Pts',(-2.31207912042537,2.2451552470456,12.1604633731655));
#251589=CARTESIAN_POINT('Ctrl Pts',(-2.28555588992159,2.27217010190448,
12.1581319648365));
#251590=CARTESIAN_POINT('Ctrl Pts',(-2.27132056528108,2.28640013088012,
12.1568866148365));
#251591=CARTESIAN_POINT('Ctrl Pts',(-2.2321866287441,2.32479336208288,12.1534785066404));
#251592=CARTESIAN_POINT('Ctrl Pts',(-2.20703017992866,2.34868877395634,
12.1513043472628));
#251593=CARTESIAN_POINT('Ctrl Pts',(-2.04525566270625,2.49745959525713,
12.1374221888023));
#251594=CARTESIAN_POINT('Ctrl Pts',(-1.89849991118504,2.61075730102037,
12.1252383884002));
#251595=CARTESIAN_POINT('Ctrl Pts',(-1.58955625604591,2.80938496431507,
12.1005604558572));
#251596=CARTESIAN_POINT('Ctrl Pts',(-1.42817162976701,2.89476424771179,
12.088121658283));
#251597=CARTESIAN_POINT('Ctrl Pts',(-1.1927814290735,2.99479439869667,12.0711870998833));
#251598=CARTESIAN_POINT('Ctrl Pts',(-1.12415887734022,3.02122319403437,
12.0663883533706));
#251599=CARTESIAN_POINT('Ctrl Pts',(-1.03659271820144,3.05155039030755,
12.0604867475294));
#251600=CARTESIAN_POINT('Ctrl Pts',(-1.01844215192525,3.05765594407239,
12.0592752926703));
#251601=CARTESIAN_POINT('Ctrl Pts',(-0.989621448227486,3.06706564511141,
12.0573715088908));
#251602=CARTESIAN_POINT('Ctrl Pts',(-0.978987021674755,3.07047662462741,
12.0566732910213));
#251603=CARTESIAN_POINT('Ctrl Pts',(-0.958699919408675,3.0768675747511,
12.0553496844724));
#251604=CARTESIAN_POINT('Ctrl Pts',(-0.949050761282024,3.07985750687117,
12.0547237623751));
#251605=CARTESIAN_POINT('Ctrl Pts',(-0.925968819948526,3.08689100704529,
12.053234853844));
#251606=CARTESIAN_POINT('Ctrl Pts',(-0.912523229581137,3.09089238198121,
12.052374271049));
#251607=CARTESIAN_POINT('Ctrl Pts',(-0.866279992821032,3.10432619972791,
12.0494361774026));
#251608=CARTESIAN_POINT('Ctrl Pts',(-0.833357702142755,3.11332576655933,
12.0473817682768));
#251609=CARTESIAN_POINT('Ctrl Pts',(-0.751572086348426,3.13429212535857,
12.0423560900462));
#251610=CARTESIAN_POINT('Ctrl Pts',(-0.702558707112971,3.14564134884796,
12.0394123172423));
#251611=CARTESIAN_POINT('Ctrl Pts',(-0.483827117064786,3.19092147106733,
12.0264964483732));
#251612=CARTESIAN_POINT('Ctrl Pts',(-0.311796114549627,3.21229811272843,
12.0169122705348));
#251613=CARTESIAN_POINT('Ctrl Pts',(0.0540203983025983,3.22807620826352,
11.9963757628994));
#251614=CARTESIAN_POINT('Ctrl Pts',(0.247245864476833,3.21904503792961,
11.9854231697317));
#251615=CARTESIAN_POINT('Ctrl Pts',(0.472968393235273,3.18804480678933,
11.9718341534057));
#251616=CARTESIAN_POINT('Ctrl Pts',(0.50736743638302,3.18275147242569,11.969742188926));
#251617=CARTESIAN_POINT('Ctrl Pts',(0.561733342691843,3.17348189353023,
11.9663994488008));
#251618=CARTESIAN_POINT('Ctrl Pts',(0.581760428228291,3.16987167747703,
11.965160176046));
#251619=CARTESIAN_POINT('Ctrl Pts',(0.619146348702774,3.16276601533336,
11.9628313834419));
#251620=CARTESIAN_POINT('Ctrl Pts',(0.636513243754918,3.15931668873031,
11.9617433606346));
#251621=CARTESIAN_POINT('Ctrl Pts',(0.675331955683889,3.15127364286836,
11.9592970466123));
#251622=CARTESIAN_POINT('Ctrl Pts',(0.696766904098041,3.14660367159537,
11.9579363801263));
#251623=CARTESIAN_POINT('Ctrl Pts',(0.760541897275907,3.132025601941,11.953857774991));
#251624=CARTESIAN_POINT('Ctrl Pts',(0.802729502317106,3.12147936094992,
11.95111974325));
#251625=CARTESIAN_POINT('Ctrl Pts',(1.00176272456347,3.06742253648839,11.9380060128546));
#251626=CARTESIAN_POINT('Ctrl Pts',(1.15535706837004,3.01292990172172,11.9272861544259));
#251627=CARTESIAN_POINT('Ctrl Pts',(1.45927209187229,2.87843939230919,11.9049853199311));
#251628=CARTESIAN_POINT('Ctrl Pts',(1.60871915080358,2.79766163874941,11.8934216892821));
#251629=CARTESIAN_POINT('Ctrl Pts',(1.82779927317281,2.65586362669371,11.8760246452035));
#251630=CARTESIAN_POINT('Ctrl Pts',(1.9023472409322,2.60298671009137,11.8700208570501));
#251631=CARTESIAN_POINT('Ctrl Pts',(1.99042062380375,2.53470833995214,11.8629135939407));
#251632=CARTESIAN_POINT('Ctrl Pts',(2.00617269266835,2.522259265515,11.8616419144701));
#251633=CARTESIAN_POINT('Ctrl Pts',(2.03075315142967,2.50245702289312,11.8596580223799));
#251634=CARTESIAN_POINT('Ctrl Pts',(2.03966002531584,2.49520269799938,11.8589392551099));
#251635=CARTESIAN_POINT('Ctrl Pts',(2.05548293932161,2.48217417050535,11.8576628630791));
#251636=CARTESIAN_POINT('Ctrl Pts',(2.06241359809402,2.47641855899643,11.8571039811424));
#251637=CARTESIAN_POINT('Ctrl Pts',(2.07914194694156,2.4624074528448,11.8557553670191));
#251638=CARTESIAN_POINT('Ctrl Pts',(2.08891465608434,2.45412250545793,11.854967765569));
#251639=CARTESIAN_POINT('Ctrl Pts',(2.119256517291,2.42808721332919,11.8525223286303));
#251640=CARTESIAN_POINT('Ctrl Pts',(2.13965136253323,2.41013440656525,11.8508783965027));
#251641=CARTESIAN_POINT('Ctrl Pts',(2.24381412457637,2.31607939324094,11.8424665181471));
#251642=CARTESIAN_POINT('Ctrl Pts',(2.32376580993048,2.23585398078988,11.8359548242589));
#251643=CARTESIAN_POINT('Ctrl Pts',(2.40244253265057,2.14811756592693,11.8292788459993));
#251644=CARTESIAN_POINT('Ctrl Pts',(2.40554054023783,2.14464773545374,11.8290155124919));
#251645=CARTESIAN_POINT('Ctrl Pts',(2.54588581002622,1.98677153598284,11.8170646190865));
#251646=CARTESIAN_POINT('Ctrl Pts',(2.66797455915245,1.81953522875919,11.80570142103));
#251647=CARTESIAN_POINT('Ctrl Pts',(2.82864427799684,1.54813664889311,11.7876452220797));
#251648=CARTESIAN_POINT('Ctrl Pts',(2.87928981638901,1.45177210694855,11.7813066169731));
#251649=CARTESIAN_POINT('Ctrl Pts',(2.93825403024683,1.32430474105206,11.7729045932504));
#251650=CARTESIAN_POINT('Ctrl Pts',(2.9511208523704,1.29537847807131,11.7709970616652));
#251651=CARTESIAN_POINT('Ctrl Pts',(2.97121093874652,1.24835987402934,11.7678928105612));
#251652=CARTESIAN_POINT('Ctrl Pts',(2.97870014408853,1.23038296616007,11.7667051050945));
#251653=CARTESIAN_POINT('Ctrl Pts',(2.9927474593539,1.19578404125955,11.7644170978832));
#251654=CARTESIAN_POINT('Ctrl Pts',(2.99933117314083,1.17917315197769,11.7633177059887));
#251655=CARTESIAN_POINT('Ctrl Pts',(3.01423203105586,1.14064557076962,11.7607652326548));
#251656=CARTESIAN_POINT('Ctrl Pts',(3.0224487766503,1.11869137900034,11.7593088783283));
#251657=CARTESIAN_POINT('Ctrl Pts',(3.04796527117049,1.04818043280959,11.75462450893));
#251658=CARTESIAN_POINT('Ctrl Pts',(3.06433918118346,0.999299459266667,
11.7513665026158));
#251659=CARTESIAN_POINT('Ctrl Pts',(3.14239104239333,0.746298515899061,
11.7344412796831));
#251660=CARTESIAN_POINT('Ctrl Pts',(3.18486369257926,0.536842684056119,
11.7201728216996));
#251661=CARTESIAN_POINT('Ctrl Pts',(3.22484646623756,0.142097678477962,
11.6933601846317));
#251662=CARTESIAN_POINT('Ctrl Pts',(3.22770628425679,-0.0418295988159529,
11.6809143422886));
#251663=CARTESIAN_POINT('Ctrl Pts',(3.21282933745172,-0.254386129646373,
11.6671958464377));
#251664=CARTESIAN_POINT('Ctrl Pts',(3.21037081183381,-0.283732348616373,
11.6653171330022));
#251665=CARTESIAN_POINT('Ctrl Pts',(3.20623882728636,-0.326069757065285,
11.6626327610921));
#251666=CARTESIAN_POINT('Ctrl Pts',(3.20488796781486,-0.339090005165756,
11.6618107871241));
#251667=CARTESIAN_POINT('Ctrl Pts',(3.20236481893419,-0.362045861035351,
11.6603682951451));
#251668=CARTESIAN_POINT('Ctrl Pts',(3.20122554550895,-0.371984752143566,
11.6597460030266));
#251669=CARTESIAN_POINT('Ctrl Pts',(3.19867238223164,-0.393377334076807,
11.6584115115451));
#251670=CARTESIAN_POINT('Ctrl Pts',(3.19724323991786,-0.404828865289943,
11.6577001554735));
#251671=CARTESIAN_POINT('Ctrl Pts',(3.19305724295462,-0.43696503795704,
11.6557117108429));
#251672=CARTESIAN_POINT('Ctrl Pts',(3.19016090560161,-0.457631346343379,
11.6544420787852));
#251673=CARTESIAN_POINT('Ctrl Pts',(3.16922481933532,-0.597144239199672,
11.6459239728885));
#251674=CARTESIAN_POINT('Ctrl Pts',(3.14474659528526,-0.714942201310361,
11.6389899008823));
#251675=CARTESIAN_POINT('Ctrl Pts',(3.06222132852555,-1.02412244843787,
11.6208443663801));
#251676=CARTESIAN_POINT('Ctrl Pts',(2.99286821069288,-1.21192757377501,
11.6098551509194));
#251677=CARTESIAN_POINT('Ctrl Pts',(2.85403989590444,-1.50178677151969,
11.5915396559895));
#251678=CARTESIAN_POINT('Ctrl Pts',(2.79534666779884,-1.60839661234649,
11.5844843505457));
#251679=CARTESIAN_POINT('Ctrl Pts',(2.71345271568018,-1.73906753574873,
11.5752664960636));
#251680=CARTESIAN_POINT('Ctrl Pts',(2.69571262982075,-1.76644129117118,
11.5733023644131));
#251681=CARTESIAN_POINT('Ctrl Pts',(2.66660729191092,-1.80989239389886,
11.5701285624632));
#251682=CARTESIAN_POINT('Ctrl Pts',(2.65550463767422,-1.82614348271027,
11.568928675114));
#251683=CARTESIAN_POINT('Ctrl Pts',(2.6340713853629,-1.85690677989992,11.5666321172972));
#251684=CARTESIAN_POINT('Ctrl Pts',(2.62376792683427,-1.87143706772608,
11.5655365024892));
#251685=CARTESIAN_POINT('Ctrl Pts',(2.59987480534259,-1.90454677271582,
11.5630144546866));
#251686=CARTESIAN_POINT('Ctrl Pts',(2.58620560127245,-1.92306733035948,
11.5615850025024));
#251687=CARTESIAN_POINT('Ctrl Pts',(2.54270527519172,-1.98070374141064,
11.5570764949692));
#251688=CARTESIAN_POINT('Ctrl Pts',(2.51217738379846,-2.01928249529493,
11.5539705294072));
#251689=CARTESIAN_POINT('Ctrl Pts',(2.43835987510959,-2.10830145597239,
11.5465891541251));
#251690=CARTESIAN_POINT('Ctrl Pts',(2.39437031213473,-2.15812968807959,
11.5422875366351));
#251691=CARTESIAN_POINT('Ctrl Pts',(2.21538209279282,-2.34866193437792,
11.5251601368135));
#251692=CARTESIAN_POINT('Ctrl Pts',(2.06928005345775,-2.47834567706285,
11.5119420351349));
#251693=CARTESIAN_POINT('Ctrl Pts',(1.7910337812451,-2.68347566034152,11.488612801425));
#251694=CARTESIAN_POINT('Ctrl Pts',(1.66355165933186,-2.76431711375781,
11.4785150562626));
#251695=CARTESIAN_POINT('Ctrl Pts',(1.51185122516423,-2.84620630750429,
11.4675004864039));
#251696=CARTESIAN_POINT('Ctrl Pts',(1.49273328447478,-2.85627937557571,
11.4661298368622));
#251697=CARTESIAN_POINT('Ctrl Pts',(1.46299362190456,-2.87156876635247,
11.464026199295));
#251698=CARTESIAN_POINT('Ctrl Pts',(1.45244245234532,-2.87691995901624,
11.4632853587038));
#251699=CARTESIAN_POINT('Ctrl Pts',(1.43295171326653,-2.88667043654046,
11.4619272638798));
#251700=CARTESIAN_POINT('Ctrl Pts',(1.42402113919662,-2.89108640842544,
11.4613090304983));
#251701=CARTESIAN_POINT('Ctrl Pts',(1.40349347805576,-2.90111868775256,
11.4598970857338));
#251702=CARTESIAN_POINT('Ctrl Pts',(1.39188305337999,-2.90670692745881,
11.4591050849716));
#251703=CARTESIAN_POINT('Ctrl Pts',(1.35533566026791,-2.92402843799959,
11.4566316925433));
#251704=CARTESIAN_POINT('Ctrl Pts',(1.33028081304983,-2.93551190262471,
11.4549646623341));
#251705=CARTESIAN_POINT('Ctrl Pts',(1.19843132842138,-2.99390801040549,
11.4463250529576));
#251706=CARTESIAN_POINT('Ctrl Pts',(1.08928506683121,-3.03532308514604,
11.4396243390244));
#251707=CARTESIAN_POINT('Ctrl Pts',(0.781781365009663,-3.13327259021256,
11.4213629732329));
#251708=CARTESIAN_POINT('Ctrl Pts',(0.579896913569947,-3.17683803605767,
11.4100287142096));
#251709=CARTESIAN_POINT('Ctrl Pts',(0.266233129897482,-3.21360884943132,
11.3919550281511));
#251710=CARTESIAN_POINT('Ctrl Pts',(0.156660750219584,-3.22080980654466,
11.3855634609525));
#251711=CARTESIAN_POINT('Ctrl Pts',(0.0151997044228281,-3.22287050556823,
11.3771003957317));
#251712=CARTESIAN_POINT('Ctrl Pts',(-0.0165464409393103,-3.22286385601687,
11.3751877202728));
#251713=CARTESIAN_POINT('Ctrl Pts',(-0.0677775800882746,-3.22209617333433,
11.3720771506789));
#251714=CARTESIAN_POINT('Ctrl Pts',(-0.0872652822184042,-3.22162727440985,
11.3708883394308));
#251715=CARTESIAN_POINT('Ctrl Pts',(-0.124599842221143,-3.2203899621812,
11.3685995913553));
#251716=CARTESIAN_POINT('Ctrl Pts',(-0.142446960526051,-3.21964989903794,
11.3675005778605));
#251717=CARTESIAN_POINT('Ctrl Pts',(-0.183658427979339,-3.21759766524008,
11.3649510417142));
#251718=CARTESIAN_POINT('Ctrl Pts',(-0.207016253011651,-3.21617931380093,
11.3634972706141));
#251719=CARTESIAN_POINT('Ctrl Pts',(-0.281541254098987,-3.21083874726651,
11.3588299928986));
#251720=CARTESIAN_POINT('Ctrl Pts',(-0.332629008933642,-3.20594890791521,
11.3555868020444));
#251721=CARTESIAN_POINT('Ctrl Pts',(-0.605866923557042,-3.17319494074689,
11.3379975773843));
#251722=CARTESIAN_POINT('Ctrl Pts',(-0.824743198926465,-3.1234611668257,
11.3229800947625));
#251723=CARTESIAN_POINT('Ctrl Pts',(-1.20039791842574,-2.99584137056866,
11.2961638492071));
#251724=CARTESIAN_POINT('Ctrl Pts',(-1.35940413753662,-2.92712339426824,
11.2844712860359));
#251725=CARTESIAN_POINT('Ctrl Pts',(-1.53836386490308,-2.83203744851931,
11.2714209817448));
#251726=CARTESIAN_POINT('Ctrl Pts',(-1.56439640265915,-2.81774085572253,
11.2695259358915));
#251727=CARTESIAN_POINT('Ctrl Pts',(-1.60165236074997,-2.79660504553247,
11.2668226967218));
#251728=CARTESIAN_POINT('Ctrl Pts',(-1.613036598909,-2.79005430231818,11.2659978790847));
#251729=CARTESIAN_POINT('Ctrl Pts',(-1.63302541208704,-2.77838905638772,
11.2645522019124));
#251730=CARTESIAN_POINT('Ctrl Pts',(-1.64164666463526,-2.77330380300996,
11.2639295412818));
#251731=CARTESIAN_POINT('Ctrl Pts',(-1.66013304671509,-2.76228317997464,
11.2625963543221));
#251732=CARTESIAN_POINT('Ctrl Pts',(-1.66999017948205,-2.75633505022361,
11.2618866521051));
#251733=CARTESIAN_POINT('Ctrl Pts',(-1.69751373800415,-2.73952454811685,
11.2599076540621));
#251734=CARTESIAN_POINT('Ctrl Pts',(-1.71510784498788,-2.72854407536489,
11.2586457015125));
#251735=CARTESIAN_POINT('Ctrl Pts',(-1.75464596448653,-2.70333479303937,
11.2558139516282));
#251736=CARTESIAN_POINT('Ctrl Pts',(-1.77652545348577,-2.68900704077793,
11.2542498653663));
#251737=CARTESIAN_POINT('Ctrl Pts',(-1.84696986491845,-2.64164146251717,
11.2492153848583));
#251738=CARTESIAN_POINT('Ctrl Pts',(-1.89480860308141,-2.60754068112921,
11.2457984886084));
#251739=CARTESIAN_POINT('Ctrl Pts',(-2.13985978661189,-2.4225539032996,
11.228158791162));
#251740=CARTESIAN_POINT('Ctrl Pts',(-2.32008150021395,-2.25055574988141,
11.2146438093973));
#251741=CARTESIAN_POINT('Ctrl Pts',(-2.54927362206534,-1.97471293658918,
11.1941238923678));
#251742=CARTESIAN_POINT('Ctrl Pts',(-2.61536401824566,-1.88630715170443,
11.1877004123705));
#251743=CARTESIAN_POINT('Ctrl Pts',(-2.69449523997219,-1.7682827858394,
11.1792006057302));
#251744=CARTESIAN_POINT('Ctrl Pts',(-2.7118100814473,-1.74161263862841,
11.1772848857963));
#251745=CARTESIAN_POINT('Ctrl Pts',(-2.73910450642408,-1.69817681284528,
11.1741705762468));
#251746=CARTESIAN_POINT('Ctrl Pts',(-2.74933167917913,-1.68156869521908,
11.1729811103567));
#251747=CARTESIAN_POINT('Ctrl Pts',(-2.76863333196253,-1.64957751748529,
11.1706919201623));
#251748=CARTESIAN_POINT('Ctrl Pts',(-2.77773194889134,-1.63420981300014,
11.1695931271475));
#251749=CARTESIAN_POINT('Ctrl Pts',(-2.79844427213071,-1.59855362606852,
11.1670453123715));
#251750=CARTESIAN_POINT('Ctrl Pts',(-2.80996578011949,-1.57821301107996,
11.1655930564882));
#251751=CARTESIAN_POINT('Ctrl Pts',(-2.84600424569816,-1.51294316674483,
11.1609357834155));
#251752=CARTESIAN_POINT('Ctrl Pts',(-2.86967164331204,-1.46755625945328,
11.1577012609336));
#251753=CARTESIAN_POINT('Ctrl Pts',(-2.95802677042889,-1.2878010431249,
11.1449002748725));
#251754=CARTESIAN_POINT('Ctrl Pts',(-3.01443074422125,-1.14958748987026,
11.1350662179998));
#251755=CARTESIAN_POINT('Ctrl Pts',(-3.12744867545686,-0.806372191506612,
11.1108275094315));
#251756=CARTESIAN_POINT('Ctrl Pts',(-3.17375701598197,-0.598698486071854,
11.0962901551797));
#251757=CARTESIAN_POINT('Ctrl Pts',(-3.20604466864878,-0.332451161387822,
11.0786868543422));
#251758=CARTESIAN_POINT('Ctrl Pts',(-3.21133215489194,-0.276754079879095,
11.0750631673019));
#251759=CARTESIAN_POINT('Ctrl Pts',(-3.21636276069522,-0.203548945142041,
11.0704007648363));
#251760=CARTESIAN_POINT('Ctrl Pts',(-3.21741698234107,-0.186143962097813,
11.0692996788549));
#251761=CARTESIAN_POINT('Ctrl Pts',(-3.21889491245675,-0.157954291515767,
11.0675292667644));
#251762=CARTESIAN_POINT('Ctrl Pts',(-3.219405784378,-0.147174791080003,
11.0668553363545));
#251763=CARTESIAN_POINT('Ctrl Pts',(-3.22026076857828,-0.126990934723725,
11.0655994332744));
#251764=CARTESIAN_POINT('Ctrl Pts',(-3.22061784823918,-0.117587384997833,
11.0650167637878));
#251765=CARTESIAN_POINT('Ctrl Pts',(-3.22127651435933,-0.0979767878061537,
11.0638065099786));
#251766=CARTESIAN_POINT('Ctrl Pts',(-3.22157078921631,-0.0877695245606001,
11.063179324094));
#251767=CARTESIAN_POINT('Ctrl Pts',(-3.22211717083128,-0.065073271156808,
11.0617905206222));
#251768=CARTESIAN_POINT('Ctrl Pts',(-3.22234519383345,-0.0525838003462824,
11.0610301613137));
#251769=CARTESIAN_POINT('Ctrl Pts',(-3.22266282296568,-0.0270542178465188,
11.0594832828966));
#251770=CARTESIAN_POINT('Ctrl Pts',(-3.22274591169252,-0.0140142783986701,
11.0586970973044));
#251771=CARTESIAN_POINT('Ctrl Pts',(-3.22274985281522,-0.000974001778823583,
11.0579144994549));
#251772=CARTESIAN_POINT('Ctrl Pts',(-3.22274985195413,-0.000976846793707469,
11.0579146701954));
#251773=CARTESIAN_POINT('Ctrl Pts',(-3.22274995065157,-0.000651230577373808,
11.0578951286835));
#251774=CARTESIAN_POINT('Ctrl Pts',(-3.22275,-0.00032561497491421,11.057875589458));
#251775=CARTESIAN_POINT('Ctrl Pts',(-3.22275,2.40369908895709E-12,11.0578560525147));
#251776=CARTESIAN_POINT('',(-3.22274890077618,-0.00266177495324583,10.8127319644804));
#251777=CARTESIAN_POINT('Ctrl Pts',(-3.22275,-7.2705680572429E-11,10.8125553006127));
#251778=CARTESIAN_POINT('Ctrl Pts',(-3.22274999999998,-0.00088725350428013,
10.8126141809251));
#251779=CARTESIAN_POINT('Ctrl Pts',(-3.22274963359612,-0.00177451187261363,
10.8126730688928));
#251780=CARTESIAN_POINT('Ctrl Pts',(-3.22274890077618,-0.00266177495322464,
10.8127319644804));
#251781=CARTESIAN_POINT('Ctrl Pts',(-3.22274890347102,-0.00265851017456808,
10.8127317477678));
#251782=CARTESIAN_POINT('Ctrl Pts',(-3.2226069773852,-0.174706803165855,
10.8241521285412));
#251783=CARTESIAN_POINT('Ctrl Pts',(-3.20868771616605,-0.346465522279838,
10.8358494098271));
#251784=CARTESIAN_POINT('Ctrl Pts',(-3.15997717365837,-0.646600032517979,
10.8563154919063));
#251785=CARTESIAN_POINT('Ctrl Pts',(-3.13083714163604,-0.775508502628825,
10.8651076131163));
#251786=CARTESIAN_POINT('Ctrl Pts',(-3.08783682633512,-0.922954612464723,
10.8749161354524));
#251787=CARTESIAN_POINT('Ctrl Pts',(-3.08159925070548,-0.943571723987823,
10.876281750581));
#251788=CARTESIAN_POINT('Ctrl Pts',(-3.07161309486545,-0.975423369346211,
10.8783807004478));
#251789=CARTESIAN_POINT('Ctrl Pts',(-3.06800863672006,-0.986701965842342,
10.8791218198553));
#251790=CARTESIAN_POINT('Ctrl Pts',(-3.06117483661154,-1.00768586032651,
10.8804963946471));
#251791=CARTESIAN_POINT('Ctrl Pts',(-3.05796144445542,-1.01739568549116,
10.8811306908383));
#251792=CARTESIAN_POINT('Ctrl Pts',(-3.0504425666293,-1.03975781453091,
10.8825876357335));
#251793=CARTESIAN_POINT('Ctrl Pts',(-3.04610454666431,-1.05239881719149,
10.8834083946757));
#251794=CARTESIAN_POINT('Ctrl Pts',(-3.03176593553887,-1.09335004662847,
10.8860591864589));
#251795=CARTESIAN_POINT('Ctrl Pts',(-3.0214480264945,-1.12154847433009,
10.887871862882));
#251796=CARTESIAN_POINT('Ctrl Pts',(-2.95713248302473,-1.28998727504354,
10.8986466690472));
#251797=CARTESIAN_POINT('Ctrl Pts',(-2.89376801402038,-1.42646986391953,
10.9071603563856));
#251798=CARTESIAN_POINT('Ctrl Pts',(-2.73912617868258,-1.7064750944649,
10.9251228701839));
#251799=CARTESIAN_POINT('Ctrl Pts',(-2.64556679777714,-1.84820014937909,
10.934531108881));
#251800=CARTESIAN_POINT('Ctrl Pts',(-2.49634674289376,-2.03953724831737,
10.9484256745151));
#251801=CARTESIAN_POINT('Ctrl Pts',(-2.44945514327004,-2.09562109177532,
10.9526600177757));
#251802=CARTESIAN_POINT('Ctrl Pts',(-2.36556745002752,-2.18928785107805,
10.9600649693526));
#251803=CARTESIAN_POINT('Ctrl Pts',(-2.32948057200955,-2.22764684295282,
10.9632008811682));
#251804=CARTESIAN_POINT('Ctrl Pts',(-2.27710228775061,-2.28065799858243,
10.9676949238489));
#251805=CARTESIAN_POINT('Ctrl Pts',(-2.26157537651787,-2.29605586079043,
10.969020259454));
#251806=CARTESIAN_POINT('Ctrl Pts',(-2.24543561097468,-2.31173893133674,
10.9703913422249));
#251807=CARTESIAN_POINT('Ctrl Pts',(-2.24497783512923,-2.3121834895762,
10.9704302251746));
#251808=CARTESIAN_POINT('Ctrl Pts',(-2.2440463510189,-2.31308754103962,
10.970509333427));
#251809=CARTESIAN_POINT('Ctrl Pts',(-2.24357263360686,-2.3135470247573,
10.9705495591329));
#251810=CARTESIAN_POINT('Ctrl Pts',(-2.24260671782949,-2.31448334219024,
10.9706315681698));
#251811=CARTESIAN_POINT('Ctrl Pts',(-2.24211450846048,-2.31496016446936,
10.9706733519866));
#251812=CARTESIAN_POINT('Ctrl Pts',(-2.24110869553655,-2.31593391270455,
10.9707587231845));
#251813=CARTESIAN_POINT('Ctrl Pts',(-2.24059507873148,-2.3164308248656,
10.970802311151));
#251814=CARTESIAN_POINT('Ctrl Pts',(-2.22695065451891,-2.32962270014803,
10.9719600643232));
#251815=CARTESIAN_POINT('Ctrl Pts',(-2.21371254624232,-2.34220577316728,
10.9730789771653));
#251816=CARTESIAN_POINT('Ctrl Pts',(-2.18579145527427,-2.36829713391313,
10.9754302925374));
#251817=CARTESIAN_POINT('Ctrl Pts',(-2.17108859586833,-2.3817829206279,
10.976663578304));
#251818=CARTESIAN_POINT('Ctrl Pts',(-2.13206592700471,-2.4169138108696,
10.9799246472093));
#251819=CARTESIAN_POINT('Ctrl Pts',(-2.10754218018669,-2.43832797656515,
10.9819618604862));
#251820=CARTESIAN_POINT('Ctrl Pts',(-1.99459936968593,-2.53397288565651,
10.9912923465963));
#251821=CARTESIAN_POINT('Ctrl Pts',(-1.90256428225074,-2.60378364421884,
10.9987585258432));
#251822=CARTESIAN_POINT('Ctrl Pts',(-1.60686238828517,-2.80401992600998,
11.0223174157064));
#251823=CARTESIAN_POINT('Ctrl Pts',(-1.39214644273215,-2.91658137129566,
11.0388993084828));
#251824=CARTESIAN_POINT('Ctrl Pts',(-1.11247204239699,-3.025215768649,11.058860394099));
#251825=CARTESIAN_POINT('Ctrl Pts',(-1.05749636306838,-3.04486890933398,
11.0627064876903));
#251826=CARTESIAN_POINT('Ctrl Pts',(-0.965727649540792,-3.07488947903642,
11.0689677988385));
#251827=CARTESIAN_POINT('Ctrl Pts',(-0.929230969969557,-3.08611491971717,
11.0714171912993));
#251828=CARTESIAN_POINT('Ctrl Pts',(-0.878274144454334,-3.10080192245904,
11.0747727019489));
#251829=CARTESIAN_POINT('Ctrl Pts',(-0.863978054521453,-3.10481561066848,
11.0757071284283));
#251830=CARTESIAN_POINT('Ctrl Pts',(-0.839609409755192,-3.11147586220572,
11.0772874828458));
#251831=CARTESIAN_POINT('Ctrl Pts',(-0.829550927441443,-3.11417264659841,
11.0779361998897));
#251832=CARTESIAN_POINT('Ctrl Pts',(-0.808614791814882,-3.11967720707168,
11.0792787888924));
#251833=CARTESIAN_POINT('Ctrl Pts',(-0.797735310536159,-3.12247692402484,
11.079972212608));
#251834=CARTESIAN_POINT('Ctrl Pts',(-0.768663978538421,-3.12979625650217,
11.0818143329938));
#251835=CARTESIAN_POINT('Ctrl Pts',(-0.750446662236314,-3.13421421798492,
11.0829574366479));
#251836=CARTESIAN_POINT('Ctrl Pts',(-0.667539375151929,-3.1535561069684,
11.0881130361248));
#251837=CARTESIAN_POINT('Ctrl Pts',(-0.602431908669004,-3.16663891719223,
11.0920331898869));
#251838=CARTESIAN_POINT('Ctrl Pts',(-0.352969632080119,-3.20879259113306,
11.1067244289763));
#251839=CARTESIAN_POINT('Ctrl Pts',(-0.166611915149471,-3.22384674457711,
11.1170380060437));
#251840=CARTESIAN_POINT('Ctrl Pts',(0.191030119251093,-3.22162589494382,
11.1371153450664));
#251841=CARTESIAN_POINT('Ctrl Pts',(0.361674210126881,-3.20695318995163,
11.1468223764289));
#251842=CARTESIAN_POINT('Ctrl Pts',(0.574599940630966,-3.17142965872212,
11.1596044219548));
#251843=CARTESIAN_POINT('Ctrl Pts',(0.618700662164427,-3.16312193405382,
11.1622874867997));
#251844=CARTESIAN_POINT('Ctrl Pts',(0.684635589440942,-3.14926945798729,
11.1663593444003));
#251845=CARTESIAN_POINT('Ctrl Pts',(0.706609649338576,-3.14441199168774,
11.1677265123958));
#251846=CARTESIAN_POINT('Ctrl Pts',(0.746012227931751,-3.13526799226979,
11.1701971019172));
#251847=CARTESIAN_POINT('Ctrl Pts',(0.763459363359172,-3.13106521932581,
11.1712978188528));
#251848=CARTESIAN_POINT('Ctrl Pts',(0.800962403960998,-3.12169916308307,
11.1736788276724));
#251849=CARTESIAN_POINT('Ctrl Pts',(0.821005376060777,-3.11648785944851,
11.1749606131778));
#251850=CARTESIAN_POINT('Ctrl Pts',(0.874940178445056,-3.10190806181315,
11.1784355910635));
#251851=CARTESIAN_POINT('Ctrl Pts',(0.908730423779365,-3.09217767940173,
11.1806402816448));
#251852=CARTESIAN_POINT('Ctrl Pts',(1.11595976230474,-3.02881302190786,
11.1943367830342));
#251853=CARTESIAN_POINT('Ctrl Pts',(1.28474293727904,-2.9611639095978,11.2062828778967));
#251854=CARTESIAN_POINT('Ctrl Pts',(1.60869341519044,-2.79839306241365,
11.2306295743778));
#251855=CARTESIAN_POINT('Ctrl Pts',(1.76333549060141,-2.70361741083642,
11.2429831728678));
#251856=CARTESIAN_POINT('Ctrl Pts',(1.95079304533275,-2.56577265987937,
11.2584036064392));
#251857=CARTESIAN_POINT('Ctrl Pts',(1.99164632244395,-2.53419184786923,
11.2617923591158));
#251858=CARTESIAN_POINT('Ctrl Pts',(2.05883684725524,-2.47962260791855,
11.2673912507402));
#251859=CARTESIAN_POINT('Ctrl Pts',(2.08559009919478,-2.45716332519871,
11.2696276203936));
#251860=CARTESIAN_POINT('Ctrl Pts',(2.12280718382041,-2.42487379340251,
11.272742493269));
#251861=CARTESIAN_POINT('Ctrl Pts',(2.13357760105103,-2.4154026355519,11.2736443789634));
#251862=CARTESIAN_POINT('Ctrl Pts',(2.15199523983047,-2.39898743870039,
11.2751868701649));
#251863=CARTESIAN_POINT('Ctrl Pts',(2.15967288048976,-2.39207803060076,
11.275829942411));
#251864=CARTESIAN_POINT('Ctrl Pts',(2.17578671500661,-2.3774357378572,11.2771795818937));
#251865=CARTESIAN_POINT('Ctrl Pts',(2.18421507987119,-2.36969470840714,
11.2778855351453));
#251866=CARTESIAN_POINT('Ctrl Pts',(2.20704155260707,-2.34850448560635,
11.2797981088515));
#251867=CARTESIAN_POINT('Ctrl Pts',(2.22135810699456,-2.33496765247142,
11.2809983649196));
#251868=CARTESIAN_POINT('Ctrl Pts',(2.29127013799473,-2.26763820679431,
11.2868684913453));
#251869=CARTESIAN_POINT('Ctrl Pts',(2.34504474167949,-2.21198304729898,
11.2914119912129));
#251870=CARTESIAN_POINT('Ctrl Pts',(2.51626883581635,-2.02150010581347,
11.3061920222048));
#251871=CARTESIAN_POINT('Ctrl Pts',(2.62450810995535,-1.87883904327364,
11.3160743244534));
#251872=CARTESIAN_POINT('Ctrl Pts',(2.8024391775278,-1.59871379414475,11.3347159627933));
#251873=CARTESIAN_POINT('Ctrl Pts',(2.87519744993961,-1.46382523818974,
11.3434075070993));
#251874=CARTESIAN_POINT('Ctrl Pts',(2.96002656067434,-1.27562127110791,
11.3555621839635));
#251875=CARTESIAN_POINT('Ctrl Pts',(2.98074746116379,-1.22642201455439,
11.3587406408925));
#251876=CARTESIAN_POINT('Ctrl Pts',(3.00902686133688,-1.15431994055603,
11.3634116325884));
#251877=CARTESIAN_POINT('Ctrl Pts',(3.01756589854231,-1.13180969136239,
11.3648716760293));
#251878=CARTESIAN_POINT('Ctrl Pts',(3.03214567893183,-1.09203688032284,
11.3674554531901));
#251879=CARTESIAN_POINT('Ctrl Pts',(3.03829324618058,-1.07481444674469,
11.368575605437));
#251880=CARTESIAN_POINT('Ctrl Pts',(3.0508161701053,-1.03876528796233,11.3709234316049));
#251881=CARTESIAN_POINT('Ctrl Pts',(3.05716457330799,-1.01993008139582,
11.3721519340931));
#251882=CARTESIAN_POINT('Ctrl Pts',(3.0733429909898,-0.970421490271061,
11.3753863142761));
#251883=CARTESIAN_POINT('Ctrl Pts',(3.08288790194672,-0.939657955471732,
11.3774013442109));
#251884=CARTESIAN_POINT('Ctrl Pts',(3.12258902727165,-0.804578247819572,
11.3862747669225));
#251885=CARTESIAN_POINT('Ctrl Pts',(3.14792034208946,-0.698928910227485,
11.3932845998921));
#251886=CARTESIAN_POINT('Ctrl Pts',(3.20576850289787,-0.38948646779044,
11.4140016725154));
#251887=CARTESIAN_POINT('Ctrl Pts',(3.22411671687954,-0.183602133046582,
11.4280455031335));
#251888=CARTESIAN_POINT('Ctrl Pts',(3.22178356804375,0.149118012565971,
11.4504196352041));
#251889=CARTESIAN_POINT('Ctrl Pts',(3.2134463995233,0.275489450037044,11.4588309540877));
#251890=CARTESIAN_POINT('Ctrl Pts',(3.19503744023209,0.422268172084959,
11.4682762805714));
#251891=CARTESIAN_POINT('Ctrl Pts',(3.19216573543396,0.443455327481237,
11.4696316099478));
#251892=CARTESIAN_POINT('Ctrl Pts',(3.18738123633073,0.476295921728712,
11.4717182276112));
#251893=CARTESIAN_POINT('Ctrl Pts',(3.18561494671247,0.487969642843626,
11.4724571607801));
#251894=CARTESIAN_POINT('Ctrl Pts',(3.18219786973034,0.509744072377771,
11.4738299137238));
#251895=CARTESIAN_POINT('Ctrl Pts',(3.18056312012334,0.519846653784449,
11.4744645504747));
#251896=CARTESIAN_POINT('Ctrl Pts',(3.17667381938333,0.543176807411602,
11.4759250784439));
#251897=CARTESIAN_POINT('Ctrl Pts',(3.17438475397495,0.556398281103199,
11.4767490468462));
#251898=CARTESIAN_POINT('Ctrl Pts',(3.16665289061677,0.599455412777923,
11.4794213425896));
#251899=CARTESIAN_POINT('Ctrl Pts',(3.16087134267973,0.629229549086772,
11.4812519201485));
#251900=CARTESIAN_POINT('Ctrl Pts',(3.12173336779103,0.816608322246431,
11.4926879128615));
#251901=CARTESIAN_POINT('Ctrl Pts',(3.07701556476825,0.971625084310848,
11.5017771194138));
#251902=CARTESIAN_POINT('Ctrl Pts',(2.96951831180388,1.26088141462643,11.5190819304013));
#251903=CARTESIAN_POINT('Ctrl Pts',(2.90872596598027,1.39541125665596,11.5272874125494));
#251904=CARTESIAN_POINT('Ctrl Pts',(2.80145664246381,1.59506425538171,11.5402214792416));
#251905=CARTESIAN_POINT('Ctrl Pts',(2.76141796283196,1.66341784472842,11.5447947298266));
#251906=CARTESIAN_POINT('Ctrl Pts',(2.68869185187118,1.77770090206581,11.5527560703656));
#251907=CARTESIAN_POINT('Ctrl Pts',(2.65724246805397,1.8243755854665,11.5561025497488));
#251908=CARTESIAN_POINT('Ctrl Pts',(2.61032939279497,1.89021210205939,11.5609751021571));
#251909=CARTESIAN_POINT('Ctrl Pts',(2.59584206968192,1.91005895932068,11.5624645030511));
#251910=CARTESIAN_POINT('Ctrl Pts',(2.57013566730735,1.94444267386075,11.5650820339151));
#251911=CARTESIAN_POINT('Ctrl Pts',(2.55901654272434,1.95905308059331,11.5662062736578));
#251912=CARTESIAN_POINT('Ctrl Pts',(2.53719221150504,1.98722716186766,11.5683980376107));
#251913=CARTESIAN_POINT('Ctrl Pts',(2.52650154828163,2.00080134424259,11.5694649666015));
#251914=CARTESIAN_POINT('Ctrl Pts',(2.49756892203279,2.0369361235634,11.5723350423054));
#251915=CARTESIAN_POINT('Ctrl Pts',(2.47913093172099,2.0593370359361,11.5741459464324));
#251916=CARTESIAN_POINT('Ctrl Pts',(2.40808546509415,2.14331543121641,11.5810580772105));
#251917=CARTESIAN_POINT('Ctrl Pts',(2.3534694124365,2.20314696155395,11.586239956163));
#251918=CARTESIAN_POINT('Ctrl Pts',(2.13827550878777,2.42174911038901,11.6061848626051));
#251919=CARTESIAN_POINT('Ctrl Pts',(1.96343453316135,2.56553943177328,11.621514370842));
#251920=CARTESIAN_POINT('Ctrl Pts',(1.66755653261322,2.76078887083364,11.6454052219535));
#251921=CARTESIAN_POINT('Ctrl Pts',(1.55591171382705,2.82521588917958,11.6540100002138));
#251922=CARTESIAN_POINT('Ctrl Pts',(1.41466056709349,2.8958074084687,11.664173151145));
#251923=CARTESIAN_POINT('Ctrl Pts',(1.3884433476693,2.90846871620018,11.6660300657538));
#251924=CARTESIAN_POINT('Ctrl Pts',(1.34996461517241,2.92641267243878,11.6687089971135));
#251925=CARTESIAN_POINT('Ctrl Pts',(1.33783694245247,2.93197679418111,11.669546691619));
#251926=CARTESIAN_POINT('Ctrl Pts',(1.31637552493878,2.94166230717733,11.6710169463326));
#251927=CARTESIAN_POINT('Ctrl Pts',(1.30705631863909,2.94581490284486,11.6716513391503));
#251928=CARTESIAN_POINT('Ctrl Pts',(1.28672759425122,2.95475782479119,11.6730263498829));
#251929=CARTESIAN_POINT('Ctrl Pts',(1.27571090610401,2.9595309425171,11.6737659481248));
#251930=CARTESIAN_POINT('Ctrl Pts',(1.24470838960872,2.97275788951337,11.6758324140191));
#251931=CARTESIAN_POINT('Ctrl Pts',(1.22466307480695,2.98107176288728,11.6771512721671));
#251932=CARTESIAN_POINT('Ctrl Pts',(1.08494706701228,3.03737236172377,11.6862345888966));
#251933=CARTESIAN_POINT('Ctrl Pts',(0.96256123432206,3.0783476589196,11.6936407305182));
#251934=CARTESIAN_POINT('Ctrl Pts',(0.797193576542146,3.1228815421372,11.7033246085221));
#251935=CARTESIAN_POINT('Ctrl Pts',(0.756137097401467,3.13307572621057,
11.7057028773094));
#251936=CARTESIAN_POINT('Ctrl Pts',(0.578954736189343,3.17338369697464,
11.7158961203492));
#251937=CARTESIAN_POINT('Ctrl Pts',(0.441155958200194,3.19545505113785,
11.7236535078379));
#251938=CARTESIAN_POINT('Ctrl Pts',(0.217144220371637,3.21656540856973,
11.736452194559));
#251939=CARTESIAN_POINT('Ctrl Pts',(0.131642196141464,3.2211975284276,11.7413791855758));
#251940=CARTESIAN_POINT('Ctrl Pts',(-0.0134855023914868,3.22327197497497,
11.7498927154529));
#251941=CARTESIAN_POINT('Ctrl Pts',(-0.0730412177703081,3.22247240567317,
11.7534290536953));
#251942=CARTESIAN_POINT('Ctrl Pts',(-0.15762821317495,3.21899075722102,
11.7585284125583));
#251943=CARTESIAN_POINT('Ctrl Pts',(-0.182704956213157,3.21766483547543,
11.7600497299663));
#251944=CARTESIAN_POINT('Ctrl Pts',(-0.226171824248095,3.21485678735417,
11.7627044069254));
#251945=CARTESIAN_POINT('Ctrl Pts',(-0.244569674268101,3.21350953159295,
11.763833536507));
#251946=CARTESIAN_POINT('Ctrl Pts',(-0.28003325312058,3.2106062625554,11.7660210750847));
#251947=CARTESIAN_POINT('Ctrl Pts',(-0.297100165231679,3.20907193280222,
11.7670787720217));
#251948=CARTESIAN_POINT('Ctrl Pts',(-0.342262058856747,3.20464848320428,
11.7698910777815));
#251949=CARTESIAN_POINT('Ctrl Pts',(-0.370332198358267,3.20152607359326,
11.771652884546));
#251950=CARTESIAN_POINT('Ctrl Pts',(-0.473215699810164,3.18871059212305,
11.7781628751098));
#251951=CARTESIAN_POINT('Ctrl Pts',(-0.547718533819655,3.1767611265088,
11.7829801384191));
#251952=CARTESIAN_POINT('Ctrl Pts',(-0.848311967222745,3.11766079624425,
11.8028439921008));
#251953=CARTESIAN_POINT('Ctrl Pts',(-1.06942771854834,3.0488916690584,11.818513527782));
#251954=CARTESIAN_POINT('Ctrl Pts',(-1.40108390359436,2.90519084761208,
11.842879498471));
#251955=CARTESIAN_POINT('Ctrl Pts',(-1.51765037326923,2.84603471151077,
11.851610427585));
#251956=CARTESIAN_POINT('Ctrl Pts',(-1.65558789475757,2.76514099505496,
11.8619040408777));
#251957=CARTESIAN_POINT('Ctrl Pts',(-1.68065920282051,2.74997468752692,
11.8637731403095));
#251958=CARTESIAN_POINT('Ctrl Pts',(-1.71687135366568,2.72738872548387,
11.8664662264588));
#251959=CARTESIAN_POINT('Ctrl Pts',(-1.72817758518681,2.72023873100847,
11.8673061167705));
#251960=CARTESIAN_POINT('Ctrl Pts',(-1.74803055190906,2.70751009321934,
11.8687787690944));
#251961=CARTESIAN_POINT('Ctrl Pts',(-1.75659573374236,2.70196098295213,
11.8694133855051));
#251962=CARTESIAN_POINT('Ctrl Pts',(-1.77516006700593,2.68980814873806,
11.8707871946287));
#251963=CARTESIAN_POINT('Ctrl Pts',(-1.78514886414004,2.68318927472652,
11.8715253838606));
#251964=CARTESIAN_POINT('Ctrl Pts',(-1.81303481518356,2.66448656042187,
11.873584060386));
#251965=CARTESIAN_POINT('Ctrl Pts',(-1.83084813357572,2.65227808500167,
11.8748966335251));
#251966=CARTESIAN_POINT('Ctrl Pts',(-1.95060920324415,2.56841747481395,
11.8837139954207));
#251967=CARTESIAN_POINT('Ctrl Pts',(-2.04846102655947,2.49107583799226,
11.890884404987));
#251968=CARTESIAN_POINT('Ctrl Pts',(-2.34760626076273,2.22505378919181,
11.9135482970079));
#251969=CARTESIAN_POINT('Ctrl Pts',(-2.52924695131744,2.01619149584354,
11.9286034010639));
#251970=CARTESIAN_POINT('Ctrl Pts',(-2.71371900606081,1.73928177831334,
11.9481494245084));
#251971=CARTESIAN_POINT('Ctrl Pts',(-2.7440794316737,1.69097588334042,11.9515406965663));
#251972=CARTESIAN_POINT('Ctrl Pts',(-2.78572504242377,1.62063681657417,
11.9564668476198));
#251973=CARTESIAN_POINT('Ctrl Pts',(-2.79806439672783,1.59923834476012,
11.9579638969909));
#251974=CARTESIAN_POINT('Ctrl Pts',(-2.81915445781292,1.56167331596258,
11.960590290173));
#251975=CARTESIAN_POINT('Ctrl Pts',(-2.8280151900197,1.54556962507962,11.9617156627545));
#251976=CARTESIAN_POINT('Ctrl Pts',(-2.84604741517343,1.5121231873291,11.964052332442));
#251977=CARTESIAN_POINT('Ctrl Pts',(-2.8551992512411,1.49477076230871,11.9652642616491));
#251978=CARTESIAN_POINT('Ctrl Pts',(-2.87840484588383,1.44978081437313,
11.9684060529069));
#251979=CARTESIAN_POINT('Ctrl Pts',(-2.89221895643368,1.42202259746327,
11.9703441272816));
#251980=CARTESIAN_POINT('Ctrl Pts',(-2.94834459176881,1.30504115757637,
11.9785126342125));
#251981=CARTESIAN_POINT('Ctrl Pts',(-2.98694080868465,1.21410444187207,
11.9848669111144));
#251982=CARTESIAN_POINT('Ctrl Pts',(-3.10186835549107,0.904504766804046,
12.0065105487312));
#251983=CARTESIAN_POINT('Ctrl Pts',(-3.15880969331165,0.67942462263731,
12.0223187939908));
#251984=CARTESIAN_POINT('Ctrl Pts',(-3.20195534518314,0.373611688638818,
12.043033553281));
#251985=CARTESIAN_POINT('Ctrl Pts',(-3.21000236929912,0.296630968749452,
12.0481782358679));
#251986=CARTESIAN_POINT('Ctrl Pts',(-3.2184370751095,0.173039251601177,
12.056258527319));
#251987=CARTESIAN_POINT('Ctrl Pts',(-3.22059892083219,0.12658153875267,
12.059255362799));
#251988=CARTESIAN_POINT('Ctrl Pts',(-3.22215222671543,0.0640977615092215,
12.063217637612));
#251989=CARTESIAN_POINT('Ctrl Pts',(-3.22243072041141,0.0481016822066572,
12.0642259748981));
#251990=CARTESIAN_POINT('Ctrl Pts',(-3.22269604935966,0.0214678861005913,
12.0658941240438));
#251991=CARTESIAN_POINT('Ctrl Pts',(-3.22274935267479,0.0108312704363253,
12.0665574697344));
#251992=CARTESIAN_POINT('Ctrl Pts',(-3.22274999804659,0.000129566408754178,
12.0672218721387));
#251993=CARTESIAN_POINT('Ctrl Pts',(-3.22275,6.47832063023646E-5,12.0672258940155));
#251994=CARTESIAN_POINT('Ctrl Pts',(-3.22275,-3.23896726357594E-13,12.0672299157825));
#251995=CARTESIAN_POINT('Origin',(0.,0.,-2.31077344927308));
#251996=CARTESIAN_POINT('',(-3.22275,7.83873563209288E-13,13.5633017710267));
#251997=CARTESIAN_POINT('',(-3.22275,-2.24100014615096E-11,13.3128542084224));
#251998=CARTESIAN_POINT('',(-3.22275,-3.50678552687464E-13,-2.31077344927308));
#251999=CARTESIAN_POINT('Ctrl Pts',(-3.22275,7.83873563209288E-13,13.5633017710267));
#252000=CARTESIAN_POINT('Ctrl Pts',(-3.22275,0.0358663401662114,13.5611946398766));
#252001=CARTESIAN_POINT('Ctrl Pts',(-3.22215126056633,0.0717294574829636,
13.5590715766439));
#252002=CARTESIAN_POINT('Ctrl Pts',(-3.21998093223654,0.136712604019992,
13.5551907275807));
#252003=CARTESIAN_POINT('Ctrl Pts',(-3.21861244358439,0.165835447558698,
13.5534391303));
#252004=CARTESIAN_POINT('Ctrl Pts',(-3.21579086853076,0.212397530855393,
13.5506170458497));
#252005=CARTESIAN_POINT('Ctrl Pts',(-3.21459051622025,0.229850855455928,
13.5495543548726));
#252006=CARTESIAN_POINT('Ctrl Pts',(-3.21194561779516,0.264217801727172,
13.5474518433432));
#252007=CARTESIAN_POINT('Ctrl Pts',(-3.2105094232961,0.281131506778595,
13.5464123146483));
#252008=CARTESIAN_POINT('Ctrl Pts',(-3.20716883802595,0.317099815306884,
13.5441911580151));
#252009=CARTESIAN_POINT('Ctrl Pts',(-3.20522810348359,0.336150305702089,
13.5430084345697));
#252010=CARTESIAN_POINT('Ctrl Pts',(-3.1997956045101,0.385141897159354,
13.5399501421897));
#252011=CARTESIAN_POINT('Ctrl Pts',(-3.19605338735088,0.415052813977154,
13.5380668360008));
#252012=CARTESIAN_POINT('Ctrl Pts',(-3.178844011077,0.538518149897557,13.5302239732648));
#252013=CARTESIAN_POINT('Ctrl Pts',(-3.16168512166983,0.631502455369941,
13.524151047291));
#252014=CARTESIAN_POINT('Ctrl Pts',(-3.08775748245068,0.952356580424882,
13.5026131197667));
#252015=CARTESIAN_POINT('Ctrl Pts',(-3.0102117915324,1.17466271469998,13.4865864710136));
#252016=CARTESIAN_POINT('Ctrl Pts',(-2.85870212786544,1.49255903783352,
13.4629476731765));
#252017=CARTESIAN_POINT('Ctrl Pts',(-2.80241117014893,1.59574673381918,
13.4551633074184));
#252018=CARTESIAN_POINT('Ctrl Pts',(-2.72967768614361,1.71330345704064,
13.4463421120735));
#252019=CARTESIAN_POINT('Ctrl Pts',(-2.71857812760522,1.73086164154363,
13.4450259673334));
#252020=CARTESIAN_POINT('Ctrl Pts',(-2.7010600263119,1.75798890667437,13.4429961812286));
#252021=CARTESIAN_POINT('Ctrl Pts',(-2.69475884302119,1.76763261150958,
13.4422753216137));
#252022=CARTESIAN_POINT('Ctrl Pts',(-2.68288689045436,1.785591122116,13.4409346086661));
#252023=CARTESIAN_POINT('Ctrl Pts',(-2.67732909499756,1.79391377782846,
13.44031398658));
#252024=CARTESIAN_POINT('Ctrl Pts',(-2.66439402059305,1.81308970241323,
13.4388855002408));
#252025=CARTESIAN_POINT('Ctrl Pts',(-2.65698912115888,1.82392395393308,
13.4380794802634));
#252026=CARTESIAN_POINT('Ctrl Pts',(-2.63264827627908,1.8590746903839,13.4354668465017));
#252027=CARTESIAN_POINT('Ctrl Pts',(-2.61544257349356,1.88320363623368,
13.4336772327723));
#252028=CARTESIAN_POINT('Ctrl Pts',(-2.49305162417735,2.04992869813666,
13.4213122866347));
#252029=CARTESIAN_POINT('Ctrl Pts',(-2.37658286303402,2.1838916971656,13.4113709393831));
#252030=CARTESIAN_POINT('Ctrl Pts',(-2.15140393087684,2.40341740256482,
13.3937606130911));
#252031=CARTESIAN_POINT('Ctrl Pts',(-2.04711282669549,2.49284602451749,
13.3861041895864));
#252032=CARTESIAN_POINT('Ctrl Pts',(-1.87589041363542,2.62165703698144,
13.3738620427079));
#252033=CARTESIAN_POINT('Ctrl Pts',(-1.81270126910884,2.6657388168922,13.3694085761401));
#252034=CARTESIAN_POINT('Ctrl Pts',(-1.70185613366309,2.73730151183758,
13.3616476746094));
#252035=CARTESIAN_POINT('Ctrl Pts',(-1.65496397457985,2.76590447863094,
13.3583795572725));
#252036=CARTESIAN_POINT('Ctrl Pts',(-1.58654231170114,2.80527685959978,
13.3536198483612));
#252037=CARTESIAN_POINT('Ctrl Pts',(-1.56558587952221,2.81702601550049,
13.3521632300672));
#252038=CARTESIAN_POINT('Ctrl Pts',(-1.52874277563977,2.83714388570301,
13.349603496562));
#252039=CARTESIAN_POINT('Ctrl Pts',(-1.51291371437355,2.84561627327218,
13.3485041049566));
#252040=CARTESIAN_POINT('Ctrl Pts',(-1.47998879469051,2.86288672154734,
13.3462176751596));
#252041=CARTESIAN_POINT('Ctrl Pts',(-1.46288337751684,2.87166491973028,
13.3450299965244));
#252042=CARTESIAN_POINT('Ctrl Pts',(-1.41843803928599,2.89397332320842,
13.3419440006812));
#252043=CARTESIAN_POINT('Ctrl Pts',(-1.39098322232348,2.90726910346661,
13.340037675965));
#252044=CARTESIAN_POINT('Ctrl Pts',(-1.27481875157701,2.96150294767342,
13.3319692947165));
#252045=CARTESIAN_POINT('Ctrl Pts',(-1.184467641818,2.99878238443524,13.3256855580095));
#252046=CARTESIAN_POINT('Ctrl Pts',(-0.893184864502717,3.10374858810872,
13.3054045072757));
#252047=CARTESIAN_POINT('Ctrl Pts',(-0.687212230240054,3.15574988780722,
13.2909909483514));
#252048=CARTESIAN_POINT('Ctrl Pts',(-0.354943453974266,3.2055466186936,
13.2683618758922));
#252049=CARTESIAN_POINT('Ctrl Pts',(-0.231259848256791,3.21683673472798,
13.2600831813729));
#252050=CARTESIAN_POINT('Ctrl Pts',(-0.0788707856187371,3.22190963768195,
13.2502762007257));
#252051=CARTESIAN_POINT('Ctrl Pts',(-0.0505059875189472,3.2224791055765,
13.2484676520801));
#252052=CARTESIAN_POINT('Ctrl Pts',(-0.00910165381677435,3.22276350853609,
13.2458558245503));
#252053=CARTESIAN_POINT('Ctrl Pts',(0.00393366097045205,3.22277396228803,
13.2450376123386));
#252054=CARTESIAN_POINT('Ctrl Pts',(0.0269438792341366,3.22265280352359,
13.2436008913908));
#252055=CARTESIAN_POINT('Ctrl Pts',(0.0369185630251869,3.2225539706236,
13.2429806325191));
#252056=CARTESIAN_POINT('Ctrl Pts',(0.0586145034701227,3.22223824757651,
13.2416371095459));
#252057=CARTESIAN_POINT('Ctrl Pts',(0.0703351560375073,3.2220037181814,
13.2409148133784));
#252058=CARTESIAN_POINT('Ctrl Pts',(0.103171899426244,3.22116739030173,
13.2389003964433));
#252059=CARTESIAN_POINT('Ctrl Pts',(0.124284152143396,3.22042191335284,
13.2376158718731));
#252060=CARTESIAN_POINT('Ctrl Pts',(0.261869204336672,3.21420870237208,
13.2293054000103));
#252061=CARTESIAN_POINT('Ctrl Pts',(0.377991897923247,3.20263032051029,
13.2225730395773));
#252062=CARTESIAN_POINT('Ctrl Pts',(0.544645701192555,3.17681984058416,
13.2130024008611));
#252063=CARTESIAN_POINT('Ctrl Pts',(0.595849692859433,3.16761528325244,
13.2100747340992));
#252064=CARTESIAN_POINT('Ctrl Pts',(0.882804882633464,3.10882688126546,
13.1936399797742));
#252065=CARTESIAN_POINT('Ctrl Pts',(1.11261345672149,3.03417701163737,13.1803029326043));
#252066=CARTESIAN_POINT('Ctrl Pts',(1.37893183780909,2.91330157529856,13.1630634293369));
#252067=CARTESIAN_POINT('Ctrl Pts',(1.42538856681701,2.89085559604023,13.1599888528237));
#252068=CARTESIAN_POINT('Ctrl Pts',(1.49214758121315,2.85659990536123,13.1554614429685));
#252069=CARTESIAN_POINT('Ctrl Pts',(1.51289253948003,2.84566750394746,13.1540389058314));
#252070=CARTESIAN_POINT('Ctrl Pts',(1.54923238495767,2.82600705679663,13.1515183180472));
#252071=CARTESIAN_POINT('Ctrl Pts',(1.56487758611687,2.81737377499035,13.1504236405808));
#252072=CARTESIAN_POINT('Ctrl Pts',(1.59741869759054,2.79906237540298,13.1481264356284));
#252073=CARTESIAN_POINT('Ctrl Pts',(1.61430026898782,2.78936037326888,13.1469230873724));
#252074=CARTESIAN_POINT('Ctrl Pts',(1.6583820652066,2.76349193208171,13.1437496960681));
#252075=CARTESIAN_POINT('Ctrl Pts',(1.68543339541205,2.74707715376231,13.1417707712434));
#252076=CARTESIAN_POINT('Ctrl Pts',(1.80426322779336,2.67255516414074,13.1329341626486));
#252077=CARTESIAN_POINT('Ctrl Pts',(1.89330242268958,2.61023342398971,13.1259239752546));
#252078=CARTESIAN_POINT('Ctrl Pts',(2.14223260359977,2.41655174426798,13.1051712088819));
#252079=CARTESIAN_POINT('Ctrl Pts',(2.29283553839621,2.27415362394656,13.0910872142394));
#252080=CARTESIAN_POINT('Ctrl Pts',(2.50575449385242,2.03003419588436,13.0692981273801));
#252081=CARTESIAN_POINT('Ctrl Pts',(2.57790072315649,1.93759576747014,13.0614993286319));
#252082=CARTESIAN_POINT('Ctrl Pts',(2.66063699322368,1.81876085031963,13.0521924775223));
#252083=CARTESIAN_POINT('Ctrl Pts',(2.67612530448039,1.79589356929337,13.0504327918974));
#252084=CARTESIAN_POINT('Ctrl Pts',(2.6984122254328,1.76205996578632,13.0478778944026));
#252085=CARTESIAN_POINT('Ctrl Pts',(2.70544156284286,1.7512480762753,13.0470686221526));
#252086=CARTESIAN_POINT('Ctrl Pts',(2.7177866054122,1.73200831473337,13.0456415978013));
#252087=CARTESIAN_POINT('Ctrl Pts',(2.72312835127333,1.72359764042373,13.0450221826393));
#252088=CARTESIAN_POINT('Ctrl Pts',(2.7347230950273,1.70515304945076,13.0436734697418));
#252089=CARTESIAN_POINT('Ctrl Pts',(2.74095995180388,1.69510940100128,13.0429452065106));
#252090=CARTESIAN_POINT('Ctrl Pts',(2.75842054246987,1.66664304050818,13.0408977659757));
#252091=CARTESIAN_POINT('Ctrl Pts',(2.76951500334876,1.64814126105842,13.0395865850921));
#252092=CARTESIAN_POINT('Ctrl Pts',(2.85097523481237,1.50914776822978,13.0298708566849));
#252093=CARTESIAN_POINT('Ctrl Pts',(2.91364346287063,1.38429681948049,13.0218891530275));
#252094=CARTESIAN_POINT('Ctrl Pts',(3.04738381157273,1.06819834571415,13.0025347886259));
#252095=CARTESIAN_POINT('Ctrl Pts',(3.10878165776468,0.873539586872534,
12.9913088706737));
#252096=CARTESIAN_POINT('Ctrl Pts',(3.165599608262,0.608031008054314,12.9757109832134));
#252097=CARTESIAN_POINT('Ctrl Pts',(3.17769983394231,0.541244427059038,
12.9717676289282));
#252098=CARTESIAN_POINT('Ctrl Pts',(3.1950345952809,0.424698562499329,12.9648149552288));
#252099=CARTESIAN_POINT('Ctrl Pts',(3.20123565035463,0.375106444609076,
12.9618344360339));
#252100=CARTESIAN_POINT('Ctrl Pts',(3.20861938951724,0.302350091821688,
12.9574203226909));
#252101=CARTESIAN_POINT('Ctrl Pts',(3.21070932288946,0.279284023725336,
12.9560148726176));
#252102=CARTESIAN_POINT('Ctrl Pts',(3.21396788717999,0.238423802997251,
12.953513661383));
#252103=CARTESIAN_POINT('Ctrl Pts',(3.2152377982239,0.220638551757844,12.9524210991844));
#252104=CARTESIAN_POINT('Ctrl Pts',(3.21759426671376,0.183273617033214,
12.9501172531451));
#252105=CARTESIAN_POINT('Ctrl Pts',(3.21864983057021,0.163692776551101,
12.948905050671));
#252106=CARTESIAN_POINT('Ctrl Pts',(3.22097013911627,0.111853116265333,
12.9456823178505));
#252107=CARTESIAN_POINT('Ctrl Pts',(3.22192894167087,0.0795834824832295,
12.9436623971926));
#252108=CARTESIAN_POINT('Ctrl Pts',(3.22410973531638,-0.0689690337821968,
12.9342973552168));
#252109=CARTESIAN_POINT('Ctrl Pts',(3.21952199336371,-0.185238243564716,
12.9267758968677));
#252110=CARTESIAN_POINT('Ctrl Pts',(3.18857647148389,-0.515123457258313,
12.9049121988007));
#252111=CARTESIAN_POINT('Ctrl Pts',(3.14710548087625,-0.726695576877911,
12.8902230967812));
#252112=CARTESIAN_POINT('Ctrl Pts',(3.06305925291084,-1.00472543769805,
12.8707532878309));
#252113=CARTESIAN_POINT('Ctrl Pts',(3.03870811460726,-1.07613174655434,
12.8657428324953));
#252114=CARTESIAN_POINT('Ctrl Pts',(2.99568113575361,-1.18915226412852,
12.8578599058794));
#252115=CARTESIAN_POINT('Ctrl Pts',(2.978589715227,-1.23133763071961,12.8549286438657));
#252116=CARTESIAN_POINT('Ctrl Pts',(2.95442247406637,-1.28753667436181,
12.8510517593429));
#252117=CARTESIAN_POINT('Ctrl Pts',(2.94813047292547,-1.30187924969768,
12.8500648434001));
#252118=CARTESIAN_POINT('Ctrl Pts',(2.93748380060396,-1.32567521985732,
12.848432307294));
#252119=CARTESIAN_POINT('Ctrl Pts',(2.93318750551928,-1.33515427345288,
12.8477832880504));
#252120=CARTESIAN_POINT('Ctrl Pts',(2.92494675392128,-1.35310434121559,
12.8465569650852));
#252121=CARTESIAN_POINT('Ctrl Pts',(2.9210112609994,-1.36157926313022,12.8459791095226));
#252122=CARTESIAN_POINT('Ctrl Pts',(2.91044992670527,-1.38406611667345,
12.8444485851779));
#252123=CARTESIAN_POINT('Ctrl Pts',(2.90375967600479,-1.39804776645132,
12.8434997748723));
#252124=CARTESIAN_POINT('Ctrl Pts',(2.87904855361857,-1.44874770573644,
12.8400675873178));
#252125=CARTESIAN_POINT('Ctrl Pts',(2.86042920244515,-1.48517191280919,
12.8376178685825));
#252126=CARTESIAN_POINT('Ctrl Pts',(2.70114737583583,-1.78265342181489,
12.8176638777577));
#252127=CARTESIAN_POINT('Ctrl Pts',(2.52575118061019,-2.02353037842577,
12.8017313189807));
#252128=CARTESIAN_POINT('Ctrl Pts',(2.26576301680282,-2.29314410800168,
12.7803420927316));
#252129=CARTESIAN_POINT('Ctrl Pts',(2.20964845128471,-2.34726319444911,
12.7758380055377));
#252130=CARTESIAN_POINT('Ctrl Pts',(2.11038564171794,-2.43627977450228,
12.7679975509954));
#252131=CARTESIAN_POINT('Ctrl Pts',(2.06819638864876,-2.47219535168871,
12.7647016432471));
#252132=CARTESIAN_POINT('Ctrl Pts',(2.0063521334228,-2.52215181298464,12.7599086681979));
#252133=CARTESIAN_POINT('Ctrl Pts',(1.98743108663119,-2.53708814959117,
12.7584472734013));
#252134=CARTESIAN_POINT('Ctrl Pts',(1.95411862971046,-2.56278378636093,
12.7558820069196));
#252135=CARTESIAN_POINT('Ctrl Pts',(1.93980133283253,-2.57363772184719,
12.7547819083152));
#252136=CARTESIAN_POINT('Ctrl Pts',(1.91186679139943,-2.59444936274832,
12.7526397918744));
#252137=CARTESIAN_POINT('Ctrl Pts',(1.8982606192465,-2.60442099672753,12.7515983630423));
#252138=CARTESIAN_POINT('Ctrl Pts',(1.86168867002207,-2.63078485859894,
12.7488039069828));
#252139=CARTESIAN_POINT('Ctrl Pts',(1.83858525667503,-2.64698278225353,
12.7470435589161));
#252140=CARTESIAN_POINT('Ctrl Pts',(1.75095070283274,-2.70672295861865,
12.7403830984852));
#252141=CARTESIAN_POINT('Ctrl Pts',(1.6850659004304,-2.74822284581297,12.7354085261731));
#252142=CARTESIAN_POINT('Ctrl Pts',(1.41935142133246,-2.90244371588403,
12.7154655071404));
#252143=CARTESIAN_POINT('Ctrl Pts',(1.20924709610444,-2.99606981572496,
12.6998922332525));
#252144=CARTESIAN_POINT('Ctrl Pts',(0.89837337492101,-3.09653406966299,
12.6778662830106));
#252145=CARTESIAN_POINT('Ctrl Pts',(0.804408848719862,-3.12226306038524,
12.6713430518917));
#252146=CARTESIAN_POINT('Ctrl Pts',(0.673954791905544,-3.15170179833793,
12.6625802457452));
#252147=CARTESIAN_POINT('Ctrl Pts',(0.638356623688517,-3.15910435567473,
12.6602187381818));
#252148=CARTESIAN_POINT('Ctrl Pts',(0.576358239115391,-3.17090593803914,
12.6561656727509));
#252149=CARTESIAN_POINT('Ctrl Pts',(0.550014829495976,-3.17558137701367,
12.6544620957646));
#252150=CARTESIAN_POINT('Ctrl Pts',(0.511051678742976,-3.1819971508875,
12.6519727925185));
#252151=CARTESIAN_POINT('Ctrl Pts',(0.498475668353988,-3.18399147414252,
12.6511739792801));
#252152=CARTESIAN_POINT('Ctrl Pts',(0.476990971310048,-3.18726813630295,
12.6498176091965));
#252153=CARTESIAN_POINT('Ctrl Pts',(0.468088332760631,-3.18858775620315,
12.6492580145221));
#252154=CARTESIAN_POINT('Ctrl Pts',(0.447757694539533,-3.19151433974754,
12.6479857245787));
#252155=CARTESIAN_POINT('Ctrl Pts',(0.436326488107356,-3.19309723296441,
12.6472743736533));
#252156=CARTESIAN_POINT('Ctrl Pts',(0.404753393820786,-3.19729647952879,
12.6453200759619));
#252157=CARTESIAN_POINT('Ctrl Pts',(0.38459451932365,-3.19978392882761,
12.6440840208563));
#252158=CARTESIAN_POINT('Ctrl Pts',(0.271988327922241,-3.21259908011242,
12.6372381695844));
#252159=CARTESIAN_POINT('Ctrl Pts',(0.17914281766099,-3.21911192069469,
12.6318134859512));
#252160=CARTESIAN_POINT('Ctrl Pts',(-0.0820541417697187,-3.22609568725263,
12.6168509453061));
#252161=CARTESIAN_POINT('Ctrl Pts',(-0.250346099388465,-3.21741478542948,
12.6075463005668));
#252162=CARTESIAN_POINT('Ctrl Pts',(-0.593129813908984,-3.17266366030316,
12.5881134168657));
#252163=CARTESIAN_POINT('Ctrl Pts',(-0.766844646278213,-3.13520908200744,
12.5779952479085));
#252164=CARTESIAN_POINT('Ctrl Pts',(-0.969558580437706,-3.0736397602419,
12.5653516299413));
#252165=CARTESIAN_POINT('Ctrl Pts',(-1.00236976531824,-3.06309646168907,
12.5632789548714));
#252166=CARTESIAN_POINT('Ctrl Pts',(-1.05401915463539,-3.0455811128256,
12.5599717030636));
#252167=CARTESIAN_POINT('Ctrl Pts',(-1.07297264065034,-3.03895547472312,
12.5587484554414));
#252168=CARTESIAN_POINT('Ctrl Pts',(-1.10855182729945,-3.02614359433572,
12.5564334887025));
#252169=CARTESIAN_POINT('Ctrl Pts',(-1.12519083083141,-3.01999632147912,
12.5553430914077));
#252170=CARTESIAN_POINT('Ctrl Pts',(-1.16266280694771,-3.00579965110571,
12.5528694460832));
#252171=CARTESIAN_POINT('Ctrl Pts',(-1.18346438730582,-2.99767048710597,
12.5514835872462));
#252172=CARTESIAN_POINT('Ctrl Pts',(-1.24500369056506,-2.97288083146991,
12.5473450454687));
#252173=CARTESIAN_POINT('Ctrl Pts',(-1.28548512443879,-2.95560185374097,
12.5445718733274));
#252174=CARTESIAN_POINT('Ctrl Pts',(-1.53068104161221,-2.84495288642643,
12.527454613147));
#252175=CARTESIAN_POINT('Ctrl Pts',(-1.7254753658575,-2.73119835378743,
12.5124102001004));
#252176=CARTESIAN_POINT('Ctrl Pts',(-2.01632944886312,-2.51773496695751,
12.4880284723794));
#252177=CARTESIAN_POINT('Ctrl Pts',(-2.12066464762074,-2.43050582611848,
12.478830284359));
#252178=CARTESIAN_POINT('Ctrl Pts',(-2.25129371644323,-2.30645932524984,
12.4669508460402));
#252179=CARTESIAN_POINT('Ctrl Pts',(-2.28277062809379,-2.27531023125222,
12.4640581776777));
#252180=CARTESIAN_POINT('Ctrl Pts',(-2.335211470524,-2.22123140567934,12.4592013210175));
#252181=CARTESIAN_POINT('Ctrl Pts',(-2.3565035845879,-2.19862970707747,
12.4572182402297));
#252182=CARTESIAN_POINT('Ctrl Pts',(-2.38658940270406,-2.16575418409494,
12.4544044977161));
#252183=CARTESIAN_POINT('Ctrl Pts',(-2.39564960061816,-2.15572799054074,
12.4535555938201));
#252184=CARTESIAN_POINT('Ctrl Pts',(-2.41132281878493,-2.13816285122721,
12.452084805416));
#252185=CARTESIAN_POINT('Ctrl Pts',(-2.41796411262604,-2.1306495899775,
12.4514608733639));
#252186=CARTESIAN_POINT('Ctrl Pts',(-2.4320976959166,-2.11450914169073,
12.450131660481));
#252187=CARTESIAN_POINT('Ctrl Pts',(-2.43957926818679,-2.10587300573941,
12.4494271429783));
#252188=CARTESIAN_POINT('Ctrl Pts',(-2.45990438737667,-2.08215760532906,
12.4475101193186));
#252189=CARTESIAN_POINT('Ctrl Pts',(-2.47265533060186,-2.06699916518631,
12.4463040833927));
#252190=CARTESIAN_POINT('Ctrl Pts',(-2.54048122110357,-1.98484122956432,
12.4398643901706));
#252191=CARTESIAN_POINT('Ctrl Pts',(-2.59297905393479,-1.91575098536107,
12.4347915702413));
#252192=CARTESIAN_POINT('Ctrl Pts',(-2.74159201450701,-1.70284600077162,
12.4198784977412));
#252193=CARTESIAN_POINT('Ctrl Pts',(-2.82898927922521,-1.55333086609714,
12.4103201763135));
#252194=CARTESIAN_POINT('Ctrl Pts',(-2.97521011732739,-1.24949167868997,
12.3913725737308));
#252195=CARTESIAN_POINT('Ctrl Pts',(-3.03501794846586,-1.09624922720985,
12.3820249483289));
#252196=CARTESIAN_POINT('Ctrl Pts',(-3.09560811580426,-0.897348988973454,
12.3697032977783));
#252197=CARTESIAN_POINT('Ctrl Pts',(-3.10748340485557,-0.855319491042631,
12.3670904620207));
#252198=CARTESIAN_POINT('Ctrl Pts',(-3.12404455585508,-0.791799256289775,
12.3631218490914));
#252199=CARTESIAN_POINT('Ctrl Pts',(-3.1293707795958,-0.770479679372991,
12.3617865514438));
#252200=CARTESIAN_POINT('Ctrl Pts',(-3.13859473982219,-0.731884021168136,
12.3593625396258));
#252201=CARTESIAN_POINT('Ctrl Pts',(-3.14256891921135,-0.714626986368407,
12.3582763146423));
#252202=CARTESIAN_POINT('Ctrl Pts',(-3.15079806254323,-0.677496973424845,
12.355933696335));
#252203=CARTESIAN_POINT('Ctrl Pts',(-3.15500765292982,-0.657614826345666,
12.3546759112392));
#252204=CARTESIAN_POINT('Ctrl Pts',(-3.16589156815588,-0.603697787038005,
12.3512553003437));
#252205=CARTESIAN_POINT('Ctrl Pts',(-3.17220482578302,-0.569593568217683,
12.3490812031752));
#252206=CARTESIAN_POINT('Ctrl Pts',(-3.20777462945284,-0.358460464424845,
12.3355529419085));
#252207=CARTESIAN_POINT('Ctrl Pts',(-3.22275000000872,-0.179374813335885,
12.3237542306299));
#252208=CARTESIAN_POINT('Ctrl Pts',(-3.22275,1.56749301039039E-10,12.3117125106066));
#252209=CARTESIAN_POINT('',(-3.22274905501283,0.00246797769559721,13.3127140476874));
#252210=CARTESIAN_POINT('Ctrl Pts',(-3.22275,-3.23896726357594E-13,12.0672299157825));
#252211=CARTESIAN_POINT('Ctrl Pts',(-3.22275,-0.0108116653985819,12.0679011082235));
#252212=CARTESIAN_POINT('Ctrl Pts',(-3.22269559361987,-0.0216234471182378,
12.06856923911));
#252213=CARTESIAN_POINT('Ctrl Pts',(-3.22241450571572,-0.0495510558761717,
12.070287609666));
#252214=CARTESIAN_POINT('Ctrl Pts',(-3.22210586925214,-0.0666659614557475,
12.0713334426425));
#252215=CARTESIAN_POINT('Ctrl Pts',(-3.2202005696579,-0.139933736446529,
12.0757826669111));
#252216=CARTESIAN_POINT('Ctrl Pts',(-3.21727216450677,-0.196045427098966,
12.0791198911071));
#252217=CARTESIAN_POINT('Ctrl Pts',(-3.20480015512225,-0.355022549124413,
12.0884469850227));
#252218=CARTESIAN_POINT('Ctrl Pts',(-3.19177644294579,-0.45754887858188,
12.0943105410957));
#252219=CARTESIAN_POINT('Ctrl Pts',(-3.13010123346049,-0.807549566361406,
12.1143090446839));
#252220=CARTESIAN_POINT('Ctrl Pts',(-3.05737824815079,-1.04980990205459,
12.1281950979036));
#252221=CARTESIAN_POINT('Ctrl Pts',(-2.93547912218258,-1.33118640648984,
12.1462284142651));
#252222=CARTESIAN_POINT('Ctrl Pts',(-2.91252111456401,-1.38069372805963,
12.1494742179247));
#252223=CARTESIAN_POINT('Ctrl Pts',(-2.8784642380786,-1.44950152486143,
12.1541011009358));
#252224=CARTESIAN_POINT('Ctrl Pts',(-2.86840468768796,-1.46930784746499,
12.1554467177226));
#252225=CARTESIAN_POINT('Ctrl Pts',(-2.84960352252361,-1.50539655882529,
12.1579247050641));
#252226=CARTESIAN_POINT('Ctrl Pts',(-2.84092502346485,-1.52171088706322,
12.1590548447711));
#252227=CARTESIAN_POINT('Ctrl Pts',(-2.82300648447529,-1.55470756187721,
12.1613613364517));
#252228=CARTESIAN_POINT('Ctrl Pts',(-2.81375772580421,-1.57138431012968,
12.1625379633914));
#252229=CARTESIAN_POINT('Ctrl Pts',(-2.79036972352057,-1.61268741928556,
12.1654798759273));
#252230=CARTESIAN_POINT('Ctrl Pts',(-2.77605218521744,-1.63721045962063,
12.1672514651459));
#252231=CARTESIAN_POINT('Ctrl Pts',(-2.718509850971,-1.73284348207593,12.174260547335));
#252232=CARTESIAN_POINT('Ctrl Pts',(-2.67286474218635,-1.80245233546225,
12.1795844814411));
#252233=CARTESIAN_POINT('Ctrl Pts',(-2.54308215496004,-1.98458397715925,
12.1941305601796));
#252234=CARTESIAN_POINT('Ctrl Pts',(-2.45420250009073,-2.09349557860879,
12.2035060361056));
#252235=CARTESIAN_POINT('Ctrl Pts',(-2.21182236916084,-2.35378254601469,
12.2274858429146));
#252236=CARTESIAN_POINT('Ctrl Pts',(-2.04971070038907,-2.49622691209908,
12.2421770468629));
#252237=CARTESIAN_POINT('Ctrl Pts',(-1.85423266076305,-2.63601321068126,
12.2576243171508));
#252238=CARTESIAN_POINT('Ctrl Pts',(-1.83369743965594,-2.65033926004513,
12.2592211010892));
#252239=CARTESIAN_POINT('Ctrl Pts',(-1.8024791572505,-2.67158160734804,
12.2616072363407));
#252240=CARTESIAN_POINT('Ctrl Pts',(-1.79191917100987,-2.67867599647793,
12.2624073559749));
#252241=CARTESIAN_POINT('Ctrl Pts',(-1.77268406442479,-2.6914338352571,
12.2638516898458));
#252242=CARTESIAN_POINT('Ctrl Pts',(-1.76402311780433,-2.69711833870525,
12.2644972572148));
#252243=CARTESIAN_POINT('Ctrl Pts',(-1.74602198009665,-2.70880935362435,
12.2658289445407));
#252244=CARTESIAN_POINT('Ctrl Pts',(-1.73667794416686,-2.71480949536175,
12.2665146581029));
#252245=CARTESIAN_POINT('Ctrl Pts',(-1.71197464127018,-2.73049263773251,
12.2683134833816));
#252246=CARTESIAN_POINT('Ctrl Pts',(-1.69656399656217,-2.74009449787688,
12.2694214562857));
#252247=CARTESIAN_POINT('Ctrl Pts',(-1.62386938675995,-2.78453966664293,
12.2745857500193));
#252248=CARTESIAN_POINT('Ctrl Pts',(-1.56558428644953,-2.81772250728463,
12.2785466805345));
#252249=CARTESIAN_POINT('Ctrl Pts',(-1.38327350089099,-2.91411031461053,
12.2905246266551));
#252250=CARTESIAN_POINT('Ctrl Pts',(-1.25615251529448,-2.97112275763455,
12.2983144308984));
#252251=CARTESIAN_POINT('Ctrl Pts',(-0.92090602837082,-3.09610012212812,
12.3183473134052));
#252252=CARTESIAN_POINT('Ctrl Pts',(-0.708861001783567,-3.15141356978549,
12.3305775561813));
#252253=CARTESIAN_POINT('Ctrl Pts',(-0.44883818415889,-3.19165257520775,
12.3461548236979));
#252254=CARTESIAN_POINT('Ctrl Pts',(-0.40468173066267,-3.19755129544435,
12.3488176651532));
#252255=CARTESIAN_POINT('Ctrl Pts',(-0.33782706892861,-3.20507523806276,
12.3528823069357));
#252256=CARTESIAN_POINT('Ctrl Pts',(-0.315209591367845,-3.20737856872806,
12.3542630655217));
#252257=CARTESIAN_POINT('Ctrl Pts',(-0.274514189483198,-3.21108832739476,
12.3567584265936));
#252258=CARTESIAN_POINT('Ctrl Pts',(-0.256445035621723,-3.21258186031607,
12.3578702696548));
#252259=CARTESIAN_POINT('Ctrl Pts',(-0.217810459464257,-3.21544724101161,
12.3602562510899));
#252260=CARTESIAN_POINT('Ctrl Pts',(-0.197242632622954,-3.21677441990757,
12.3615317276216));
#252261=CARTESIAN_POINT('Ctrl Pts',(-0.141088100996727,-3.21985731977652,
12.3650290063479));
#252262=CARTESIAN_POINT('Ctrl Pts',(-0.105483590736053,-3.22122027530737,
12.3672628404062));
#252263=CARTESIAN_POINT('Ctrl Pts',(0.135150039778801,-3.22643811629139,
12.3824762249249));
#252264=CARTESIAN_POINT('Ctrl Pts',(0.340086804586179,-3.21130558336976,
12.3960463404819));
#252265=CARTESIAN_POINT('Ctrl Pts',(0.759497727149738,-3.13972768514377,
12.4247186045829));
#252266=CARTESIAN_POINT('Ctrl Pts',(0.972462498864557,-3.0804311012453,
12.4397823840852));
#252267=CARTESIAN_POINT('Ctrl Pts',(1.20303459997072,-2.98991057316739,
12.4556962333496));
#252268=CARTESIAN_POINT('Ctrl Pts',(1.22822883655403,-2.97964956350198,
12.4574288926517));
#252269=CARTESIAN_POINT('Ctrl Pts',(1.26525465708179,-2.96402038548086,
12.4599628554394));
#252270=CARTESIAN_POINT('Ctrl Pts',(1.27718786066931,-2.9588980000777,12.4607776162736));
#252271=CARTESIAN_POINT('Ctrl Pts',(1.29841747619625,-2.94963272171546,
12.4622232501823));
#252272=CARTESIAN_POINT('Ctrl Pts',(1.30772557412219,-2.94551777566178,
12.4628557271971));
#252273=CARTESIAN_POINT('Ctrl Pts',(1.32821835710458,-2.93634198500777,
12.4642451676979));
#252274=CARTESIAN_POINT('Ctrl Pts',(1.33939373822714,-2.93126127843539,
12.4650009291463));
#252275=CARTESIAN_POINT('Ctrl Pts',(1.37198439257983,-2.9162191639148,12.4672000207704));
#252276=CARTESIAN_POINT('Ctrl Pts',(1.39332001465352,-2.90608582039925,
12.468633411942));
#252277=CARTESIAN_POINT('Ctrl Pts',(1.5683549204797,-2.8205822053027,12.4803564929219));
#252278=CARTESIAN_POINT('Ctrl Pts',(1.71595641474372,-2.73330012597788,
12.4900182227751));
#252279=CARTESIAN_POINT('Ctrl Pts',(2.05768908746965,-2.49257571272217,
12.5134599421667));
#252280=CARTESIAN_POINT('Ctrl Pts',(2.24242730152477,-2.32777255850444,
12.527153345655));
#252281=CARTESIAN_POINT('Ctrl Pts',(2.43254262309196,-2.1143276402088,12.5440962445621));
#252282=CARTESIAN_POINT('Ctrl Pts',(2.45800305580413,-2.0846740194608,12.5464326937897));
#252283=CARTESIAN_POINT('Ctrl Pts',(2.4978504954696,-2.036518881496,12.5502042128577));
#252284=CARTESIAN_POINT('Ctrl Pts',(2.51258632278443,-2.01831022858024,
12.5516252842279));
#252285=CARTESIAN_POINT('Ctrl Pts',(2.53844879580541,-1.98563048282747,
12.5541677630924));
#252286=CARTESIAN_POINT('Ctrl Pts',(2.54965355446168,-1.9712223197959,12.5552860172622));
#252287=CARTESIAN_POINT('Ctrl Pts',(2.57287431879275,-1.94083359389321,
12.5576393676332));
#252288=CARTESIAN_POINT('Ctrl Pts',(2.5848651747574,-1.92483487584867,12.5588753778602));
#252289=CARTESIAN_POINT('Ctrl Pts',(2.61610534813925,-1.88233450886695,
12.5621516481261));
#252290=CARTESIAN_POINT('Ctrl Pts',(2.63510045191288,-1.85564971861654,
12.5642014980096));
#252291=CARTESIAN_POINT('Ctrl Pts',(2.72858158420027,-1.71999483726189,
12.5745894499862));
#252292=CARTESIAN_POINT('Ctrl Pts',(2.79672122269646,-1.60682375380725,
12.5831588671375));
#252293=CARTESIAN_POINT('Ctrl Pts',(2.92073442302465,-1.36894337336954,
12.6009464482311));
#252294=CARTESIAN_POINT('Ctrl Pts',(2.9760093246865,-1.24421071456987,12.6101592313755));
#252295=CARTESIAN_POINT('Ctrl Pts',(3.03916628701579,-1.07317528191686,
12.6224774611929));
#252296=CARTESIAN_POINT('Ctrl Pts',(3.05418626554493,-1.02965200465071,
12.6255850428885));
#252297=CARTESIAN_POINT('Ctrl Pts',(3.1065133206303,-0.866789382905741,
12.6370866928499));
#252298=CARTESIAN_POINT('Ctrl Pts',(3.13780283494966,-0.745619637495051,
12.6453974488158));
#252299=CARTESIAN_POINT('Ctrl Pts',(3.16614987928917,-0.601730212744978,
12.6547666806572));
#252300=CARTESIAN_POINT('Ctrl Pts',(3.1701126605227,-0.58049124414732,12.6561369635489));
#252301=CARTESIAN_POINT('Ctrl Pts',(3.17594126178828,-0.547410537029383,
12.6582499091828));
#252302=CARTESIAN_POINT('Ctrl Pts',(3.1779550301302,-0.535595959267617,
12.6590003198636));
#252303=CARTESIAN_POINT('Ctrl Pts',(3.18156149502111,-0.5137004638538,12.6603828841193));
#252304=CARTESIAN_POINT('Ctrl Pts',(3.18317222925918,-0.503623148651342,
12.6610159787355));
#252305=CARTESIAN_POINT('Ctrl Pts',(3.1867832007952,-0.480322025424383,
12.6624725607338));
#252306=CARTESIAN_POINT('Ctrl Pts',(3.18874902365361,-0.467093240840651,
12.6632941393678));
#252307=CARTESIAN_POINT('Ctrl Pts',(3.19475606490874,-0.424863071571294,
12.6659008450927));
#252308=CARTESIAN_POINT('Ctrl Pts',(3.19848453792757,-0.395817810729946,
12.6676696519372));
#252309=CARTESIAN_POINT('Ctrl Pts',(3.21665618253989,-0.237163961044718,
12.6772200842411));
#252310=CARTESIAN_POINT('Ctrl Pts',(3.22361951518452,-0.106807994125102,
12.6846655259858));
#252311=CARTESIAN_POINT('Ctrl Pts',(3.22097457393141,0.254016113668192,
12.7050046911416));
#252312=CARTESIAN_POINT('Ctrl Pts',(3.19458544268126,0.483551503888421,
12.7176860567073));
#252313=CARTESIAN_POINT('Ctrl Pts',(3.12725151356476,0.782423885700084,
12.7354822964245));
#252314=CARTESIAN_POINT('Ctrl Pts',(3.10793989867352,0.855919069656302,
12.7399600410749));
#252315=CARTESIAN_POINT('Ctrl Pts',(3.07789030556825,0.955777596185538,
12.7462195377369));
#252316=CARTESIAN_POINT('Ctrl Pts',(3.06937299764526,0.982786279327296,
12.7479303971352));
#252317=CARTESIAN_POINT('Ctrl Pts',(3.05512807243269,1.02596497961939,12.7506958691305));
#252318=CARTESIAN_POINT('Ctrl Pts',(3.0496252524777,1.04220798316683,12.7517431404847));
#252319=CARTESIAN_POINT('Ctrl Pts',(3.03793789795327,1.07582100609374,12.7539251830342));
#252320=CARTESIAN_POINT('Ctrl Pts',(3.03173342818392,1.09318338220801,12.7550605760712));
#252321=CARTESIAN_POINT('Ctrl Pts',(3.01674711674301,1.13401152181053,12.7577505294154));
#252322=CARTESIAN_POINT('Ctrl Pts',(3.00784003044211,1.15742973560635,12.7593091784661));
#252323=CARTESIAN_POINT('Ctrl Pts',(2.97697109858458,1.23582579891384,12.7645813691162));
#252324=CARTESIAN_POINT('Ctrl Pts',(2.95376872060867,1.29029916666848,12.7683357026217));
#252325=CARTESIAN_POINT('Ctrl Pts',(2.89367126342721,1.42126434581914,12.7775903954254));
#252326=CARTESIAN_POINT('Ctrl Pts',(2.85522913879484,1.49699378489056,12.7831380543887));
#252327=CARTESIAN_POINT('Ctrl Pts',(2.74551070657163,1.69349824737261,12.7980408025117));
#252328=CARTESIAN_POINT('Ctrl Pts',(2.66926832270308,1.81128897407097,12.807513174005));
#252329=CARTESIAN_POINT('Ctrl Pts',(2.5631115958955,1.95396944977359,12.8195287745353));
#252330=CARTESIAN_POINT('Ctrl Pts',(2.54008825317846,1.98380678795915,12.8220731677239));
#252331=CARTESIAN_POINT('Ctrl Pts',(2.43294956760782,2.11773039346671,12.8336217887591));
#252332=CARTESIAN_POINT('Ctrl Pts',(2.34291559360804,2.21693021938233,12.8425413711901));
#252333=CARTESIAN_POINT('Ctrl Pts',(2.23133919773066,2.32545008280748,12.8524872643093));
#252334=CARTESIAN_POINT('Ctrl Pts',(2.2155590606225,2.34048943839346,12.853870060507));
#252335=CARTESIAN_POINT('Ctrl Pts',(2.19083653107725,2.36357727235018,12.8559981191068));
#252336=CARTESIAN_POINT('Ctrl Pts',(2.18199994746851,2.37173743664087,12.8567512995002));
#252337=CARTESIAN_POINT('Ctrl Pts',(2.16558558665581,2.38672593045997,12.8581363170549));
#252338=CARTESIAN_POINT('Ctrl Pts',(2.15802102212413,2.39356781235491,12.8587691248359));
#252339=CARTESIAN_POINT('Ctrl Pts',(2.14050900894474,2.40925630513186,12.8602216600435));
#252340=CARTESIAN_POINT('Ctrl Pts',(2.13053910306067,2.41807731593574,12.8610395179291));
#252341=CARTESIAN_POINT('Ctrl Pts',(2.0987203477208,2.44587982210592,12.8636220515042));
#252342=CARTESIAN_POINT('Ctrl Pts',(2.07666967631904,2.46462946261879,12.8653708295544));
#252343=CARTESIAN_POINT('Ctrl Pts',(1.95640680614481,2.56412856777508,12.8747089927733));
#252344=CARTESIAN_POINT('Ctrl Pts',(1.85372413750043,2.63931739258312,12.8819783878121));
#252345=CARTESIAN_POINT('Ctrl Pts',(1.56098937823813,2.82813536626981,12.90163027055));
#252346=CARTESIAN_POINT('Ctrl Pts',(1.36328168961745,2.92856598854802,12.9138040341982));
#252347=CARTESIAN_POINT('Ctrl Pts',(1.07648000843115,3.03886866487142,12.9315655452101));
#252348=CARTESIAN_POINT('Ctrl Pts',(0.99491114224724,3.06654234560991,12.9366214159458));
#252349=CARTESIAN_POINT('Ctrl Pts',(0.883911754314504,3.09930572080196,
12.9435592611539));
#252350=CARTESIAN_POINT('Ctrl Pts',(0.855373062985978,3.10730313545883,
12.9453479159326));
#252351=CARTESIAN_POINT('Ctrl Pts',(0.808048001081882,3.11986370637131,
12.9483238931976));
#252352=CARTESIAN_POINT('Ctrl Pts',(0.789323275947957,3.1246535582669,12.9495039063071));
#252353=CARTESIAN_POINT('Ctrl Pts',(0.752571737535052,3.13370330792907,
12.9518253974347));
#252354=CARTESIAN_POINT('Ctrl Pts',(0.734549023204998,3.13797679280485,
12.9529663900513));
#252355=CARTESIAN_POINT('Ctrl Pts',(0.691578066684137,3.14777544537713,
12.9556933160061));
#252356=CARTESIAN_POINT('Ctrl Pts',(0.666599280645446,3.1531596559746,12.9572836536412));
#252357=CARTESIAN_POINT('Ctrl Pts',(0.58046935611948,3.1706559128626,12.9627864206629));
#252358=CARTESIAN_POINT('Ctrl Pts',(0.51903548494956,3.18128981754247,12.9667446629822));
#252359=CARTESIAN_POINT('Ctrl Pts',(0.367029604247455,3.20308125393506,
12.9766250369327));
#252360=CARTESIAN_POINT('Ctrl Pts',(0.276221976231348,3.21218607373902,
12.9826033785493));
#252361=CARTESIAN_POINT('Ctrl Pts',(0.0524266143072708,3.22506504934053,
12.9974921978879));
#252362=CARTESIAN_POINT('Ctrl Pts',(-0.0806429826780814,3.22448237731509,
13.0064828006704));
#252363=CARTESIAN_POINT('Ctrl Pts',(-0.262392435181865,3.21242735997643,
13.0187879061566));
#252364=CARTESIAN_POINT('Ctrl Pts',(-0.311415627205631,3.20804609746697,
13.0221086069927));
#252365=CARTESIAN_POINT('Ctrl Pts',(-0.47895269091911,3.18919641864129,
13.0334317628747));
#252366=CARTESIAN_POINT('Ctrl Pts',(-0.59676503580555,3.16926596555096,
13.0413532599369));
#252367=CARTESIAN_POINT('Ctrl Pts',(-0.734136456740328,3.13809204692987,
13.0503510009613));
#252368=CARTESIAN_POINT('Ctrl Pts',(-0.755015641236812,3.13313412901258,
13.0517118595416));
#252369=CARTESIAN_POINT('Ctrl Pts',(-0.787444994441657,3.12509052616088,
13.0538134158527));
#252370=CARTESIAN_POINT('Ctrl Pts',(-0.799029731764655,3.12214860542844,
13.0545617344599));
#252371=CARTESIAN_POINT('Ctrl Pts',(-0.820385712246099,3.11659864498664,
13.0559364129018));
#252372=CARTESIAN_POINT('Ctrl Pts',(-0.830161110617933,3.11400905021913,
13.056563744027));
#252373=CARTESIAN_POINT('Ctrl Pts',(-0.852826989807537,3.10789032818082,
13.0580140430726));
#252374=CARTESIAN_POINT('Ctrl Pts',(-0.865707880587451,3.10432698769259,
13.058835060059));
#252375=CARTESIAN_POINT('Ctrl Pts',(-0.906689103639183,3.09271511927801,
13.0614381073684));
#252376=CARTESIAN_POINT('Ctrl Pts',(-0.93470311424843,3.08436414225242,
13.0632038817703));
#252377=CARTESIAN_POINT('Ctrl Pts',(-1.08657964048925,3.03683036332583,
13.0727219313425));
#252378=CARTESIAN_POINT('Ctrl Pts',(-1.20811232344508,2.99056274072579,
13.0801405192197));
#252379=CARTESIAN_POINT('Ctrl Pts',(-1.53516340042591,2.84285028010065,
13.1003710269674));
#252380=CARTESIAN_POINT('Ctrl Pts',(-1.73315211754213,2.72666557733372,
13.1129711417625));
#252381=CARTESIAN_POINT('Ctrl Pts',(-1.97948173744517,2.54436258243106,
13.1307583469665));
#252382=CARTESIAN_POINT('Ctrl Pts',(-2.04011481872142,2.49600862429209,
13.1353253715005));
#252383=CARTESIAN_POINT('Ctrl Pts',(-2.12059934712943,2.42693026424612,
13.1416904261008));
#252384=CARTESIAN_POINT('Ctrl Pts',(-2.14200798631051,2.40805602227281,
13.1434143185947));
#252385=CARTESIAN_POINT('Ctrl Pts',(-2.17590532109481,2.37736179648213,
13.1461953519196));
#252386=CARTESIAN_POINT('Ctrl Pts',(-2.18855529557036,2.36572161891581,
13.1472449918131));
#252387=CARTESIAN_POINT('Ctrl Pts',(-2.21455954665957,2.34140610698522,
13.1494276984574));
#252388=CARTESIAN_POINT('Ctrl Pts',(-2.22789951029634,2.328716447612,13.1505613528939));
#252389=CARTESIAN_POINT('Ctrl Pts',(-2.24159867544874,2.3154596447477,13.1517402787114));
#252390=CARTESIAN_POINT('Ctrl Pts',(-2.2420674178426,2.31500576286028,13.1517806358802));
#252391=CARTESIAN_POINT('Ctrl Pts',(-2.25808350758134,2.2994880029553,13.1531601849085));
#252392=CARTESIAN_POINT('Ctrl Pts',(-2.27347850635729,2.28426829591267,
13.1545061103698));
#252393=CARTESIAN_POINT('Ctrl Pts',(-2.32481767671573,2.23248056523255,
13.159062890899));
#252394=CARTESIAN_POINT('Ctrl Pts',(-2.36004069270859,2.19521164223313,
13.1623044486392));
#252395=CARTESIAN_POINT('Ctrl Pts',(-2.44158482961055,2.10469935224396,
13.1700931062916));
#252396=CARTESIAN_POINT('Ctrl Pts',(-2.48707433785513,2.05074521609687,
13.1746708089397));
#252397=CARTESIAN_POINT('Ctrl Pts',(-2.63738370747775,1.8601034402774,13.1906184533807));
#252398=CARTESIAN_POINT('Ctrl Pts',(-2.73299312892165,1.71654216275024,
13.2022626838592));
#252399=CARTESIAN_POINT('Ctrl Pts',(-2.82960754566598,1.54277274100984,
13.2156920595346));
#252400=CARTESIAN_POINT('Ctrl Pts',(-2.8422579722284,1.51934072146388,13.2174893068008));
#252401=CARTESIAN_POINT('Ctrl Pts',(-2.91868461735447,1.37348204504094,
13.2285843055178));
#252402=CARTESIAN_POINT('Ctrl Pts',(-2.97483747244983,1.24720599821555,
13.2377967686764));
#252403=CARTESIAN_POINT('Ctrl Pts',(-3.03030237718131,1.09720678875932,
13.2480167627886));
#252404=CARTESIAN_POINT('Ctrl Pts',(-3.03767383326058,1.07663038086709,
13.249403310659));
#252405=CARTESIAN_POINT('Ctrl Pts',(-3.04878088649798,1.04460406108585,
13.2515358982324));
#252406=CARTESIAN_POINT('Ctrl Pts',(-3.05266244826398,1.03320594566034,
13.2522899072096));
#252407=CARTESIAN_POINT('Ctrl Pts',(-3.05971353362597,1.01211395635714,
13.2536756646648));
#252408=CARTESIAN_POINT('Ctrl Pts',(-3.06290095363996,1.0024267159078,13.2543083925862));
#252409=CARTESIAN_POINT('Ctrl Pts',(-3.07013731548548,0.980077109436237,
13.2557597436963));
#252410=CARTESIAN_POINT('Ctrl Pts',(-3.07415395166695,0.967404657883401,
13.2565765088654));
#252411=CARTESIAN_POINT('Ctrl Pts',(-3.08663656168474,0.927159215834664,
13.2591519718711));
#252412=CARTESIAN_POINT('Ctrl Pts',(-3.09481110469368,0.899496431827873,
13.2608948946132));
#252413=CARTESIAN_POINT('Ctrl Pts',(-3.13674971870449,0.750230236260733,
13.2701717119449));
#252414=CARTESIAN_POINT('Ctrl Pts',(-3.16372351484846,0.626820695123975,
13.2773902213747));
#252415=CARTESIAN_POINT('Ctrl Pts',(-3.20946250911634,0.33684920937127,
13.2939553016046));
#252416=CARTESIAN_POINT('Ctrl Pts',(-3.22262092036357,0.169789514087309,
13.3032126210189));
#252417=CARTESIAN_POINT('Ctrl Pts',(-3.22274905501283,0.00246797769559721,
13.3127140476874));
#252418=CARTESIAN_POINT('Ctrl Pts',(-3.22274905766543,0.002464511434038,
13.3127142445206));
#252419=CARTESIAN_POINT('Ctrl Pts',(-3.2227496858912,0.00164300417895,13.3127608941841));
#252420=CARTESIAN_POINT('Ctrl Pts',(-3.22275000000001,0.000821500300428959,
13.312807548805));
#252421=CARTESIAN_POINT('Ctrl Pts',(-3.22275,-2.24100014615096E-11,13.3128542084224));
#252422=CARTESIAN_POINT('Origin',(0.,0.,-2.31077344927308));
#252423=CARTESIAN_POINT('',(-3.22275,1.96138700782895E-11,14.8083262771147));
#252424=CARTESIAN_POINT('',(-3.22275,-2.92740584967668E-11,14.5620312016861));
#252425=CARTESIAN_POINT('',(-3.22275,-3.50678552687464E-13,-2.31077344927308));
#252426=CARTESIAN_POINT('',(-3.22274971943303,-0.00134476552198701,13.5633807678595));
#252427=CARTESIAN_POINT('Ctrl Pts',(-3.22274999999999,1.96136509811318E-11,
14.8083262771147));
#252428=CARTESIAN_POINT('Ctrl Pts',(-3.22275,0.148140140194331,14.7997354942855));
#252429=CARTESIAN_POINT('Ctrl Pts',(-3.21253566175653,0.296114577246409,
14.7914703204814));
#252430=CARTESIAN_POINT('Ctrl Pts',(-3.16369340120223,0.64816620807127,
14.7715750645874));
#252431=CARTESIAN_POINT('Ctrl Pts',(-3.11547760387864,0.850213307944121,
14.7599397844463));
#252432=CARTESIAN_POINT('Ctrl Pts',(-3.03356085628352,1.08888020164107,
14.7450014001518));
#252433=CARTESIAN_POINT('Ctrl Pts',(-3.01802653476388,1.13122371791246,
14.742305122163));
#252434=CARTESIAN_POINT('Ctrl Pts',(-2.99350871717841,1.19395069523688,
14.7382350415779));
#252435=CARTESIAN_POINT('Ctrl Pts',(-2.98519381711226,1.21459068770951,
14.7368833542097));
#252436=CARTESIAN_POINT('Ctrl Pts',(-2.96987051709815,1.25151949960226,
14.7344417096045));
#252437=CARTESIAN_POINT('Ctrl Pts',(-2.96294010309425,1.26783984476883,
14.7333544071053));
#252438=CARTESIAN_POINT('Ctrl Pts',(-2.94785415913837,1.30256619407087,
14.7310228085355));
#252439=CARTESIAN_POINT('Ctrl Pts',(-2.93966015860541,1.32095456250108,
14.7297772436186));
#252440=CARTESIAN_POINT('Ctrl Pts',(-2.9168698715098,1.37083644777244,14.7263679274287));
#252441=CARTESIAN_POINT('Ctrl Pts',(-2.9019365236218,1.40217212803042,14.724192761338));
#252442=CARTESIAN_POINT('Ctrl Pts',(-2.80393653046073,1.59953834891227,
14.7102740193285));
#252443=CARTESIAN_POINT('Ctrl Pts',(-2.70717279067632,1.75834545936386,
14.6980515599366));
#252444=CARTESIAN_POINT('Ctrl Pts',(-2.48884107283377,2.05556538518971,
14.6732698896435));
#252445=CARTESIAN_POINT('Ctrl Pts',(-2.367993675611,2.19369239913319,14.6607656120188));
#252446=CARTESIAN_POINT('Ctrl Pts',(-2.18409061269887,2.37088056252323,
14.643866678352));
#252447=CARTESIAN_POINT('Ctrl Pts',(-2.13044502111172,2.41920071877906,
14.6391576703012));
#252448=CARTESIAN_POINT('Ctrl Pts',(-2.06064918224078,2.47794372575322,
14.6333487588759));
#252449=CARTESIAN_POINT('Ctrl Pts',(-2.04597160903183,2.49007637950605,
14.6321442058995));
#252450=CARTESIAN_POINT('Ctrl Pts',(-2.02253469429064,2.50910246298826,
14.630248750036));
#252451=CARTESIAN_POINT('Ctrl Pts',(-2.0138459042662,2.51608156504868,14.6295520420253));
#252452=CARTESIAN_POINT('Ctrl Pts',(-1.99720596174648,2.52930585799812,
14.6282294484163));
#252453=CARTESIAN_POINT('Ctrl Pts',(-1.98926145708896,2.53555884064357,
14.6276030465009));
#252454=CARTESIAN_POINT('Ctrl Pts',(-1.97018230734015,2.5504308456802,14.6261104713961));
#252455=CARTESIAN_POINT('Ctrl Pts',(-1.95902021333611,2.55901458442358,
14.6252467345037));
#252456=CARTESIAN_POINT('Ctrl Pts',(-1.9203538141917,2.588348081423,14.6222858165679));
#252457=CARTESIAN_POINT('Ctrl Pts',(-1.89257225145693,2.60873054360133,
14.6202122222528));
#252458=CARTESIAN_POINT('Ctrl Pts',(-1.82290423879382,2.65814490504265,
14.6151295758977));
#252459=CARTESIAN_POINT('Ctrl Pts',(-1.78064504940145,2.68663691807925,
14.6121488348821));
#252460=CARTESIAN_POINT('Ctrl Pts',(-1.58805790567409,2.80994176387,14.5989330656304));
#252461=CARTESIAN_POINT('Ctrl Pts',(-1.43071132507348,2.89322890819596,
14.5891039821416));
#252462=CARTESIAN_POINT('Ctrl Pts',(-1.09530611526263,3.03667774786743,
14.5686300186313));
#252463=CARTESIAN_POINT('Ctrl Pts',(-0.917264354072286,3.09511248946058,
14.5580002777238));
#252464=CARTESIAN_POINT('Ctrl Pts',(-0.701155773222532,3.14574614331847,
14.5447634677183));
#252465=CARTESIAN_POINT('Ctrl Pts',(-0.667012803188848,3.15316222147736,
14.5426635583024));
#252466=CARTESIAN_POINT('Ctrl Pts',(-0.612773564528106,3.16402298812207,
14.5393109683348));
#252467=CARTESIAN_POINT('Ctrl Pts',(-0.592753011810873,3.16783470974708,
14.5380699078766));
#252468=CARTESIAN_POINT('Ctrl Pts',(-0.555276449089201,3.17460218533928,
14.5357395226645));
#252469=CARTESIAN_POINT('Ctrl Pts',(-0.537829551089867,3.17760449464132,
14.5346517142143));
#252470=CARTESIAN_POINT('Ctrl Pts',(-0.498749808025363,3.18399837494501,
14.5322082039764));
#252471=CARTESIAN_POINT('Ctrl Pts',(-0.477105510850074,3.18731349517535,
14.5308501513789));
#252472=CARTESIAN_POINT('Ctrl Pts',(-0.412589642057926,3.19652311168084,
14.5267873741388));
#252473=CARTESIAN_POINT('Ctrl Pts',(-0.369632688953488,3.20177475811275,
14.5240627883828));
#252474=CARTESIAN_POINT('Ctrl Pts',(-0.16631840047032,3.22248468086062,
14.5110703174464));
#252475=CARTESIAN_POINT('Ctrl Pts',(-0.00507571090419254,3.22676787167101,
14.5004656305962));
#252476=CARTESIAN_POINT('Ctrl Pts',(0.321506716508821,3.21096194663564,
14.4785340216004));
#252477=CARTESIAN_POINT('Ctrl Pts',(0.486351303687658,3.19015749285242,
14.4672278495375));
#252478=CARTESIAN_POINT('Ctrl Pts',(0.743467752234609,3.13730808837392,
14.4496996323184));
#252479=CARTESIAN_POINT('Ctrl Pts',(0.837162800326893,3.11361659398127,
14.4433396759822));
#252480=CARTESIAN_POINT('Ctrl Pts',(0.94913337956593,3.07988263206984,14.4358791424483));
#252481=CARTESIAN_POINT('Ctrl Pts',(0.968551475032696,3.07383136956429,
14.434590570981));
#252482=CARTESIAN_POINT('Ctrl Pts',(0.998901842722178,3.06405711191491,
14.432586194843));
#252483=CARTESIAN_POINT('Ctrl Pts',(1.00987323976845,3.06045861362566,14.4318636208296));
#252484=CARTESIAN_POINT('Ctrl Pts',(1.02936085497042,3.05395068303854,14.4305840159081));
#252485=CARTESIAN_POINT('Ctrl Pts',(1.03788429021441,3.05106452683078,14.4300256882927));
#252486=CARTESIAN_POINT('Ctrl Pts',(1.05843028634901,3.04401129873306,14.4286829474812));
#252487=CARTESIAN_POINT('Ctrl Pts',(1.070440388535,3.03980868560207,14.4279006129375));
#252488=CARTESIAN_POINT('Ctrl Pts',(1.107580020436,3.0265652587633,14.4254883839327));
#252489=CARTESIAN_POINT('Ctrl Pts',(1.13262297856476,3.01728289355477,14.4238718584384));
#252490=CARTESIAN_POINT('Ctrl Pts',(1.36291499676283,2.92865201843427,14.4090742981013));
#252491=CARTESIAN_POINT('Ctrl Pts',(1.55967504224381,2.82877711929414,14.3969045269014));
#252492=CARTESIAN_POINT('Ctrl Pts',(1.90481381243417,2.60653985197629,14.3739101128091));
#252493=CARTESIAN_POINT('Ctrl Pts',(2.05542279027351,2.48949635406364,14.3631685976186));
#252494=CARTESIAN_POINT('Ctrl Pts',(2.22799367889522,2.32899438751498,14.3492186054157));
#252495=CARTESIAN_POINT('Ctrl Pts',(2.26051711321325,2.29744048220432,14.3465099699215));
#252496=CARTESIAN_POINT('Ctrl Pts',(2.30803227647258,2.24935580183815,14.3424248804728));
#252497=CARTESIAN_POINT('Ctrl Pts',(2.32353592335006,2.23333725333107,14.3410707891188));
#252498=CARTESIAN_POINT('Ctrl Pts',(2.35107266358738,2.20428886605547,14.3386265346934));
#252499=CARTESIAN_POINT('Ctrl Pts',(2.3631668379991,2.19131799393622,14.3375390506334));
#252500=CARTESIAN_POINT('Ctrl Pts',(2.38874186333595,2.16343108777896,14.3352089544445));
#252501=CARTESIAN_POINT('Ctrl Pts',(2.40219137197464,2.14848745505957,14.33396509077));
#252502=CARTESIAN_POINT('Ctrl Pts',(2.43839574760883,2.10749613639129,14.3305653340168));
#252503=CARTESIAN_POINT('Ctrl Pts',(2.46087201404647,2.08120699807592,14.328398133837));
#252504=CARTESIAN_POINT('Ctrl Pts',(2.5985491691138,1.91482536472876,14.3147586780835));
#252505=CARTESIAN_POINT('Ctrl Pts',(2.70215743046299,1.76559924611675,14.3028307606079));
#252506=CARTESIAN_POINT('Ctrl Pts',(2.88035914128407,1.45620309563204,14.2788572825919));
#252507=CARTESIAN_POINT('Ctrl Pts',(2.95546096074407,1.29701466453965,14.2668704679057));
#252508=CARTESIAN_POINT('Ctrl Pts',(3.04629389790864,1.05501665610646,14.2496915789419));
#252509=CARTESIAN_POINT('Ctrl Pts',(3.07238339562138,0.9764370435369,14.2442694857146));
#252510=CARTESIAN_POINT('Ctrl Pts',(3.10092882768087,0.877923517333849,
14.2377323375367));
#252511=CARTESIAN_POINT('Ctrl Pts',(3.10626219682884,0.85886233262069,14.2364793897809));
#252512=CARTESIAN_POINT('Ctrl Pts',(3.11436632712284,0.828835216562373,
14.2345255904426));
#252513=CARTESIAN_POINT('Ctrl Pts',(3.11725545327477,0.817902123637985,
14.2338183360548));
#252514=CARTESIAN_POINT('Ctrl Pts',(3.12260542073369,0.797216474897416,
14.2324883001637));
#252515=CARTESIAN_POINT('Ctrl Pts',(3.12507815491088,0.787467618004659,
14.2318648979844));
#252516=CARTESIAN_POINT('Ctrl Pts',(3.13081966461822,0.764378456350037,
14.2303962854714));
#252517=CARTESIAN_POINT('Ctrl Pts',(3.1340488571539,0.7510286103166,14.2295533106254));
#252518=CARTESIAN_POINT('Ctrl Pts',(3.14459650288914,0.706170443545754,
14.2267401257486));
#252519=CARTESIAN_POINT('Ctrl Pts',(3.15152617013043,0.674571596866852,
14.224790456632));
#252520=CARTESIAN_POINT('Ctrl Pts',(3.16731102124927,0.597031749129717,
14.2200723398118));
#252521=CARTESIAN_POINT('Ctrl Pts',(3.17564407235114,0.550991069651247,
14.217327216804));
#252522=CARTESIAN_POINT('Ctrl Pts',(3.20650750855755,0.356377890194215,
14.2058993117215));
#252523=CARTESIAN_POINT('Ctrl Pts',(3.21963660859419,0.206498451853521,
14.1975202337013));
#252524=CARTESIAN_POINT('Ctrl Pts',(3.22584158959593,-0.149003278958,14.1776168000608));
#252525=CARTESIAN_POINT('Ctrl Pts',(3.20980662768336,-0.354098121355896,
14.1660861844325));
#252526=CARTESIAN_POINT('Ctrl Pts',(3.16658984502299,-0.600718857115544,
14.1512638561868));
#252527=CARTESIAN_POINT('Ctrl Pts',(3.15786730819869,-0.645002447521561,
14.1485657463951));
#252528=CARTESIAN_POINT('Ctrl Pts',(3.14345893058849,-0.710829742323324,
14.1444934406876));
#252529=CARTESIAN_POINT('Ctrl Pts',(3.13847475741943,-0.732522443202241,
14.1431413965845));
#252530=CARTESIAN_POINT('Ctrl Pts',(3.12911702190624,-0.771400433149129,
14.1406993650608));
#252531=CARTESIAN_POINT('Ctrl Pts',(3.12482553080471,-0.788604683836959,
14.13961203598));
#252532=CARTESIAN_POINT('Ctrl Pts',(3.11535998098308,-0.825260481470628,
14.1372806621072));
#252533=CARTESIAN_POINT('Ctrl Pts',(3.1101452465862,-0.844700650728657,
14.1360353510475));
#252534=CARTESIAN_POINT('Ctrl Pts',(3.09544705619467,-0.897512477042214,
14.1326274617118));
#252535=CARTESIAN_POINT('Ctrl Pts',(3.08560649843472,-0.930781129536284,
14.1304534847241));
#252536=CARTESIAN_POINT('Ctrl Pts',(3.01990378884756,-1.1404029652338,14.116577911595));
#252537=CARTESIAN_POINT('Ctrl Pts',(2.94949004587681,-1.31180286543515,
14.1044010676474));
#252538=CARTESIAN_POINT('Ctrl Pts',(2.78137757448909,-1.63805047283622,
14.0797418660787));
#252539=CARTESIAN_POINT('Ctrl Pts',(2.68440889589213,-1.79254587073826,
14.0673149180768));
#252540=CARTESIAN_POINT('Ctrl Pts',(2.53056148215358,-1.99695148677586,
14.0503739117438));
#252541=CARTESIAN_POINT('Ctrl Pts',(2.48419784821713,-2.05434161307253,
14.0455589032327));
#252542=CARTESIAN_POINT('Ctrl Pts',(2.42335188153119,-2.12458246095315,
14.0396405341435));
#252543=CARTESIAN_POINT('Ctrl Pts',(2.41067227151651,-2.13895867554608,
14.0384278555955));
#252544=CARTESIAN_POINT('Ctrl Pts',(2.39040046484082,-2.16153371305155,
14.0365225955276));
#252545=CARTESIAN_POINT('Ctrl Pts',(2.38289282614953,-2.16980740224573,
14.0358241101477));
#252546=CARTESIAN_POINT('Ctrl Pts',(2.36851605719503,-2.18548650546368,
14.0345003222121));
#252547=CARTESIAN_POINT('Ctrl Pts',(2.36165499594903,-2.19289882597374,
14.033874483219));
#252548=CARTESIAN_POINT('Ctrl Pts',(2.34518806509989,-2.21052188998329,
14.0323862155953));
#252549=CARTESIAN_POINT('Ctrl Pts',(2.33555008843706,-2.22070256625548,
14.0315261848932));
#252550=CARTESIAN_POINT('Ctrl Pts',(2.30226245470397,-2.25540814277195,
14.0285920720486));
#252551=CARTESIAN_POINT('Ctrl Pts',(2.2782896485405,-2.27962163206156,14.0265410075842));
#252552=CARTESIAN_POINT('Ctrl Pts',(2.21806552820342,-2.33855117074672,
14.0215252406461));
#252553=CARTESIAN_POINT('Ctrl Pts',(2.18137791784707,-2.3728099685099,14.0185878940764));
#252554=CARTESIAN_POINT('Ctrl Pts',(2.01528212106606,-2.52079991441807,
14.0057233377888));
#252555=CARTESIAN_POINT('Ctrl Pts',(1.87767146566831,-2.62490981129512,
13.9961809964709));
#252556=CARTESIAN_POINT('Ctrl Pts',(1.56873640097201,-2.8218523300357,13.9756346998822));
#252557=CARTESIAN_POINT('Ctrl Pts',(1.39601377651298,-2.91117109621544,
13.964628246277));
#252558=CARTESIAN_POINT('Ctrl Pts',(1.18409918400143,-2.99753851965681,
13.950979627456));
#252559=CARTESIAN_POINT('Ctrl Pts',(1.15167061114463,-3.01014662725304,
13.9488882853055));
#252560=CARTESIAN_POINT('Ctrl Pts',(1.09996379568074,-3.02929219925,13.9455463167466));
#252561=CARTESIAN_POINT('Ctrl Pts',(1.08081627325872,-3.03617649921441,
13.9443071840704));
#252562=CARTESIAN_POINT('Ctrl Pts',(1.0448870835615,-3.04871154086945,13.9419785158581));
#252563=CARTESIAN_POINT('Ctrl Pts',(1.02812147535925,-3.05440620891101,
13.9408904758525));
#252564=CARTESIAN_POINT('Ctrl Pts',(0.990477446063168,-3.06684746828097,
13.9384439401889));
#252565=CARTESIAN_POINT('Ctrl Pts',(0.969575495562537,-3.07351952741286,
13.9370830673289));
#252566=CARTESIAN_POINT('Ctrl Pts',(0.907034853582364,-3.09278152484734,
13.9330032110686));
#252567=CARTESIAN_POINT('Ctrl Pts',(0.865209000106622,-3.10474199859709,
13.9302641161829));
#252568=CARTESIAN_POINT('Ctrl Pts',(0.665662568000436,-3.15745879727107,
13.9171407610229));
#252569=CARTESIAN_POINT('Ctrl Pts',(0.505263576687523,-3.18705951855238,
13.9064117530493));
#252570=CARTESIAN_POINT('Ctrl Pts',(0.174391316319274,-3.2225106101127,
13.8840818863798));
#252571=CARTESIAN_POINT('Ctrl Pts',(0.00428405712409704,-3.22722298857725,
13.8724981151371));
#252572=CARTESIAN_POINT('Ctrl Pts',(-0.256217350877482,-3.213835660241,
13.8551114467391));
#252573=CARTESIAN_POINT('Ctrl Pts',(-0.34680433199176,-3.20532631008748,
13.8491355133135));
#252574=CARTESIAN_POINT('Ctrl Pts',(-0.456787553832832,-3.19027661865676,
13.8420559743072));
#252575=CARTESIAN_POINT('Ctrl Pts',(-0.476632347246486,-3.18737218179777,
13.8407856711441));
#252576=CARTESIAN_POINT('Ctrl Pts',(-0.507794408818161,-3.18251382414491,
13.8388034488152));
#252577=CARTESIAN_POINT('Ctrl Pts',(-0.519130187009412,-3.1806844013405,
13.8380849923677));
#252578=CARTESIAN_POINT('Ctrl Pts',(-0.539343246600434,-3.17731137988055,
13.8368088596243));
#252579=CARTESIAN_POINT('Ctrl Pts',(-0.548223884968563,-3.17579113240856,
13.8362499293904));
#252580=CARTESIAN_POINT('Ctrl Pts',(-0.569724312181716,-3.17201766949623,
13.8349008221916));
#252581=CARTESIAN_POINT('Ctrl Pts',(-0.582337175821552,-3.16972637841278,
13.8341127803183));
#252582=CARTESIAN_POINT('Ctrl Pts',(-0.621676285563726,-3.16233717583866,
13.831664553716));
#252583=CARTESIAN_POINT('Ctrl Pts',(-0.648352611273866,-3.15697589773968,
13.8300183177228));
#252584=CARTESIAN_POINT('Ctrl Pts',(-0.785956442394575,-3.12750311188815,
13.8215839228754));
#252585=CARTESIAN_POINT('Ctrl Pts',(-0.895631769467868,-3.09787862839589,
13.8150535391911));
#252586=CARTESIAN_POINT('Ctrl Pts',(-1.18873223666557,-3.00183582955961,
13.7975827537467));
#252587=CARTESIAN_POINT('Ctrl Pts',(-1.36805206936515,-2.92447226222963,
13.7868515234532));
#252588=CARTESIAN_POINT('Ctrl Pts',(-1.64703229867231,-2.77280413373081,
13.7687620686333));
#252589=CARTESIAN_POINT('Ctrl Pts',(-1.75133735728306,-2.70813052545463,
13.7616498210041));
#252590=CARTESIAN_POINT('Ctrl Pts',(-1.8784938655598,-2.61886431594096,
13.7523642688644));
#252591=CARTESIAN_POINT('Ctrl Pts',(-1.90500156491888,-2.59964582746207,
13.7503929506691));
#252592=CARTESIAN_POINT('Ctrl Pts',(-1.94698862946235,-2.5682175218419,
13.7472103146443));
#252593=CARTESIAN_POINT('Ctrl Pts',(-1.96265716147386,-2.5562634454516,
13.7460088792095));
#252594=CARTESIAN_POINT('Ctrl Pts',(-1.99159649625403,-2.5337616878497,
13.7437635842171));
#252595=CARTESIAN_POINT('Ctrl Pts',(-2.00489568420024,-2.52325150805083,
13.7427212246087));
#252596=CARTESIAN_POINT('Ctrl Pts',(-2.01869561671053,-2.51216761613525,
13.741628404508));
#252597=CARTESIAN_POINT('Ctrl Pts',(-2.01927992691387,-2.51169797174067,
13.7415821117042));
#252598=CARTESIAN_POINT('Ctrl Pts',(-2.02042215540262,-2.51077923948155,
13.7414915756762));
#252599=CARTESIAN_POINT('Ctrl Pts',(-2.02098008798839,-2.51033016940132,
13.7414473331644));
#252600=CARTESIAN_POINT('Ctrl Pts',(-2.0220736471648,-2.50944938207923,
13.7413605790553));
#252601=CARTESIAN_POINT('Ctrl Pts',(-2.0226092853375,-2.5090176792206,13.7413180680343));
#252602=CARTESIAN_POINT('Ctrl Pts',(-2.02366175885197,-2.50816887177791,
13.7412345032012));
#252603=CARTESIAN_POINT('Ctrl Pts',(-2.02417860359046,-2.50775177885711,
13.7411934498571));
#252604=CARTESIAN_POINT('Ctrl Pts',(-2.02519653059653,-2.50692979358846,
13.7411125623886));
#252605=CARTESIAN_POINT('Ctrl Pts',(-2.02569762048562,-2.50652491068404,
13.7410727286432));
#252606=CARTESIAN_POINT('Ctrl Pts',(-2.02668670875336,-2.50572523255615,
13.7409940708887));
#252607=CARTESIAN_POINT('Ctrl Pts',(-2.02717471327031,-2.50533044494786,
13.7409552471857));
#252608=CARTESIAN_POINT('Ctrl Pts',(-2.0446127367826,-2.49121494060882,
13.7395674145988));
#252609=CARTESIAN_POINT('Ctrl Pts',(-2.06142282798318,-2.47732295245378,
13.7382115599284));
#252610=CARTESIAN_POINT('Ctrl Pts',(-2.09802724692377,-2.44644223501679,
13.7352187753613));
#252611=CARTESIAN_POINT('Ctrl Pts',(-2.11775876191193,-2.42938175280243,
13.7335789896997));
#252612=CARTESIAN_POINT('Ctrl Pts',(-2.17065512987335,-2.38251175250846,
13.7291096661124));
#252613=CARTESIAN_POINT('Ctrl Pts',(-2.20341096700817,-2.35225120797216,
13.7262619901629));
#252614=CARTESIAN_POINT('Ctrl Pts',(-2.30665749346402,-2.25282061419605,
13.717022720101));
#252615=CARTESIAN_POINT('Ctrl Pts',(-2.37459594228146,-2.18109164809226,
13.7105312047655));
#252616=CARTESIAN_POINT('Ctrl Pts',(-2.5753784215234,-1.94858912772462,
13.6900612606086));
#252617=CARTESIAN_POINT('Ctrl Pts',(-2.6959904761406,-1.77797747682808,
13.6757932781427));
#252618=CARTESIAN_POINT('Ctrl Pts',(-2.84133960572528,-1.52319124252239,
13.6562827180402));
#252619=CARTESIAN_POINT('Ctrl Pts',(-2.88047395406218,-1.44782410792709,
13.6507170529368));
#252620=CARTESIAN_POINT('Ctrl Pts',(-2.92497995215966,-1.35314405807114,
13.644047728717));
#252621=CARTESIAN_POINT('Ctrl Pts',(-2.9332065790361,-1.3352174998084,13.6427988657966));
#252622=CARTESIAN_POINT('Ctrl Pts',(-2.94593054544261,-1.30680560802012,
13.6408426699356));
#252623=CARTESIAN_POINT('Ctrl Pts',(-2.95053752818565,-1.29637030967679,
13.6401290678809));
#252624=CARTESIAN_POINT('Ctrl Pts',(-2.9590920851437,-1.27671149496586,
13.6387941865063));
#252625=CARTESIAN_POINT('Ctrl Pts',(-2.963051998443,-1.26749401054196,13.6381722168549));
#252626=CARTESIAN_POINT('Ctrl Pts',(-2.97225834141134,-1.24578547568564,
13.6367163628319));
#252627=CARTESIAN_POINT('Ctrl Pts',(-2.97746913274882,-1.23327964310522,
13.6358845984754));
#252628=CARTESIAN_POINT('Ctrl Pts',(-2.99443773575078,-1.19182075076126,
13.6331488140221));
#252629=CARTESIAN_POINT('Ctrl Pts',(-3.00585369432996,-1.16272859511286,
13.6312638267463));
#252630=CARTESIAN_POINT('Ctrl Pts',(-3.03255259729587,-1.0916670003113,
13.6267327926392));
#252631=CARTESIAN_POINT('Ctrl Pts',(-3.04739005716418,-1.04953623337256,
13.6241077184834));
#252632=CARTESIAN_POINT('Ctrl Pts',(-3.10446385881446,-0.876046783213798,
13.613495341954));
#252633=CARTESIAN_POINT('Ctrl Pts',(-3.13912199289558,-0.742342228008782,
13.6057694407136));
#252634=CARTESIAN_POINT('Ctrl Pts',(-3.20336795107731,-0.407242692695266,
13.5866687710079));
#252635=CARTESIAN_POINT('Ctrl Pts',(-3.22266494010861,-0.204519623547666,
13.5753149239524));
#252636=CARTESIAN_POINT('Ctrl Pts',(-3.22274971943303,-0.00134476552198701,
13.5633807678595));
#252637=CARTESIAN_POINT('Ctrl Pts',(-3.2227497208408,-0.00134138754393476,
13.5633805694426));
#252638=CARTESIAN_POINT('Ctrl Pts',(-3.22274990694714,-0.000894257881103293,
13.563354305771));
#252639=CARTESIAN_POINT('Ctrl Pts',(-3.22275,-0.000447128689908073,13.5633280396337));
#252640=CARTESIAN_POINT('Ctrl Pts',(-3.22275,7.83873563209288E-13,13.5633017710267));
#252641=CARTESIAN_POINT('Ctrl Pts',(-3.22275,-2.24100014615096E-11,13.3128542084224));
#252642=CARTESIAN_POINT('Ctrl Pts',(-3.22274999999937,-0.0899329648665014,
13.3179622255554));
#252643=CARTESIAN_POINT('Ctrl Pts',(-3.21898558460739,-0.179823228001732,
13.3231316752801));
#252644=CARTESIAN_POINT('Ctrl Pts',(-3.207149078492,-0.320905013689379,
13.3314326182287));
#252645=CARTESIAN_POINT('Ctrl Pts',(-3.20159446116282,-0.372260286167885,
13.3344933286003));
#252646=CARTESIAN_POINT('Ctrl Pts',(-3.19194700081472,-0.445046231040555,
13.3388977292782));
#252647=CARTESIAN_POINT('Ctrl Pts',(-3.18886687955547,-0.466604536510036,
13.3402105684859));
#252648=CARTESIAN_POINT('Ctrl Pts',(-3.18293878851294,-0.505291682551132,
13.3425822717539));
#252649=CARTESIAN_POINT('Ctrl Pts',(-3.18017040715958,-0.522431985199073,
13.3436386364612));
#252650=CARTESIAN_POINT('Ctrl Pts',(-3.17423421164326,-0.557388707507025,
13.3458048548984));
#252651=CARTESIAN_POINT('Ctrl Pts',(-3.17105457333871,-0.575202463141507,
13.3469150437404));
#252652=CARTESIAN_POINT('Ctrl Pts',(-3.16386704210488,-0.613598037790565,
13.3493219526887));
#252653=CARTESIAN_POINT('Ctrl Pts',(-3.15980797773742,-0.634169317271281,
13.3506202430632));
#252654=CARTESIAN_POINT('Ctrl Pts',(-3.14817046930335,-0.69026030657834,
13.3541848074946));
#252655=CARTESIAN_POINT('Ctrl Pts',(-3.14019204928681,-0.725692990679699,
13.3564636014382));
#252656=CARTESIAN_POINT('Ctrl Pts',(-3.09966039951675,-0.892490060864858,
13.3673230058039));
#252657=CARTESIAN_POINT('Ctrl Pts',(-3.05945612483903,-1.0218382299263,
13.3761423260181));
#252658=CARTESIAN_POINT('Ctrl Pts',(-2.91586407907642,-1.3983989610192,
13.4029436732885));
#252659=CARTESIAN_POINT('Ctrl Pts',(-2.78969372900423,-1.63566064835666,
13.4214266917264));
#252660=CARTESIAN_POINT('Ctrl Pts',(-2.61161325015087,-1.88873973878736,
13.4415466202323));
#252661=CARTESIAN_POINT('Ctrl Pts',(-2.58691808649203,-1.92242470805476,
13.4442312792123));
#252662=CARTESIAN_POINT('Ctrl Pts',(-2.55224868566321,-1.96783646783211,
13.4478494861375));
#252663=CARTESIAN_POINT('Ctrl Pts',(-2.54283604782479,-1.97998448815521,
13.4488172750452));
#252664=CARTESIAN_POINT('Ctrl Pts',(-2.52684023747063,-2.0003265818774,
13.4504370113076));
#252665=CARTESIAN_POINT('Ctrl Pts',(-2.52030328791533,-2.00855653846788,
13.4510920812447));
#252666=CARTESIAN_POINT('Ctrl Pts',(-2.50680790624113,-2.02537747043851,
13.4524302246069));
#252667=CARTESIAN_POINT('Ctrl Pts',(-2.49984536031816,-2.03396483734155,
13.4531130006493));
#252668=CARTESIAN_POINT('Ctrl Pts',(-2.48147363890198,-2.05638705049397,
13.4548953143164));
#252669=CARTESIAN_POINT('Ctrl Pts',(-2.46999276728986,-2.07016300928138,
13.4559898824912));
#252670=CARTESIAN_POINT('Ctrl Pts',(-2.42068553041011,-2.1283328361924,
13.4606132857697));
#252671=CARTESIAN_POINT('Ctrl Pts',(-2.38177050360163,-2.17179402347281,
13.4640714943244));
#252672=CARTESIAN_POINT('Ctrl Pts',(-2.16496811612824,-2.40108230138489,
13.4824895727432));
#252673=CARTESIAN_POINT('Ctrl Pts',(-1.96648888556209,-2.56616990062601,
13.4964584098184));
#252674=CARTESIAN_POINT('Ctrl Pts',(-1.67729244903322,-2.75325349678787,
13.5160359146764));
#252675=CARTESIAN_POINT('Ctrl Pts',(-1.60222253511323,-2.79760544157164,
13.5210490350353));
#252676=CARTESIAN_POINT('Ctrl Pts',(-1.47230273643974,-2.86741740154549,
13.529696183272));
#252677=CARTESIAN_POINT('Ctrl Pts',(-1.41836580872615,-2.89447674918599,
13.5332777847565));
#252678=CARTESIAN_POINT('Ctrl Pts',(-1.34083741890371,-2.93068413197448,
13.538431072146));
#252679=CARTESIAN_POINT('Ctrl Pts',(-1.3178471029279,-2.94109391615876,
13.5399598069635));
#252680=CARTESIAN_POINT('Ctrl Pts',(-1.27782517742385,-2.9586519652023,
13.5426231746355));
#252681=CARTESIAN_POINT('Ctrl Pts',(-1.26084978676305,-2.96592589730945,
13.5437534978821));
#252682=CARTESIAN_POINT('Ctrl Pts',(-1.22803297368019,-2.97965521055178,
13.5459402937505));
#252683=CARTESIAN_POINT('Ctrl Pts',(-1.21220079795623,-2.98613117022875,
13.5469960281558));
#252684=CARTESIAN_POINT('Ctrl Pts',(-1.17024692691346,-3.00290326624806,
13.5497959360242));
#252685=CARTESIAN_POINT('Ctrl Pts',(-1.14404138918197,-3.01298442027949,
13.5515471890428));
#252686=CARTESIAN_POINT('Ctrl Pts',(-1.04802570399631,-3.04848802390875,
13.5579739099326));
#252687=CARTESIAN_POINT('Ctrl Pts',(-0.977478103508532,-3.07183532091763,
13.5627161836479));
#252688=CARTESIAN_POINT('Ctrl Pts',(-0.683552096844328,-3.15795786010056,
13.5825642108918));
#252689=CARTESIAN_POINT('Ctrl Pts',(-0.454542326915349,-3.19895389068393,
13.5983048224551));
#252690=CARTESIAN_POINT('Ctrl Pts',(-0.0925098144984718,-3.22408287626044,
13.622770100066));
#252691=CARTESIAN_POINT('Ctrl Pts',(0.0385812291964583,-3.22518003382034,
13.6315272571589));
#252692=CARTESIAN_POINT('Ctrl Pts',(0.198682864991038,-3.21675354740473,
13.6418479676219));
#252693=CARTESIAN_POINT('Ctrl Pts',(0.227958834799953,-3.21481153008997,
13.6437195828405));
#252694=CARTESIAN_POINT('Ctrl Pts',(0.270546634060667,-3.21140175190029,
13.646415590169));
#252695=CARTESIAN_POINT('Ctrl Pts',(0.283881409146017,-3.2102504658608,
13.6472559326816));
#252696=CARTESIAN_POINT('Ctrl Pts',(0.307371579817887,-3.20807488074887,
13.6487290795585));
#252697=CARTESIAN_POINT('Ctrl Pts',(0.317529785492987,-3.20708537052336,
13.6493637428067));
#252698=CARTESIAN_POINT('Ctrl Pts',(0.339599080367137,-3.20482971312209,
13.6507373080323));
#252699=CARTESIAN_POINT('Ctrl Pts',(0.351507947050802,-3.20354541083504,
13.6514752098383));
#252700=CARTESIAN_POINT('Ctrl Pts',(0.384844669861352,-3.19976210405955,
13.6535322986173));
#252701=CARTESIAN_POINT('Ctrl Pts',(0.406255429687084,-3.19711424957678,
13.6548435908077));
#252702=CARTESIAN_POINT('Ctrl Pts',(0.550314258521002,-3.17782800367955,
13.6636093933054));
#252703=CARTESIAN_POINT('Ctrl Pts',(0.671955985320854,-3.15434913428427,
13.6707340651659));
#252704=CARTESIAN_POINT('Ctrl Pts',(0.837618305168215,-3.11235153628912,
13.6804120381007));
#252705=CARTESIAN_POINT('Ctrl Pts',(0.883020986371203,-3.09977589227275,
13.6830615435408));
#252706=CARTESIAN_POINT('Ctrl Pts',(1.05815036124308,-3.04710829521904,
13.6933209861705));
#252707=CARTESIAN_POINT('Ctrl Pts',(1.18556651522669,-2.99983036803342,
13.700876747816));
#252708=CARTESIAN_POINT('Ctrl Pts',(1.39009306170021,-2.90886851641838,
13.7135944144543));
#252709=CARTESIAN_POINT('Ctrl Pts',(1.46906238839584,-2.86979596995303,
13.7186577812724));
#252710=CARTESIAN_POINT('Ctrl Pts',(1.59966322387328,-2.79837281829352,
13.7273827325615));
#252711=CARTESIAN_POINT('Ctrl Pts',(1.65215886781773,-2.76770360358913,
13.7309905676729));
#252712=CARTESIAN_POINT('Ctrl Pts',(1.72523667329897,-2.72218965789974,
13.7361750863304));
#252713=CARTESIAN_POINT('Ctrl Pts',(1.74656096607412,-2.7085573371852,13.7377080869675));
#252714=CARTESIAN_POINT('Ctrl Pts',(1.78317427761115,-2.68453880281972,
13.7403764617772));
#252715=CARTESIAN_POINT('Ctrl Pts',(1.79853878587422,-2.67426948935603,
13.7415074804176));
#252716=CARTESIAN_POINT('Ctrl Pts',(1.8298530804593,-2.65294775503036,13.7438362397307));
#252717=CARTESIAN_POINT('Ctrl Pts',(1.84579303896979,-2.64188230590005,
13.7450344392933));
#252718=CARTESIAN_POINT('Ctrl Pts',(1.88612091926002,-2.61334373670873,
13.7480991436312));
#252719=CARTESIAN_POINT('Ctrl Pts',(1.91036614016374,-2.59567307686122,
13.7499731058671));
#252720=CARTESIAN_POINT('Ctrl Pts',(2.00590438297721,-2.52397824398705,
13.7574860699488));
#252721=CARTESIAN_POINT('Ctrl Pts',(2.07517594631369,-2.4673388316857,13.7632251699227));
#252722=CARTESIAN_POINT('Ctrl Pts',(2.30509618093428,-2.26280817786928,
13.7833120122935));
#252723=CARTESIAN_POINT('Ctrl Pts',(2.45301800569522,-2.101535750111,13.7981452494028));
#252724=CARTESIAN_POINT('Ctrl Pts',(2.65887379114078,-1.82548895909439,
13.8213430445429));
#252725=CARTESIAN_POINT('Ctrl Pts',(2.72826843502348,-1.72005144740038,
13.8297622198412));
#252726=CARTESIAN_POINT('Ctrl Pts',(2.80572110424314,-1.58583667587258,
13.8397330250678));
#252727=CARTESIAN_POINT('Ctrl Pts',(2.8197971124363,-1.56067077057854,13.8415717543002));
#252728=CARTESIAN_POINT('Ctrl Pts',(2.83986608147024,-1.52363212915626,
13.8442295400417));
#252729=CARTESIAN_POINT('Ctrl Pts',(2.84612591274203,-1.51190658736587,
13.8450639399335));
#252730=CARTESIAN_POINT('Ctrl Pts',(2.85706016199703,-1.49111662597587,
13.8465306094882));
#252731=CARTESIAN_POINT('Ctrl Pts',(2.86176432373188,-1.48206832722486,
13.84716467904));
#252732=CARTESIAN_POINT('Ctrl Pts',(2.87192957501705,-1.46228693732336,
13.8485415475877));
#252733=CARTESIAN_POINT('Ctrl Pts',(2.87737352218324,-1.45154545073523,
13.8492833022315));
#252734=CARTESIAN_POINT('Ctrl Pts',(2.89253085031161,-1.42121806255129,
13.8513617087933));
#252735=CARTESIAN_POINT('Ctrl Pts',(2.90210552945349,-1.40156307597027,
13.8526902040262));
#252736=CARTESIAN_POINT('Ctrl Pts',(2.97092565188509,-1.25655894125373,
13.8623669302209));
#252737=CARTESIAN_POINT('Ctrl Pts',(3.02223423380832,-1.12758537439685,
13.8702998978876));
#252738=CARTESIAN_POINT('Ctrl Pts',(3.07526219935315,-0.964347587803793,
13.8799812130817));
#252739=CARTESIAN_POINT('Ctrl Pts',(3.08496379565228,-0.932846334111955,
13.8818332620063));
#252740=CARTESIAN_POINT('Ctrl Pts',(3.13400589721659,-0.764465446248853,
13.8916705845994));
#252741=CARTESIAN_POINT('Ctrl Pts',(3.16472314045262,-0.6252412025472,13.8995948245035));
#252742=CARTESIAN_POINT('Ctrl Pts',(3.1986777825188,-0.401926502558706,
13.9124568517353));
#252743=CARTESIAN_POINT('Ctrl Pts',(3.20801350066146,-0.318955293056436,
13.9172663476996));
#252744=CARTESIAN_POINT('Ctrl Pts',(3.2183949468099,-0.177400366619265,
13.9255970795024));
#252745=CARTESIAN_POINT('Ctrl Pts',(3.22108371457834,-0.1189789984745,13.929071065933));
#252746=CARTESIAN_POINT('Ctrl Pts',(3.22264998953787,-0.0355871182076339,
13.9340960470871));
#252747=CARTESIAN_POINT('Ctrl Pts',(3.22282886677761,-0.0106508416402976,
13.935607026977));
#252748=CARTESIAN_POINT('Ctrl Pts',(3.22263670586035,0.0327025410947999,
13.9382496266437));
#252749=CARTESIAN_POINT('Ctrl Pts',(3.22239718123915,0.0511192578369016,
13.9393771269992));
#252750=CARTESIAN_POINT('Ctrl Pts',(3.22162914835204,0.0867083373539033,
13.941565845018));
#252751=CARTESIAN_POINT('Ctrl Pts',(3.22112115861991,0.103880550126878,
13.9426263876769));
#252752=CARTESIAN_POINT('Ctrl Pts',(3.21940612627436,0.149509041303053,
13.9454565912277));
#252753=CARTESIAN_POINT('Ctrl Pts',(3.21795912865062,0.177954271636137,
13.9472336219981));
#252754=CARTESIAN_POINT('Ctrl Pts',(3.21119705662962,0.283333538447894,
13.9538655899249));
#252755=CARTESIAN_POINT('Ctrl Pts',(3.20349851419942,0.360083475353739,
13.9587930123759));
#252756=CARTESIAN_POINT('Ctrl Pts',(3.16199329879808,0.663714501517062,
13.9786806533261));
#252757=CARTESIAN_POINT('Ctrl Pts',(3.10676522488322,0.886962963958601,
13.9942465054189));
#252758=CARTESIAN_POINT('Ctrl Pts',(2.98384772930271,1.22461386753326,14.0184675935417));
#252759=CARTESIAN_POINT('Ctrl Pts',(2.93200739577582,1.34401088003475,14.0271601626155));
#252760=CARTESIAN_POINT('Ctrl Pts',(2.85984178951104,1.48602746287767,14.0374141278109));
#252761=CARTESIAN_POINT('Ctrl Pts',(2.84623974995362,1.51191669901134,14.0392795369095));
#252762=CARTESIAN_POINT('Ctrl Pts',(2.82590928195695,1.54936534059637,14.0419683372359));
#252763=CARTESIAN_POINT('Ctrl Pts',(2.81945874085534,1.56107291686202,14.0428075635071));
#252764=CARTESIAN_POINT('Ctrl Pts',(2.80800024522166,1.58156708809748,14.0442737591968));
#252765=CARTESIAN_POINT('Ctrl Pts',(2.80302353192458,1.5903706865092,14.0449026254392));
#252766=CARTESIAN_POINT('Ctrl Pts',(2.79207529488783,1.60952661556224,14.0462688078414));
#252767=CARTESIAN_POINT('Ctrl Pts',(2.78608756514042,1.61986927511282,14.047005090751));
#252768=CARTESIAN_POINT('Ctrl Pts',(2.76919139481088,1.64868333841733,14.049053244291));
#252769=CARTESIAN_POINT('Ctrl Pts',(2.75815564052515,1.66707985702906,14.0503573287521));
#252770=CARTESIAN_POINT('Ctrl Pts',(2.68464832256004,1.78688767624556,14.0588359363063));
#252771=CARTESIAN_POINT('Ctrl Pts',(2.61677267848089,1.88489018473704,14.0657053634493));
#252772=CARTESIAN_POINT('Ctrl Pts',(2.51238157905057,2.01907016569537,14.0753462260572));
#252773=CARTESIAN_POINT('Ctrl Pts',(2.48019685688869,2.05847741361839,14.0782087780148));
#252774=CARTESIAN_POINT('Ctrl Pts',(2.36027401084341,2.19841413946955,14.0885489594701));
#252775=CARTESIAN_POINT('Ctrl Pts',(2.2672490782906,2.29423166422355,14.0959738408909));
#252776=CARTESIAN_POINT('Ctrl Pts',(2.10188697793125,2.444649481736,14.1086625235947));
#252777=CARTESIAN_POINT('Ctrl Pts',(2.03270759988753,2.50246640915943,14.1138385631095));
#252778=CARTESIAN_POINT('Ctrl Pts',(1.91216118428086,2.59491353919623,14.1227375873199));
#252779=CARTESIAN_POINT('Ctrl Pts',(1.86205369644798,2.63110090467948,14.126403790174));
#252780=CARTESIAN_POINT('Ctrl Pts',(1.78987219133869,2.68013502063906,14.1316577321123));
#252781=CARTESIAN_POINT('Ctrl Pts',(1.76863677019333,2.69419563299343,14.1332001374005));
#252782=CARTESIAN_POINT('Ctrl Pts',(1.73168572182384,2.71803691314577,14.1358795735217));
#252783=CARTESIAN_POINT('Ctrl Pts',(1.71604817182152,2.72793672032573,14.1370121472487));
#252784=CARTESIAN_POINT('Ctrl Pts',(1.68584079334861,2.74669786435102,14.1391977881598));
#252785=CARTESIAN_POINT('Ctrl Pts',(1.67128416721454,2.75557934984631,14.1402500698036));
#252786=CARTESIAN_POINT('Ctrl Pts',(1.63282583240599,2.77862723713339,14.1430280436932));
#252787=CARTESIAN_POINT('Ctrl Pts',(1.60881061979741,2.79260055049327,14.1447606074511));
#252788=CARTESIAN_POINT('Ctrl Pts',(1.52165677444151,2.84181392265326,14.1510422665374));
#252789=CARTESIAN_POINT('Ctrl Pts',(1.45752093068754,2.87523514329244,14.1556543050729));
#252790=CARTESIAN_POINT('Ctrl Pts',(1.1813842471838,3.00751606002114,14.175475539009));
#252791=CARTESIAN_POINT('Ctrl Pts',(0.960097848557707,3.08528864479673,
14.1913405278997));
#252792=CARTESIAN_POINT('Ctrl Pts',(0.604211141572892,3.16833867826064,
14.21597960179));
#252793=CARTESIAN_POINT('Ctrl Pts',(0.474311635944655,3.19037237932285,
14.224782556928));
#252794=CARTESIAN_POINT('Ctrl Pts',(0.314180600480588,3.20753375138397,
14.2351505608911));
#252795=CARTESIAN_POINT('Ctrl Pts',(0.284900319798646,3.21026699254901,
14.2370265546954));
#252796=CARTESIAN_POINT('Ctrl Pts',(0.242231561340866,3.21366160192668,
14.2397276450768));
#252797=CARTESIAN_POINT('Ctrl Pts',(0.22887077286196,3.21464075832496,14.2405687736708));
#252798=CARTESIAN_POINT('Ctrl Pts',(0.205319522871526,3.21621915382045,
14.2420427808878));
#252799=CARTESIAN_POINT('Ctrl Pts',(0.195131812259069,3.21685332859405,
14.2426775261903));
#252800=CARTESIAN_POINT('Ctrl Pts',(0.17299125468655,3.2181259845369,14.2440506702943));
#252801=CARTESIAN_POINT('Ctrl Pts',(0.161037728247452,3.21874629121891,
14.2447880746575));
#252802=CARTESIAN_POINT('Ctrl Pts',(0.127568428574896,3.22029620271252,
14.2468424165207));
#252803=CARTESIAN_POINT('Ctrl Pts',(0.106045955685324,3.22107678403984,
14.2481514927013));
#252804=CARTESIAN_POINT('Ctrl Pts',(-0.0377753779472141,3.22484979665145,
14.2568288524661));
#252805=CARTESIAN_POINT('Ctrl Pts',(-0.160164806522306,3.22109250585219,
14.2638750152667));
#252806=CARTESIAN_POINT('Ctrl Pts',(-0.330249195292158,3.20614933345786,
14.273547891956));
#252807=CARTESIAN_POINT('Ctrl Pts',(-0.378341771696867,3.20083047518754,
14.2762693100423));
#252808=CARTESIAN_POINT('Ctrl Pts',(-0.563233652342623,3.17615663865755,
14.2867339908872));
#252809=CARTESIAN_POINT('Ctrl Pts',(-0.698852357471505,3.14909629859429,
14.2944210292981));
#252810=CARTESIAN_POINT('Ctrl Pts',(-0.916174401936716,3.09099942372904,
14.3072094492987));
#252811=CARTESIAN_POINT('Ctrl Pts',(-0.999091358457022,3.06520275442988,
14.312203009074));
#252812=CARTESIAN_POINT('Ctrl Pts',(-1.13753594058407,3.01591587017614,
14.3208198397685));
#252813=CARTESIAN_POINT('Ctrl Pts',(-1.19363074620879,2.99415789764203,
14.3243911944309));
#252814=CARTESIAN_POINT('Ctrl Pts',(-1.27231954796944,2.9610734549913,14.3295322780443));
#252815=CARTESIAN_POINT('Ctrl Pts',(-1.29544179754858,2.95103092704319,
14.3310593400453));
#252816=CARTESIAN_POINT('Ctrl Pts',(-1.33529096372843,2.93316492903347,
14.3337207459741));
#252817=CARTESIAN_POINT('Ctrl Pts',(-1.35207305538455,2.92546695238619,
14.3348507982782));
#252818=CARTESIAN_POINT('Ctrl Pts',(-1.3842798294875,2.9103573221763,14.3370377543101));
#252819=CARTESIAN_POINT('Ctrl Pts',(-1.39971347748136,2.90296616448933,
14.3380939256902));
#252820=CARTESIAN_POINT('Ctrl Pts',(-1.44034626643518,2.88310780298086,
14.3408965981759));
#252821=CARTESIAN_POINT('Ctrl Pts',(-1.46544195240657,2.87043337760533,
14.3426502051858));
#252822=CARTESIAN_POINT('Ctrl Pts',(-1.55646496402981,2.82295796739221,
14.3490954114921));
#252823=CARTESIAN_POINT('Ctrl Pts',(-1.62134115476139,2.7862028441973,14.3538543178011));
#252824=CARTESIAN_POINT('Ctrl Pts',(-1.88244431456586,2.62606806139971,
14.3737058245852));
#252825=CARTESIAN_POINT('Ctrl Pts',(-2.06634082897956,2.48395635686017,
14.3894306313799));
#252826=CARTESIAN_POINT('Ctrl Pts',(-2.32773679544921,2.23268627170491,
14.4138738344179));
#252827=CARTESIAN_POINT('Ctrl Pts',(-2.41648738666187,2.1363149538985,14.4226251706268));
#252828=CARTESIAN_POINT('Ctrl Pts',(-2.51765532593124,2.01206098882546,
14.4329398681062));
#252829=CARTESIAN_POINT('Ctrl Pts',(-2.53586282601865,1.98906451107695,
14.4348109255038));
#252830=CARTESIAN_POINT('Ctrl Pts',(-2.56191759893059,1.95521734542149,
14.4375062851637));
#252831=CARTESIAN_POINT('Ctrl Pts',(-2.57001467840759,1.94456196070487,
14.4383465274446));
#252832=CARTESIAN_POINT('Ctrl Pts',(-2.58416958701507,1.92569189414272,
14.4398195646805));
#252833=CARTESIAN_POINT('Ctrl Pts',(-2.59025507355398,1.91749847183039,
14.4404542175249));
#252834=CARTESIAN_POINT('Ctrl Pts',(-2.60339839594501,1.89962571127736,
14.4418278367121));
#252835=CARTESIAN_POINT('Ctrl Pts',(-2.61044127254434,1.88993582541328,
14.4425658021505));
#252836=CARTESIAN_POINT('Ctrl Pts',(-2.63001872586191,1.86268211182718,
14.444623242391));
#252837=CARTESIAN_POINT('Ctrl Pts',(-2.64243142973143,1.84503098722193,
14.4459348181242));
#252838=CARTESIAN_POINT('Ctrl Pts',(-2.72494701578867,1.72515104414752,
14.4547119954144));
#252839=CARTESIAN_POINT('Ctrl Pts',(-2.78928644385263,1.6190646147455,14.4618467594385));
#252840=CARTESIAN_POINT('Ctrl Pts',(-2.9766093496822,1.26572442235873,14.4844926102662));
#252841=CARTESIAN_POINT('Ctrl Pts',(-3.07400709813576,1.00635028865636,
14.4995587974972));
#252842=CARTESIAN_POINT('Ctrl Pts',(-3.15030109991386,0.681915629059473,
14.5191339023975));
#252843=CARTESIAN_POINT('Ctrl Pts',(-3.1619352446837,0.625756232218863,
14.522542394354));
#252844=CARTESIAN_POINT('Ctrl Pts',(-3.17643689682374,0.544957600591357,
14.5274891358243));
#252845=CARTESIAN_POINT('Ctrl Pts',(-3.18052833432557,0.5205474124033,14.5289891059011));
#252846=CARTESIAN_POINT('Ctrl Pts',(-3.18716871191596,0.477923939774208,
14.5316188901645));
#252847=CARTESIAN_POINT('Ctrl Pts',(-3.18984370069301,0.459731262481757,
14.5327447021233));
#252848=CARTESIAN_POINT('Ctrl Pts',(-3.19504790839321,0.422102541666997,
14.5350806298218));
#252849=CARTESIAN_POINT('Ctrl Pts',(-3.19755579717454,0.402664363595528,
14.5362913629958));
#252850=CARTESIAN_POINT('Ctrl Pts',(-3.20356249556793,0.352506462283499,
14.5394264579095));
#252851=CARTESIAN_POINT('Ctrl Pts',(-3.20679674749047,0.321757646781563,
14.5413589654211));
#252852=CARTESIAN_POINT('Ctrl Pts',(-3.21835897682462,0.194217824163122,
14.5494206885913));
#252853=CARTESIAN_POINT('Ctrl Pts',(-3.22275000000088,0.0971299973001183,
14.5556693739565));
#252854=CARTESIAN_POINT('Ctrl Pts',(-3.22275,-2.92740584967668E-11,14.5620312016861));
#252855=CARTESIAN_POINT('Origin',(0.,0.,-2.31077344927308));
#252856=CARTESIAN_POINT('',(-3.22275,1.40950318212534E-10,16.0607604048379));
#252857=CARTESIAN_POINT('',(-3.22275,-2.40695369623669E-12,15.8170600220821));
#252858=CARTESIAN_POINT('',(-3.22275,-3.50678552687464E-13,-2.31077344927308));
#252859=CARTESIAN_POINT('',(-3.22274878243092,0.002869896163636,16.0605665950451));
#252860=CARTESIAN_POINT('Ctrl Pts',(-3.22275,1.40950318212534E-10,16.0607604048379));
#252861=CARTESIAN_POINT('Ctrl Pts',(-3.22274999999996,0.000956430655831547,
16.0606957817113));
#252862=CARTESIAN_POINT('Ctrl Pts',(-3.22274957423342,0.00191286908978262,
16.0606311566737));
#252863=CARTESIAN_POINT('Ctrl Pts',(-3.22274872267921,0.00286931516118902,
16.0605665297975));
#252864=CARTESIAN_POINT('Ctrl Pts',(-3.22274872216818,0.00286988908068463,
16.0605664910178));
#252865=CARTESIAN_POINT('Ctrl Pts',(-3.22260972635913,0.158955561182205,
16.0500198122335));
#252866=CARTESIAN_POINT('Ctrl Pts',(-3.21113152782019,0.314837082433518,
16.0394394156062));
#252867=CARTESIAN_POINT('Ctrl Pts',(-3.18170605861958,0.51475909849832,
16.0262081803247));
#252868=CARTESIAN_POINT('Ctrl Pts',(-3.17404025376148,0.560088659893377,
16.0232319863822));
#252869=CARTESIAN_POINT('Ctrl Pts',(-3.16266995805416,0.619555231068851,
16.0193721379485));
#252870=CARTESIAN_POINT('Ctrl Pts',(-3.15983590497499,0.633850944097037,
16.0184476507336));
#252871=CARTESIAN_POINT('Ctrl Pts',(-3.15426675574805,0.660977214373375,
16.0167005540241));
#252872=CARTESIAN_POINT('Ctrl Pts',(-3.15155010899918,0.673811226303109,
16.0158770090402));
#252873=CARTESIAN_POINT('Ctrl Pts',(-3.14664724261537,0.696294890361333,
16.0144400295048));
#252874=CARTESIAN_POINT('Ctrl Pts',(-3.14449485317703,0.705951536183913,
16.0138247462876));
#252875=CARTESIAN_POINT('Ctrl Pts',(-3.13971572226225,0.726937400389772,
16.0124918147524));
#252876=CARTESIAN_POINT('Ctrl Pts',(-3.13707210484498,0.738262432658298,
16.0117751206014));
#252877=CARTESIAN_POINT('Ctrl Pts',(-3.12955106159701,0.769711948252847,
16.0097915425632));
#252878=CARTESIAN_POINT('Ctrl Pts',(-3.12454080497809,0.789804494042163,
16.0085318896235));
#252879=CARTESIAN_POINT('Ctrl Pts',(-3.09340347988852,0.90973788958046,
16.001051051618));
#252880=CARTESIAN_POINT('Ctrl Pts',(-3.06268400828473,1.00833476375011,
15.9950588056923));
#252881=CARTESIAN_POINT('Ctrl Pts',(-2.98977302668113,1.20802979414192,
15.9829360412511));
#252882=CARTESIAN_POINT('Ctrl Pts',(-2.94705725392159,1.30879098813273,
15.976825690958));
#252883=CARTESIAN_POINT('Ctrl Pts',(-2.83349118563899,1.54277683754517,
15.9622669189802));
#252884=CARTESIAN_POINT('Ctrl Pts',(-2.75825501028418,1.67357642035437,
15.9538196767181));
#252885=CARTESIAN_POINT('Ctrl Pts',(-2.62593432969368,1.87030728632341,
15.9401076233613));
#252886=CARTESIAN_POINT('Ctrl Pts',(-2.57486171042167,1.94001694707925,
15.9350313224493));
#252887=CARTESIAN_POINT('Ctrl Pts',(-2.50468067599009,2.02814769930656,
15.9282714031852));
#252888=CARTESIAN_POINT('Ctrl Pts',(-2.48805711098293,2.04850680493808,
15.926684849749));
#252889=CARTESIAN_POINT('Ctrl Pts',(-2.45883951243787,2.08340966336813,
15.92391995623));
#252890=CARTESIAN_POINT('Ctrl Pts',(-2.44636068320589,2.09804836839196,
15.9227462770801));
#252891=CARTESIAN_POINT('Ctrl Pts',(-2.42198510766311,2.12612979563819,
15.920466956722));
#252892=CARTESIAN_POINT('Ctrl Pts',(-2.41010560004475,2.13958658289417,
15.9193620491992));
#252893=CARTESIAN_POINT('Ctrl Pts',(-2.38235832019316,2.17049364683553,
15.9167944684855));
#252894=CARTESIAN_POINT('Ctrl Pts',(-2.36641031599306,2.18787019861879,
15.9153284677141));
#252895=CARTESIAN_POINT('Ctrl Pts',(-2.3134263507492,2.24434315146159,15.9104885695104));
#252896=CARTESIAN_POINT('Ctrl Pts',(-2.27560264465087,2.2826847593611,15.907081329368));
#252897=CARTESIAN_POINT('Ctrl Pts',(-2.04519299181885,2.5048295533577,15.8865922233264));
#252898=CARTESIAN_POINT('Ctrl Pts',(-1.83141718761829,2.66511726410687,
15.8685296782356));
#252899=CARTESIAN_POINT('Ctrl Pts',(-1.51733543492343,2.84481551581273,
15.8441412764353));
#252900=CARTESIAN_POINT('Ctrl Pts',(-1.43216014884925,2.88863317697712,
15.8377311712224));
#252901=CARTESIAN_POINT('Ctrl Pts',(-1.31246525100365,2.94361116032971,
15.8291034678364));
#252902=CARTESIAN_POINT('Ctrl Pts',(-1.2795241445829,2.9580787476784,15.8267674380387));
#252903=CARTESIAN_POINT('Ctrl Pts',(-1.22187280613736,2.98225563955925,
15.8227534894175));
#252904=CARTESIAN_POINT('Ctrl Pts',(-1.19727247523683,2.99221666640101,
15.8210638453471));
#252905=CARTESIAN_POINT('Ctrl Pts',(-1.16072902758536,3.0064907732883,15.8185908677699));
#252906=CARTESIAN_POINT('Ctrl Pts',(-1.14887963559707,3.01103873121741,
15.8177946841833));
#252907=CARTESIAN_POINT('Ctrl Pts',(-1.12858657003711,3.01869025110008,
15.8164412351724));
#252908=CARTESIAN_POINT('Ctrl Pts',(-1.12015640305096,3.02182860493725,
15.8158819564421));
#252909=CARTESIAN_POINT('Ctrl Pts',(-1.10085459346881,3.0289223420184,15.8146082630671));
#252910=CARTESIAN_POINT('Ctrl Pts',(-1.08997469728975,3.03285452318925,
15.8138952116988));
#252911=CARTESIAN_POINT('Ctrl Pts',(-1.05981679122292,3.04357086038286,
15.8119316098156));
#252912=CARTESIAN_POINT('Ctrl Pts',(-1.04049470115015,3.05023048940808,
15.8106880579799));
#252913=CARTESIAN_POINT('Ctrl Pts',(-0.927820452374565,3.08786996190277,
15.8035134757691));
#252914=CARTESIAN_POINT('Ctrl Pts',(-0.833143814375739,3.11474987712732,
15.7977902180428));
#252915=CARTESIAN_POINT('Ctrl Pts',(-0.54066079439401,3.18349472553782,
15.780622805304));
#252916=CARTESIAN_POINT('Ctrl Pts',(-0.340027393483033,3.21112752891242,
15.7695221294154));
#252917=CARTESIAN_POINT('Ctrl Pts',(0.00279891694355588,3.22583396828578,
15.7500744269696));
#252918=CARTESIAN_POINT('Ctrl Pts',(0.143949010686181,3.22262077444897,
15.7419363219876));
#252919=CARTESIAN_POINT('Ctrl Pts',(0.317151762627454,3.20727482009551,
15.7315449327428));
#252920=CARTESIAN_POINT('Ctrl Pts',(0.349831336743204,3.20387498649939,
15.7295668766696));
#252921=CARTESIAN_POINT('Ctrl Pts',(0.40204543872915,3.19763450077293,15.7263759574915));
#252922=CARTESIAN_POINT('Ctrl Pts',(0.421616262292587,3.19511293006904,
15.7251730703873));
#252923=CARTESIAN_POINT('Ctrl Pts',(0.458795715507767,3.18997506680548,
15.7228742849616));
#252924=CARTESIAN_POINT('Ctrl Pts',(0.476408288283485,3.18739228182276,
15.7217794773664));
#252925=CARTESIAN_POINT('Ctrl Pts',(0.516649413305925,3.18115016387692,
15.7192643172621));
#252926=CARTESIAN_POINT('Ctrl Pts',(0.539261928140943,3.17739508261763,
15.7178410032293));
#252927=CARTESIAN_POINT('Ctrl Pts',(0.598640768329683,3.16688240171998,
15.7140764217167));
#252928=CARTESIAN_POINT('Ctrl Pts',(0.635332063261136,3.15972592139947,
15.711722774622));
#252929=CARTESIAN_POINT('Ctrl Pts',(0.927791534051816,3.09738309549999,
15.6927360979667));
#252930=CARTESIAN_POINT('Ctrl Pts',(1.17605641186558,3.01188008016421,15.6751095270028));
#252931=CARTESIAN_POINT('Ctrl Pts',(1.51228289806673,2.84811490572361,15.6498465504233));
#252932=CARTESIAN_POINT('Ctrl Pts',(1.61072112697769,2.79362458950032,15.6422790304295));
#252933=CARTESIAN_POINT('Ctrl Pts',(1.75613586838751,2.70288379807742,15.6310160485125));
#252934=CARTESIAN_POINT('Ctrl Pts',(1.80529482685637,2.67030065281587,15.6271934841891));
#252935=CARTESIAN_POINT('Ctrl Pts',(1.86757903349072,2.62651115213157,15.6223575882719));
#252936=CARTESIAN_POINT('Ctrl Pts',(1.88154405970112,2.61652522633831,15.621273808906));
#252937=CARTESIAN_POINT('Ctrl Pts',(1.90410881087191,2.60011583991129,15.6195243302889));
#252938=CARTESIAN_POINT('Ctrl Pts',(1.91275721227781,2.59376032033087,15.6188542175049));
#252939=CARTESIAN_POINT('Ctrl Pts',(1.9295609133977,2.58128189760317,15.6175532650286));
#252940=CARTESIAN_POINT('Ctrl Pts',(1.93771913436894,2.57516331780016,15.6169221649739));
#252941=CARTESIAN_POINT('Ctrl Pts',(1.95596751695147,2.56134140274547,15.6155113437579));
#252942=CARTESIAN_POINT('Ctrl Pts',(1.96604159271992,2.55361688135561,15.6147330671847));
#252943=CARTESIAN_POINT('Ctrl Pts',(1.99620871114506,2.53020122962557,15.6124033390887));
#252944=CARTESIAN_POINT('Ctrl Pts',(2.01616197097816,2.51433062197575,15.6108635366975));
#252945=CARTESIAN_POINT('Ctrl Pts',(2.19488250374719,2.3686825010964,15.5970605094616));
#252946=CARTESIAN_POINT('Ctrl Pts',(2.34113429493131,2.22424772385679,15.5856649111666));
#252947=CARTESIAN_POINT('Ctrl Pts',(2.59698092367115,1.91816895056077,15.5633325604899));
#252948=CARTESIAN_POINT('Ctrl Pts',(2.70760218407184,1.75856830394266,15.5524434078279));
#252949=CARTESIAN_POINT('Ctrl Pts',(2.82854479679251,1.54534408081916,15.5379915228506));
#252950=CARTESIAN_POINT('Ctrl Pts',(2.85280534587881,1.50008507146384,15.5349311229411));
#252951=CARTESIAN_POINT('Ctrl Pts',(2.88653540269198,1.43338019057793,15.5304207724012));
#252952=CARTESIAN_POINT('Ctrl Pts',(2.8968692738074,1.41237876224875,15.5290007885634));
#252953=CARTESIAN_POINT('Ctrl Pts',(2.91468482541555,1.37515418177084,15.5264831077506));
#252954=CARTESIAN_POINT('Ctrl Pts',(2.92226216176746,1.35897773820573,15.5253887578686));
#252955=CARTESIAN_POINT('Ctrl Pts',(2.93782523594117,1.3250208818162,15.5230906175132));
#252956=CARTESIAN_POINT('Ctrl Pts',(2.94578491297969,1.30722938850427,15.521885991991));
#252957=CARTESIAN_POINT('Ctrl Pts',(2.9662787527886,1.2602836826764,15.5187054831029));
#252958=CARTESIAN_POINT('Ctrl Pts',(2.97854428562282,1.23101520050028,15.5167206452769));
#252959=CARTESIAN_POINT('Ctrl Pts',(3.03124718854209,1.09985238574996,15.5078145811562));
#252960=CARTESIAN_POINT('Ctrl Pts',(3.06689830851785,0.996125057331645,
15.5007378527394));
#252961=CARTESIAN_POINT('Ctrl Pts',(3.15420020344595,0.692585296934231,
15.4799479270727));
#252962=CARTESIAN_POINT('Ctrl Pts',(3.19204527176955,0.489374328821014,
15.4659004638993));
#252963=CARTESIAN_POINT('Ctrl Pts',(3.22049146510838,0.16779226887119,15.4441870250105));
#252964=CARTESIAN_POINT('Ctrl Pts',(3.22445495720684,0.0511349104559339,
15.4364252064716));
#252965=CARTESIAN_POINT('Ctrl Pts',(3.22152451972878,-0.0930415730923461,
15.4271570369367));
#252966=CARTESIAN_POINT('Ctrl Pts',(3.22061114091543,-0.120585907043692,
15.4254012090784));
#252967=CARTESIAN_POINT('Ctrl Pts',(3.21875235365261,-0.160987145916595,
15.4228508139463));
#252968=CARTESIAN_POINT('Ctrl Pts',(3.21808298931553,-0.173854716253167,
15.4220422542098));
#252969=CARTESIAN_POINT('Ctrl Pts',(3.21675924280161,-0.196664160630129,
15.420615997628));
#252970=CARTESIAN_POINT('Ctrl Pts',(3.21613591126108,-0.206607422912724,
15.4199966446743));
#252971=CARTESIAN_POINT('Ctrl Pts',(3.21467151848355,-0.22835181483957,
15.4186474954993));
#252972=CARTESIAN_POINT('Ctrl Pts',(3.21381158072826,-0.240151320870031,
15.4179187392443));
#252973=CARTESIAN_POINT('Ctrl Pts',(3.21119732532101,-0.273489040244611,
15.4158685615721));
#252974=CARTESIAN_POINT('Ctrl Pts',(3.20929129682661,-0.295015162756862,
15.4145551701727));
#252975=CARTESIAN_POINT('Ctrl Pts',(3.19235287051026,-0.466644754464044,
15.404154966665));
#252976=CARTESIAN_POINT('Ctrl Pts',(3.16701253893829,-0.61556224868986,
15.3955639554509));
#252977=CARTESIAN_POINT('Ctrl Pts',(3.08523970276169,-0.951520070690083,
15.3761122300471));
#252978=CARTESIAN_POINT('Ctrl Pts',(3.022074748761,-1.13629068817429,15.3653427971495));
#252979=CARTESIAN_POINT('Ctrl Pts',(2.91551271530059,-1.3748882260526,15.3503176906445));
#252980=CARTESIAN_POINT('Ctrl Pts',(2.88654996086614,-1.43469877402239,
15.3464536433615));
#252981=CARTESIAN_POINT('Ctrl Pts',(2.83296640255694,-1.53715257184504,
15.3396277231778));
#252982=CARTESIAN_POINT('Ctrl Pts',(2.80917834337105,-1.58020673331712,
15.3366931751038));
#252983=CARTESIAN_POINT('Ctrl Pts',(2.77282587982729,-1.64258454548052,
15.3323345342145));
#252984=CARTESIAN_POINT('Ctrl Pts',(2.76102399011721,-1.66234588243408,
15.3309375621765));
#252985=CARTESIAN_POINT('Ctrl Pts',(2.73971520074275,-1.6971727858827,15.3284458940265));
#252986=CARTESIAN_POINT('Ctrl Pts',(2.73029307683862,-1.71228926905903,
15.3273543107294));
#252987=CARTESIAN_POINT('Ctrl Pts',(2.7101969713993,-1.74394304133163,15.3250468203785));
#252988=CARTESIAN_POINT('Ctrl Pts',(2.69949586384522,-1.76046215778765,
15.3238299440067));
#252989=CARTESIAN_POINT('Ctrl Pts',(2.67065799523871,-1.80409745491183,
15.3205811532836));
#252990=CARTESIAN_POINT('Ctrl Pts',(2.65226005168593,-1.83103747856497,
15.3185395756064));
#252991=CARTESIAN_POINT('Ctrl Pts',(2.56332037546018,-1.95711795759643,
15.3088107924947));
#252992=CARTESIAN_POINT('Ctrl Pts',(2.48761769447146,-2.05248003318512,
15.3009293311116));
#252993=CARTESIAN_POINT('Ctrl Pts',(2.27380501007805,-2.29256755214937,
15.2796752256792));
#252994=CARTESIAN_POINT('Ctrl Pts',(2.12730754000876,-2.42911668537106,
15.2660507554026));
#252995=CARTESIAN_POINT('Ctrl Pts',(1.88177720789917,-2.61862697568247,
15.2452189209509));
#252996=CARTESIAN_POINT('Ctrl Pts',(1.79101527097696,-2.68152222767975,
15.2378915409905));
#252997=CARTESIAN_POINT('Ctrl Pts',(1.67437808777581,-2.75377852587573,
15.2290793815153));
#252998=CARTESIAN_POINT('Ctrl Pts',(1.65138174554023,-2.76763013947763,
15.2273699118184));
#252999=CARTESIAN_POINT('Ctrl Pts',(1.61721102877943,-2.78763495006677,
15.2248737083911));
#253000=CARTESIAN_POINT('Ctrl Pts',(1.60616953977432,-2.79401137233572,
15.2240737869116));
#253001=CARTESIAN_POINT('Ctrl Pts',(1.58726843148564,-2.80477762414213,
15.2227161830266));
#253002=CARTESIAN_POINT('Ctrl Pts',(1.57942790737277,-2.80920025751278,
15.2221564524602));
#253003=CARTESIAN_POINT('Ctrl Pts',(1.56150407913006,-2.8192118531124,15.2208847405414));
#253004=CARTESIAN_POINT('Ctrl Pts',(1.55140922635653,-2.82477961685034,
15.2201740956495));
#253005=CARTESIAN_POINT('Ctrl Pts',(1.52349300814275,-2.83998187063616,
15.21822365771));
#253006=CARTESIAN_POINT('Ctrl Pts',(1.50561000792679,-2.84950285536709,
15.2169907121405));
#253007=CARTESIAN_POINT('Ctrl Pts',(1.40340641488157,-2.90268566709607,
15.2100308374864));
#253008=CARTESIAN_POINT('Ctrl Pts',(1.3172707507851,-2.94277671732208,15.2044973467694));
#253009=CARTESIAN_POINT('Ctrl Pts',(1.07506092857759,-3.0427404457207,15.1895036831677));
#253010=CARTESIAN_POINT('Ctrl Pts',(0.915912046568545,-3.09437151982397,
15.1802642517259));
#253011=CARTESIAN_POINT('Ctrl Pts',(0.581554778721295,-3.17477183297286,
15.1609308371604));
#253012=CARTESIAN_POINT('Ctrl Pts',(0.406547780230568,-3.20188852858029,
15.1508453944993));
#253013=CARTESIAN_POINT('Ctrl Pts',(0.195857889254473,-3.21697739001396,
15.1382390617403));
#253014=CARTESIAN_POINT('Ctrl Pts',(0.16146729386,-3.21888676676952,15.1361675615575));
#253015=CARTESIAN_POINT('Ctrl Pts',(0.106995431247289,-3.22103593569282,
15.1328617541528));
#253016=CARTESIAN_POINT('Ctrl Pts',(0.0869306077220727,-3.22163988716715,
15.1316387587998));
#253017=CARTESIAN_POINT('Ctrl Pts',(0.049126765924715,-3.22242436530274,
15.1293240026776));
#253018=CARTESIAN_POINT('Ctrl Pts',(0.0313892863587283,-3.22264595047502,
15.1282335609304));
#253019=CARTESIAN_POINT('Ctrl Pts',(-0.00868875170015642,-3.22281571743229,
15.125759451026));
#253020=CARTESIAN_POINT('Ctrl Pts',(-0.0310285771806581,-3.22267805254223,
15.1243731680973));
#253021=CARTESIAN_POINT('Ctrl Pts',(-0.097403294180263,-3.22157881916003,
15.120232145332));
#253022=CARTESIAN_POINT('Ctrl Pts',(-0.141420439396597,-3.21994680760062,
15.1174568799119));
#253023=CARTESIAN_POINT('Ctrl Pts',(-0.409190200943396,-3.20451780634388,
15.1003896339542));
#253024=CARTESIAN_POINT('Ctrl Pts',(-0.630999839408173,-3.16830851183655,
15.0854030798675));
#253025=CARTESIAN_POINT('Ctrl Pts',(-0.978859255657224,-3.07352687871825,
15.0610381434794));
#253026=CARTESIAN_POINT('Ctrl Pts',(-1.1080935222725,-3.02933408084008,
15.0517992006517));
#253027=CARTESIAN_POINT('Ctrl Pts',(-1.27514194498351,-2.9600845322329,
15.0398733113168));
#253028=CARTESIAN_POINT('Ctrl Pts',(-1.31578821753152,-2.94224219923064,
15.036973507921));
#253029=CARTESIAN_POINT('Ctrl Pts',(-1.38427122702853,-2.91047731321657,
15.0321059981082));
#253030=CARTESIAN_POINT('Ctrl Pts',(-1.41229793631762,-2.89698113973942,
15.0301192974133));
#253031=CARTESIAN_POINT('Ctrl Pts',(-1.45222334730055,-2.87703802064566,
15.027301390109));
#253032=CARTESIAN_POINT('Ctrl Pts',(-1.46428278359424,-2.87091908062637,
15.0264518695625));
#253033=CARTESIAN_POINT('Ctrl Pts',(-1.48521826956498,-2.86013021228494,
15.0249803860178));
#253034=CARTESIAN_POINT('Ctrl Pts',(-1.49411156481751,-2.85549448989673,
15.0243563695138));
#253035=CARTESIAN_POINT('Ctrl Pts',(-1.51308591807896,-2.84549099370784,
15.0230273956593));
#253036=CARTESIAN_POINT('Ctrl Pts',(-1.52316020871888,-2.84011108561211,
15.022323197854));
#253037=CARTESIAN_POINT('Ctrl Pts',(-1.55060731429737,-2.82526563628965,
15.0204079137619));
#253038=CARTESIAN_POINT('Ctrl Pts',(-1.56792221867907,-2.81569332831976,
15.0192032783224));
#253039=CARTESIAN_POINT('Ctrl Pts',(-1.66031222517607,-2.76350022233958,
15.0127890340651));
#253040=CARTESIAN_POINT('Ctrl Pts',(-1.73374645397744,-2.71803164723146,
15.007738748511));
#253041=CARTESIAN_POINT('Ctrl Pts',(-1.9487327321651,-2.57265433837315,
14.9928295280849));
#253042=CARTESIAN_POINT('Ctrl Pts',(-2.08414691045551,-2.4642335877769,
14.9832556799089));
#253043=CARTESIAN_POINT('Ctrl Pts',(-2.32985279997184,-2.23269669021705,
14.9642850550483));
#253044=CARTESIAN_POINT('Ctrl Pts',(-2.44069163567604,-2.11096293798475,
14.9549302786212));
#253045=CARTESIAN_POINT('Ctrl Pts',(-2.56861352591344,-1.94685664948597,
14.9425998820218));
#253046=CARTESIAN_POINT('Ctrl Pts',(-2.59476838965091,-1.91185851764458,
14.9399860794798));
#253047=CARTESIAN_POINT('Ctrl Pts',(-2.63299878097278,-1.85847195590325,
14.9360162897142));
#253048=CARTESIAN_POINT('Ctrl Pts',(-2.6456113326674,-1.84047309983463,
14.9346808006205));
#253049=CARTESIAN_POINT('Ctrl Pts',(-2.66796033888545,-1.80787528997435,
14.9322665221954));
#253050=CARTESIAN_POINT('Ctrl Pts',(-2.67776359925488,-1.79332303876533,
14.9311903059231));
#253051=CARTESIAN_POINT('Ctrl Pts',(-2.69863006067927,-1.76179564263779,
14.9288616572182));
#253052=CARTESIAN_POINT('Ctrl Pts',(-2.70965293741618,-1.74479483601776,
14.9276077854255));
#253053=CARTESIAN_POINT('Ctrl Pts',(-2.7389612006861,-1.69864449239057,
14.9242083371454));
#253054=CARTESIAN_POINT('Ctrl Pts',(-2.75694083973245,-1.66930483447005,
14.9220517227058));
#253055=CARTESIAN_POINT('Ctrl Pts',(-2.85797542106756,-1.49834805414221,
14.9095074121094));
#253056=CARTESIAN_POINT('Ctrl Pts',(-2.9305701316707,-1.35085719686086,
14.8987520889994));
#253057=CARTESIAN_POINT('Ctrl Pts',(-3.06498357548507,-1.015343676264,14.8745641533478));
#253058=CARTESIAN_POINT('Ctrl Pts',(-3.12138250328075,-0.825843134724053,
14.861072194129));
#253059=CARTESIAN_POINT('Ctrl Pts',(-3.17059709252073,-0.579909243797049,
14.8444311187627));
#253060=CARTESIAN_POINT('Ctrl Pts',(-3.17978879926637,-0.527185401921884,
14.8409150934723));
#253061=CARTESIAN_POINT('Ctrl Pts',(-3.19291800919129,-0.438938468991591,
14.8351405265175));
#253062=CARTESIAN_POINT('Ctrl Pts',(-3.19758525627638,-0.403535827775161,
14.8328533034425));
#253063=CARTESIAN_POINT('Ctrl Pts',(-3.20329412037733,-0.353875999502981,
14.8296927176033));
#253064=CARTESIAN_POINT('Ctrl Pts',(-3.20483059793441,-0.339679703426401,
14.8287946424856));
#253065=CARTESIAN_POINT('Ctrl Pts',(-3.20729702365965,-0.315382681112745,
14.827267424476));
#253066=CARTESIAN_POINT('Ctrl Pts',(-3.20827372351705,-0.30528701214969,
14.8266357581805));
#253067=CARTESIAN_POINT('Ctrl Pts',(-3.21021583315862,-0.284172827007799,
14.825320948772));
#253068=CARTESIAN_POINT('Ctrl Pts',(-3.21117220368781,-0.273153762225458,
14.8246382985928));
#253069=CARTESIAN_POINT('Ctrl Pts',(-3.21358946746526,-0.24353322742016,
14.8228121934577));
#253070=CARTESIAN_POINT('Ctrl Pts',(-3.21494560370638,-0.224923322443813,
14.8216743556143));
#253071=CARTESIAN_POINT('Ctrl Pts',(-3.2205056898234,-0.138244574017291,
14.8164143686205));
#253072=CARTESIAN_POINT('Ctrl Pts',(-3.2227102601513,-0.0700602807453514,
14.8123903960569));
#253073=CARTESIAN_POINT('Ctrl Pts',(-3.22274982252387,-0.00123500483905878,
14.8083979017871));
#253074=CARTESIAN_POINT('Ctrl Pts',(-3.22275,-0.000617500973495014,14.8083620865646));
#253075=CARTESIAN_POINT('Ctrl Pts',(-3.22275,1.96138700782895E-11,14.8083262771147));
#253076=CARTESIAN_POINT('Ctrl Pts',(-3.22275,-2.92740584967668E-11,14.5620312016861));
#253077=CARTESIAN_POINT('Ctrl Pts',(-3.22274999999999,-0.000767382685586242,
14.5620814637719));
#253078=CARTESIAN_POINT('Ctrl Pts',(-3.22274972607258,-0.00153476798980013,
14.5621317326809));
#253079=CARTESIAN_POINT('Ctrl Pts',(-3.22262792044864,-0.172048925614069,
14.5733030758767));
#253080=CARTESIAN_POINT('Ctrl Pts',(-3.20909564308139,-0.341507159977076,
14.5847558065709));
#253081=CARTESIAN_POINT('Ctrl Pts',(-3.15666552162296,-0.669240997370065,
14.6071826385691));
#253082=CARTESIAN_POINT('Ctrl Pts',(-3.11899104670159,-0.827239278373474,
14.6181198783632));
#253083=CARTESIAN_POINT('Ctrl Pts',(-3.06037229256215,-1.01052066348497,
14.6305171017099));
#253084=CARTESIAN_POINT('Ctrl Pts',(-3.05076289908809,-1.03917104696589,
14.6324459323832));
#253085=CARTESIAN_POINT('Ctrl Pts',(-3.03631282695233,-1.08032471510789,
14.6351991464015));
#253086=CARTESIAN_POINT('Ctrl Pts',(-3.03179519261813,-1.09293869815829,
14.6360406527494));
#253087=CARTESIAN_POINT('Ctrl Pts',(-3.02368909401783,-1.11513519884456,
14.6375167664725));
#253088=CARTESIAN_POINT('Ctrl Pts',(-3.02013347537823,-1.12472932323589,
14.6381532311103));
#253089=CARTESIAN_POINT('Ctrl Pts',(-3.0123722909868,-1.14536912080494,
14.6395189697861));
#253090=CARTESIAN_POINT('Ctrl Pts',(-3.00815160885961,-1.15640872996861,
14.6402473546126));
#253091=CARTESIAN_POINT('Ctrl Pts',(-2.99610459724462,-1.18740657319459,
14.6422872906105));
#253092=CARTESIAN_POINT('Ctrl Pts',(-2.98813956500924,-1.20731069876947,
14.6435909772437));
#253093=CARTESIAN_POINT('Ctrl Pts',(-2.9310664369083,-1.34590722029258,
14.6526352805466));
#253094=CARTESIAN_POINT('Ctrl Pts',(-2.87509363803544,-1.46166367253961,
14.660018389446));
#253095=CARTESIAN_POINT('Ctrl Pts',(-2.66912284152672,-1.82973444896855,
14.6838768977901));
#253096=CARTESIAN_POINT('Ctrl Pts',(-2.49163642882076,-2.06491867333873,
14.6998860792243));
#253097=CARTESIAN_POINT('Ctrl Pts',(-2.25721071448654,-2.30057520782022,
14.7195886782357));
#253098=CARTESIAN_POINT('Ctrl Pts',(-2.2291329057991,-2.32779139763092,
14.7219262570076));
#253099=CARTESIAN_POINT('Ctrl Pts',(-2.18345042807594,-2.37048744727025,
14.7256992478237));
#253100=CARTESIAN_POINT('Ctrl Pts',(-2.16615952956548,-2.38629825415869,
14.727120643631));
#253101=CARTESIAN_POINT('Ctrl Pts',(-2.13509420835349,-2.41408853449397,
14.7296634916327));
#253102=CARTESIAN_POINT('Ctrl Pts',(-2.12138738289456,-2.42614226318123,
14.7307817871995));
#253103=CARTESIAN_POINT('Ctrl Pts',(-2.0924557422095,-2.45115200607763,
14.7331350055754));
#253104=CARTESIAN_POINT('Ctrl Pts',(-2.07721132979201,-2.46408405961907,
14.7343708404358));
#253105=CARTESIAN_POINT('Ctrl Pts',(-2.03668415535031,-2.49782049272015,
14.7376461321974));
#253106=CARTESIAN_POINT('Ctrl Pts',(-2.0112034680001,-2.51838242667737,
14.7396951686319));
#253107=CARTESIAN_POINT('Ctrl Pts',(-1.88159835097917,-2.61974725971168,
14.7500698591014));
#253108=CARTESIAN_POINT('Ctrl Pts',(-1.77291187542261,-2.6944877146309,
14.7586261025567));
#253109=CARTESIAN_POINT('Ctrl Pts',(-1.54217406319262,-2.83314355611134,
14.7764741240285));
#253110=CARTESIAN_POINT('Ctrl Pts',(-1.41997959155703,-2.89631790401781,
14.7857640834384));
#253111=CARTESIAN_POINT('Ctrl Pts',(-1.24805070249182,-2.97170303841608,
14.7984471437018));
#253112=CARTESIAN_POINT('Ctrl Pts',(-1.20150000534579,-2.9908272047466,
14.8018431480429));
#253113=CARTESIAN_POINT('Ctrl Pts',(-1.04242728965904,-3.05186461663847,
14.8132879123654));
#253114=CARTESIAN_POINT('Ctrl Pts',(-0.928006460376373,-3.08858255019199,
14.8212562453868));
#253115=CARTESIAN_POINT('Ctrl Pts',(-0.791009219811731,-3.12424122018396,
14.8302987420042));
#253116=CARTESIAN_POINT('Ctrl Pts',(-0.770171365661151,-3.12944322718091,
14.8316607387411));
#253117=CARTESIAN_POINT('Ctrl Pts',(-0.737654004471244,-3.13721645406425,
14.8337636708378));
#253118=CARTESIAN_POINT('Ctrl Pts',(-0.726009976777438,-3.13993153336891,
14.8345122423729));
#253119=CARTESIAN_POINT('Ctrl Pts',(-0.704490228448732,-3.14482326011948,
14.8358871411926));
#253120=CARTESIAN_POINT('Ctrl Pts',(-0.694619309379324,-3.1470182455876,
14.8365144424809));
#253121=CARTESIAN_POINT('Ctrl Pts',(-0.671684335039595,-3.15200510238433,
14.8379643598919));
#253122=CARTESIAN_POINT('Ctrl Pts',(-0.658613079192044,-3.15476224742492,
14.8387850287275));
#253123=CARTESIAN_POINT('Ctrl Pts',(-0.616918582158315,-3.16328651007499,
14.841385810054));
#253124=CARTESIAN_POINT('Ctrl Pts',(-0.588233085062097,-3.16874613265094,
14.8431497064004));
#253125=CARTESIAN_POINT('Ctrl Pts',(-0.43184286827307,-3.19631440646347,
14.8526477448267));
#253126=CARTESIAN_POINT('Ctrl Pts',(-0.302954750400545,-3.21109628466694,
14.8600497376072));
#253127=CARTESIAN_POINT('Ctrl Pts',(0.0542576625291786,-3.23035677095754,
14.8802181176223));
#253128=CARTESIAN_POINT('Ctrl Pts',(0.282678902479633,-3.21842175425126,
14.8927728652563));
#253129=CARTESIAN_POINT('Ctrl Pts',(0.58538006046655,-3.17011037273422,
14.9105566519764));
#253130=CARTESIAN_POINT('Ctrl Pts',(0.66235250231329,-3.15492588422435,
14.9151752055714));
#253131=CARTESIAN_POINT('Ctrl Pts',(0.766592766396783,-3.13037933925601,
14.9216011050474));
#253132=CARTESIAN_POINT('Ctrl Pts',(0.794405547796953,-3.12343705283311,
14.9233324053845));
#253133=CARTESIAN_POINT('Ctrl Pts',(0.838765670823335,-3.11173360490088,
14.9261222914766));
#253134=CARTESIAN_POINT('Ctrl Pts',(0.855374271370775,-3.10720915235227,
14.9271732849796));
#253135=CARTESIAN_POINT('Ctrl Pts',(0.889656632818029,-3.09757438899982,
14.9293564181183));
#253136=CARTESIAN_POINT('Ctrl Pts',(0.907324439732689,-3.09244536874144,
14.9304891263085));
#253137=CARTESIAN_POINT('Ctrl Pts',(0.948709965642377,-3.08004583198981,
14.9331607486942));
#253138=CARTESIAN_POINT('Ctrl Pts',(0.972389308870204,-3.07265225877324,
14.934703595816));
#253139=CARTESIAN_POINT('Ctrl Pts',(1.05084018315465,-3.04715931055071,
14.9398637979903));
#253140=CARTESIAN_POINT('Ctrl Pts',(1.10520840908769,-3.02786371032272,
14.9435196171964));
#253141=CARTESIAN_POINT('Ctrl Pts',(1.41682459348787,-2.90775826472048,
14.9649494238707));
#253142=CARTESIAN_POINT('Ctrl Pts',(1.66074425899616,-2.77566733771619,
14.9837707369428));
#253143=CARTESIAN_POINT('Ctrl Pts',(1.98471372622241,-2.54208720145296,
15.0106153840908));
#253144=CARTESIAN_POINT('Ctrl Pts',(2.080444939307,-2.46435610055872,15.0188001601895));
#253145=CARTESIAN_POINT('Ctrl Pts',(2.18742684176691,-2.36680081505183,
15.0280492950521));
#253146=CARTESIAN_POINT('Ctrl Pts',(2.20321023855988,-2.35211542838452,
15.0294165496566));
#253147=CARTESIAN_POINT('Ctrl Pts',(2.22752976226661,-2.32902814548161,
15.0315258362517));
#253148=CARTESIAN_POINT('Ctrl Pts',(2.23616810642243,-2.32073547711821,
15.0322755752576));
#253149=CARTESIAN_POINT('Ctrl Pts',(2.25208382637645,-2.30528527109465,
15.0336575493209));
#253150=CARTESIAN_POINT('Ctrl Pts',(2.25937346856661,-2.2981412653412,15.0342907182267));
#253151=CARTESIAN_POINT('Ctrl Pts',(2.27614719799126,-2.28154569535308,
15.0357483026882));
#253152=CARTESIAN_POINT('Ctrl Pts',(2.28560645558018,-2.27206953495655,
15.0365707998224));
#253153=CARTESIAN_POINT('Ctrl Pts',(2.31562241257233,-2.24162278668299,
15.0391834957291));
#253154=CARTESIAN_POINT('Ctrl Pts',(2.33595228933482,-2.22042944342507,
15.0409572686508));
#253155=CARTESIAN_POINT('Ctrl Pts',(2.44553006920246,-2.10302659896107,
15.0505609231054));
#253156=CARTESIAN_POINT('Ctrl Pts',(2.52913628919186,-2.00170300407092,
15.0580504976579));
#253157=CARTESIAN_POINT('Ctrl Pts',(2.74323394131785,-1.7073242326538,15.0785640187537));
#253158=CARTESIAN_POINT('Ctrl Pts',(2.8593304076003,-1.50483039954838,15.09137500281));
#253159=CARTESIAN_POINT('Ctrl Pts',(2.98205684632037,-1.22427705960473,
15.1091860068409));
#253160=CARTESIAN_POINT('Ctrl Pts',(3.00919415828918,-1.15597002005049,
15.113521356035));
#253161=CARTESIAN_POINT('Ctrl Pts',(3.0434004154401,-1.06047779841409,15.119612144367));
#253162=CARTESIAN_POINT('Ctrl Pts',(3.05248568779449,-1.03403592843406,
15.1213017080211));
#253163=CARTESIAN_POINT('Ctrl Pts',(3.06656622505557,-0.991252241567517,
15.1240417947097));
#253164=CARTESIAN_POINT('Ctrl Pts',(3.07177767952471,-0.974982712250784,
15.1250852348271));
#253165=CARTESIAN_POINT('Ctrl Pts',(3.08235784674524,-0.94102567389393,
15.1272664441877));
#253166=CARTESIAN_POINT('Ctrl Pts',(3.08770422337394,-0.923331912604987,
15.128404892531));
#253167=CARTESIAN_POINT('Ctrl Pts',(3.10001548794778,-0.881284913735006,
15.1311152056547));
#253168=CARTESIAN_POINT('Ctrl Pts',(3.10684597185512,-0.856893910354364,
15.132691332695));
#253169=CARTESIAN_POINT('Ctrl Pts',(3.12912232057025,-0.773577239534555,
15.1380896817673));
#253170=CARTESIAN_POINT('Ctrl Pts',(3.14318398662438,-0.714298167223327,
15.1419554046626));
#253171=CARTESIAN_POINT('Ctrl Pts',(3.17350006404845,-0.568170087036102,
15.151550005026));
#253172=CARTESIAN_POINT('Ctrl Pts',(3.18787861788167,-0.480986189516279,
15.1573309124744));
#253173=CARTESIAN_POINT('Ctrl Pts',(3.21519197869008,-0.258865712997641,
15.1721747905934));
#253174=CARTESIAN_POINT('Ctrl Pts',(3.22323047421431,-0.123501466520903,
15.1813323999834));
#253175=CARTESIAN_POINT('Ctrl Pts',(3.2225484698029,0.0602889171238125,
15.1937496464241));
#253176=CARTESIAN_POINT('Ctrl Pts',(3.22128196385264,0.108609442932034,
15.1970118086537));
#253177=CARTESIAN_POINT('Ctrl Pts',(3.21296707059381,0.279213865080282,
15.208490706513));
#253178=CARTESIAN_POINT('Ctrl Pts',(3.20003567244147,0.401117954041918,
15.2166254546426));
#253179=CARTESIAN_POINT('Ctrl Pts',(3.17670512328315,0.543255038579436,
15.2258268565323));
#253180=CARTESIAN_POINT('Ctrl Pts',(3.17300332814693,0.564474458401743,
15.2271928970535));
#253181=CARTESIAN_POINT('Ctrl Pts',(3.16691370069047,0.597426527976927,
15.2293007165237));
#253182=CARTESIAN_POINT('Ctrl Pts',(3.16467283983157,0.609185252185454,
15.2300501861064));
#253183=CARTESIAN_POINT('Ctrl Pts',(3.1603997966497,0.630947604235671,15.2314319239441));
#253184=CARTESIAN_POINT('Ctrl Pts',(3.1583855948625,0.640954126186585,15.2320651231602));
#253185=CARTESIAN_POINT('Ctrl Pts',(3.15361816376711,0.664070379874472,
15.2335231120442));
#253186=CARTESIAN_POINT('Ctrl Pts',(3.15083070781573,0.677172694024774,
15.2343459793919));
#253187=CARTESIAN_POINT('Ctrl Pts',(3.14166480165795,0.718974369403137,
15.2369610924942));
#253188=CARTESIAN_POINT('Ctrl Pts',(3.13497511682382,0.747604857574493,
15.2387368696829));
#253189=CARTESIAN_POINT('Ctrl Pts',(3.09621062325606,0.903828087792487,
15.2483620720358));
#253190=CARTESIAN_POINT('Ctrl Pts',(3.05673448154163,1.02946922177239,15.2558695136295));
#253191=CARTESIAN_POINT('Ctrl Pts',(2.92611878125399,1.37060672301495,15.2764538909851));
#253192=CARTESIAN_POINT('Ctrl Pts',(2.81906855047291,1.57910818887085,15.2893176559885));
#253193=CARTESIAN_POINT('Ctrl Pts',(2.65051278262038,1.83470785784223,15.307135252183));
#253194=CARTESIAN_POINT('Ctrl Pts',(2.60858329678742,1.89384872119884,15.311413123281));
#253195=CARTESIAN_POINT('Ctrl Pts',(2.54785766296859,1.9736545538385,15.3174356940224));
#253196=CARTESIAN_POINT('Ctrl Pts',(2.53073197158215,1.99556673244552,15.3191164886264));
#253197=CARTESIAN_POINT('Ctrl Pts',(2.50264863222939,2.03055616094981,15.321846138496));
#253198=CARTESIAN_POINT('Ctrl Pts',(2.49186675303018,2.04377312022222,15.3228880162837));
#253199=CARTESIAN_POINT('Ctrl Pts',(2.46917045085927,2.07114877547519,15.3250689792181));
#253200=CARTESIAN_POINT('Ctrl Pts',(2.45723801238995,2.08529165669815,15.3262087675979));
#253201=CARTESIAN_POINT('Ctrl Pts',(2.42860811102907,2.11863818598469,15.3289278661098));
#253202=CARTESIAN_POINT('Ctrl Pts',(2.41180388185956,2.13774813681059,15.3305115135603));
#253203=CARTESIAN_POINT('Ctrl Pts',(2.35350943979924,2.20247893214203,15.3359649118618));
#253204=CARTESIAN_POINT('Ctrl Pts',(2.31093917566014,2.24710467707102,15.3398793745825));
#253205=CARTESIAN_POINT('Ctrl Pts',(2.20325759252548,2.35368793583731,15.3496241255134));
#253206=CARTESIAN_POINT('Ctrl Pts',(2.1367872393462,2.41419324126008,15.3555086166336));
#253207=CARTESIAN_POINT('Ctrl Pts',(1.96526969834919,2.55768066347925,15.3703518457181));
#253208=CARTESIAN_POINT('Ctrl Pts',(1.85741781148559,2.6370458943435,15.3793966080237));
#253209=CARTESIAN_POINT('Ctrl Pts',(1.70213803905913,2.7370489699189,15.3918745100475));
#253210=CARTESIAN_POINT('Ctrl Pts',(1.65867513142002,2.76360415220034,15.3953113102629));
#253211=CARTESIAN_POINT('Ctrl Pts',(1.51147842547885,2.84881526876242,15.4067338443869));
#253212=CARTESIAN_POINT('Ctrl Pts',(1.40511364272094,2.90275332807333,15.4146397494747));
#253213=CARTESIAN_POINT('Ctrl Pts',(1.27635418013286,2.9593069775233,15.4236225872744));
#253214=CARTESIAN_POINT('Ctrl Pts',(1.2566263008223,2.96773788889347,15.4249830664332));
#253215=CARTESIAN_POINT('Ctrl Pts',(1.22577940705626,2.98055787225596,15.4270841640641));
#253216=CARTESIAN_POINT('Ctrl Pts',(1.21471807378909,2.98508297983287,15.4278323983157));
#253217=CARTESIAN_POINT('Ctrl Pts',(1.19425044427644,2.9933235225987,15.4292070032503));
#253218=CARTESIAN_POINT('Ctrl Pts',(1.18485177272872,2.9970562415297,15.4298343443191));
#253219=CARTESIAN_POINT('Ctrl Pts',(1.16298982712552,3.00561988287328,15.4312847706754));
#253220=CARTESIAN_POINT('Ctrl Pts',(1.15051390417519,3.0104175771992,15.4321059038115));
#253221=CARTESIAN_POINT('Ctrl Pts',(1.11065158094814,3.02546287801877,15.4347097077152));
#253222=CARTESIAN_POINT('Ctrl Pts',(1.08315458504291,3.03541576060018,15.4364761092655));
#253223=CARTESIAN_POINT('Ctrl Pts',(0.932683714788523,3.08757539610112,
15.4460008493636));
#253224=CARTESIAN_POINT('Ctrl Pts',(0.807365070279258,3.12268943643086,
15.4534249855466));
#253225=CARTESIAN_POINT('Ctrl Pts',(0.456150134045896,3.19853249709384,
15.4736803000677));
#253226=CARTESIAN_POINT('Ctrl Pts',(0.227531665699287,3.22287285220127,
15.4862994576544));
#253227=CARTESIAN_POINT('Ctrl Pts',(-0.07891087263912,3.22270802118565,
15.504089336431));
#253228=CARTESIAN_POINT('Ctrl Pts',(-0.156056923781871,3.21989422122287,
15.5086360512408));
#253229=CARTESIAN_POINT('Ctrl Pts',(-0.261439217191516,3.21225447175947,
15.5149771082864));
#253230=CARTESIAN_POINT('Ctrl Pts',(-0.289825591467194,3.2098177991622,
15.5166980578801));
#253231=CARTESIAN_POINT('Ctrl Pts',(-0.33527265443123,3.2053088786997,15.5194755757948));
#253232=CARTESIAN_POINT('Ctrl Pts',(-0.352355945046317,3.20347592950716,
15.5205246793437));
#253233=CARTESIAN_POINT('Ctrl Pts',(-0.387719329030133,3.19939533012292,
15.5227072261354));
#253234=CARTESIAN_POINT('Ctrl Pts',(-0.405996407502154,3.19712740619109,
15.5238412647199));
#253235=CARTESIAN_POINT('Ctrl Pts',(-0.448966159931648,3.19142107427935,
15.5265220272803));
#253236=CARTESIAN_POINT('Ctrl Pts',(-0.473640084332162,3.18785258459176,
15.5280727618363));
#253237=CARTESIAN_POINT('Ctrl Pts',(-0.556004149865956,3.17496328462266,
15.5332886217382));
#253238=CARTESIAN_POINT('Ctrl Pts',(-0.61347906660195,3.16436015697816,
15.5369933591114));
#253239=CARTESIAN_POINT('Ctrl Pts',(-0.752199399764213,3.13484738905813,
15.5460981285163));
#253240=CARTESIAN_POINT('Ctrl Pts',(-0.833057519184828,3.11433547559767,
15.5515434560678));
#253241=CARTESIAN_POINT('Ctrl Pts',(-1.04968617135856,3.05034142511166,
15.5664892216815));
#253242=CARTESIAN_POINT('Ctrl Pts',(-1.18351263293232,3.00095271139991,
15.576118095521));
#253243=CARTESIAN_POINT('Ctrl Pts',(-1.45893570678965,2.87801098793581,
15.5964967507057));
#253244=CARTESIAN_POINT('Ctrl Pts',(-1.5992579213983,2.80246743793846,15.6072194817099));
#253245=CARTESIAN_POINT('Ctrl Pts',(-1.75879094935539,2.70068077691521,
15.6194097825894));
#253246=CARTESIAN_POINT('Ctrl Pts',(-1.783920978429,2.68414760287178,15.6213296248371));
#253247=CARTESIAN_POINT('Ctrl Pts',(-1.81988549782616,2.65975810852582,
15.624072457675));
#253248=CARTESIAN_POINT('Ctrl Pts',(-1.83090753582403,2.65218288037971,
15.6249123989887));
#253249=CARTESIAN_POINT('Ctrl Pts',(-1.84997421598674,2.63890322002242,
15.6263637981408));
#253250=CARTESIAN_POINT('Ctrl Pts',(-1.85804029279344,2.63323016172793,
15.6269772912239));
#253251=CARTESIAN_POINT('Ctrl Pts',(-1.86624909445508,2.62740022126393,
15.6276010601598));
#253252=CARTESIAN_POINT('Ctrl Pts',(-1.8664176600901,2.62728048052659,15.6276138688601));
#253253=CARTESIAN_POINT('Ctrl Pts',(-1.86670813507835,2.62707409931672,
15.6276359406142));
#253254=CARTESIAN_POINT('Ctrl Pts',(-1.86683004989755,2.62698746659895,
15.6276452041946));
#253255=CARTESIAN_POINT('Ctrl Pts',(-1.86713779217371,2.62676875257682,
15.6276685873888));
#253256=CARTESIAN_POINT('Ctrl Pts',(-1.86732361168996,2.62663666000887,
15.6276827062381));
#253257=CARTESIAN_POINT('Ctrl Pts',(-1.86768387906037,2.62638050103607,
15.6277100793555));
#253258=CARTESIAN_POINT('Ctrl Pts',(-1.86785832856042,2.62625643697488,
15.627723333782));
#253259=CARTESIAN_POINT('Ctrl Pts',(-1.86819701832462,2.62601551858567,
15.6277490664731));
#253260=CARTESIAN_POINT('Ctrl Pts',(-1.86836125998449,2.625898666232,15.6277615448717));
#253261=CARTESIAN_POINT('Ctrl Pts',(-1.86868053723207,2.62567146621253,
15.6277858018073));
#253262=CARTESIAN_POINT('Ctrl Pts',(-1.86883557400796,2.62556112022459,
15.6277975804582));
#253263=CARTESIAN_POINT('Ctrl Pts',(-1.86913731257558,2.6253463203299,15.6278205041488));
#253264=CARTESIAN_POINT('Ctrl Pts',(-1.86928401537687,2.62524186786447,
15.6278316492853));
#253265=CARTESIAN_POINT('Ctrl Pts',(-1.86956984662064,2.62503831977431,
15.6278533637931));
#253266=CARTESIAN_POINT('Ctrl Pts',(-1.86970897594874,2.62493922537902,
15.6278639332489));
#253267=CARTESIAN_POINT('Ctrl Pts',(-1.86998032796107,2.62474592330315,
15.6278845471724));
#253268=CARTESIAN_POINT('Ctrl Pts',(-1.87011255139784,2.62465171669732,
15.6278945917123));
#253269=CARTESIAN_POINT('Ctrl Pts',(-1.87037068053567,2.62446777533981,
15.627914200586));
#253270=CARTESIAN_POINT('Ctrl Pts',(-1.87049658689426,2.62437804152175,
15.6279237649827));
#253271=CARTESIAN_POINT('Ctrl Pts',(-1.87074260362601,2.62420267800289,
15.6279424532436));
#253272=CARTESIAN_POINT('Ctrl Pts',(-1.87086271457068,2.62411704912113,
15.6279515771623));
#253273=CARTESIAN_POINT('Ctrl Pts',(-1.87109760463354,2.62394956817173,
15.6279694197596));
#253274=CARTESIAN_POINT('Ctrl Pts',(-1.87121238425372,2.62386771682368,
15.6279781384862));
#253275=CARTESIAN_POINT('Ctrl Pts',(-1.87143702615721,2.62370749852932,
15.6279952022136));
#253276=CARTESIAN_POINT('Ctrl Pts',(-1.87154688889624,2.62362913220865,
15.6280035472578));
#253277=CARTESIAN_POINT('Ctrl Pts',(-1.87176206862088,2.62347562171071,
15.6280198918716));
#253278=CARTESIAN_POINT('Ctrl Pts',(-1.87186738598043,2.62340047810873,
15.6280278914773));
#253279=CARTESIAN_POINT('Ctrl Pts',(-1.87207380899988,2.62325317718014,
15.628043570611));
#253280=CARTESIAN_POINT('Ctrl Pts',(-1.87217491503742,2.62318102033269,
15.6280512501744));
#253281=CARTESIAN_POINT('Ctrl Pts',(-1.8723732168645,2.6230394799792,15.6280663121408));
#253282=CARTESIAN_POINT('Ctrl Pts',(-1.87247041297913,2.62297009690901,
15.6280736945745));
#253283=CARTESIAN_POINT('Ctrl Pts',(-1.87266116776736,2.6228339113356,15.6280881830205));
#253284=CARTESIAN_POINT('Ctrl Pts',(-1.87275472671033,2.62276710923786,
15.6280952890586));
#253285=CARTESIAN_POINT('Ctrl Pts',(-1.87293845464365,2.6226359106621,15.6281092435268));
#253286=CARTESIAN_POINT('Ctrl Pts',(-1.87302862389671,2.6225715145332,15.6281160919817));
#253287=CARTESIAN_POINT('Ctrl Pts',(-1.87320579768508,2.6224449686221,15.628129548405));
#253288=CARTESIAN_POINT('Ctrl Pts',(-1.8732928024416,2.62238281916521,15.6281361563945));
#253289=CARTESIAN_POINT('Ctrl Pts',(-1.87346385268252,2.62226062126964,
15.6281491475035));
#253290=CARTESIAN_POINT('Ctrl Pts',(-1.87354789836182,2.62220057312813,
15.6281555306417));
#253291=CARTESIAN_POINT('Ctrl Pts',(-1.87371321826917,2.622082444959,15.6281680863245));
#253292=CARTESIAN_POINT('Ctrl Pts',(-1.87379449268754,2.6220243651905,15.6281742588871));
#253293=CARTESIAN_POINT('Ctrl Pts',(-1.87395444223003,2.6219100519084,15.6281864065042));
#253294=CARTESIAN_POINT('Ctrl Pts',(-1.87403311752096,2.62185381863419,
15.6281923815745));
#253295=CARTESIAN_POINT('Ctrl Pts',(-1.8741880269229,2.6217430863875,15.6282041462247));
#253296=CARTESIAN_POINT('Ctrl Pts',(-1.8742642611832,2.62168858763453,15.6282099358189));
#253297=CARTESIAN_POINT('Ctrl Pts',(-1.87441443402612,2.62158122137698,
15.6282213405757));
#253298=CARTESIAN_POINT('Ctrl Pts',(-1.8744883727487,2.62152835406979,15.6282269557516));
#253299=CARTESIAN_POINT('Ctrl Pts',(-1.87463408876017,2.62142415559657,
15.6282380218747));
#253300=CARTESIAN_POINT('Ctrl Pts',(-1.87470586615115,2.62137282462936,
15.6282434728321));
#253301=CARTESIAN_POINT('Ctrl Pts',(-1.87484738340222,2.6212716110319,15.6282542199349));
#253302=CARTESIAN_POINT('Ctrl Pts',(-1.87491712340862,2.62122172854588,
15.6282595160937));
#253303=CARTESIAN_POINT('Ctrl Pts',(-1.87505468066352,2.62112333055405,
15.6282699623219));
#253304=CARTESIAN_POINT('Ctrl Pts',(-1.87512249803183,2.62107481519086,
15.6282751124025));
#253305=CARTESIAN_POINT('Ctrl Pts',(-1.87525631643748,2.62097907598431,
15.6282852745625));
#253306=CARTESIAN_POINT('Ctrl Pts',(-1.87532231756739,2.62093185228459,
15.6282902866508));
#253307=CARTESIAN_POINT('Ctrl Pts',(-1.87545260232371,2.62083862631521,
15.6283001803367));
#253308=CARTESIAN_POINT('Ctrl Pts',(-1.87551688603248,2.62079262417987,
15.6283050619422));
#253309=CARTESIAN_POINT('Ctrl Pts',(-1.87564382787277,2.62070177612791,
15.6283147016485));
#253310=CARTESIAN_POINT('Ctrl Pts',(-1.87570648608583,2.62065693033116,
15.6283194597569));
#253311=CARTESIAN_POINT('Ctrl Pts',(-1.87583026254316,2.62056833421241,
15.6283288589745));
#253312=CARTESIAN_POINT('Ctrl Pts',(-1.87589138087947,2.62052458398918,
15.6283335000921));
#253313=CARTESIAN_POINT('Ctrl Pts',(-1.87601215759189,2.62043812223277,
15.6283426714078));
#253314=CARTESIAN_POINT('Ctrl Pts',(-1.87607181600051,2.62039541082867,
15.6283472016098));
#253315=CARTESIAN_POINT('Ctrl Pts',(-1.87618974744126,2.62031097376496,
15.628356156762));
#253316=CARTESIAN_POINT('Ctrl Pts',(-1.87624802056013,2.62026924818443,
15.62836058172));
#253317=CARTESIAN_POINT('Ctrl Pts',(-1.87636325136359,2.62018673310514,
15.6283693316989));
#253318=CARTESIAN_POINT('Ctrl Pts',(-1.87642020909066,2.62014594370697,
15.6283736567242));
#253319=CARTESIAN_POINT('Ctrl Pts',(-1.87653287452234,2.62006525453705,
15.6283822118081));
#253320=CARTESIAN_POINT('Ctrl Pts',(-1.87658858230475,2.62002535483129,
15.6283864418736));
#253321=CARTESIAN_POINT('Ctrl Pts',(-1.87669880930821,2.61994640138662,
15.6283948117082));
#253322=CARTESIAN_POINT('Ctrl Pts',(-1.87675332857785,2.61990734772616,
15.6283989514819));
#253323=CARTESIAN_POINT('Ctrl Pts',(-1.87691024925368,2.61979493369505,
15.628410866767));
#253324=CARTESIAN_POINT('Ctrl Pts',(-1.87701264758681,2.61972156901586,
15.6284186419897));
#253325=CARTESIAN_POINT('Ctrl Pts',(-1.87721724407751,2.61957496492208,
15.6284341770814));
#253326=CARTESIAN_POINT('Ctrl Pts',(-1.87731944226978,2.61950172551658,
15.6284419369535));
#253327=CARTESIAN_POINT('Ctrl Pts',(-1.87752367084564,2.61935534887376,
15.628457443803));
#253328=CARTESIAN_POINT('Ctrl Pts',(-1.87762570123898,2.61928221165763,
15.6284651907815));
#253329=CARTESIAN_POINT('Ctrl Pts',(-1.87782962599359,2.61913601669723,
15.6284806742579));
#253330=CARTESIAN_POINT('Ctrl Pts',(-1.87793152035875,2.61906295897272,
15.6284884107563));
#253331=CARTESIAN_POINT('Ctrl Pts',(-1.87813520429762,2.61891690066106,
15.6285038756457));
#253332=CARTESIAN_POINT('Ctrl Pts',(-1.87823699387892,2.61884390008547,
15.6285116040374));
#253333=CARTESIAN_POINT('Ctrl Pts',(-1.88916629700184,2.6110047515994,15.6293414052162));
#253334=CARTESIAN_POINT('Ctrl Pts',(-1.89994576314816,2.6031713777499,15.6301589802004));
#253335=CARTESIAN_POINT('Ctrl Pts',(-1.92330019800536,2.58597750192634,
15.6319291915597));
#253336=CARTESIAN_POINT('Ctrl Pts',(-1.93585614447994,2.57659160546083,
15.6328801878));
#253337=CARTESIAN_POINT('Ctrl Pts',(-1.97029114301436,2.55045673400706,
15.6354878577077));
#253338=CARTESIAN_POINT('Ctrl Pts',(-1.992025123539,2.53351786041642,15.6371331960816));
#253339=CARTESIAN_POINT('Ctrl Pts',(-2.06270326845192,2.47696134302616,
15.6424918463238));
#253340=CARTESIAN_POINT('Ctrl Pts',(-2.11070594480127,2.43618627518454,
15.6461443635419));
#253341=CARTESIAN_POINT('Ctrl Pts',(-2.26113225222904,2.30062291250157,
15.6577446723567));
#253342=CARTESIAN_POINT('Ctrl Pts',(-2.35860798800838,2.20058094534829,
15.6655086373386));
#253343=CARTESIAN_POINT('Ctrl Pts',(-2.58189276261271,1.93947710011177,
15.6847610400964));
#253344=CARTESIAN_POINT('Ctrl Pts',(-2.69945017098937,1.77220108057633,
15.6962931780687));
#253345=CARTESIAN_POINT('Ctrl Pts',(-2.81790597933807,1.56421679439629,
15.7105634891989));
#253346=CARTESIAN_POINT('Ctrl Pts',(-2.83490093590786,1.53320084301653,
15.7126887227133));
#253347=CARTESIAN_POINT('Ctrl Pts',(-2.86105406119845,1.4835491188399,15.7160896322425));
#253348=CARTESIAN_POINT('Ctrl Pts',(-2.87054876905024,1.46509319244849,
15.7173534962801));
#253349=CARTESIAN_POINT('Ctrl Pts',(-2.88799489422117,1.43036050243356,
15.7197320938652));
#253350=CARTESIAN_POINT('Ctrl Pts',(-2.89598866102847,1.4141058411986,15.7208453003968));
#253351=CARTESIAN_POINT('Ctrl Pts',(-2.91361436388942,1.37748911567723,
15.7233535106355));
#253352=CARTESIAN_POINT('Ctrl Pts',(-2.92317062803156,1.35709187742357,
15.7247510474688));
#253353=CARTESIAN_POINT('Ctrl Pts',(-2.95116611824056,1.29566936795446,
15.7289613414877));
#253354=CARTESIAN_POINT('Ctrl Pts',(-2.96896050363633,1.25435791219073,
15.7317956530741));
#253355=CARTESIAN_POINT('Ctrl Pts',(-3.05056776920302,1.05342446855012,
15.7455996201529));
#253356=CARTESIAN_POINT('Ctrl Pts',(-3.10239654097435,0.889262344481743,
15.7569536220342));
#253357=CARTESIAN_POINT('Ctrl Pts',(-3.16408158506127,0.620831967904263,
15.7754694559997));
#253358=CARTESIAN_POINT('Ctrl Pts',(-3.18239798081183,0.518832589372446,
15.7824886074584));
#253359=CARTESIAN_POINT('Ctrl Pts',(-3.213736755432,0.278159051720678,15.7988503639988));
#253360=CARTESIAN_POINT('Ctrl Pts',(-3.22275000000011,0.139157621639885,
15.8081488051135));
#253361=CARTESIAN_POINT('Ctrl Pts',(-3.22275,-2.40758801783869E-12,15.8170600220821));
#253362=CARTESIAN_POINT('Origin',(0.,0.,-2.31077344927308));
#253363=CARTESIAN_POINT('',(-3.22275,-2.95105326763967E-13,17.3136802073254));
#253364=CARTESIAN_POINT('',(-3.22275,-9.68142638581001E-11,17.0635026513638));
#253365=CARTESIAN_POINT('',(-3.22275,-3.50678552687464E-13,-2.31077344927308));
#253366=CARTESIAN_POINT('Ctrl Pts',(-3.22275,-2.95105326763967E-13,17.3136802073254));
#253367=CARTESIAN_POINT('Ctrl Pts',(-3.22275,0.0221340923676759,17.3123467173463));
#253368=CARTESIAN_POINT('Ctrl Pts',(-3.22252197224614,0.0442671683107299,
17.3110064138654));
#253369=CARTESIAN_POINT('Ctrl Pts',(-3.22172476662145,0.0829541292113185,
17.3086508721571));
#253370=CARTESIAN_POINT('Ctrl Pts',(-3.22125592312253,0.0995094026487866,
17.30763877143));
#253371=CARTESIAN_POINT('Ctrl Pts',(-3.22000437711349,0.134239718201456,
17.3055066188397));
#253372=CARTESIAN_POINT('Ctrl Pts',(-3.21919534889757,0.15241317123072,
17.3043857851612));
#253373=CARTESIAN_POINT('Ctrl Pts',(-3.21688684133087,0.195966805603421,
17.3016869121675));
#253374=CARTESIAN_POINT('Ctrl Pts',(-3.21524081658911,0.221337685758173,
17.3001043773044));
#253375=CARTESIAN_POINT('Ctrl Pts',(-3.20842005984311,0.310183886830126,
17.2945247943625));
#253376=CARTESIAN_POINT('Ctrl Pts',(-3.20166449506103,0.373519576776114,
17.290479341787));
#253377=CARTESIAN_POINT('Ctrl Pts',(-3.18023109811769,0.530267269741759,
17.2802930108338));
#253378=CARTESIAN_POINT('Ctrl Pts',(-3.16331116959225,0.623308208622568,
17.2740903019683));
#253379=CARTESIAN_POINT('Ctrl Pts',(-3.09664976237345,0.916085756411005,
17.2541179036814));
#253380=CARTESIAN_POINT('Ctrl Pts',(-3.03186698205914,1.1118583672275,17.2400466897267));
#253381=CARTESIAN_POINT('Ctrl Pts',(-2.94713543724367,1.30404322042824,
17.2260342330169));
#253382=CARTESIAN_POINT('Ctrl Pts',(-2.94539505726775,1.30796940447217,
17.2257478988381));
#253383=CARTESIAN_POINT('Ctrl Pts',(-2.90711857334532,1.39385485934604,
17.219482928634));
#253384=CARTESIAN_POINT('Ctrl Pts',(-2.86717950771309,1.4742640048828,17.2135885508711));
#253385=CARTESIAN_POINT('Ctrl Pts',(-2.814299379662,1.57042549547647,17.2065902847308));
#253386=CARTESIAN_POINT('Ctrl Pts',(-2.80450308663605,1.58785380897961,
17.2053240717278));
#253387=CARTESIAN_POINT('Ctrl Pts',(-2.78883314886903,1.61513427838849,
17.2033468211409));
#253388=CARTESIAN_POINT('Ctrl Pts',(-2.78306819337775,1.62504784850364,
17.2026292975505));
#253389=CARTESIAN_POINT('Ctrl Pts',(-2.77267824925687,1.64269720661336,
17.2013539539672));
#253390=CARTESIAN_POINT('Ctrl Pts',(-2.76807370477194,1.65044441099464,
17.2007948896313));
#253391=CARTESIAN_POINT('Ctrl Pts',(-2.75682986245909,1.66918289875122,
17.1994443433879));
#253392=CARTESIAN_POINT('Ctrl Pts',(-2.75015730008055,1.68015394466326,
17.1986550094659));
#253393=CARTESIAN_POINT('Ctrl Pts',(-2.72908204504571,1.71434398155703,
17.1961985407646));
#253394=CARTESIAN_POINT('Ctrl Pts',(-2.71444913373042,1.73742053261069,
17.1945454897634));
#253395=CARTESIAN_POINT('Ctrl Pts',(-2.63696352269972,1.85624868133193,
17.1860441248338));
#253396=CARTESIAN_POINT('Ctrl Pts',(-2.56932665281482,1.94879487588652,
17.179458149908));
#253397=CARTESIAN_POINT('Ctrl Pts',(-2.3679877295483,2.195523934105,17.1614261217301));
#253398=CARTESIAN_POINT('Ctrl Pts',(-2.22437756788122,2.34090521190639,
17.1502111179564));
#253399=CARTESIAN_POINT('Ctrl Pts',(-1.98067281953882,2.5448015241628,17.1320534087972));
#253400=CARTESIAN_POINT('Ctrl Pts',(-1.88955072030984,2.61317313269437,
17.1254314875921));
#253401=CARTESIAN_POINT('Ctrl Pts',(-1.76841860602868,2.69440869501883,
17.1167088847139));
#253402=CARTESIAN_POINT('Ctrl Pts',(-1.7415650592748,2.71184321375901,17.1147802616634));
#253403=CARTESIAN_POINT('Ctrl Pts',(-1.69790169758138,2.73927538699542,
17.1116501121912));
#253404=CARTESIAN_POINT('Ctrl Pts',(-1.68125245274873,2.74952541077057,
17.1104578836641));
#253405=CARTESIAN_POINT('Ctrl Pts',(-1.64923023598831,2.76884012785152,
17.1081668247405));
#253406=CARTESIAN_POINT('Ctrl Pts',(-1.63387317535597,2.77792988600331,
17.1070689592419));
#253407=CARTESIAN_POINT('Ctrl Pts',(-1.59831272634414,2.79858103518565,
17.1045283651802));
#253408=CARTESIAN_POINT('Ctrl Pts',(-1.57805817918991,2.81005190690838,
17.1030824623203));
#253409=CARTESIAN_POINT('Ctrl Pts',(-1.51336376426435,2.84577062572734,
17.0984668925374));
#253410=CARTESIAN_POINT('Ctrl Pts',(-1.46847772326269,2.86919031288539,
17.0952684593487));
#253411=CARTESIAN_POINT('Ctrl Pts',(-1.24775096912036,2.9778200847304,17.0795514973403));
#253412=CARTESIAN_POINT('Ctrl Pts',(-1.06498364484869,3.04796391723238,
17.0665362728454));
#253413=CARTESIAN_POINT('Ctrl Pts',(-0.680188839499378,3.15678653021748,
17.0395428911061));
#253414=CARTESIAN_POINT('Ctrl Pts',(-0.478493101586672,3.19358961664113,
17.0256121868813));
#253415=CARTESIAN_POINT('Ctrl Pts',(-0.249236803563963,3.21319926940639,
17.0108140400078));
#253416=CARTESIAN_POINT('Ctrl Pts',(-0.223789751114986,3.2150718137908,
17.0091861445789));
#253417=CARTESIAN_POINT('Ctrl Pts',(-0.185647075553658,3.21742350292292,
17.0067706672793));
#253418=CARTESIAN_POINT('Ctrl Pts',(-0.172967125082773,3.21813008125857,
17.0059717417844));
#253419=CARTESIAN_POINT('Ctrl Pts',(-0.150097049295865,3.21926893113066,
17.0045384888951));
#253420=CARTESIAN_POINT('Ctrl Pts',(-0.13990843234287,3.21972781700876,
17.0039027376001));
#253421=CARTESIAN_POINT('Ctrl Pts',(-0.118995964128202,3.22057023864025,
17.0026037319432));
#253422=CARTESIAN_POINT('Ctrl Pts',(-0.108272104127282,3.22094859641696,
17.0019407630907));
#253423=CARTESIAN_POINT('Ctrl Pts',(-0.0803962523175764,3.22179273099283,
17.0002251719284));
#253424=CARTESIAN_POINT('Ctrl Pts',(-0.0632418268091256,3.22217511313888,
16.9991770382943));
#253425=CARTESIAN_POINT('Ctrl Pts',(0.0127754717451602,3.22326225782861,
16.9945629278761));
#253426=CARTESIAN_POINT('Ctrl Pts',(0.0716517921642314,3.22249123567755,
16.9910703011667));
#253427=CARTESIAN_POINT('Ctrl Pts',(0.242516430491498,3.21556785150419,
16.9810857233447));
#253428=CARTESIAN_POINT('Ctrl Pts',(0.354249598976605,3.20518352056544,
16.974744089558));
#253429=CARTESIAN_POINT('Ctrl Pts',(0.72462013875817,3.15115271151844,16.9537280380013));
#253430=CARTESIAN_POINT('Ctrl Pts',(0.978406290591503,3.08180897347347,
16.9392458621548));
#253431=CARTESIAN_POINT('Ctrl Pts',(1.2555277019743,2.96835993899214,16.9214720426081));
#253432=CARTESIAN_POINT('Ctrl Pts',(1.28981860436541,2.95362122417121,16.9192384434453));
#253433=CARTESIAN_POINT('Ctrl Pts',(1.34472817760542,2.92888175511218,16.9156020385143));
#253434=CARTESIAN_POINT('Ctrl Pts',(1.36551022615871,2.91925058668897,16.9142116914732));
#253435=CARTESIAN_POINT('Ctrl Pts',(1.40225588798655,2.90174306130282,16.9117274353743));
#253436=CARTESIAN_POINT('Ctrl Pts',(1.41826037357369,2.89395436419616,16.9106365718158));
#253437=CARTESIAN_POINT('Ctrl Pts',(1.45187855244221,2.87724798646731,16.9083260286129));
#253438=CARTESIAN_POINT('Ctrl Pts',(1.46947640981608,2.86830025627436,16.9071053388752));
#253439=CARTESIAN_POINT('Ctrl Pts',(1.51617747987021,2.84401225295308,16.903835312422));
#253440=CARTESIAN_POINT('Ctrl Pts',(1.54512927587043,2.82838739185515,16.9017760878545));
#253441=CARTESIAN_POINT('Ctrl Pts',(1.69758866867872,2.74306784674055,16.8907574276256));
#253442=CARTESIAN_POINT('Ctrl Pts',(1.81661903684733,2.66572963972247,16.8815276053146));
#253443=CARTESIAN_POINT('Ctrl Pts',(2.09487014210991,2.45762921491592,16.8584203764023));
#253444=CARTESIAN_POINT('Ctrl Pts',(2.24740047017898,2.31896676001625,16.8443551525489));
#253445=CARTESIAN_POINT('Ctrl Pts',(2.44907765487224,2.09690961777653,16.8243384914274));
#253446=CARTESIAN_POINT('Ctrl Pts',(2.50939325827023,2.02434188957196,16.8181336074175));
#253447=CARTESIAN_POINT('Ctrl Pts',(2.57867747593482,1.93311902359514,16.8108265978599));
#253448=CARTESIAN_POINT('Ctrl Pts',(2.59075974268731,1.91689610776433,16.8095452157002));
#253449=CARTESIAN_POINT('Ctrl Pts',(2.60948318804215,1.89125561195732,16.8075495492701));
#253450=CARTESIAN_POINT('Ctrl Pts',(2.61622773908035,1.8819146434649,16.806828587524));
#253451=CARTESIAN_POINT('Ctrl Pts',(2.62815337945841,1.86521002424517,16.8055503464257));
#253452=CARTESIAN_POINT('Ctrl Pts',(2.63335374223698,1.85786078360184,16.8049917871335));
#253453=CARTESIAN_POINT('Ctrl Pts',(2.64585063360493,1.84004207159366,16.8036465732125));
#253454=CARTESIAN_POINT('Ctrl Pts',(2.65311585941672,1.82955094211429,16.8028620191493));
#253455=CARTESIAN_POINT('Ctrl Pts',(2.67550204160882,1.79681106759752,16.8004358352164));
#253456=CARTESIAN_POINT('Ctrl Pts',(2.69040730192114,1.77441535253602,16.7988077975343));
#253457=CARTESIAN_POINT('Ctrl Pts',(2.7652757898506,1.65880994643778,16.790550097089));
#253458=CARTESIAN_POINT('Ctrl Pts',(2.82068795959516,1.56272991840634,16.7841663816454));
#253459=CARTESIAN_POINT('Ctrl Pts',(2.96196601678823,1.28566585130246,16.7665335636342));
#253460=CARTESIAN_POINT('Ctrl Pts',(3.03607966109708,1.09927335303053,16.7555234523345));
#253461=CARTESIAN_POINT('Ctrl Pts',(3.12644747462702,0.791233951948551,
16.7372244233817));
#253462=CARTESIAN_POINT('Ctrl Pts',(3.15391607491818,0.67344922870197,16.7302110681384));
#253463=CARTESIAN_POINT('Ctrl Pts',(3.18030848583938,0.522318535957917,
16.7210403679275));
#253464=CARTESIAN_POINT('Ctrl Pts',(3.18542539084461,0.490146591868484,
16.7190787806957));
#253465=CARTESIAN_POINT('Ctrl Pts',(3.19284872609865,0.438430806233579,
16.7159081073655));
#253466=CARTESIAN_POINT('Ctrl Pts',(3.19546544593634,0.418933308364208,
16.7147087691225));
#253467=CARTESIAN_POINT('Ctrl Pts',(3.20011134368749,0.38173592766078,16.712412616033));
#253468=CARTESIAN_POINT('Ctrl Pts',(3.20217258339169,0.364040734737923,
16.7113168504109));
#253469=CARTESIAN_POINT('Ctrl Pts',(3.20656255481724,0.323426681658127,
16.7087935246698));
#253470=CARTESIAN_POINT('Ctrl Pts',(3.20879244354722,0.30049833065699,16.7073629346496));
#253471=CARTESIAN_POINT('Ctrl Pts',(3.2150212509779,0.22844135100925,16.7028470770423));
#253472=CARTESIAN_POINT('Ctrl Pts',(3.21813885512107,0.179245578684574,
16.6997347738277));
#253473=CARTESIAN_POINT('Ctrl Pts',(3.2228147469549,0.0634225309152199,
16.6923354388443));
#253474=CARTESIAN_POINT('Ctrl Pts',(3.22343698247599,-0.00321804575677445,
16.68802202482));
#253475=CARTESIAN_POINT('Ctrl Pts',(3.21774612871357,-0.265810141087278,
16.6708117038668));
#253476=CARTESIAN_POINT('Ctrl Pts',(3.19562617229909,-0.46098259338203,
16.6575181695119));
#253477=CARTESIAN_POINT('Ctrl Pts',(3.12565512404511,-0.799194405453589,
16.6342131926274));
#253478=CARTESIAN_POINT('Ctrl Pts',(3.08525434098856,-0.94321086565765,
16.6242113304533));
#253479=CARTESIAN_POINT('Ctrl Pts',(3.0277367250502,-1.10426201086679,16.6132848444565));
#253480=CARTESIAN_POINT('Ctrl Pts',(3.02026621107624,-1.12453383100118,
16.6119145045287));
#253481=CARTESIAN_POINT('Ctrl Pts',(3.00839042980441,-1.1557873998848,16.60981124224));
#253482=CARTESIAN_POINT('Ctrl Pts',(3.00412774671895,-1.16682217308307,
16.6090704714741));
#253483=CARTESIAN_POINT('Ctrl Pts',(2.99616311240045,-1.18710716747405,
16.6077124425826));
#253484=CARTESIAN_POINT('Ctrl Pts',(2.99247899861826,-1.19636376997639,
16.6070942060089));
#253485=CARTESIAN_POINT('Ctrl Pts',(2.98393121763331,-1.21755414941524,
16.6056821758134));
#253486=CARTESIAN_POINT('Ctrl Pts',(2.9790388460684,-1.22947597983675,16.604890093675));
#253487=CARTESIAN_POINT('Ctrl Pts',(2.96345675790082,-1.26680760493885,
16.6024161756487));
#253488=CARTESIAN_POINT('Ctrl Pts',(2.9525121542454,-1.29211050486844,16.6007487099799));
#253489=CARTESIAN_POINT('Ctrl Pts',(2.89354045319857,-1.42378438141158,
16.5921047489965));
#253490=CARTESIAN_POINT('Ctrl Pts',(2.84008144207243,-1.52763905857051,
16.5854004228981));
#253491=CARTESIAN_POINT('Ctrl Pts',(2.67694755225337,-1.80625561236203,
16.5671318092718));
#253492=CARTESIAN_POINT('Ctrl Pts',(2.55597111123807,-1.97373258313,16.5557937671983));
#253493=CARTESIAN_POINT('Ctrl Pts',(2.34742527470843,-2.210820968182,16.5377223823779));
#253494=CARTESIAN_POINT('Ctrl Pts',(2.27087699831267,-2.28937741023895,
16.5313377541164));
#253495=CARTESIAN_POINT('Ctrl Pts',(2.16720384516061,-2.38544589102352,
16.5228826836516));
#253496=CARTESIAN_POINT('Ctrl Pts',(2.14361043998848,-2.40666964488602,
16.5209706780231));
#253497=CARTESIAN_POINT('Ctrl Pts',(2.10502660068808,-2.44036072426009,
16.5178609328343));
#253498=CARTESIAN_POINT('Ctrl Pts',(2.09022938269425,-2.45304679041607,
16.5166722672198));
#253499=CARTESIAN_POINT('Ctrl Pts',(2.06165188942269,-2.47710075296049,
16.5143836203004));
#253500=CARTESIAN_POINT('Ctrl Pts',(2.04789034910675,-2.4884898535557,16.5132845605839));
#253501=CARTESIAN_POINT('Ctrl Pts',(2.01588003747714,-2.51453635297142,
16.5107346518562));
#253502=CARTESIAN_POINT('Ctrl Pts',(1.99756502286316,-2.52911038298497,
16.5092805512584));
#253503=CARTESIAN_POINT('Ctrl Pts',(1.93856974806943,-2.57501481244328,
16.504611085909));
#253504=CARTESIAN_POINT('Ctrl Pts',(1.89730045811374,-2.60557180716549,
16.5013659976067));
#253505=CARTESIAN_POINT('Ctrl Pts',(1.73574744841238,-2.71931678159805,
16.4887373880845));
#253506=CARTESIAN_POINT('Ctrl Pts',(1.61059722078433,-2.79525853746499,
16.4790985113957));
#253507=CARTESIAN_POINT('Ctrl Pts',(1.25750737924223,-2.9779119387294,16.4524457426059));
#253508=CARTESIAN_POINT('Ctrl Pts',(1.02153384805029,-3.06688119368647,
16.4351499102641));
#253509=CARTESIAN_POINT('Ctrl Pts',(0.75205986533862,-3.13388209683342,
16.4172764779589));
#253510=CARTESIAN_POINT('Ctrl Pts',(0.726426171640689,-3.13992295367267,
16.4155951667989));
#253511=CARTESIAN_POINT('Ctrl Pts',(0.688131035205691,-3.1484535248025,
16.413114331227));
#253512=CARTESIAN_POINT('Ctrl Pts',(0.675524691433461,-3.15118236916276,
16.4123026352241));
#253513=CARTESIAN_POINT('Ctrl Pts',(0.653773988568329,-3.15575413129464,
16.4109111015018));
#253514=CARTESIAN_POINT('Ctrl Pts',(0.644637493471649,-3.1576331440656,
16.410329292817));
#253515=CARTESIAN_POINT('Ctrl Pts',(0.625270809779749,-3.16152853759815,
16.4091019555778));
#253516=CARTESIAN_POINT('Ctrl Pts',(0.615038737212195,-3.16353499063816,
16.4084570141463));
#253517=CARTESIAN_POINT('Ctrl Pts',(0.589321173864843,-3.16844857296294,
16.4068443813674));
#253518=CARTESIAN_POINT('Ctrl Pts',(0.573823539471145,-3.17129190932853,
16.4058802064245));
#253519=CARTESIAN_POINT('Ctrl Pts',(0.512749774940117,-3.18203468691038,
16.4021082538866));
#253520=CARTESIAN_POINT('Ctrl Pts',(0.467024373763913,-3.18906660359083,
16.399344807801));
#253521=CARTESIAN_POINT('Ctrl Pts',(0.344584765653447,-3.20520587356563,
16.3920686167063));
#253522=CARTESIAN_POINT('Ctrl Pts',(0.267665652606262,-3.21254414897306,
16.3876258948032));
#253523=CARTESIAN_POINT('Ctrl Pts',(-0.0394683104706741,-3.23073601011831,
16.370143786787));
#253524=CARTESIAN_POINT('Ctrl Pts',(-0.270284306237842,-3.21965260845996,
16.3575299719374));
#253525=CARTESIAN_POINT('Ctrl Pts',(-0.597666587090349,-3.16845371827434,
16.3384995093227));
#253526=CARTESIAN_POINT('Ctrl Pts',(-0.696588235332892,-3.14818460744293,
16.3326035463904));
#253527=CARTESIAN_POINT('Ctrl Pts',(-0.824311183577491,-3.11569925318654,
16.3247137261901));
#253528=CARTESIAN_POINT('Ctrl Pts',(-0.854120780753608,-3.10765962685984,
16.3228524222783));
#253529=CARTESIAN_POINT('Ctrl Pts',(-0.902375066969929,-3.09389875584659,
16.319804923058));
#253530=CARTESIAN_POINT('Ctrl Pts',(-0.920892344947074,-3.08843771780778,
16.31862713244));
#253531=CARTESIAN_POINT('Ctrl Pts',(-0.956504638005302,-3.07758634363401,
16.3163454087994));
#253532=CARTESIAN_POINT('Ctrl Pts',(-0.973605980380738,-3.07221910018391,
16.3152422621458));
#253533=CARTESIAN_POINT('Ctrl Pts',(-1.01333562459316,-3.05938494558483,
16.3126616624615));
#253534=CARTESIAN_POINT('Ctrl Pts',(-1.03592742299457,-3.05180924355685,
16.3111807028089));
#253535=CARTESIAN_POINT('Ctrl Pts',(-1.1092145816413,-3.02632634819424,
16.3063312626484));
#253536=CARTESIAN_POINT('Ctrl Pts',(-1.15954407470954,-3.00740172582723,
16.3029297414502));
#253537=CARTESIAN_POINT('Ctrl Pts',(-1.37334295423957,-2.92084559793913,
16.2881646956274));
#253538=CARTESIAN_POINT('Ctrl Pts',(-1.5315456011658,-2.84108473286912,
16.2764119305378));
#253539=CARTESIAN_POINT('Ctrl Pts',(-1.87041256869448,-2.63368022947694,
16.24963057482));
#253540=CARTESIAN_POINT('Ctrl Pts',(-2.04614434337394,-2.49960409013341,
16.2345667581741));
#253541=CARTESIAN_POINT('Ctrl Pts',(-2.22645035693762,-2.33018496176872,
16.2186749359695));
#253542=CARTESIAN_POINT('Ctrl Pts',(-2.24584962092683,-2.31149361609812,
16.216959430421));
#253543=CARTESIAN_POINT('Ctrl Pts',(-2.274095498464,-2.28358714326564,16.214456160969));
#253544=CARTESIAN_POINT('Ctrl Pts',(-2.28312481337023,-2.27455966649519,
16.2136551057796));
#253545=CARTESIAN_POINT('Ctrl Pts',(-2.29909825237014,-2.25839852230205,
16.212236885685));
#253546=CARTESIAN_POINT('Ctrl Pts',(-2.30606323789365,-2.25128607926038,
16.2116181380409));
#253547=CARTESIAN_POINT('Ctrl Pts',(-2.32129584480191,-2.235586108604,16.2102641719657));
#253548=CARTESIAN_POINT('Ctrl Pts',(-2.32954886105725,-2.22698490396622,
16.2095300525521));
#253549=CARTESIAN_POINT('Ctrl Pts',(-2.35232256966274,-2.20298525546188,
16.2075021070763));
#253550=CARTESIAN_POINT('Ctrl Pts',(-2.3667398666266,-2.18748896332091,
16.2062157823282));
#253551=CARTESIAN_POINT('Ctrl Pts',(-2.47734929976644,-2.06622767400258,
16.1963169852764));
#253552=CARTESIAN_POINT('Ctrl Pts',(-2.56657165419683,-1.95429681063372,
16.1881495374682));
#253553=CARTESIAN_POINT('Ctrl Pts',(-2.73615200715337,-1.70981634247521,
16.1713840028849));
#253554=CARTESIAN_POINT('Ctrl Pts',(-2.81498256581248,-1.57666516886901,
16.1628216381901));
#253555=CARTESIAN_POINT('Ctrl Pts',(-2.94660823852137,-1.31275385016655,
16.1461114078824));
#253556=CARTESIAN_POINT('Ctrl Pts',(-3.0009795661544,-1.18318971804714,
16.1380162340517));
#253557=CARTESIAN_POINT('Ctrl Pts',(-3.05772614337729,-1.01861008598675,
16.1276203509488));
#253558=CARTESIAN_POINT('Ctrl Pts',(-3.06822107645807,-0.986546994701005,
16.1255904250421));
#253559=CARTESIAN_POINT('Ctrl Pts',(-3.08410983781181,-0.935297259735878,
16.1223357334479));
#253560=CARTESIAN_POINT('Ctrl Pts',(-3.08983254843574,-0.916214631412177,
16.1211216765873));
#253561=CARTESIAN_POINT('Ctrl Pts',(-3.10032239091618,-0.880019411052094,
16.1188142289955));
#253562=CARTESIAN_POINT('Ctrl Pts',(-3.10512569364858,-0.862918013593345,
16.1177220571399));
#253563=CARTESIAN_POINT('Ctrl Pts',(-3.11571471317966,-0.823983923748545,
16.1152307279973));
#253564=CARTESIAN_POINT('Ctrl Pts',(-3.12141273010731,-0.802128547994979,
16.1138288097059));
#253565=CARTESIAN_POINT('Ctrl Pts',(-3.13280450001761,-0.756473595440243,
16.1108925583858));
#253566=CARTESIAN_POINT('Ctrl Pts',(-3.13845782726533,-0.73266551019231,
16.1093570354481));
#253567=CARTESIAN_POINT('Ctrl Pts',(-3.15804586205618,-0.645783464476143,
16.1037368946275));
#253568=CARTESIAN_POINT('Ctrl Pts',(-3.17035384394086,-0.58236201985508,
16.099602235878));
#253569=CARTESIAN_POINT('Ctrl Pts',(-3.20870733247854,-0.347134940052192,
16.084146813724));
#253570=CARTESIAN_POINT('Ctrl Pts',(-3.2227500000076,-0.173697287956936,
16.0724966069576));
#253571=CARTESIAN_POINT('Ctrl Pts',(-3.22275,1.40950411064988E-10,16.0607604048379));
#253572=CARTESIAN_POINT('',(-3.22274995225749,-0.000554729076348744,15.8170955430526));
#253573=CARTESIAN_POINT('Ctrl Pts',(-3.22275,-2.40695369623669E-12,15.8170600220821));
#253574=CARTESIAN_POINT('Ctrl Pts',(-3.22275,-0.000184909417959676,15.8170718631003));
#253575=CARTESIAN_POINT('Ctrl Pts',(-3.22274998408588,-0.000369819109989661,
15.817083703424));
#253576=CARTESIAN_POINT('Ctrl Pts',(-3.22274995225749,-0.000554729076422944,
15.8170955430526));
#253577=CARTESIAN_POINT('Ctrl Pts',(-3.22274995179883,-0.000557387331382724,
15.8170957132584));
#253578=CARTESIAN_POINT('Ctrl Pts',(-3.22274622160231,-0.0221249580166652,
15.8184766657508));
#253579=CARTESIAN_POINT('Ctrl Pts',(-3.22252598667833,-0.0436927045790141,
15.8198479352303));
#253580=CARTESIAN_POINT('Ctrl Pts',(-3.22187697376683,-0.075737791702557,
15.8218693625049));
#253581=CARTESIAN_POINT('Ctrl Pts',(-3.22161357567128,-0.0862173026417503,
15.8225278756371));
#253582=CARTESIAN_POINT('Ctrl Pts',(-3.22101093159705,-0.106293693097024,
15.8237843297505));
#253583=CARTESIAN_POINT('Ctrl Pts',(-3.22067991482886,-0.115890747819191,
15.8243827088868));
#253584=CARTESIAN_POINT('Ctrl Pts',(-3.21987769869423,-0.136477688288322,
15.8256613105752));
#253585=CARTESIAN_POINT('Ctrl Pts',(-3.21939312303517,-0.147466883328992,
15.8263407862734));
#253586=CARTESIAN_POINT('Ctrl Pts',(-3.21798302430099,-0.176111864232991,
15.8281045242701));
#253587=CARTESIAN_POINT('Ctrl Pts',(-3.2169684492768,-0.193763159298838,
15.8291840051577));
#253588=CARTESIAN_POINT('Ctrl Pts',(-3.21213045874513,-0.267356513596312,
15.8336573008867));
#253589=CARTESIAN_POINT('Ctrl Pts',(-3.2069924509369,-0.323205552586246,
15.8369860387962));
#253590=CARTESIAN_POINT('Ctrl Pts',(-3.17713258251152,-0.575421495207651,
15.8518325092794));
#253591=CARTESIAN_POINT('Ctrl Pts',(-3.13581152067092,-0.769402875317582,
15.8627585826249));
#253592=CARTESIAN_POINT('Ctrl Pts',(-3.02581556858593,-1.12255294862985,
15.8835199118992));
#253593=CARTESIAN_POINT('Ctrl Pts',(-2.96162936142449,-1.28235233319276,
15.8932765193052));
#253594=CARTESIAN_POINT('Ctrl Pts',(-2.86496036934638,-1.47653082854844,
15.9061192481573));
#253595=CARTESIAN_POINT('Ctrl Pts',(-2.84407206164505,-1.51637561926554,
15.908808834336));
#253596=CARTESIAN_POINT('Ctrl Pts',(-2.81148298794204,-1.57549623809707,
15.9128886266384));
#253597=CARTESIAN_POINT('Ctrl Pts',(-2.80040229238955,-1.59510875775955,
15.9142570789168));
#253598=CARTESIAN_POINT('Ctrl Pts',(-2.78012518211908,-1.63013608690666,
15.9167290501684));
#253599=CARTESIAN_POINT('Ctrl Pts',(-2.77100379326756,-1.6455934028116,
15.9178298513538));
#253600=CARTESIAN_POINT('Ctrl Pts',(-2.75108842276154,-1.67870732844369,
15.9202099781359));
#253601=CARTESIAN_POINT('Ctrl Pts',(-2.74025257742111,-1.69633769771502,
15.921490787352));
#253602=CARTESIAN_POINT('Ctrl Pts',(-2.71058483821589,-1.74358222885284,
15.9249604841978));
#253603=CARTESIAN_POINT('Ctrl Pts',(-2.69143819782519,-1.77299448008669,
15.9271608109834));
#253604=CARTESIAN_POINT('Ctrl Pts',(-2.57221442698824,-1.94975835636564,
15.9406361298049));
#253605=CARTESIAN_POINT('Ctrl Pts',(-2.46055773983435,-2.08889513110084,
15.9523472752103));
#253606=CARTESIAN_POINT('Ctrl Pts',(-2.25174993994693,-2.308991860177,15.9727083442235));
#253607=CARTESIAN_POINT('Ctrl Pts',(-2.16027298165056,-2.39479456253173,
15.9812133661752));
#253608=CARTESIAN_POINT('Ctrl Pts',(-1.96312563952537,-2.55920292059544,
15.9984900944032));
#253609=CARTESIAN_POINT('Ctrl Pts',(-1.85715294909779,-2.63711433568977,
16.0072386647248));
#253610=CARTESIAN_POINT('Ctrl Pts',(-1.72862252117434,-2.72000825678943,
16.0170057584367));
#253611=CARTESIAN_POINT('Ctrl Pts',(-1.71041926112583,-2.7314916705471,
16.0183702550734));
#253612=CARTESIAN_POINT('Ctrl Pts',(-1.68202801344849,-2.74900698954575,
16.0204678640938));
#253613=CARTESIAN_POINT('Ctrl Pts',(-1.67191990156382,-2.75516633249483,
16.0212087458991));
#253614=CARTESIAN_POINT('Ctrl Pts',(-1.65301397657644,-2.76654423063013,
16.022583121127));
#253615=CARTESIAN_POINT('Ctrl Pts',(-1.64422522596628,-2.77177661370795,
16.0232174527754));
#253616=CARTESIAN_POINT('Ctrl Pts',(-1.62389076141627,-2.78375198492425,
16.0246747806862));
#253617=CARTESIAN_POINT('Ctrl Pts',(-1.61232783325735,-2.79046506718093,
16.0254958836393));
#253618=CARTESIAN_POINT('Ctrl Pts',(-1.5746363402173,-2.81203509192934,
16.0281489765303));
#253619=CARTESIAN_POINT('Ctrl Pts',(-1.54834082467919,-2.82659898074328,
16.0299635681521));
#253620=CARTESIAN_POINT('Ctrl Pts',(-1.38271429106032,-2.91532694106923,
16.0411919241792));
#253621=CARTESIAN_POINT('Ctrl Pts',(-1.23828017586229,-2.97954751102875,
16.0501093534808));
#253622=CARTESIAN_POINT('Ctrl Pts',(-0.962038282793848,-3.07879899258903,
16.0665765586549));
#253623=CARTESIAN_POINT('Ctrl Pts',(-0.83160184226044,-3.1165619399603,
16.0741261161211));
#253624=CARTESIAN_POINT('Ctrl Pts',(-0.613107506517491,-3.16512095736399,
16.08684228272));
#253625=CARTESIAN_POINT('Ctrl Pts',(-0.5262938833522,-3.18070820382678,
16.091910869633));
#253626=CARTESIAN_POINT('Ctrl Pts',(-0.378685421786308,-3.20100233218306,
16.1006438979073));
#253627=CARTESIAN_POINT('Ctrl Pts',(-0.318196972275388,-3.20757986127694,
16.1042544513831));
#253628=CARTESIAN_POINT('Ctrl Pts',(-0.232325759855905,-3.21446468807705,
16.1094422049998));
#253629=CARTESIAN_POINT('Ctrl Pts',(-0.207067804046164,-3.2161905040946,
16.1109756460109));
#253630=CARTESIAN_POINT('Ctrl Pts',(-0.163340418892367,-3.21866106363281,
16.1136445378053));
#253631=CARTESIAN_POINT('Ctrl Pts',(-0.144879848093298,-3.21954483466493,
16.1147756283059));
#253632=CARTESIAN_POINT('Ctrl Pts',(-0.109339430121923,-3.22093998814506,
16.1169619951952));
#253633=CARTESIAN_POINT('Ctrl Pts',(-0.0922610748377415,-3.22147441313818,
16.1180165169475));
#253634=CARTESIAN_POINT('Ctrl Pts',(-0.0472124967724841,-3.222525581534,
16.1208087410951));
#253635=CARTESIAN_POINT('Ctrl Pts',(-0.0192388792029165,-3.22281397702412,
16.1225534499698));
#253636=CARTESIAN_POINT('Ctrl Pts',(0.0823263794919396,-3.22253871489787,
16.128929040253));
#253637=CARTESIAN_POINT('Ctrl Pts',(0.155884887511749,-3.2198186154196,
16.1336253518705));
#253638=CARTESIAN_POINT('Ctrl Pts',(0.461355511051301,-3.19803080783324,
16.1534638085808));
#253639=CARTESIAN_POINT('Ctrl Pts',(0.690930735350458,-3.15639631513609,
16.1692481628474));
#253640=CARTESIAN_POINT('Ctrl Pts',(1.03979238434662,-3.05322140805999,
16.1937745719172));
#253641=CARTESIAN_POINT('Ctrl Pts',(1.16322163631314,-3.00836349501601,
16.202547860252));
#253642=CARTESIAN_POINT('Ctrl Pts',(1.31051402350762,-2.94440701197638,
16.212885232079));
#253643=CARTESIAN_POINT('Ctrl Pts',(1.33728616539138,-2.93234471181988,
16.2147583917237));
#253644=CARTESIAN_POINT('Ctrl Pts',(1.37602100144484,-2.91425170713505,
16.2174561922053));
#253645=CARTESIAN_POINT('Ctrl Pts',(1.38811606377214,-2.9085100338793,16.2182968122072));
#253646=CARTESIAN_POINT('Ctrl Pts',(1.40936819328606,-2.89825862074025,
16.2197702632288));
#253647=CARTESIAN_POINT('Ctrl Pts',(1.41854007594948,-2.89378053760286,
16.2204049558762));
#253648=CARTESIAN_POINT('Ctrl Pts',(1.43842646828937,-2.88395392666391,
16.2217783742875));
#253649=CARTESIAN_POINT('Ctrl Pts',(1.44913256573407,-2.87858919843438,
16.2225161018952));
#253650=CARTESIAN_POINT('Ctrl Pts',(1.47902961237556,-2.86339899119203,
16.2245722246131));
#253651=CARTESIAN_POINT('Ctrl Pts',(1.49815261827548,-2.85344023343766,
16.2258827367525));
#253652=CARTESIAN_POINT('Ctrl Pts',(1.62592385741443,-2.78526171305187,
16.2346172787183));
#253653=CARTESIAN_POINT('Ctrl Pts',(1.73126660821293,-2.72103542144094,
16.2417142090766));
#253654=CARTESIAN_POINT('Ctrl Pts',(2.05989203463373,-2.49384474386652,
16.2643414192517));
#253655=CARTESIAN_POINT('Ctrl Pts',(2.26595431378871,-2.30821730218388,
16.2794198053766));
#253656=CARTESIAN_POINT('Ctrl Pts',(2.4833673846921,-2.05483041340132,16.2990259904808));
#253657=CARTESIAN_POINT('Ctrl Pts',(2.51972794221395,-2.01007763326026,
16.3024524410071));
#253658=CARTESIAN_POINT('Ctrl Pts',(2.56998461622273,-1.94471379961092,
16.3074206487033));
#253659=CARTESIAN_POINT('Ctrl Pts',(2.58487432635543,-1.92487852985945,
16.3089236545582));
#253660=CARTESIAN_POINT('Ctrl Pts',(2.61040692230232,-1.89003483897039,
16.3115569687875));
#253661=CARTESIAN_POINT('Ctrl Pts',(2.62115310125099,-1.87510330126874,
16.3126832426938));
#253662=CARTESIAN_POINT('Ctrl Pts',(2.64170677548839,-1.84602254475498,
16.3148729948378));
#253663=CARTESIAN_POINT('Ctrl Pts',(2.65152990908911,-1.83188510732037,
16.3159358271638));
#253664=CARTESIAN_POINT('Ctrl Pts',(2.67741079878549,-1.79399305742347,
16.3187803634508));
#253665=CARTESIAN_POINT('Ctrl Pts',(2.69326531372663,-1.77010212724308,
16.3205695758416));
#253666=CARTESIAN_POINT('Ctrl Pts',(2.75131995214272,-1.68003453780286,
16.3273008251798));
#253667=CARTESIAN_POINT('Ctrl Pts',(2.79141412785753,-1.61253930783438,
16.3323181860534));
#253668=CARTESIAN_POINT('Ctrl Pts',(2.93824792845134,-1.34344168877698,
16.3522257070446));
#253669=CARTESIAN_POINT('Ctrl Pts',(3.02592023151001,-1.13221853590028,
16.3677075295291));
#253670=CARTESIAN_POINT('Ctrl Pts',(3.12729129717424,-0.789277731108036,
16.3918111988924));
#253671=CARTESIAN_POINT('Ctrl Pts',(3.15649968118027,-0.662892249386649,
16.4004726069453));
#253672=CARTESIAN_POINT('Ctrl Pts',(3.18286670129963,-0.506289980585192,
16.4106943510359));
#253673=CARTESIAN_POINT('Ctrl Pts',(3.18732295208164,-0.477433260996854,
16.4125567535897));
#253674=CARTESIAN_POINT('Ctrl Pts',(3.19324569101909,-0.43529066170121,
16.4152420619719));
#253675=CARTESIAN_POINT('Ctrl Pts',(3.19502255949809,-0.42205078166261,
16.4160807470759));
#253676=CARTESIAN_POINT('Ctrl Pts',(3.19801142459324,-0.398678577935066,
16.4175520825572));
#253677=CARTESIAN_POINT('Ctrl Pts',(3.19925769030617,-0.388551053522888,
16.4181865753791));
#253678=CARTESIAN_POINT('Ctrl Pts',(3.20186437669141,-0.366505064229631,
16.4195610396806));
#253679=CARTESIAN_POINT('Ctrl Pts',(3.20320637587783,-0.354584789629988,
16.4202999988224));
#253680=CARTESIAN_POINT('Ctrl Pts',(3.20678394364183,-0.321127868673782,
16.4223629335847));
#253681=CARTESIAN_POINT('Ctrl Pts',(3.20886912132477,-0.299575347016243,
16.4236789429605));
#253682=CARTESIAN_POINT('Ctrl Pts',(3.22168472647574,-0.151564111531097,
16.4326380981155));
#253683=CARTESIAN_POINT('Ctrl Pts',(3.22515540721181,-0.0245743919984683,
16.4399342120575));
#253684=CARTESIAN_POINT('Ctrl Pts',(3.21987394639421,0.141720761726979,
16.449347432257));
#253685=CARTESIAN_POINT('Ctrl Pts',(3.21789849625259,0.181114195381315,
16.4515667027689));
#253686=CARTESIAN_POINT('Ctrl Pts',(3.20642571309684,0.34843243615402,16.4609804148846));
#253687=CARTESIAN_POINT('Ctrl Pts',(3.19001859213704,0.475764498709609,
16.4681185509057));
#253688=CARTESIAN_POINT('Ctrl Pts',(3.14829381116591,0.695286644568743,
16.4807748549173));
#253689=CARTESIAN_POINT('Ctrl Pts',(3.12638749826881,0.787957355092488,
16.4862284074992));
#253690=CARTESIAN_POINT('Ctrl Pts',(3.08288132279225,0.941322171998878,
16.4955538559582));
#253691=CARTESIAN_POINT('Ctrl Pts',(3.0635057862567,1.00258474115839,16.4993611325552));
#253692=CARTESIAN_POINT('Ctrl Pts',(3.03378703663959,1.08762204635964,16.5047825126736));
#253693=CARTESIAN_POINT('Ctrl Pts',(3.02496765374033,1.11191552480378,16.5063471625471));
#253694=CARTESIAN_POINT('Ctrl Pts',(3.00930936095517,1.15348157065268,16.509052873603));
#253695=CARTESIAN_POINT('Ctrl Pts',(3.00261145178311,1.17080613718983,16.510189235546));
#253696=CARTESIAN_POINT('Ctrl Pts',(2.98867094749735,1.20595760955327,16.5125129830378));
#253697=CARTESIAN_POINT('Ctrl Pts',(2.98141771564702,1.22377946047961,16.513700686603));
#253698=CARTESIAN_POINT('Ctrl Pts',(2.96274651106771,1.26850495315987,16.5167060002835));
#253699=CARTESIAN_POINT('Ctrl Pts',(2.9511215314979,1.29531977589778,16.518530502663));
#253700=CARTESIAN_POINT('Ctrl Pts',(2.90525031244094,1.39730502098797,16.5255589108867));
#253701=CARTESIAN_POINT('Ctrl Pts',(2.86848580199242,1.47130145085753,16.5308470023867));
#253702=CARTESIAN_POINT('Ctrl Pts',(2.72147463280352,1.74069087486416,16.5508167466326));
#253703=CARTESIAN_POINT('Ctrl Pts',(2.59377440525216,1.92580913902128,16.5660488785749));
#253704=CARTESIAN_POINT('Ctrl Pts',(2.36449895855361,2.19356116169624,16.5898036897366));
#253705=CARTESIAN_POINT('Ctrl Pts',(2.27533289806995,2.28592041707759,16.5983721715885));
#253706=CARTESIAN_POINT('Ctrl Pts',(2.15949814495306,2.39238994956994,16.6084977425058));
#253707=CARTESIAN_POINT('Ctrl Pts',(2.13783883425448,2.411764325689,16.6103511232412));
#253708=CARTESIAN_POINT('Ctrl Pts',(2.10586298439437,2.4395975932194,16.6130259460462));
#253709=CARTESIAN_POINT('Ctrl Pts',(2.09575194187463,2.4482890226771,16.6138630006887));
#253710=CARTESIAN_POINT('Ctrl Pts',(2.07780974626949,2.46351949288468,16.6153325561184));
#253711=CARTESIAN_POINT('Ctrl Pts',(2.07000111296112,2.470084418722,16.6159668831856));
#253712=CARTESIAN_POINT('Ctrl Pts',(2.05292954398928,2.48429912788716,16.6173422428042));
#253713=CARTESIAN_POINT('Ctrl Pts',(2.04365490896799,2.4919342874903,16.6180822509565));
#253714=CARTESIAN_POINT('Ctrl Pts',(2.0174836024499,2.51323490752009,16.6201509927765));
#253715=CARTESIAN_POINT('Ctrl Pts',(2.00049075089985,2.52678186628411,16.6214716889104));
#253716=CARTESIAN_POINT('Ctrl Pts',(1.88063844739336,2.62036290377296,16.6306406404235));
#253717=CARTESIAN_POINT('Ctrl Pts',(1.77313232798418,2.69427394813547,16.6381226741575));
#253718=CARTESIAN_POINT('Ctrl Pts',(1.63111676052175,2.77971716298425,16.647490780855));
#253719=CARTESIAN_POINT('Ctrl Pts',(1.60050100625079,2.79745705542498,16.649481414978));
#253720=CARTESIAN_POINT('Ctrl Pts',(1.45745246414847,2.87722743925628,16.6586754796325));
#253721=CARTESIAN_POINT('Ctrl Pts',(1.34166887955809,2.93300690710608,16.6658206704963));
#253722=CARTESIAN_POINT('Ctrl Pts',(1.13459312079449,3.01793295285181,16.6784962946494));
#253723=CARTESIAN_POINT('Ctrl Pts',(1.04475825284476,3.05019658122446,16.6839623205248));
#253724=CARTESIAN_POINT('Ctrl Pts',(0.892159887368074,3.09746821841046,
16.6933068648918));
#253725=CARTESIAN_POINT('Ctrl Pts',(0.830137409549292,3.11466365596257,
16.6971203977656));
#253726=CARTESIAN_POINT('Ctrl Pts',(0.742528122999598,3.13615024127863,
16.702549192892));
#253727=CARTESIAN_POINT('Ctrl Pts',(0.717338899430118,3.14200751011786,
16.7041148145031));
#253728=CARTESIAN_POINT('Ctrl Pts',(0.673938702284614,3.15155030094685,
16.7068216774083));
#253729=CARTESIAN_POINT('Ctrl Pts',(0.65576109741242,3.15538270807807,16.7079582088303));
#253730=CARTESIAN_POINT('Ctrl Pts',(0.618695246035927,3.16286322843693,
16.7102818298027));
#253731=CARTESIAN_POINT('Ctrl Pts',(0.599805463360756,3.16649980104512,
16.7114692331996));
#253732=CARTESIAN_POINT('Ctrl Pts',(0.552159498864665,3.1752307455466,16.7144728374886));
#253733=CARTESIAN_POINT('Ctrl Pts',(0.523364987499283,3.18010367758402,
16.7162959145612));
#253734=CARTESIAN_POINT('Ctrl Pts',(0.413053825467058,3.19723302633357,
16.7233120228146));
#253735=CARTESIAN_POINT('Ctrl Pts',(0.331149816409503,3.2067507471146,16.7285888616959));
#253736=CARTESIAN_POINT('Ctrl Pts',(0.0251911439521461,3.23045872347178,
16.7485558893281));
#253737=CARTESIAN_POINT('Ctrl Pts',(-0.199773368623699,3.22437068052218,
16.7637982351436));
#253738=CARTESIAN_POINT('Ctrl Pts',(-0.549444883315904,3.17815831441755,
16.7875673142268));
#253739=CARTESIAN_POINT('Ctrl Pts',(-0.675539618838877,3.15376477163643,
16.7961396045584));
#253740=CARTESIAN_POINT('Ctrl Pts',(-0.828007868655634,3.11470146448752,
16.8062691237319));
#253741=CARTESIAN_POINT('Ctrl Pts',(-0.856064191567081,3.10710741341235,
16.8081228787851));
#253742=CARTESIAN_POINT('Ctrl Pts',(-0.896837468873169,3.09547700837977,
16.8107981390015));
#253743=CARTESIAN_POINT('Ctrl Pts',(-0.909637345366491,3.0917398450466,
16.811635263557));
#253744=CARTESIAN_POINT('Ctrl Pts',(-0.932188832620323,3.08500334161735,
16.8131049011151));
#253745=CARTESIAN_POINT('Ctrl Pts',(-0.941949866683177,3.08203700429875,
16.8137392410099));
#253746=CARTESIAN_POINT('Ctrl Pts',(-0.963173664154548,3.07547693062523,
16.8151145852727));
#253747=CARTESIAN_POINT('Ctrl Pts',(-0.974630549964727,3.07186542021568,
16.8158545656487));
#253748=CARTESIAN_POINT('Ctrl Pts',(-1.0067531555517,3.06154172817584,16.8179231173744));
#253749=CARTESIAN_POINT('Ctrl Pts',(-1.02737199532258,3.05468435529223,
16.8192436538562));
#253750=CARTESIAN_POINT('Ctrl Pts',(-1.17103920688375,3.00528453473384,
16.8284044340231));
#253751=CARTESIAN_POINT('Ctrl Pts',(-1.29149395777692,2.95552346271042,
16.8358792239531));
#253752=CARTESIAN_POINT('Ctrl Pts',(-1.53626769814081,2.83657211369362,
16.8512625298992));
#253753=CARTESIAN_POINT('Ctrl Pts',(-1.65968013394142,2.76617473683709,
16.8591358341182));
#253754=CARTESIAN_POINT('Ctrl Pts',(-1.91472184588331,2.59746228654541,
16.8763708297612));
#253755=CARTESIAN_POINT('Ctrl Pts',(-2.04428201536366,2.4967722862904,16.8857549371368));
#253756=CARTESIAN_POINT('Ctrl Pts',(-2.191117783336,2.36353679077418,16.8975894816669));
#253757=CARTESIAN_POINT('Ctrl Pts',(-2.21624576679139,2.33999099718552,
16.8996607286598));
#253758=CARTESIAN_POINT('Ctrl Pts',(-2.25561912331138,2.30189362390212,
16.9029834003136));
#253759=CARTESIAN_POINT('Ctrl Pts',(-2.27011261066873,2.28760149299407,
16.9042237000457));
#253760=CARTESIAN_POINT('Ctrl Pts',(-2.29728609412987,2.26029297476584,
16.9065825677269));
#253761=CARTESIAN_POINT('Ctrl Pts',(-2.30999332905642,2.24730472533306,
16.9076998755978));
#253762=CARTESIAN_POINT('Ctrl Pts',(-2.33863449835674,2.21753058077326,
16.9102512344071));
#253763=CARTESIAN_POINT('Ctrl Pts',(-2.3544986684942,2.20067925178266,16.9116881944861));
#253764=CARTESIAN_POINT('Ctrl Pts',(-2.39541192476044,2.15627132302239,
16.9154575888654));
#253765=CARTESIAN_POINT('Ctrl Pts',(-2.42016673171305,2.12844946242157,
16.9178020807243));
#253766=CARTESIAN_POINT('Ctrl Pts',(-2.61679113848599,1.899597981639,16.9369569201223));
#253767=CARTESIAN_POINT('Ctrl Pts',(-2.7637706830185,1.67856776028842,16.9547833683786));
#253768=CARTESIAN_POINT('Ctrl Pts',(-2.95343956640391,1.29951634979094,
16.9834035323129));
#253769=CARTESIAN_POINT('Ctrl Pts',(-3.0141236507671,1.151788710399,16.9941110107567));
#253770=CARTESIAN_POINT('Ctrl Pts',(-3.07048166104438,0.979156861753478,
17.0057157522141));
#253771=CARTESIAN_POINT('Ctrl Pts',(-3.07712300845376,0.958081334463621,
17.0071173901006));
#253772=CARTESIAN_POINT('Ctrl Pts',(-3.08702393418855,0.925496514704128,
17.0092594756491));
#253773=CARTESIAN_POINT('Ctrl Pts',(-3.09043694730224,0.914035040027978,
17.0100082057343));
#253774=CARTESIAN_POINT('Ctrl Pts',(-3.09664524104275,0.892754185977941,
17.0113892922575));
#253775=CARTESIAN_POINT('Ctrl Pts',(-3.09945768247206,0.882940464430938,
17.0120225717708));
#253776=CARTESIAN_POINT('Ctrl Pts',(-3.10579629462377,0.860418993414859,
17.0134677836102));
#253777=CARTESIAN_POINT('Ctrl Pts',(-3.10929114913333,0.847702796837297,
17.0142779355073));
#253778=CARTESIAN_POINT('Ctrl Pts',(-3.12023078536697,0.806920390358045,
17.016858540799));
#253779=CARTESIAN_POINT('Ctrl Pts',(-3.12737458536215,0.778774039625884,
17.0186128896932));
#253780=CARTESIAN_POINT('Ctrl Pts',(-3.19278584275539,0.50562467217549,
17.0354148590709));
#253781=CARTESIAN_POINT('Ctrl Pts',(-3.22253397295609,0.254652021912385,
17.0491740595322));
#253782=CARTESIAN_POINT('Ctrl Pts',(-3.22274960926121,0.00183250105543022,
17.0633995295227));
#253783=CARTESIAN_POINT('Ctrl Pts',(-3.22275000000003,0.000916246347937087,
17.0634510886575));
#253784=CARTESIAN_POINT('Ctrl Pts',(-3.22275,-9.68142638581001E-11,17.0635026513638));
#253785=CARTESIAN_POINT('Origin',(0.,0.,-2.31077344927308));
#253786=CARTESIAN_POINT('',(-3.2227491362909,-0.00235945677226465,18.5607734492731));
#253787=CARTESIAN_POINT('',(-3.22274955323411,-0.00169694707575843,18.3142265507618));
#253788=CARTESIAN_POINT('',(-3.22275,-3.50678552687464E-13,-2.31077344927308));
#253789=CARTESIAN_POINT('Ctrl Pts',(-3.22274907157671,-0.00244625253626111,
18.5592428712784));
#253790=CARTESIAN_POINT('Ctrl Pts',(-3.22289265676903,0.186716165640959,
18.5485157862865));
#253791=CARTESIAN_POINT('Ctrl Pts',(-3.20638176666725,0.375530774842403,
18.538092345269));
#253792=CARTESIAN_POINT('Ctrl Pts',(-3.15034419603654,0.692057453392939,
18.5198245147944));
#253793=CARTESIAN_POINT('Ctrl Pts',(-3.11929282742046,0.820742737597622,
18.5121709164876));
#253794=CARTESIAN_POINT('Ctrl Pts',(-3.07092396691331,0.9780536930799,18.5023304837446));
#253795=CARTESIAN_POINT('Ctrl Pts',(-3.06095693997436,1.00881392503395,
18.500383046183));
#253796=CARTESIAN_POINT('Ctrl Pts',(-3.0441992194529,1.05799520194429,18.4972294032883));
#253797=CARTESIAN_POINT('Ctrl Pts',(-3.03769994845516,1.07651369328513,
18.4960327417886));
#253798=CARTESIAN_POINT('Ctrl Pts',(-3.02497181905704,1.1117469146277,18.4937378319867));
#253799=CARTESIAN_POINT('Ctrl Pts',(-3.01877252145473,1.12847159991908,
18.4926405949002));
#253800=CARTESIAN_POINT('Ctrl Pts',(-3.00434360828263,1.16642854819456,
18.4901320169461));
#253801=CARTESIAN_POINT('Ctrl Pts',(-2.9960272208709,1.18762659287769,18.4887178333907));
#253802=CARTESIAN_POINT('Ctrl Pts',(-2.97335059846975,1.24367374548421,
18.4849428155627));
#253803=CARTESIAN_POINT('Ctrl Pts',(-2.95860278808216,1.27836126251055,
18.4825691734736));
#253804=CARTESIAN_POINT('Ctrl Pts',(-2.8375692250755,1.54971809102887,18.4636983257894));
#253805=CARTESIAN_POINT('Ctrl Pts',(-2.70368078570787,1.77298838242029,
18.4462272055401));
#253806=CARTESIAN_POINT('Ctrl Pts',(-2.47456335328253,2.06776451096623,
18.421001454548));
#253807=CARTESIAN_POINT('Ctrl Pts',(-2.39987166523696,2.15400388294558,
18.4133240966872));
#253808=CARTESIAN_POINT('Ctrl Pts',(-2.29299434564181,2.26492741216265,
18.4031990806177));
#253809=CARTESIAN_POINT('Ctrl Pts',(-2.26468996333598,2.29322892615946,
18.4005921272635));
#253810=CARTESIAN_POINT('Ctrl Pts',(-2.21551382074105,2.34060132247369,
18.396198429975));
#253811=CARTESIAN_POINT('Ctrl Pts',(-2.19490534987753,2.35993785306692,
18.3943960646057));
#253812=CARTESIAN_POINT('Ctrl Pts',(-2.16471738561906,2.38752504626452,
18.39181497478));
#253813=CARTESIAN_POINT('Ctrl Pts',(-2.15534011743283,2.39599378060399,
18.3910212753626));
#253814=CARTESIAN_POINT('Ctrl Pts',(-2.14583998281727,2.40447257007618,
18.3902254784126));
#253815=CARTESIAN_POINT('Ctrl Pts',(-2.14576685713346,2.40453782813529,
18.3902193533928));
#253816=CARTESIAN_POINT('Ctrl Pts',(-2.14562004521291,2.40466883246587,
18.3902070573914));
#253817=CARTESIAN_POINT('Ctrl Pts',(-2.14554635892637,2.40473457869055,
18.390200886413));
#253818=CARTESIAN_POINT('Ctrl Pts',(-2.14539840308711,2.40486657934217,
18.3901884966149));
#253819=CARTESIAN_POINT('Ctrl Pts',(-2.14532413348151,2.4049328337206,18.3901822777987));
#253820=CARTESIAN_POINT('Ctrl Pts',(-2.1451749876093,2.40506587126047,18.3901697903902));
#253821=CARTESIAN_POINT('Ctrl Pts',(-2.14510011130034,2.40513265435937,
18.3901635218026));
#253822=CARTESIAN_POINT('Ctrl Pts',(-2.14494972793376,2.40526677052088,
18.3901509328599));
#253823=CARTESIAN_POINT('Ctrl Pts',(-2.1448742208241,2.40533410352476,18.3901446125091));
#253824=CARTESIAN_POINT('Ctrl Pts',(-2.14472255103112,2.40546934131582,
18.3901319179883));
#253825=CARTESIAN_POINT('Ctrl Pts',(-2.14464638829686,2.4055372460382,18.3901255438232));
#253826=CARTESIAN_POINT('Ctrl Pts',(-2.14449338165679,2.40567364975537,
18.3901127395591));
#253827=CARTESIAN_POINT('Ctrl Pts',(-2.1444165376944,2.40574214868507,18.390106309465));
#253828=CARTESIAN_POINT('Ctrl Pts',(-2.14426214219056,2.40587976400727,
18.3900933911624));
#253829=CARTESIAN_POINT('Ctrl Pts',(-2.14418459058588,2.40594888033503,
18.3900869029585));
#253830=CARTESIAN_POINT('Ctrl Pts',(-2.1440287525332,2.40608775438591,18.3900738661858));
#253831=CARTESIAN_POINT('Ctrl Pts',(-2.14395046602077,2.40615751203953,
18.3900673176219));
#253832=CARTESIAN_POINT('Ctrl Pts',(-2.14379312998843,2.40629769345415,
18.3900541578052));
#253833=CARTESIAN_POINT('Ctrl Pts',(-2.14371408040529,2.40636811713845,
18.390047546558));
#253834=CARTESIAN_POINT('Ctrl Pts',(-2.14355518912952,2.40650965613853,
18.390034258974));
#253835=CARTESIAN_POINT('Ctrl Pts',(-2.14347534736779,2.4065807713764,18.390027582643));
#253836=CARTESIAN_POINT('Ctrl Pts',(-2.14331484164867,2.40672371985968,
18.3900141624106));
#253837=CARTESIAN_POINT('Ctrl Pts',(-2.14323417761161,2.40679555302983,
18.3900074185147));
#253838=CARTESIAN_POINT('Ctrl Pts',(-2.14307199621088,2.40693996465833,
18.3899938605866));
#253839=CARTESIAN_POINT('Ctrl Pts',(-2.14299047876653,2.40701254303519,
18.3899870465603));
#253840=CARTESIAN_POINT('Ctrl Pts',(-2.13547016417003,2.41370750757851,
18.389358481527));
#253841=CARTESIAN_POINT('Ctrl Pts',(-2.12800069466802,2.42029539655638,
18.3887392887263));
#253842=CARTESIAN_POINT('Ctrl Pts',(-2.11161461749736,2.43461301049126,
18.3873921436935));
#253843=CARTESIAN_POINT('Ctrl Pts',(-2.10268600934501,2.44232847094139,
18.3866652153393));
#253844=CARTESIAN_POINT('Ctrl Pts',(-2.07737037182655,2.46396269251239,
18.3846234513338));
#253845=CARTESIAN_POINT('Ctrl Pts',(-2.06088581758185,2.47776704208275,
18.3833165590309));
#253846=CARTESIAN_POINT('Ctrl Pts',(-1.93380051263754,2.58204387048164,
18.3734018989864));
#253847=CARTESIAN_POINT('Ctrl Pts',(-1.81741748455037,2.66524640239701,
18.3652389028851));
#253848=CARTESIAN_POINT('Ctrl Pts',(-1.52479823513691,2.84632866918401,
18.3458498945639));
#253849=CARTESIAN_POINT('Ctrl Pts',(-1.34418133543501,2.93594477651714,
18.3347532156109));
#253850=CARTESIAN_POINT('Ctrl Pts',(-1.09342143822162,3.0323419879976,18.319317376898));
#253851=CARTESIAN_POINT('Ctrl Pts',(-1.02971272886994,3.05456367741998,
18.3153966448098));
#253852=CARTESIAN_POINT('Ctrl Pts',(-0.917897780646437,3.08966916607696,
18.3084805638168));
#253853=CARTESIAN_POINT('Ctrl Pts',(-0.870102649171766,3.10346787904315,
18.3055136291425));
#253854=CARTESIAN_POINT('Ctrl Pts',(-0.799668068809054,3.12204778911762,
18.3011166901102));
#253855=CARTESIAN_POINT('Ctrl Pts',(-0.777264718889288,3.12770058222117,
18.2997145608484));
#253856=CARTESIAN_POINT('Ctrl Pts',(-0.737489410724561,3.13728291489456,
18.2972180130621));
#253857=CARTESIAN_POINT('Ctrl Pts',(-0.720141864803557,3.14131029884364,
18.2961267705086));
#253858=CARTESIAN_POINT('Ctrl Pts',(-0.683628100468923,3.14946893473035,
18.2938244559817));
#253859=CARTESIAN_POINT('Ctrl Pts',(-0.664455832561879,3.15356946493662,
18.2926124551757));
#253860=CARTESIAN_POINT('Ctrl Pts',(-0.613578293327099,3.16396650961847,
18.2893873627523));
#253861=CARTESIAN_POINT('Ctrl Pts',(-0.581814301881632,3.16996126044856,
18.287364832157));
#253862=CARTESIAN_POINT('Ctrl Pts',(-0.434557798851252,3.19546487112564,
18.2779439075572));
#253863=CARTESIAN_POINT('Ctrl Pts',(-0.318158166711865,3.20914416131536,
18.2703662463738));
#253864=CARTESIAN_POINT('Ctrl Pts',(0.000583492502514438,3.22909071952589,
18.2492850145463));
#253865=CARTESIAN_POINT('Ctrl Pts',(0.203182023034414,3.22269036192606,
18.2354985925683));
#253866=CARTESIAN_POINT('Ctrl Pts',(0.515746792402945,3.18321375305085,
18.2143245794595));
#253867=CARTESIAN_POINT('Ctrl Pts',(0.626863036132827,3.16320912599812,
18.2068259779797));
#253868=CARTESIAN_POINT('Ctrl Pts',(0.763109223612543,3.13121657159533,
18.1978347342203));
#253869=CARTESIAN_POINT('Ctrl Pts',(0.78943012282361,3.12468447973809,18.1961074641414));
#253870=CARTESIAN_POINT('Ctrl Pts',(0.828043772463393,3.11458259768344,
18.1935909508561));
#253871=CARTESIAN_POINT('Ctrl Pts',(0.840401990859866,3.11127076186023,
18.1927881944016));
#253872=CARTESIAN_POINT('Ctrl Pts',(0.861422044966705,3.1055032874127,18.1914276937007));
#253873=CARTESIAN_POINT('Ctrl Pts',(0.870093711013847,3.10308484392979,
18.1908678724106));
#253874=CARTESIAN_POINT('Ctrl Pts',(0.88981034595826,3.09749691485816,18.1895983618062));
#253875=CARTESIAN_POINT('Ctrl Pts',(0.900848598557094,3.09430467169069,
18.1888899864163));
#253876=CARTESIAN_POINT('Ctrl Pts',(0.931135949951803,3.08536981499655,
18.1869521872327));
#253877=CARTESIAN_POINT('Ctrl Pts',(0.950349154847304,3.07950606147134,
18.1857294649824));
#253878=CARTESIAN_POINT('Ctrl Pts',(1.0567833801761,3.04593197530457,18.1789860516857));
#253879=CARTESIAN_POINT('Ctrl Pts',(1.14285593849067,3.01469336616768,18.1736447628338));
#253880=CARTESIAN_POINT('Ctrl Pts',(1.38422193025158,2.91526684752681,18.1586846372908));
#253881=CARTESIAN_POINT('Ctrl Pts',(1.53562272305683,2.83843602488646,18.1493112682678));
#253882=CARTESIAN_POINT('Ctrl Pts',(1.81914689099172,2.66520251733294,18.1306354007406));
#253883=CARTESIAN_POINT('Ctrl Pts',(1.95137111153841,2.56996934147149,18.1213703445541));
#253884=CARTESIAN_POINT('Ctrl Pts',(2.10909688270586,2.43715390995463,18.109149262779));
#253885=CARTESIAN_POINT('Ctrl Pts',(2.1417909646266,2.40847255271934,18.1065471119432));
#253886=CARTESIAN_POINT('Ctrl Pts',(2.19009365838177,2.36433688115209,18.1025911698138));
#253887=CARTESIAN_POINT('Ctrl Pts',(2.20614181592318,2.34936956895683,18.101257642436));
#253888=CARTESIAN_POINT('Ctrl Pts',(2.23486556242298,2.32202654013214,18.0988350767202));
#253889=CARTESIAN_POINT('Ctrl Pts',(2.24759443710301,2.30970789534828,18.0977485050319));
#253890=CARTESIAN_POINT('Ctrl Pts',(2.27473485807694,2.28300535576677,18.0954031421203));
#253891=CARTESIAN_POINT('Ctrl Pts',(2.2891128756103,2.26858862324514,18.0941429399683));
#253892=CARTESIAN_POINT('Ctrl Pts',(2.3277127063239,2.22914426486944,18.0907106872668));
#253893=CARTESIAN_POINT('Ctrl Pts',(2.35166642512312,2.20385922195507,18.0885272481012));
#253894=CARTESIAN_POINT('Ctrl Pts',(2.50375068066485,2.0380192396147,18.0743081932357));
#253895=CARTESIAN_POINT('Ctrl Pts',(2.61961519151745,1.88676578086715,18.0617689980249));
#253896=CARTESIAN_POINT('Ctrl Pts',(2.79549768026726,1.60947748514098,18.0396857429976));
#253897=CARTESIAN_POINT('Ctrl Pts',(2.86195065340621,1.4881073368923,18.0302902104782));
#253898=CARTESIAN_POINT('Ctrl Pts',(2.95150431113851,1.29620521709324,18.0161055242689));
#253899=CARTESIAN_POINT('Ctrl Pts',(2.98031482430023,1.22851556222435,18.0112240321775));
#253900=CARTESIAN_POINT('Ctrl Pts',(3.02288525410323,1.11816068621147,18.0035182878308));
#253901=CARTESIAN_POINT('Ctrl Pts',(3.0381152030706,1.07609249040335,18.0006382333831));
#253902=CARTESIAN_POINT('Ctrl Pts',(3.057458715557,1.01897307599925,17.996817085121));
#253903=CARTESIAN_POINT('Ctrl Pts',(3.06234548039941,1.00419127077684,17.9958361912822));
#253904=CARTESIAN_POINT('Ctrl Pts',(3.07031540624611,0.979483979114567,
17.9942105995237));
#253905=CARTESIAN_POINT('Ctrl Pts',(3.07345797221054,0.969578084257697,
17.9935625674794));
#253906=CARTESIAN_POINT('Ctrl Pts',(3.07934128880534,0.950716830511556,
17.9923359702249));
#253907=CARTESIAN_POINT('Ctrl Pts',(3.08209100349124,0.941764469582951,
17.9917568711489));
#253908=CARTESIAN_POINT('Ctrl Pts',(3.08931848818855,0.917862932002773,
17.9902186902545));
#253909=CARTESIAN_POINT('Ctrl Pts',(3.09372683225813,0.902892791693413,
17.9892635370282));
#253910=CARTESIAN_POINT('Ctrl Pts',(3.10949988179563,0.847857511358168,
17.9857802691206));
#253911=CARTESIAN_POINT('Ctrl Pts',(3.12019694500608,0.807603405350767,
17.9832871337268));
#253912=CARTESIAN_POINT('Ctrl Pts',(3.20048233435499,0.480024960892568,
17.9633550802903));
#253913=CARTESIAN_POINT('Ctrl Pts',(3.23102057869182,0.184553969359728,
17.947467070587));
#253914=CARTESIAN_POINT('Ctrl Pts',(3.21815755737333,-0.188796176570578,
17.9261325374059));
#253915=CARTESIAN_POINT('Ctrl Pts',(3.21265618676044,-0.266497884558532,
17.9216319260998));
#253916=CARTESIAN_POINT('Ctrl Pts',(3.198437993779,-0.398970354423279,17.9137969797588));
#253917=CARTESIAN_POINT('Ctrl Pts',(3.19111220268402,-0.453856053319911,
17.9105030208264));
#253918=CARTESIAN_POINT('Ctrl Pts',(3.17857384596906,-0.532321984482374,
17.9057123614175));
#253919=CARTESIAN_POINT('Ctrl Pts',(3.17450425545294,-0.556076499646197,
17.9042512814675));
#253920=CARTESIAN_POINT('Ctrl Pts',(3.16693659525158,-0.597455384115182,
17.9016863593282));
#253921=CARTESIAN_POINT('Ctrl Pts',(3.16355681204449,-0.615100488439679,
17.9005862866126));
#253922=CARTESIAN_POINT('Ctrl Pts',(3.15626068666414,-0.651540167683742,
17.8983009871887));
#253923=CARTESIAN_POINT('Ctrl Pts',(3.1523235919564,-0.670329813301026,
17.8971151421686));
#253924=CARTESIAN_POINT('Ctrl Pts',(3.14172541162423,-0.718749814050308,
17.894039479047));
#253925=CARTESIAN_POINT('Ctrl Pts',(3.13481306293851,-0.748322669066041,
17.8921417550143));
#253926=CARTESIAN_POINT('Ctrl Pts',(3.1042159592421,-0.871352828823828,
17.8841639006274));
#253927=CARTESIAN_POINT('Ctrl Pts',(3.07676349182583,-0.963813173747749,
17.8779654979819));
#253928=CARTESIAN_POINT('Ctrl Pts',(2.96818310575658,-1.2772562202947,17.8562486567092));
#253929=CARTESIAN_POINT('Ctrl Pts',(2.86703582966643,-1.4904960917351,17.8401744759062));
#253930=CARTESIAN_POINT('Ctrl Pts',(2.68337422031547,-1.78851827437921,
17.8166894609929));
#253931=CARTESIAN_POINT('Ctrl Pts',(2.61796438130813,-1.88296646264973,
17.8090873496476));
#253932=CARTESIAN_POINT('Ctrl Pts',(2.53498569952396,-1.99007348316253,
17.8004424870812));
#253933=CARTESIAN_POINT('Ctrl Pts',(2.5221670050057,-2.00629474785566,17.7991326313734));
#253934=CARTESIAN_POINT('Ctrl Pts',(2.50197733683822,-2.03134417850028,
17.7971104346578));
#253935=CARTESIAN_POINT('Ctrl Pts',(2.49471396413578,-2.04025782984851,
17.7963909571666));
#253936=CARTESIAN_POINT('Ctrl Pts',(2.48103771707673,-2.05685916504241,
17.7950514651011));
#253937=CARTESIAN_POINT('Ctrl Pts',(2.4746367245951,-2.0645558511334,17.7944306957874));
#253938=CARTESIAN_POINT('Ctrl Pts',(2.4597418607655,-2.08229694391672,17.7930001745159));
#253939=CARTESIAN_POINT('Ctrl Pts',(2.45122224052103,-2.09231931732119,
17.7921922864226));
#253940=CARTESIAN_POINT('Ctrl Pts',(2.42319191719161,-2.12488763291403,
17.7895667518686));
#253941=CARTESIAN_POINT('Ctrl Pts',(2.40342906115388,-2.14721573445124,
17.7877663433793));
#253942=CARTESIAN_POINT('Ctrl Pts',(2.26861571506168,-2.29533419436434,
17.7757947133883));
#253943=CARTESIAN_POINT('Ctrl Pts',(2.14403728381326,-2.4121140214532,17.7662081555279));
#253944=CARTESIAN_POINT('Ctrl Pts',(1.8772630285072,-2.62510884218131,17.7470841331315));
#253945=CARTESIAN_POINT('Ctrl Pts',(1.73547155627702,-2.7209277081484,17.7375714086374));
#253946=CARTESIAN_POINT('Ctrl Pts',(1.53270587971579,-2.83562817915063,
17.724138046052));
#253947=CARTESIAN_POINT('Ctrl Pts',(1.47778100201632,-2.86463560360211,
17.7205170399961));
#253948=CARTESIAN_POINT('Ctrl Pts',(1.38011983398281,-2.91265695079055,
17.7140815238228));
#253949=CARTESIAN_POINT('Ctrl Pts',(1.33774322908415,-2.93236150435328,
17.7112900843765));
#253950=CARTESIAN_POINT('Ctrl Pts',(1.27429577444581,-2.96020215701313,
17.707104649604));
#253951=CARTESIAN_POINT('Ctrl Pts',(1.25354262021145,-2.96904991383025,
17.7057347131584));
#253952=CARTESIAN_POINT('Ctrl Pts',(1.21629062550533,-2.98447148427544,
17.7032732465998));
#253953=CARTESIAN_POINT('Ctrl Pts',(1.1998269723624,-2.99112823910091,17.7021845569713));
#253954=CARTESIAN_POINT('Ctrl Pts',(1.16476870288429,-3.00496734664593,
17.6998641089949));
#253955=CARTESIAN_POINT('Ctrl Pts',(1.14616084572861,-3.01211390438744,
17.698631210315));
#253956=CARTESIAN_POINT('Ctrl Pts',(1.09583018101518,-3.03091005914756,
17.6952924626129));
#253957=CARTESIAN_POINT('Ctrl Pts',(1.06398915215974,-3.04223380393089,
17.6931759802756));
#253958=CARTESIAN_POINT('Ctrl Pts',(0.898003063781035,-3.09833952047665,
17.6821172241117));
#253959=CARTESIAN_POINT('Ctrl Pts',(0.761211314198354,-3.13475126065524,
17.6729074610022));
#253960=CARTESIAN_POINT('Ctrl Pts',(0.359974574203611,-3.21373904878994,
17.6457022911956));
#253961=CARTESIAN_POINT('Ctrl Pts',(0.0920652514683722,-3.23252509157068,
17.6272256620244));
#253962=CARTESIAN_POINT('Ctrl Pts',(-0.216769407828373,-3.21572260629027,
17.6071164595651));
#253963=CARTESIAN_POINT('Ctrl Pts',(-0.258414812413189,-3.21264424075758,
17.6044324806253));
#253964=CARTESIAN_POINT('Ctrl Pts',(-0.315088636555306,-3.20734573300469,
17.6008280514753));
#253965=CARTESIAN_POINT('Ctrl Pts',(-0.33017668287957,-3.20582764337693,
17.5998731244586));
#253966=CARTESIAN_POINT('Ctrl Pts',(-0.355499536651544,-3.20309909868199,
17.5982789058878));
#253967=CARTESIAN_POINT('Ctrl Pts',(-0.36574016072204,-3.20194595547756,
17.5976365334628));
#253968=CARTESIAN_POINT('Ctrl Pts',(-0.386653523051162,-3.19948936744569,
17.5963296839163));
#253969=CARTESIAN_POINT('Ctrl Pts',(-0.397325538418083,-3.19818160579537,
17.5956654458054));
#253970=CARTESIAN_POINT('Ctrl Pts',(-0.425106483149743,-3.19463609069579,
17.59394275232));
#253971=CARTESIAN_POINT('Ctrl Pts',(-0.442204590101602,-3.19231427094593,
17.5928888549849));
#253972=CARTESIAN_POINT('Ctrl Pts',(-0.513038613184772,-3.18211540391633,
17.5885460985855));
#253973=CARTESIAN_POINT('Ctrl Pts',(-0.566592830316869,-3.17301755137519,
17.5853184957343));
#253974=CARTESIAN_POINT('Ctrl Pts',(-0.812597715321352,-3.12479817419771,
17.5706455773933));
#253975=CARTESIAN_POINT('Ctrl Pts',(-1.00146171427537,-3.06948964035161,
17.5597968991057));
#253976=CARTESIAN_POINT('Ctrl Pts',(-1.33861990628245,-2.93629140283928,
17.5394641099352));
#253977=CARTESIAN_POINT('Ctrl Pts',(-1.48814685387385,-2.86341084085395,
17.5300591942345));
#253978=CARTESIAN_POINT('Ctrl Pts',(-1.67602261696069,-2.7531336722922,
17.5172193693333));
#253979=CARTESIAN_POINT('Ctrl Pts',(-1.72002270675444,-2.72586101548764,
17.5141347982859));
#253980=CARTESIAN_POINT('Ctrl Pts',(-1.78299902768415,-2.68469427638844,
17.5095953097727));
#253981=CARTESIAN_POINT('Ctrl Pts',(-1.8025114237413,-2.67163272421818,
17.5081709195013));
#253982=CARTESIAN_POINT('Ctrl Pts',(-1.83662312005357,-2.64825462776954,
17.5056481574118));
#253983=CARTESIAN_POINT('Ctrl Pts',(-1.85128271409607,-2.63802754931779,
17.5045531769896));
#253984=CARTESIAN_POINT('Ctrl Pts',(-1.88172191122941,-2.61641335612001,
17.5022564434706));
#253985=CARTESIAN_POINT('Ctrl Pts',(-1.89748493373297,-2.60500424206966,
17.5010538792809));
#253986=CARTESIAN_POINT('Ctrl Pts',(-1.9385573931954,-2.57470583432497,
17.4978850969095));
#253987=CARTESIAN_POINT('Ctrl Pts',(-1.96369369149169,-2.55558640489592,
17.495910045533));
#253988=CARTESIAN_POINT('Ctrl Pts',(-2.07218293515721,-2.47052053146101,
17.4872252116354));
#253989=CARTESIAN_POINT('Ctrl Pts',(-2.15251780084418,-2.40084920090603,
17.4803700407907));
#253990=CARTESIAN_POINT('Ctrl Pts',(-2.37943224253378,-2.18349799222926,
17.4597123312903));
#253991=CARTESIAN_POINT('Ctrl Pts',(-2.51532219767696,-2.02546329964362,
17.4455528138737));
#253992=CARTESIAN_POINT('Ctrl Pts',(-2.70311051878341,-1.75877642124855,
17.4236083599625));
#253993=CARTESIAN_POINT('Ctrl Pts',(-2.76582600409758,-1.65840666523159,
17.4157341560036));
#253994=CARTESIAN_POINT('Ctrl Pts',(-2.83626884054577,-1.53051168669115,
17.4063484025657));
#253995=CARTESIAN_POINT('Ctrl Pts',(-2.84933726048621,-1.50604258025941,
17.4045808330466));
#253996=CARTESIAN_POINT('Ctrl Pts',(-2.86802715091668,-1.46993357904964,
17.4020166896389));
#253997=CARTESIAN_POINT('Ctrl Pts',(-2.87389676301276,-1.45842444920831,
17.4012059180587));
#253998=CARTESIAN_POINT('Ctrl Pts',(-2.88417141466274,-1.43797501138345,
17.3997772397499));
#253999=CARTESIAN_POINT('Ctrl Pts',(-2.88860438535316,-1.42904919308393,
17.3991576556842));
#254000=CARTESIAN_POINT('Ctrl Pts',(-2.89819853603028,-1.40950423861687,
17.3978097375175));
#254001=CARTESIAN_POINT('Ctrl Pts',(-2.90334282201466,-1.39887720010469,
17.3970824269107));
#254002=CARTESIAN_POINT('Ctrl Pts',(-2.91768982336112,-1.36881916030356,
17.3950403087782));
#254003=CARTESIAN_POINT('Ctrl Pts',(-2.92675685106363,-1.34932360453472,
17.393733432173));
#254004=CARTESIAN_POINT('Ctrl Pts',(-2.99083166330623,-1.20786730980781,
17.3843674630359));
#254005=CARTESIAN_POINT('Ctrl Pts',(-3.03839891047501,-1.08266234440226,
17.3766965786054));
#254006=CARTESIAN_POINT('Ctrl Pts',(-3.08934340044724,-0.918437975359805,
17.3669871660932));
#254007=CARTESIAN_POINT('Ctrl Pts',(-3.09999191628583,-0.881828295867643,
17.3648447110038));
#254008=CARTESIAN_POINT('Ctrl Pts',(-3.14663311000897,-0.710174966302317,
17.3548691720586));
#254009=CARTESIAN_POINT('Ctrl Pts',(-3.17446613581936,-0.573072446619124,
17.3470946691516));
#254010=CARTESIAN_POINT('Ctrl Pts',(-3.20487799820405,-0.349615226686832,
17.3342678168282));
#254011=CARTESIAN_POINT('Ctrl Pts',(-3.21304634824452,-0.264207274741575,
17.329330984468));
#254012=CARTESIAN_POINT('Ctrl Pts',(-3.22109031821581,-0.119263850536278,
17.3208150886266));
#254013=CARTESIAN_POINT('Ctrl Pts',(-3.22274128749274,-0.0598718822926805,
17.3172869848923));
#254014=CARTESIAN_POINT('Ctrl Pts',(-3.22274998853597,-0.000313882066399077,
17.3136991171112));
#254015=CARTESIAN_POINT('Ctrl Pts',(-3.22275,-0.000156941007807153,17.3136896623894));
#254016=CARTESIAN_POINT('Ctrl Pts',(-3.22275,-2.95105326763967E-13,17.3136802073254));
#254017=CARTESIAN_POINT('Ctrl Pts',(-3.22275,-9.68149171942656E-11,17.0635026513638));
#254018=CARTESIAN_POINT('Ctrl Pts',(-3.22274999999488,-0.170393836325402,
17.0730917388645));
#254019=CARTESIAN_POINT('Ctrl Pts',(-3.20923696781612,-0.340500790962171,
17.082824205386));
#254020=CARTESIAN_POINT('Ctrl Pts',(-3.17681918572208,-0.543288175441212,
17.0950718298512));
#254021=CARTESIAN_POINT('Ctrl Pts',(-3.17073276211461,-0.577750628907981,
17.0971752596468));
#254022=CARTESIAN_POINT('Ctrl Pts',(-3.16016034217372,-0.632401363187258,
17.1005491225351));
#254023=CARTESIAN_POINT('Ctrl Pts',(-3.15603904588094,-0.652657936893176,
17.1018080669125));
#254024=CARTESIAN_POINT('Ctrl Pts',(-3.14797543408352,-0.69042772216104,
17.1041717981521));
#254025=CARTESIAN_POINT('Ctrl Pts',(-3.14408109531189,-0.707950435224602,
17.1052750235425));
#254026=CARTESIAN_POINT('Ctrl Pts',(-3.13496294018237,-0.747418069020755,
17.107775237951));
#254027=CARTESIAN_POINT('Ctrl Pts',(-3.12965473120727,-0.769342335082444,
17.1091748672982));
#254028=CARTESIAN_POINT('Ctrl Pts',(-3.11303273091276,-0.83497492524587,
17.113398022427));
#254029=CARTESIAN_POINT('Ctrl Pts',(-3.10103056160646,-0.878501586427535,
17.1162432993291));
#254030=CARTESIAN_POINT('Ctrl Pts',(-3.07122824657916,-0.978346526626052,
17.1228762661628));
#254031=CARTESIAN_POINT('Ctrl Pts',(-3.05278676010583,-1.03445501352186,
17.1266830898872));
#254032=CARTESIAN_POINT('Ctrl Pts',(-2.98047410371263,-1.23565353176753,
17.1406215054443));
#254033=CARTESIAN_POINT('Ctrl Pts',(-2.91771633781987,-1.37731205804534,
17.1509985527858));
#254034=CARTESIAN_POINT('Ctrl Pts',(-2.75462437299016,-1.68380623296778,
17.1744465641999));
#254035=CARTESIAN_POINT('Ctrl Pts',(-2.64916987278993,-1.84528301323793,
17.187517671197));
#254036=CARTESIAN_POINT('Ctrl Pts',(-2.51184634270894,-2.01930618621883,
17.201786218988));
#254037=CARTESIAN_POINT('Ctrl Pts',(-2.49345387167668,-2.04197391013941,
17.203648110753));
#254038=CARTESIAN_POINT('Ctrl Pts',(-2.46629030520907,-2.07453713454269,
17.2063238664436));
#254039=CARTESIAN_POINT('Ctrl Pts',(-2.45776285477622,-2.08463281083364,
17.2071535894951));
#254040=CARTESIAN_POINT('Ctrl Pts',(-2.44253633224151,-2.10243622981725,
17.2086166076807));
#254041=CARTESIAN_POINT('Ctrl Pts',(-2.4358624045583,-2.11016496770706,
17.2092516458132));
#254042=CARTESIAN_POINT('Ctrl Pts',(-2.42130564541515,-2.12686132059507,
17.2106232563471));
#254043=CARTESIAN_POINT('Ctrl Pts',(-2.41340962875784,-2.13581695842871,
17.211358855025));
#254044=CARTESIAN_POINT('Ctrl Pts',(-2.39081957523888,-2.16115329045661,
17.2134403126916));
#254045=CARTESIAN_POINT('Ctrl Pts',(-2.37600697816514,-2.1774279978556,
17.2147777873293));
#254046=CARTESIAN_POINT('Ctrl Pts',(-2.25656255859755,-2.30599203304808,
17.2253591880144));
#254047=CARTESIAN_POINT('Ctrl Pts',(-2.14418411864865,-2.41084215175647,
17.2340913995234));
#254048=CARTESIAN_POINT('Ctrl Pts',(-1.82199512393724,-2.67102370508856,
17.2573818631441));
#254049=CARTESIAN_POINT('Ctrl Pts',(-1.60015208613001,-2.80954403288955,
17.2717444013117));
#254050=CARTESIAN_POINT('Ctrl Pts',(-1.32095529249746,-2.93997580848012,
17.2899573378653));
#254051=CARTESIAN_POINT('Ctrl Pts',(-1.27741603426991,-2.95915335324738,
17.2927978727887));
#254052=CARTESIAN_POINT('Ctrl Pts',(-1.21220155010863,-2.98617061486797,
17.2970609756012));
#254053=CARTESIAN_POINT('Ctrl Pts',(-1.19083987285442,-2.99475339458461,
17.2984586982096));
#254054=CARTESIAN_POINT('Ctrl Pts',(-1.15246842095333,-3.00969496777741,
17.300972558276));
#254055=CARTESIAN_POINT('Ctrl Pts',(-1.13549324915439,-3.01614030183761,
17.3020857611783));
#254056=CARTESIAN_POINT('Ctrl Pts',(-1.09930682502073,-3.02953121042691,
17.3044615381262));
#254057=CARTESIAN_POINT('Ctrl Pts',(-1.08008225251045,-3.03643823382723,
17.3057253283553));
#254058=CARTESIAN_POINT('Ctrl Pts',(-1.0279570095341,-3.0546081929117,17.3091569333583));
#254059=CARTESIAN_POINT('Ctrl Pts',(-0.994938321355894,-3.06552188243654,
17.3113360305214));
#254060=CARTESIAN_POINT('Ctrl Pts',(-0.796946840958239,-3.12742847165649,
17.3244388196282));
#254061=CARTESIAN_POINT('Ctrl Pts',(-0.628293598271117,-3.16562224884237,
17.3357713150107));
#254062=CARTESIAN_POINT('Ctrl Pts',(-0.208374407446207,-3.22583236506848,
17.3642046743258));
#254063=CARTESIAN_POINT('Ctrl Pts',(0.043993330221262,-3.23225712954553,
17.3815152739279));
#254064=CARTESIAN_POINT('Ctrl Pts',(0.323514552051184,-3.20660292339507,
17.399580839431));
#254065=CARTESIAN_POINT('Ctrl Pts',(0.352449781020123,-3.20355166355927,
17.4014365297001));
#254066=CARTESIAN_POINT('Ctrl Pts',(0.394445991978551,-3.19854718669193,
17.4041051128582));
#254067=CARTESIAN_POINT('Ctrl Pts',(0.407541684627146,-3.19690499318935,
17.4049337492644));
#254068=CARTESIAN_POINT('Ctrl Pts',(0.430750181589535,-3.19384972949573,
17.4063956102614));
#254069=CARTESIAN_POINT('Ctrl Pts',(0.440866847708669,-3.19246898906937,
17.4070305667339));
#254070=CARTESIAN_POINT('Ctrl Pts',(0.462812382340604,-3.18936751256247,
17.4084029231252));
#254071=CARTESIAN_POINT('Ctrl Pts',(0.474638375686615,-3.18762903336086,
17.4091393404628));
#254072=CARTESIAN_POINT('Ctrl Pts',(0.508267319334487,-3.18249411323786,
17.4112252692579));
#254073=CARTESIAN_POINT('Ctrl Pts',(0.530045894287881,-3.17893942361998,
17.4125663417633));
#254074=CARTESIAN_POINT('Ctrl Pts',(0.706725246801083,-3.14823567433904,
17.4233785294668));
#254075=CARTESIAN_POINT('Ctrl Pts',(0.859505318591126,-3.11000182259476,
17.4323123378207));
#254076=CARTESIAN_POINT('Ctrl Pts',(1.26278638728043,-2.97707085685767,
17.4561780496207));
#254077=CARTESIAN_POINT('Ctrl Pts',(1.50524980976448,-2.86213060248004,
17.4709263150195));
#254078=CARTESIAN_POINT('Ctrl Pts',(1.76185596040298,-2.69876677822356,
17.4889895270773));
#254079=CARTESIAN_POINT('Ctrl Pts',(1.79263266942669,-2.67842238959554,
17.4911980161354));
#254080=CARTESIAN_POINT('Ctrl Pts',(1.84205388601283,-2.64451999473144,
17.4948173875626));
#254081=CARTESIAN_POINT('Ctrl Pts',(1.86091457434846,-2.63128208794607,
17.4962163750274));
#254082=CARTESIAN_POINT('Ctrl Pts',(1.8943834326313,-2.60725119441303,17.4987316968925));
#254083=CARTESIAN_POINT('Ctrl Pts',(1.90904550758403,-2.59653473103001,
17.4998450845511));
#254084=CARTESIAN_POINT('Ctrl Pts',(1.93999725359777,-2.57350832161721,
17.5022203868674));
#254085=CARTESIAN_POINT('Ctrl Pts',(1.95626202558186,-2.56116639097569,
17.5034835097581));
#254086=CARTESIAN_POINT('Ctrl Pts',(1.99986726422881,-2.52742043922812,
17.5069111082397));
#254087=CARTESIAN_POINT('Ctrl Pts',(2.02698027544262,-2.50572823030897,
17.5090868192187));
#254088=CARTESIAN_POINT('Ctrl Pts',(2.18564816010552,-2.37452284945741,
17.5220908092559));
#254089=CARTESIAN_POINT('Ctrl Pts',(2.30863987473912,-2.25512370250672,
17.5333203396417));
#254090=CARTESIAN_POINT('Ctrl Pts',(2.45318471498812,-2.09052620106113,
17.5479980961817));
#254091=CARTESIAN_POINT('Ctrl Pts',(2.48400486706362,-2.05380980503142,
17.5512249111246));
#254092=CARTESIAN_POINT('Ctrl Pts',(2.64301499665363,-1.85556217976798,
17.5683731689268));
#254093=CARTESIAN_POINT('Ctrl Pts',(2.75630799408501,-1.68268168361495,
17.5824200300711));
#254094=CARTESIAN_POINT('Ctrl Pts',(2.86422989469445,-1.47748452604716,
17.5973317919552));
#254095=CARTESIAN_POINT('Ctrl Pts',(2.87588067932428,-1.45467653613732,
17.5989658731962));
#254096=CARTESIAN_POINT('Ctrl Pts',(2.89297326422821,-1.42020727849262,
17.6013978532029));
#254097=CARTESIAN_POINT('Ctrl Pts',(2.89861885385363,-1.40864891807924,
17.6022070814707));
#254098=CARTESIAN_POINT('Ctrl Pts',(2.90870161678703,-1.38768891788807,
17.603662818071));
#254099=CARTESIAN_POINT('Ctrl Pts',(2.91316278873692,-1.37829902619283,
17.6043107503904));
#254100=CARTESIAN_POINT('Ctrl Pts',(2.9222679433687,-1.35889275292914,17.6056409185257));
#254101=CARTESIAN_POINT('Ctrl Pts',(2.92690601132153,-1.34887384738379,
17.606322801986));
#254102=CARTESIAN_POINT('Ctrl Pts',(2.93891563976133,-1.32257767317141,
17.6081003610918));
#254103=CARTESIAN_POINT('Ctrl Pts',(2.94620358698882,-1.30626233825424,
17.6091911138976));
#254104=CARTESIAN_POINT('Ctrl Pts',(2.9789033759737,-1.23139212052146,17.614145026199));
#254105=CARTESIAN_POINT('Ctrl Pts',(3.00270951209356,-1.17214702216034,
17.6179219690615));
#254106=CARTESIAN_POINT('Ctrl Pts',(3.06878763241124,-0.992445624685405,
17.6290646505522));
#254107=CARTESIAN_POINT('Ctrl Pts',(3.10568223115024,-0.870142540775785,
17.6362381785194));
#254108=CARTESIAN_POINT('Ctrl Pts',(3.18966941857093,-0.517152262960961,
17.6565681261711));
#254109=CARTESIAN_POINT('Ctrl Pts',(3.21889482918857,-0.283091292451115,
17.6696624132014));
#254110=CARTESIAN_POINT('Ctrl Pts',(3.2230447656583,-0.00416058469771298,
17.6861864963438));
#254111=CARTESIAN_POINT('Ctrl Pts',(3.22280377362748,0.0396287285173819,
17.6888050265731));
#254112=CARTESIAN_POINT('Ctrl Pts',(3.22108651637423,0.105966463044588,
17.6928151405759));
#254113=CARTESIAN_POINT('Ctrl Pts',(3.22026518119588,0.128527663682848,
17.6941865318673));
#254114=CARTESIAN_POINT('Ctrl Pts',(3.21835765600317,0.1691736914367,17.6966716616179));
#254115=CARTESIAN_POINT('Ctrl Pts',(3.21735586921932,0.187261660894645,
17.6977827357985));
#254116=CARTESIAN_POINT('Ctrl Pts',(3.21488185213883,0.226011734927106,
17.7001744824493));
#254117=CARTESIAN_POINT('Ctrl Pts',(3.21336280870301,0.246669932122547,
17.701456562589));
#254118=CARTESIAN_POINT('Ctrl Pts',(3.20864859130283,0.303309402027997,
17.7049915723206));
#254119=CARTESIAN_POINT('Ctrl Pts',(3.20504752209932,0.339252985407323,
17.7072569776868));
#254120=CARTESIAN_POINT('Ctrl Pts',(3.17465999247405,0.598540196015575,
17.7237645958112));
#254121=CARTESIAN_POINT('Ctrl Pts',(3.12516304193874,0.818559122455604,
17.7387277352509));
#254122=CARTESIAN_POINT('Ctrl Pts',(2.99019542212305,1.21801893674395,17.7671974048475));
#254123=CARTESIAN_POINT('Ctrl Pts',(2.91026122179156,1.39829543549186,17.7805752354162));
#254124=CARTESIAN_POINT('Ctrl Pts',(2.80018069953023,1.59560468903524,17.7951173219205));
#254125=CARTESIAN_POINT('Ctrl Pts',(2.78564201857704,1.62085315623993,17.7969755961859));
#254126=CARTESIAN_POINT('Ctrl Pts',(2.76401902211784,1.65725397830087,17.7996471012775));
#254127=CARTESIAN_POINT('Ctrl Pts',(2.75720581692301,1.66856465277019,17.8004761261338));
#254128=CARTESIAN_POINT('Ctrl Pts',(2.74500158550529,1.68854614677531,17.8019383218671));
#254129=CARTESIAN_POINT('Ctrl Pts',(2.73963861681907,1.69723364729802,17.8025732295041));
#254130=CARTESIAN_POINT('Ctrl Pts',(2.72791163193,1.71602982574597,17.8039450375322));
#254131=CARTESIAN_POINT('Ctrl Pts',(2.72153263148444,1.72612872659547,17.8046809597432));
#254132=CARTESIAN_POINT('Ctrl Pts',(2.70322765242405,1.75475447758592,17.8067644329155));
#254133=CARTESIAN_POINT('Ctrl Pts',(2.69116737660465,1.77319520321267,17.8081035726699));
#254134=CARTESIAN_POINT('Ctrl Pts',(2.59261650338571,1.92056226395534,17.8187929099076));
#254135=CARTESIAN_POINT('Ctrl Pts',(2.4970907871426,2.04322520949682,17.8276194100026));
#254136=CARTESIAN_POINT('Ctrl Pts',(2.21214419093881,2.35913423244255,17.8515379758648));
#254137=CARTESIAN_POINT('Ctrl Pts',(2.00672256738518,2.53616821985772,17.8664297422117));
#254138=CARTESIAN_POINT('Ctrl Pts',(1.75116489487495,2.70571166991323,17.8846457079835));
#254139=CARTESIAN_POINT('Ctrl Pts',(1.72035965033006,2.72540210677262,17.8868347560242));
#254140=CARTESIAN_POINT('Ctrl Pts',(1.66968715060385,2.75659007136546,17.890428595659));
#254141=CARTESIAN_POINT('Ctrl Pts',(1.65001983023987,2.7684072172705,17.8918217730422));
#254142=CARTESIAN_POINT('Ctrl Pts',(1.61457153500309,2.78919446343336,17.8943306737719));
#254143=CARTESIAN_POINT('Ctrl Pts',(1.59883765729354,2.79824322048986,17.8954435097196));
#254144=CARTESIAN_POINT('Ctrl Pts',(1.56519309686511,2.81721624845205,17.897821968735));
#254145=CARTESIAN_POINT('Ctrl Pts',(1.5472626499982,2.82710365608828,17.8990888401014));
#254146=CARTESIAN_POINT('Ctrl Pts',(1.49843256145489,2.85342641127833,17.9025376496282));
#254147=CARTESIAN_POINT('Ctrl Pts',(1.46735813742212,2.86952999092026,17.904731063632));
#254148=CARTESIAN_POINT('Ctrl Pts',(1.2755355418821,2.96500690746804,17.9182675303777));
#254149=CARTESIAN_POINT('Ctrl Pts',(1.10868202814845,3.03134676820635,17.9300533699625));
#254150=CARTESIAN_POINT('Ctrl Pts',(0.772078383168696,3.13365563484924,
17.9536648232202));
#254151=CARTESIAN_POINT('Ctrl Pts',(0.603191002180882,3.17049889863778,
17.9654310779));
#254152=CARTESIAN_POINT('Ctrl Pts',(0.346826190347902,3.20519039019052,
17.9826451653539));
#254153=CARTESIAN_POINT('Ctrl Pts',(0.261049687578217,3.21331441310618,
17.9882947677988));
#254154=CARTESIAN_POINT('Ctrl Pts',(0.154805113255489,3.21909362352279,
17.9950794848238));
#254155=CARTESIAN_POINT('Ctrl Pts',(0.134555860861409,3.22000359451736,
17.9963630267748));
#254156=CARTESIAN_POINT('Ctrl Pts',(0.102737977576258,3.22113276520516,
17.998363460765));
#254157=CARTESIAN_POINT('Ctrl Pts',(0.0911748333047187,3.22148079966251,
17.9990870495901));
#254158=CARTESIAN_POINT('Ctrl Pts',(0.0693165475858998,3.22202091794257,
18.0004481332105));
#254159=CARTESIAN_POINT('Ctrl Pts',(0.0590223576691214,3.22222592986436,
18.001086271458));
#254160=CARTESIAN_POINT('Ctrl Pts',(0.0346314056356175,3.22259475555631,
18.0025917458571));
#254161=CARTESIAN_POINT('Ctrl Pts',(0.0205342981301641,3.22271541595605,
18.0034567202424));
#254162=CARTESIAN_POINT('Ctrl Pts',(-0.0269631770823556,3.22281027926975,
18.0063551317153));
#254163=CARTESIAN_POINT('Ctrl Pts',(-0.0603633991475908,3.2223577648033,
18.0083667228297));
#254164=CARTESIAN_POINT('Ctrl Pts',(-0.142306577188397,3.21997297284797,
18.0132497434561));
#254165=CARTESIAN_POINT('Ctrl Pts',(-0.190825420876284,3.21746223368574,
18.0160960634046));
#254166=CARTESIAN_POINT('Ctrl Pts',(-0.398940866597498,3.20196805962423,
18.0281808549244));
#254167=CARTESIAN_POINT('Ctrl Pts',(-0.557512702577019,3.17819749897144,
18.0370833854247));
#254168=CARTESIAN_POINT('Ctrl Pts',(-0.899483691786537,3.10054096992262,
18.0567327738122));
#254169=CARTESIAN_POINT('Ctrl Pts',(-1.08117002524418,3.0419543006877,18.0674831467215));
#254170=CARTESIAN_POINT('Ctrl Pts',(-1.29804426104915,2.95012261467738,
18.0814221791403));
#254171=CARTESIAN_POINT('Ctrl Pts',(-1.33910664827585,2.93171203144293,
18.084111453524));
#254172=CARTESIAN_POINT('Ctrl Pts',(-1.40040285689572,2.90267303153688,
18.0882088660067));
#254173=CARTESIAN_POINT('Ctrl Pts',(-1.42093212867533,2.89267881630506,
18.0895954617038));
#254174=CARTESIAN_POINT('Ctrl Pts',(-1.45758354693915,2.87435158989831,
18.0920975995986));
#254175=CARTESIAN_POINT('Ctrl Pts',(-1.47374491415386,2.86609887575268,
18.0932103273759));
#254176=CARTESIAN_POINT('Ctrl Pts',(-1.50806819134597,2.84820481673572,
18.0955941043907));
#254177=CARTESIAN_POINT('Ctrl Pts',(-1.52620918206665,2.83852529482359,
18.0968664540015));
#254178=CARTESIAN_POINT('Ctrl Pts',(-1.57530515822351,2.81172235425866,
18.100344530231));
#254179=CARTESIAN_POINT('Ctrl Pts',(-1.60607210872606,2.79426218562843,
18.1025620552704));
#254180=CARTESIAN_POINT('Ctrl Pts',(-1.80221023428528,2.67864470670798,
18.1169499368491));
#254181=CARTESIAN_POINT('Ctrl Pts',(-1.95877594731079,2.56637377176082,
18.1296345684365));
#254182=CARTESIAN_POINT('Ctrl Pts',(-2.25199018614511,2.31357764317786,
18.1556769105649));
#254183=CARTESIAN_POINT('Ctrl Pts',(-2.38775284644008,2.17318699958612,
18.1689847211067));
#254184=CARTESIAN_POINT('Ctrl Pts',(-2.54469862468332,1.97830395846192,
18.1854026417963));
#254185=CARTESIAN_POINT('Ctrl Pts',(-2.57828274893087,1.93433102609601,
18.1889856346784));
#254186=CARTESIAN_POINT('Ctrl Pts',(-2.62103777781216,1.87525683729302,
18.1936193642435));
#254187=CARTESIAN_POINT('Ctrl Pts',(-2.6312386711322,1.86091652856936,18.1947306589211));
#254188=CARTESIAN_POINT('Ctrl Pts',(-2.64761437313051,1.83749185316269,
18.1965231200787));
#254189=CARTESIAN_POINT('Ctrl Pts',(-2.65386095401943,1.8284584283938,18.1972089183166));
#254190=CARTESIAN_POINT('Ctrl Pts',(-2.66601606803106,1.81068692589094,
18.1985471808549));
#254191=CARTESIAN_POINT('Ctrl Pts',(-2.67192805558701,1.80195152212593,
18.1991998513965));
#254192=CARTESIAN_POINT('Ctrl Pts',(-2.68647385832126,1.78023002569174,
18.2008104893122));
#254193=CARTESIAN_POINT('Ctrl Pts',(-2.69505664827311,1.76720978406804,
18.2017651314263));
#254194=CARTESIAN_POINT('Ctrl Pts',(-2.72721350748557,1.71764810096852,
18.2053603173965));
#254195=CARTESIAN_POINT('Ctrl Pts',(-2.75014276367233,1.68069143605924,
18.2079621638664));
#254196=CARTESIAN_POINT('Ctrl Pts',(-2.80810865319885,1.58289928559105,
18.2146738034993));
#254197=CARTESIAN_POINT('Ctrl Pts',(-2.84191908301163,1.52136170477148,
18.2187269178208));
#254198=CARTESIAN_POINT('Ctrl Pts',(-2.98089375547082,1.2475886256167,18.2362361508487));
#254199=CARTESIAN_POINT('Ctrl Pts',(-3.06448938295378,1.02523947877056,
18.2491745562937));
#254200=CARTESIAN_POINT('Ctrl Pts',(-3.14858394382219,0.695197772479143,
18.268710488841));
#254201=CARTESIAN_POINT('Ctrl Pts',(-3.16932841715508,0.593494019285088,
18.2747641589785));
#254202=CARTESIAN_POINT('Ctrl Pts',(-3.18992542040926,0.459873426055491,
18.2828545129448));
#254203=CARTESIAN_POINT('Ctrl Pts',(-3.1942634608599,0.428705719113672,
18.2847509793399));
#254204=CARTESIAN_POINT('Ctrl Pts',(-3.2005745536457,0.377926382253047,
18.2878581487327));
#254205=CARTESIAN_POINT('Ctrl Pts',(-3.20282537718829,0.358350945811895,
18.2890601425752));
#254206=CARTESIAN_POINT('Ctrl Pts',(-3.20672645333371,0.321443763535929,
18.2913347412043));
#254207=CARTESIAN_POINT('Ctrl Pts',(-3.20841605407078,0.304116827648259,
18.2924060738819));
#254208=CARTESIAN_POINT('Ctrl Pts',(-3.21154891869243,0.269049945751382,
18.2945816062546));
#254209=CARTESIAN_POINT('Ctrl Pts',(-3.21298577170707,0.251310049660437,
18.2956859668293));
#254210=CARTESIAN_POINT('Ctrl Pts',(-3.21670070412515,0.200184663514372,
18.2988799647788));
#254211=CARTESIAN_POINT('Ctrl Pts',(-3.21860578846535,0.166775188916709,
18.3009810583889));
#254212=CARTESIAN_POINT('Ctrl Pts',(-3.22185559410359,0.0882983566951195,
18.3059503638159));
#254213=CARTESIAN_POINT('Ctrl Pts',(-3.2227754459306,0.0432216725679329,
18.3088310051166));
#254214=CARTESIAN_POINT('Ctrl Pts',(-3.22274946474069,-0.00185742123099253,
18.3117384119226));
#254215=CARTESIAN_POINT('Origin',(0.,0.,-2.31077344927308));
#254216=CARTESIAN_POINT('',(-3.22274894448647,-0.00260831580021831,19.564226550678));
#254217=CARTESIAN_POINT('',(-3.22275,-3.50678552687464E-13,-2.31077344927308));
#254218=CARTESIAN_POINT('Ctrl Pts',(-3.2227491362909,-0.00235945677226465,
18.5607734492731));
#254219=CARTESIAN_POINT('Ctrl Pts',(-3.22263491557699,-0.158371938722146,
18.5704359656195));
#254220=CARTESIAN_POINT('Ctrl Pts',(-3.21119034460807,-0.313970114175422,
18.5800984819659));
#254221=CARTESIAN_POINT('Ctrl Pts',(-3.1886034015463,-0.467895191412923,
18.5897609983122));
#254222=CARTESIAN_POINT('Ctrl Pts',(-3.17416265308995,-0.56630573397433,
18.5959386367661));
#254223=CARTESIAN_POINT('Ctrl Pts',(-3.15513682808653,-0.664216922908074,
18.60211627522));
#254224=CARTESIAN_POINT('Ctrl Pts',(-3.13157146815107,-0.761168642524225,
18.6082939136738));
#254225=CARTESIAN_POINT('Ctrl Pts',(-3.10803764030761,-0.85799063399059,
18.6144632860174));
#254226=CARTESIAN_POINT('Ctrl Pts',(-3.07997645292916,-0.953855290442885,
18.6206326583609));
#254227=CARTESIAN_POINT('Ctrl Pts',(-3.04748497176422,-1.0483095484499,
18.6268020307045));
#254228=CARTESIAN_POINT('Ctrl Pts',(-3.01502741669461,-1.14266518170832,
18.6329649612761));
#254229=CARTESIAN_POINT('Ctrl Pts',(-2.97814890538086,-1.23561293679921,
18.6391278918476));
#254230=CARTESIAN_POINT('Ctrl Pts',(-2.9369968944381,-1.326712781487,18.6452908224192));
#254231=CARTESIAN_POINT('Ctrl Pts',(-2.89587431896789,-1.41774746369751,
18.6514493447305));
#254232=CARTESIAN_POINT('Ctrl Pts',(-2.85048449945467,-1.50693646966807,
18.6576078670418));
#254233=CARTESIAN_POINT('Ctrl Pts',(-2.80102346763223,-1.59385855591816,
18.6637663893531));
#254234=CARTESIAN_POINT('Ctrl Pts',(-2.75158067595274,-1.68074858721064,
18.6699226405365));
#254235=CARTESIAN_POINT('Ctrl Pts',(-2.69806986956362,-1.76537298367274,
18.67607889172));
#254236=CARTESIAN_POINT('Ctrl Pts',(-2.64073319146657,-1.8473347758289,
18.6822351429034));
#254237=CARTESIAN_POINT('Ctrl Pts',(-2.58340239936084,-1.929288154062,18.6883907621068));
#254238=CARTESIAN_POINT('Ctrl Pts',(-2.52224676498393,-2.00857911631731,
18.6945463813101));
#254239=CARTESIAN_POINT('Ctrl Pts',(-2.45755138823881,-2.08484021849769,
18.7007020005134));
#254240=CARTESIAN_POINT('Ctrl Pts',(-2.39284543631133,-2.16111378640751,
18.7068586259215));
#254241=CARTESIAN_POINT('Ctrl Pts',(-2.32459887311663,-2.23435617990362,
18.7130152513296));
#254242=CARTESIAN_POINT('Ctrl Pts',(-2.25313599070401,-2.30423431314922,
18.7191718767377));
#254243=CARTESIAN_POINT('Ctrl Pts',(-2.18159729072221,-2.37418658264601,
18.7253350339334));
#254244=CARTESIAN_POINT('Ctrl Pts',(-2.10683576834955,-2.44076716120869,
18.7314981911291));
#254245=CARTESIAN_POINT('Ctrl Pts',(-2.02921127881055,-2.50368111956137,
18.7376613483248));
#254246=CARTESIAN_POINT('Ctrl Pts',(-1.95154310885515,-2.56663048050302,
18.7438279736177));
#254247=CARTESIAN_POINT('Ctrl Pts',(-1.87100911233369,-2.62590885520437,
18.7499945989106));
#254248=CARTESIAN_POINT('Ctrl Pts',(-1.78799912244338,-2.68126401173807,
18.7561612242035));
#254249=CARTESIAN_POINT('Ctrl Pts',(-1.70485344079599,-2.73670965422969,
18.7623379297316));
#254250=CARTESIAN_POINT('Ctrl Pts',(-1.61922405341512,-2.78821904617793,
18.7685146352597));
#254251=CARTESIAN_POINT('Ctrl Pts',(-1.53152651426979,-2.83558531851691,
18.7746913407878));
#254252=CARTESIAN_POINT('Ctrl Pts',(-1.47007477354461,-2.86877598629687,
18.7790195045008));
#254253=CARTESIAN_POINT('Ctrl Pts',(-1.4076080480359,-2.8999333021914,18.7833476682138));
#254254=CARTESIAN_POINT('Ctrl Pts',(-1.34427466814874,-2.9290003719825,
18.7876758319268));
#254255=CARTESIAN_POINT('Ctrl Pts',(-1.25402867214141,-2.97041907834217,
18.7938431870539));
#254256=CARTESIAN_POINT('Ctrl Pts',(-1.16170749812771,-3.00773603028649,
18.800010542181));
#254257=CARTESIAN_POINT('Ctrl Pts',(-1.06772021979529,-3.0407385771783,
18.8061778973081));
#254258=CARTESIAN_POINT('Ctrl Pts',(-0.973859503312663,-3.0736966833388,
18.8123369475679));
#254259=CARTESIAN_POINT('Ctrl Pts',(-0.878337548590659,-3.10235178867337,
18.8184959978276));
#254260=CARTESIAN_POINT('Ctrl Pts',(-0.781585685924161,-3.12653824189925,
18.8246550480874));
#254261=CARTESIAN_POINT('Ctrl Pts',(-0.684935410674578,-3.15069929985894,
18.8308076314742));
#254262=CARTESIAN_POINT('Ctrl Pts',(-0.587058214574734,-3.17040092864544,
18.8369602148611));
#254263=CARTESIAN_POINT('Ctrl Pts',(-0.488402038454336,-3.18552680279631,
18.8431127982479));
#254264=CARTESIAN_POINT('Ctrl Pts',(-0.389816478391465,-3.20064185015821,
18.8492609777423));
#254265=CARTESIAN_POINT('Ctrl Pts',(-0.290453475577518,-3.21118758843733,
18.8554091572367));
#254266=CARTESIAN_POINT('Ctrl Pts',(-0.190771749568043,-3.21709864661728,
18.8615573367311));
#254267=CARTESIAN_POINT('Ctrl Pts',(-0.0911267494434237,-3.22300752697738,
18.8677032510428));
#254268=CARTESIAN_POINT('Ctrl Pts',(0.00883630669787303,-3.22428509431965,
18.8738491653544));
#254269=CARTESIAN_POINT('Ctrl Pts',(0.108653885497284,-3.22091786540209,
18.879995079666));
#254270=CARTESIAN_POINT('Ctrl Pts',(0.208461492104258,-3.21755097288473,
18.8861403799752));
#254271=CARTESIAN_POINT('Ctrl Pts',(0.308123215422906,-3.20954022137823,
18.8922856802843));
#254272=CARTESIAN_POINT('Ctrl Pts',(0.407176852162359,-3.19692423644402,
18.8984309805934));
#254273=CARTESIAN_POINT('Ctrl Pts',(0.506247191523591,-3.18430612417726,
18.9045773171354));
#254274=CARTESIAN_POINT('Ctrl Pts',(0.604708809017923,-3.1670812910456,
18.9107236536773));
#254275=CARTESIAN_POINT('Ctrl Pts',(0.702106957157816,-3.14533994716161,
18.9168699902193));
#254276=CARTESIAN_POINT('Ctrl Pts',(0.799610339987803,-3.12357511265044,
18.9230229676249));
#254277=CARTESIAN_POINT('Ctrl Pts',(0.896047533704754,-3.09728411840606,
18.9291759450304));
#254278=CARTESIAN_POINT('Ctrl Pts',(0.990976416704811,-3.06660778451286,
18.935328922436));
#254279=CARTESIAN_POINT('Ctrl Pts',(1.08595950261818,-3.03591393491092,
18.9414854130959));
#254280=CARTESIAN_POINT('Ctrl Pts',(1.17943215562444,-3.0008299124464,18.9476419037557));
#254281=CARTESIAN_POINT('Ctrl Pts',(1.27097176605301,-2.96154492324464,
18.9537983944155));
#254282=CARTESIAN_POINT('Ctrl Pts',(1.36266388336373,-2.92219448443925,
18.959965141916));
#254283=CARTESIAN_POINT('Ctrl Pts',(1.45241613451464,-2.8786292902949,18.9661318894164));
#254284=CARTESIAN_POINT('Ctrl Pts',(1.53982997182799,-2.83108481334633,
18.9722986369169));
#254285=CARTESIAN_POINT('Ctrl Pts',(1.60263494466419,-2.79692512335855,
18.9767293131251));
#254286=CARTESIAN_POINT('Ctrl Pts',(1.66423333746347,-2.76071224339878,
18.9811599893334));
#254287=CARTESIAN_POINT('Ctrl Pts',(1.72448723673025,-2.72254684676949,
18.9855906655416));
#254288=CARTESIAN_POINT('Ctrl Pts',(1.80863382998711,-2.66924758903294,
18.9917782536194));
#254289=CARTESIAN_POINT('Ctrl Pts',(1.89045070208243,-2.61195262486537,
18.9979658416973));
#254290=CARTESIAN_POINT('Ctrl Pts',(1.96953527651378,-2.55089167881895,
19.0041534297751));
#254291=CARTESIAN_POINT('Ctrl Pts',(2.04851354162897,-2.48991281385427,
19.0103327001973));
#254292=CARTESIAN_POINT('Ctrl Pts',(2.1247664712536,-2.42517829223164,19.0165119706195));
#254293=CARTESIAN_POINT('Ctrl Pts',(2.19791893460797,-2.3569620105958,19.0226912410417));
#254294=CARTESIAN_POINT('Ctrl Pts',(2.27099438078598,-2.2888175491715,19.0288640057368));
#254295=CARTESIAN_POINT('Ctrl Pts',(2.34097553693579,-2.217198909505,19.035036770432));
#254296=CARTESIAN_POINT('Ctrl Pts',(2.40751970038534,-2.14242069975915,
19.0412095351271));
#254297=CARTESIAN_POINT('Ctrl Pts',(2.47401488161133,-2.06769753320262,
19.0473777561369));
#254298=CARTESIAN_POINT('Ctrl Pts',(2.53707781468965,-1.98981974315313,
19.0535459771467));
#254299=CARTESIAN_POINT('Ctrl Pts',(2.59640273859391,-1.90913864910908,
19.0597141981565));
#254300=CARTESIAN_POINT('Ctrl Pts',(2.65570498379905,-1.82848839778907,
19.0658800611822));
#254301=CARTESIAN_POINT('Ctrl Pts',(2.71127180405957,-1.74503731985311,
19.0720459242079));
#254302=CARTESIAN_POINT('Ctrl Pts',(2.76283836520404,-1.65916898785407,
19.0782117872335));
#254303=CARTESIAN_POINT('Ctrl Pts',(2.81439882063367,-1.57331082305517,
19.0843769201931));
#254304=CARTESIAN_POINT('Ctrl Pts',(2.86195973645811,-1.48503634368721,
19.0905420531526));
#254305=CARTESIAN_POINT('Ctrl Pts',(2.9053007100739,-1.39475637533732,19.0967071861121));
#254306=CARTESIAN_POINT('Ctrl Pts',(2.94864798825801,-1.30446327446685,
19.1028732158789));
#254307=CARTESIAN_POINT('Ctrl Pts',(2.98777391800282,-1.21216449463458,
19.1090392456457));
#254308=CARTESIAN_POINT('Ctrl Pts',(3.02250540681059,-1.11829272925329,
19.1152052754126));
#254309=CARTESIAN_POINT('Ctrl Pts',(3.05727241787762,-1.02432495482368,
19.121377611598));
#254310=CARTESIAN_POINT('Ctrl Pts',(3.08763586295672,-0.928781388184056,
19.1275499477835));
#254311=CARTESIAN_POINT('Ctrl Pts',(3.11347195787857,-0.832111729279073,
19.1337222839689));
#254312=CARTESIAN_POINT('Ctrl Pts',(3.13932209911106,-0.73538951397717,
19.1398979758686));
#254313=CARTESIAN_POINT('Ctrl Pts',(3.16063989537245,-0.637540409039791,
19.1460736677683));
#254314=CARTESIAN_POINT('Ctrl Pts',(3.17735274297709,-0.539024219489208,
19.152249359668));
#254315=CARTESIAN_POINT('Ctrl Pts',(3.19409213289811,-0.44035157258716,
19.1584348594216));
#254316=CARTESIAN_POINT('Ctrl Pts',(3.20621191430031,-0.341010153933086,
19.1646203591753));
#254317=CARTESIAN_POINT('Ctrl Pts',(3.213691377452,-0.241464889767976,19.1708058589289));
#254318=CARTESIAN_POINT('Ctrl Pts',(3.21881014957514,-0.173338406240326,
19.175039072338));
#254319=CARTESIAN_POINT('Ctrl Pts',(3.2217566198565,-0.105116506468508,
19.1792722857471));
#254320=CARTESIAN_POINT('Ctrl Pts',(3.22253820001393,-0.0369474214390013,
19.1835054991562));
#254321=CARTESIAN_POINT('Ctrl Pts',(3.2236800145404,0.0626411502551009,
19.1896898226938));
#254322=CARTESIAN_POINT('Ctrl Pts',(3.22020294928591,0.162450337127328,
19.1958741462315));
#254323=CARTESIAN_POINT('Ctrl Pts',(3.2120810071948,0.262017491245266,19.2020584697691));
#254324=CARTESIAN_POINT('Ctrl Pts',(3.20396976937468,0.361453421354353,
19.20823464271));
#254325=CARTESIAN_POINT('Ctrl Pts',(3.19122585870917,0.460647525493929,
19.2144108156509));
#254326=CARTESIAN_POINT('Ctrl Pts',(3.17387527688867,0.559136199199179,
19.2205869885917));
#254327=CARTESIAN_POINT('Ctrl Pts',(3.15654249795328,0.657523816780688,
19.2267568243562));
#254328=CARTESIAN_POINT('Ctrl Pts',(3.13461252095266,0.755207019593721,
19.2329266601207));
#254329=CARTESIAN_POINT('Ctrl Pts',(3.10816314671735,0.851727313104451,
19.2390964958852));
#254330=CARTESIAN_POINT('Ctrl Pts',(3.08173213102797,0.948180611750678,
19.2452620491584));
#254331=CARTESIAN_POINT('Ctrl Pts',(3.05078806917497,1.04347219025267,19.2514276024317));
#254332=CARTESIAN_POINT('Ctrl Pts',(3.01545965903013,1.1371546100957,19.2575931557049));
#254333=CARTESIAN_POINT('Ctrl Pts',(2.98014383587855,1.23080365226953,19.2637565122822));
#254334=CARTESIAN_POINT('Ctrl Pts',(2.94044692111502,1.32284427106072,19.2699198688594));
#254335=CARTESIAN_POINT('Ctrl Pts',(2.89654692491375,1.41284587774914,19.2760832254367));
#254336=CARTESIAN_POINT('Ctrl Pts',(2.85265096692754,1.50283920548822,19.2822460150672));
#254337=CARTESIAN_POINT('Ctrl Pts',(2.80455288589184,1.59079350559452,19.2884088046977));
#254338=CARTESIAN_POINT('Ctrl Pts',(2.7524777063539,1.67630070050834,19.2945715943282));
#254339=CARTESIAN_POINT('Ctrl Pts',(2.70039355390231,1.76182262890334,19.30073544585));
#254340=CARTESIAN_POINT('Ctrl Pts',(2.64433116641951,1.84489624523154,19.3068992973718));
#254341=CARTESIAN_POINT('Ctrl Pts',(2.58455962065447,1.92514132722313,19.3130631488936));
#254342=CARTESIAN_POINT('Ctrl Pts',(2.52472435288427,2.00547195790622,19.3192335716521));
#254343=CARTESIAN_POINT('Ctrl Pts',(2.46117228960451,2.08296768566591,19.3254039944107));
#254344=CARTESIAN_POINT('Ctrl Pts',(2.39421357354202,2.15728044694406,19.3315744171692));
#254345=CARTESIAN_POINT('Ctrl Pts',(2.3272168682355,2.23163536980755,19.3377483407371));
#254346=CARTESIAN_POINT('Ctrl Pts',(2.25680996467729,2.30280342221827,19.3439222643049));
#254347=CARTESIAN_POINT('Ctrl Pts',(2.1833392719104,2.37047404251423,19.3500961878727));
#254348=CARTESIAN_POINT('Ctrl Pts',(2.10974889556082,2.43825489808871,19.3562801687473));
#254349=CARTESIAN_POINT('Ctrl Pts',(2.03308509281522,2.50252666436514,19.3624641496219));
#254350=CARTESIAN_POINT('Ctrl Pts',(1.95372675394799,2.56301957335636,19.3686481304964));
#254351=CARTESIAN_POINT('Ctrl Pts',(1.89909200346803,2.6046662992798,19.3729055312545));
#254352=CARTESIAN_POINT('Ctrl Pts',(1.84318076274415,2.64452283837463,19.3771629320126));
#254353=CARTESIAN_POINT('Ctrl Pts',(1.7861237533846,2.6825136532915,19.3814203327707));
#254354=CARTESIAN_POINT('Ctrl Pts',(1.70423945491699,2.73703545986005,19.3875302617398));
#254355=CARTESIAN_POINT('Ctrl Pts',(1.61969680972089,2.78791060612936,19.3936401907088));
#254356=CARTESIAN_POINT('Ctrl Pts',(1.53285811260511,2.83486570565886,19.3997501196778));
#254357=CARTESIAN_POINT('Ctrl Pts',(1.44613776612968,2.88175681106729,19.4058517215527));
#254358=CARTESIAN_POINT('Ctrl Pts',(1.35712797066862,2.92473827409539,19.4119533234276));
#254359=CARTESIAN_POINT('Ctrl Pts',(1.26622081447294,2.963579324313,19.4180549253025));
#254360=CARTESIAN_POINT('Ctrl Pts',(1.1754093790248,3.00237947682225,19.4241501024918));
#254361=CARTESIAN_POINT('Ctrl Pts',(1.08270495831135,3.03704770620832,19.4302452796812));
#254362=CARTESIAN_POINT('Ctrl Pts',(0.988524154686375,3.06739915206704,
19.4363404568705));
#254363=CARTESIAN_POINT('Ctrl Pts',(0.894407107911653,3.09773005114219,
19.4424315078549));
#254364=CARTESIAN_POINT('Ctrl Pts',(0.798816084730114,3.12374983613484,
19.4485225588393));
#254365=CARTESIAN_POINT('Ctrl Pts',(0.702186646086671,3.14532215783337,
19.4546136098237));
#254366=CARTESIAN_POINT('Ctrl Pts',(0.605590349578068,3.16688708061905,
19.4607025716887));
#254367=CARTESIAN_POINT('Ctrl Pts',(0.507956777553867,3.18400747241715,
19.4667915335537));
#254368=CARTESIAN_POINT('Ctrl Pts',(0.409734566881214,3.19659743277171,
19.4728804954187));
#254369=CARTESIAN_POINT('Ctrl Pts',(0.311518511539175,3.20918660414618,
19.4789690757042));
#254370=CARTESIAN_POINT('Ctrl Pts',(0.212714331128225,3.2172458517047,19.4850576559898));
#254371=CARTESIAN_POINT('Ctrl Pts',(0.11377758964899,3.22074094310512,19.4911462362754));
#254372=CARTESIAN_POINT('Ctrl Pts',(0.0148193130990093,3.22423679526479,
19.4972361418321));
#254373=CARTESIAN_POINT('Ctrl Pts',(-0.084271138243295,3.22316650286517,
19.5033260473889));
#254374=CARTESIAN_POINT('Ctrl Pts',(-0.183037525869199,3.21754795249794,
19.5094159529456));
#254375=CARTESIAN_POINT('Ctrl Pts',(-0.281924322382909,3.21192255239755,
19.5155132828779));
#254376=CARTESIAN_POINT('Ctrl Pts',(-0.380485822456895,3.20173784935418,
19.5216106128101));
#254377=CARTESIAN_POINT('Ctrl Pts',(-0.478270400625576,3.18706369349366,
19.5277079427424));
#254378=CARTESIAN_POINT('Ctrl Pts',(-0.576116712843525,3.17238027344161,
19.533809122084));
#254379=CARTESIAN_POINT('Ctrl Pts',(-0.673184692280438,3.15320184736592,
19.5399103014256));
#254380=CARTESIAN_POINT('Ctrl Pts',(-0.769034697704354,3.12964905320497,
19.5460114807672));
#254381=CARTESIAN_POINT('Ctrl Pts',(-0.865063614285654,3.1060522960036,
19.5521240484134));
#254382=CARTESIAN_POINT('Ctrl Pts',(-0.959869591586191,3.07806499120141,
19.5582366160596));
#254383=CARTESIAN_POINT('Ctrl Pts',(-1.0530297578369,3.04585716861608,19.5643491837058));
#254384=CARTESIAN_POINT('Ctrl Pts',(-1.1291623379385,3.01953621265861,19.5693445112656));
#254385=CARTESIAN_POINT('Ctrl Pts',(-1.20419602804471,2.99039753654828,
19.5743398388255));
#254386=CARTESIAN_POINT('Ctrl Pts',(-1.27791235770485,2.95855666981811,
19.5793351663853));
#254387=CARTESIAN_POINT('Ctrl Pts',(-1.37157794975161,2.91809896326499,
19.5856823396035));
#254388=CARTESIAN_POINT('Ctrl Pts',(-1.46345307865358,2.87313197893506,
19.5920295128216));
#254389=CARTESIAN_POINT('Ctrl Pts',(-1.55308779875617,2.82383353826934,
19.5983766860398));
#254390=CARTESIAN_POINT('Ctrl Pts',(-1.64258957084072,2.77460821804145,
19.604714445003));
#254391=CARTESIAN_POINT('Ctrl Pts',(-1.72985719519464,2.72106442031479,
19.6110522039663));
#254392=CARTESIAN_POINT('Ctrl Pts',(-1.8144617058491,2.66342754369387,19.6173899629296));
#254393=CARTESIAN_POINT('Ctrl Pts',(-1.90337904692538,2.60285254860875,
19.6240507978075));
#254394=CARTESIAN_POINT('Ctrl Pts',(-1.98935416775711,2.53775630464971,
19.6307116326855));
#254395=CARTESIAN_POINT('Ctrl Pts',(-2.07191849325825,2.46845524970466,
19.6373724675634));
#254396=CARTESIAN_POINT('Ctrl Pts',(-2.15028314560458,2.4026792254346,19.6436944959501));
#254397=CARTESIAN_POINT('Ctrl Pts',(-2.22557506805531,2.33311589840458,
19.6500165243368));
#254398=CARTESIAN_POINT('Ctrl Pts',(-2.29742423981357,2.26007951736594,
19.6563385527235));
#254399=CARTESIAN_POINT('Ctrl Pts',(-2.36922414243632,2.18709321956788,
19.6626562459054));
#254400=CARTESIAN_POINT('Ctrl Pts',(-2.43758570973843,2.11063889506989,
19.6689739390873));
#254401=CARTESIAN_POINT('Ctrl Pts',(-2.50217437088175,2.03106892551743,
19.6752916322692));
#254402=CARTESIAN_POINT('Ctrl Pts',(-2.56673232691967,1.95153678310457,
19.6816063220534));
#254403=CARTESIAN_POINT('Ctrl Pts',(-2.62752069280269,1.86889225787235,
19.6879210118376));
#254404=CARTESIAN_POINT('Ctrl Pts',(-2.68424435865614,1.78352173676765,
19.6942357016218));
#254405=CARTESIAN_POINT('Ctrl Pts',(-2.74095298125601,1.69817385613193,
19.700548716735));
#254406=CARTESIAN_POINT('Ctrl Pts',(-2.79359882727932,1.61010175635542,
19.7068617318482));
#254407=CARTESIAN_POINT('Ctrl Pts',(-2.84192976801594,1.51972127581504,
19.7131747469614));
#254408=CARTESIAN_POINT('Ctrl Pts',(-2.89027069290591,1.42932212457295,
19.7194890662104));
#254409=CARTESIAN_POINT('Ctrl Pts',(-2.93429473679977,1.3366139946142,19.7258033854594));
#254410=CARTESIAN_POINT('Ctrl Pts',(-2.97379558060105,1.24203760301276,
19.7321177047084));
#254411=CARTESIAN_POINT('Ctrl Pts',(-3.01330036367614,1.14745177965577,
19.7384326536612));
#254412=CARTESIAN_POINT('Ctrl Pts',(-3.04828089850386,1.05099769957376,
19.7447476026141));
#254413=CARTESIAN_POINT('Ctrl Pts',(-3.07857931707185,0.953135326696814,
19.7510625515669));
#254414=CARTESIAN_POINT('Ctrl Pts',(-3.1088972785572,0.855209831176631,
19.757381573753));
#254415=CARTESIAN_POINT('Ctrl Pts',(-3.13452697951299,0.755874617500144,
19.7637005959391));
#254416=CARTESIAN_POINT('Ctrl Pts',(-3.15536069062618,0.655603900652743,
19.7700196181251));
#254417=CARTESIAN_POINT('Ctrl Pts',(-3.16330684024571,0.617359820459896,
19.7724297454168));
#254418=CARTESIAN_POINT('Ctrl Pts',(-3.17055583629552,0.578979757896498,
19.7748398727084));
#254419=CARTESIAN_POINT('Ctrl Pts',(-3.1771036721075,0.54049035068261,19.77725));
#254420=CARTESIAN_POINT('Ctrl Pts',(-3.22274955323411,-0.00169694707575843,
18.3142265507618));
#254421=CARTESIAN_POINT('Ctrl Pts',(-3.22269119943203,-0.112519312871419,
18.3210373034113));
#254422=CARTESIAN_POINT('Ctrl Pts',(-3.21691235126228,-0.223143969137743,
18.3278480560609));
#254423=CARTESIAN_POINT('Ctrl Pts',(-3.20549873162767,-0.333009675585234,
18.3346588087104));
#254424=CARTESIAN_POINT('Ctrl Pts',(-3.19404741079341,-0.44323828784753,
18.3414920584777));
#254425=CARTESIAN_POINT('Ctrl Pts',(-3.17692415128044,-0.552702677011318,
18.3483253082451));
#254426=CARTESIAN_POINT('Ctrl Pts',(-3.15426565045729,-0.660852304864885,
18.3551585580124));
#254427=CARTESIAN_POINT('Ctrl Pts',(-3.13149845498245,-0.769520735185664,
18.3620245874287));
#254428=CARTESIAN_POINT('Ctrl Pts',(-3.10314290388034,-0.876861513512687,
18.368890616845));
#254429=CARTESIAN_POINT('Ctrl Pts',(-3.06938641079325,-0.982336308876813,
18.3757566462613));
#254430=CARTESIAN_POINT('Ctrl Pts',(-3.04138582663005,-1.06982631789733,
18.3814519308409));
#254431=CARTESIAN_POINT('Ctrl Pts',(-3.00967004785188,-1.15603274305358,
18.3871472154204));
#254432=CARTESIAN_POINT('Ctrl Pts',(-2.97437034114833,-1.24066056445636,
18.3928425));
#254433=CARTESIAN_POINT('Ctrl Pts',(-2.93607974300623,-1.33245877479811,
18.3990203375376));
#254434=CARTESIAN_POINT('Ctrl Pts',(-2.89346925596554,-1.42264127094073,
18.4051981750752));
#254435=CARTESIAN_POINT('Ctrl Pts',(-2.84669655593796,-1.51077340488605,
18.4113760126129));
#254436=CARTESIAN_POINT('Ctrl Pts',(-2.79998654716334,-1.59878741193469,
18.4175455697567));
#254437=CARTESIAN_POINT('Ctrl Pts',(-2.74912561595544,-1.68475613980992,
18.4237151269005));
#254438=CARTESIAN_POINT('Ctrl Pts',(-2.69431962895281,-1.768264488005,18.4298846840443));
#254439=CARTESIAN_POINT('Ctrl Pts',(-2.63957099284961,-1.85168545014719,
18.436047785148));
#254440=CARTESIAN_POINT('Ctrl Pts',(-2.5808857453445,-1.93265079106924,
18.4422108862517));
#254441=CARTESIAN_POINT('Ctrl Pts',(-2.51851537038606,-2.01077047213976,
18.4483739873553));
#254442=CARTESIAN_POINT('Ctrl Pts',(-2.45618985016622,-2.08883397208461,
18.4545326561578));
#254443=CARTESIAN_POINT('Ctrl Pts',(-2.39018474155369,-2.164055543465,18.4606913249603));
#254444=CARTESIAN_POINT('Ctrl Pts',(-2.32079396422091,-2.23607534267873,
18.4668499937628));
#254445=CARTESIAN_POINT('Ctrl Pts',(-2.25142893072578,-2.30806842269304,
18.4730063777116));
#254446=CARTESIAN_POINT('Ctrl Pts',(-2.17868102495851,-2.37686177917559,
18.4791627616604));
#254447=CARTESIAN_POINT('Ctrl Pts',(-2.10288286258792,-2.44213046922846,
18.4853191456092));
#254448=CARTESIAN_POINT('Ctrl Pts',(-2.02709265060043,-2.50739231332263,
18.491474883822));
#254449=CARTESIAN_POINT('Ctrl Pts',(-1.94825314665773,-2.56912994328705,
18.4976306220347));
#254450=CARTESIAN_POINT('Ctrl Pts',(-1.86673131002766,-2.62705762758688,
18.5037863602474));
#254451=CARTESIAN_POINT('Ctrl Pts',(-1.78519633072657,-2.68499465078938,
18.5099430908671));
#254452=CARTESIAN_POINT('Ctrl Pts',(-1.70097851313821,-2.73912025719183,
18.5160998214869));
#254453=CARTESIAN_POINT('Ctrl Pts',(-1.61447431948844,-2.78919168115286,
18.5222565521066));
#254454=CARTESIAN_POINT('Ctrl Pts',(-1.52787882874598,-2.83931595082278,
18.5284197805802));
#254455=CARTESIAN_POINT('Ctrl Pts',(-1.43899251942865,-2.88537727666669,
18.5345830090537));
#254456=CARTESIAN_POINT('Ctrl Pts',(-1.34823689880374,-2.92717864627427,
18.5407462375273));
#254457=CARTESIAN_POINT('Ctrl Pts',(-1.25743037763656,-2.96900346029627,
18.5469129226647));
#254458=CARTESIAN_POINT('Ctrl Pts',(-1.16475285886501,-3.00656339701394,
18.5530796078021));
#254459=CARTESIAN_POINT('Ctrl Pts',(-1.07064436653945,-3.03971021692815,
18.5592462929395));
#254460=CARTESIAN_POINT('Ctrl Pts',(-0.976382816372253,-3.07291094675619,
18.5654230075598));
#254461=CARTESIAN_POINT('Ctrl Pts',(-0.880686059437438,-3.10168409941806,
18.5715997221801));
#254462=CARTESIAN_POINT('Ctrl Pts',(-0.784007844963939,-3.12593174294241,
18.5777764368005));
#254463=CARTESIAN_POINT('Ctrl Pts',(-0.717024589148058,-3.14273166128978,
18.582055957867));
#254464=CARTESIAN_POINT('Ctrl Pts',(-0.649570441744555,-3.15736023489492,
18.5863354789335));
#254465=CARTESIAN_POINT('Ctrl Pts',(-0.581797922398236,-3.16979947946129,
18.5906150000001));
#254466=CARTESIAN_POINT('Ctrl Pts',(-0.483956754347427,-3.18775764642606,
18.5967932171283));
#254467=CARTESIAN_POINT('Ctrl Pts',(-0.385114911041173,-3.2012124448069,
18.6029714342565));
#254468=CARTESIAN_POINT('Ctrl Pts',(-0.285722838716668,-3.21005919290216,
18.6091496513847));
#254469=CARTESIAN_POINT('Ctrl Pts',(-0.18646356636356,-3.21889412065938,
18.6153196136588));
#254470=CARTESIAN_POINT('Ctrl Pts',(-0.0866559543274809,-3.22313319840321,
18.621489575933));
#254471=CARTESIAN_POINT('Ctrl Pts',(0.0132396819434576,-3.22272280429485,
18.6276595382071));
#254472=CARTESIAN_POINT('Ctrl Pts',(0.11303118964346,-3.22231283797046,
18.6338230690756));
#254473=CARTESIAN_POINT('Ctrl Pts',(0.212910108083359,-3.21726303748307,
18.6399865999441));
#254474=CARTESIAN_POINT('Ctrl Pts',(0.312412277492494,-3.20757168764347,
18.6461501308126));
#254475=CARTESIAN_POINT('Ctrl Pts',(0.411843453749759,-3.19788725242166,
18.6523092641038));
#254476=CARTESIAN_POINT('Ctrl Pts',(0.510897985349236,-3.18356789422133,
18.6584683973949));
#254477=CARTESIAN_POINT('Ctrl Pts',(0.609113902321486,-3.16466393421145,
18.6646275306861));
#254478=CARTESIAN_POINT('Ctrl Pts',(0.707293721249057,-3.1457669221181,
18.6707844002641));
#254479=CARTESIAN_POINT('Ctrl Pts',(0.80463511292835,-3.12228873843662,
18.6769412698421));
#254480=CARTESIAN_POINT('Ctrl Pts',(0.900684282413903,-3.09433116939874,
18.6830981394201));
#254481=CARTESIAN_POINT('Ctrl Pts',(0.996723696617756,-3.06637643988526,
18.6892543836725));
#254482=CARTESIAN_POINT('Ctrl Pts',(1.0914707335095,-3.03394335079898,18.695410627925));
#254483=CARTESIAN_POINT('Ctrl Pts',(1.1844857581927,-2.99718385340951,18.7015668721774));
#254484=CARTESIAN_POINT('Ctrl Pts',(1.27751607481518,-2.96041831265226,
18.7077241285343));
#254485=CARTESIAN_POINT('Ctrl Pts',(1.36881341055787,-2.91932511002519,
18.7138813848911));
#254486=CARTESIAN_POINT('Ctrl Pts',(1.45795807544929,-2.8741043496596,18.7200386412479));
#254487=CARTESIAN_POINT('Ctrl Pts',(1.54719720423113,-2.82883567022944,
18.7262024222621));
#254488=CARTESIAN_POINT('Ctrl Pts',(1.63427872009203,-2.7794308958885,18.7323662032762));
#254489=CARTESIAN_POINT('Ctrl Pts',(1.71880764188016,-2.72613606643439,
18.7385299842904));
#254490=CARTESIAN_POINT('Ctrl Pts',(1.80338418411655,-2.67281121265707,
18.7446972377493));
#254491=CARTESIAN_POINT('Ctrl Pts',(1.88540491295446,-2.61559218715906,
18.7508644912082));
#254492=CARTESIAN_POINT('Ctrl Pts',(1.96450564697361,-2.55476713723752,
18.7570317446672));
#254493=CARTESIAN_POINT('Ctrl Pts',(2.04373526782585,-2.49384297890499,
18.7632090470565));
#254494=CARTESIAN_POINT('Ctrl Pts',(2.12003506016258,-2.42930134066297,
18.7693863494458));
#254495=CARTESIAN_POINT('Ctrl Pts',(2.1930755387374,-2.36146929768136,18.7755636518351));
#254496=CARTESIAN_POINT('Ctrl Pts',(2.24361863711628,-2.31453037164257,
18.7798382678901));
#254497=CARTESIAN_POINT('Ctrl Pts',(2.29260178746872,-2.26601663405651,
18.784112883945));
#254498=CARTESIAN_POINT('Ctrl Pts',(2.33992711965106,-2.21604572092308,
18.7883875));
#254499=CARTESIAN_POINT('Ctrl Pts',(2.40821357708754,-2.14394191360905,
18.7945554099509));
#254500=CARTESIAN_POINT('Ctrl Pts',(2.47328428732285,-2.06855195506756,
18.8007233199017));
#254501=CARTESIAN_POINT('Ctrl Pts',(2.53480618406806,-1.99019475723114,
18.8068912298526));
#254502=CARTESIAN_POINT('Ctrl Pts',(2.59624535620559,-1.91194292136816,
18.8130508462046));
#254503=CARTESIAN_POINT('Ctrl Pts',(2.65414493297046,-1.83073211545638,
18.8192104625566));
#254504=CARTESIAN_POINT('Ctrl Pts',(2.70820918384563,-1.74691745054946,
18.8253700789086));
#254505=CARTESIAN_POINT('Ctrl Pts',(2.76221676533419,-1.66319063899427,
18.8315232388375));
#254506=CARTESIAN_POINT('Ctrl Pts',(2.81239677867969,-1.57686575804496,
18.8376763987664));
#254507=CARTESIAN_POINT('Ctrl Pts',(2.85849484813504,-1.48832952187527,
18.8438295586953));
#254508=CARTESIAN_POINT('Ctrl Pts',(2.90456000676338,-1.39985649444264,
18.8499783256944));
#254509=CARTESIAN_POINT('Ctrl Pts',(2.94654881483495,-1.30917563511837,
18.8561270926935));
#254510=CARTESIAN_POINT('Ctrl Pts',(2.98425166953833,-1.21670026520819,
18.8622758596926));
#254511=CARTESIAN_POINT('Ctrl Pts',(3.02194068156101,-1.12425884782043,
18.8684223691592));
#254512=CARTESIAN_POINT('Ctrl Pts',(3.05534670282206,-1.03002463133725,
18.8745688786259));
#254513=CARTESIAN_POINT('Ctrl Pts',(3.08430770680721,-0.9344321977702,18.8807153880925));
#254514=CARTESIAN_POINT('Ctrl Pts',(3.11326585052714,-0.838849205164271,
18.8868612905137));
#254515=CARTESIAN_POINT('Ctrl Pts',(3.13777972369421,-0.741908678491949,
18.8930071929348));
#254516=CARTESIAN_POINT('Ctrl Pts',(3.15773706262155,-0.64406071596259,
18.899153095356));
#254517=CARTESIAN_POINT('Ctrl Pts',(3.17769778682209,-0.546196155925537,
18.9053000402788));
#254518=CARTESIAN_POINT('Ctrl Pts',(3.19310035465664,-0.447424280537048,
18.9114469852016));
#254519=CARTESIAN_POINT('Ctrl Pts',(3.2038837406487,-0.348204737054074,
18.9175939301244));
#254520=CARTESIAN_POINT('Ctrl Pts',(3.21467876505075,-0.248878106824262,
18.9237475093886));
#254521=CARTESIAN_POINT('Ctrl Pts',(3.2208446059332,-0.149103276992905,
18.9299010886529));
#254522=CARTESIAN_POINT('Ctrl Pts',(3.22237221764993,-0.0493442338867971,
18.9360546679172));
#254523=CARTESIAN_POINT('Ctrl Pts',(3.22390070271224,0.0504718421146573,
18.9422117652229));
#254524=CARTESIAN_POINT('Ctrl Pts',(3.2207856918871,0.150271678729752,18.9483688625286));
#254525=CARTESIAN_POINT('Ctrl Pts',(3.21307023060905,0.249594181971336,
18.9545259598343));
#254526=CARTESIAN_POINT('Ctrl Pts',(3.20534195516567,0.349081644238824,
18.9606932831083));
#254527=CARTESIAN_POINT('Ctrl Pts',(3.19299802298441,0.448089758120606,
18.9668606063823));
#254528=CARTESIAN_POINT('Ctrl Pts',(3.17613302734705,0.546165318466194,
18.9730279296563));
#254529=CARTESIAN_POINT('Ctrl Pts',(3.16416282573154,0.615776023154999,
18.9774052864375));
#254530=CARTESIAN_POINT('Ctrl Pts',(3.14991613980794,0.684917140423283,
18.9817826432187));
#254531=CARTESIAN_POINT('Ctrl Pts',(3.13344196559922,0.753431490396909,
18.9861599999999));
#254532=CARTESIAN_POINT('Ctrl Pts',(3.11015303936351,0.85028767404578,18.9923481061771));
#254533=CARTESIAN_POINT('Ctrl Pts',(3.08232946493969,0.946227958167857,
18.9985362123543));
#254534=CARTESIAN_POINT('Ctrl Pts',(3.05005884314237,1.04079710600531,19.0047243185314));
#254535=CARTESIAN_POINT('Ctrl Pts',(3.01783153905458,1.13523931117331,19.0109041182499));
#254536=CARTESIAN_POINT('Ctrl Pts',(2.98116919236648,1.22831363344948,19.0170839179684));
#254537=CARTESIAN_POINT('Ctrl Pts',(2.94021006787556,1.31957656816996,19.023263717687));
#254538=CARTESIAN_POINT('Ctrl Pts',(2.89929399412784,1.41074357952256,19.0294370220281));
#254539=CARTESIAN_POINT('Ctrl Pts',(2.85409029833497,1.50010259697893,19.0356103263692));
#254540=CARTESIAN_POINT('Ctrl Pts',(2.80478624091127,1.587227679098,19.0417836307103));
#254541=CARTESIAN_POINT('Ctrl Pts',(2.75551838527931,1.67428878911737,19.0479524022667));
#254542=CARTESIAN_POINT('Ctrl Pts',(2.70215636711459,1.75911885081006,19.0541211738231));
#254543=CARTESIAN_POINT('Ctrl Pts',(2.64493411252976,1.84131504715419,19.0602899453795));
#254544=CARTESIAN_POINT('Ctrl Pts',(2.58773366141699,1.92347992417188,19.0664563664407));
#254545=CARTESIAN_POINT('Ctrl Pts',(2.52667614353655,2.00301257626303,19.0726227875018));
#254546=CARTESIAN_POINT('Ctrl Pts',(2.46203921655881,2.07953852059212,19.078789208563));
#254547=CARTESIAN_POINT('Ctrl Pts',(2.39740987128964,2.15605548866825,19.0849549063223));
#254548=CARTESIAN_POINT('Ctrl Pts',(2.32920223054317,2.22956612039436,19.0911206040816));
#254549=CARTESIAN_POINT('Ctrl Pts',(2.257734082123,2.29972919643166,19.0972863018409));
#254550=CARTESIAN_POINT('Ctrl Pts',(2.18625546851525,2.36990254655285,19.1034529024526));
#254551=CARTESIAN_POINT('Ctrl Pts',(2.11151570713167,2.43672706475663,19.1096195030642));
#254552=CARTESIAN_POINT('Ctrl Pts',(2.03386854812448,2.49989925626015,19.1157861036759));
#254553=CARTESIAN_POINT('Ctrl Pts',(1.95614206139006,2.5631359872322,19.1219590043559));
#254554=CARTESIAN_POINT('Ctrl Pts',(1.87550258139099,2.62271266746531,19.1281319050359));
#254555=CARTESIAN_POINT('Ctrl Pts',(1.79233586273541,2.67836698711221,19.1343048057159));
#254556=CARTESIAN_POINT('Ctrl Pts',(1.70912387208835,2.73405160231392,19.1404810666284));
#254557=CARTESIAN_POINT('Ctrl Pts',(1.62338227227255,2.78580938069555,19.1466573275408));
#254558=CARTESIAN_POINT('Ctrl Pts',(1.53552289710391,2.83342319376573,19.1528335884533));
#254559=CARTESIAN_POINT('Ctrl Pts',(1.44752442554782,2.88111238762913,19.159019627441));
#254560=CARTESIAN_POINT('Ctrl Pts',(1.35740187087157,2.92464432432897,19.1652056664287));
#254561=CARTESIAN_POINT('Ctrl Pts',(1.26558865316282,2.96384934223815,19.1713917054164));
#254562=CARTESIAN_POINT('Ctrl Pts',(1.20354514381144,2.99034244373238,19.1755719702777));
#254563=CARTESIAN_POINT('Ctrl Pts',(1.14072999841011,3.01486067514458,19.1797522351389));
#254564=CARTESIAN_POINT('Ctrl Pts',(1.07728058697486,3.03736466355739,19.1839325000001));
#254565=CARTESIAN_POINT('Ctrl Pts',(0.983403360390098,3.07066067011604,
19.1901174536928));
#254566=CARTESIAN_POINT('Ctrl Pts',(0.88782340821703,3.09965626757547,19.1963024073856));
#254567=CARTESIAN_POINT('Ctrl Pts',(0.790970226279181,3.12417727788291,
19.2024873610783));
#254568=CARTESIAN_POINT('Ctrl Pts',(0.69424450171438,3.14866601889887,19.2086641754623));
#254569=CARTESIAN_POINT('Ctrl Pts',(0.596249293724536,3.16869177320447,
19.2148409898464));
#254570=CARTESIAN_POINT('Ctrl Pts',(0.497431809052479,3.18412926211277,
19.2210178042304));
#254571=CARTESIAN_POINT('Ctrl Pts',(0.39871554260407,3.19955093848333,19.2271882917363));
#254572=CARTESIAN_POINT('Ctrl Pts',(0.299179099001634,3.21039362789837,
19.2333587792422));
#254573=CARTESIAN_POINT('Ctrl Pts',(0.199281591826288,3.21658272234046,
19.2395292667481));
#254574=CARTESIAN_POINT('Ctrl Pts',(0.0994532499881565,3.2227675316826,
19.2456954820368));
#254575=CARTESIAN_POINT('Ctrl Pts',(-0.000735228215647935,3.224305125701,
19.2518616973255));
#254576=CARTESIAN_POINT('Ctrl Pts',(-0.100818739265824,3.22117263497517,
19.2580279126142));
#254577=CARTESIAN_POINT('Ctrl Pts',(-0.200866711603791,3.21804125656729,
19.264191938338));
#254578=CARTESIAN_POINT('Ctrl Pts',(-0.300809359324772,3.21024310247892,
19.2703559640617));
#254579=CARTESIAN_POINT('Ctrl Pts',(-0.400181583041801,3.19780741494765,
19.2765199897854));
#254580=CARTESIAN_POINT('Ctrl Pts',(-0.499544768059179,3.18537285854176,
19.2826834548417));
#254581=CARTESIAN_POINT('Ctrl Pts',(-0.598337203424098,3.1683016612416,
19.2888469198979));
#254582=CARTESIAN_POINT('Ctrl Pts',(-0.6960998926732,3.14667483256856,19.2950103849541));
#254583=CARTESIAN_POINT('Ctrl Pts',(-0.793879511426865,3.12504425879094,
19.3011749173338));
#254584=CARTESIAN_POINT('Ctrl Pts',(-0.890628607825077,3.09885657975683,
19.3073394497134));
#254585=CARTESIAN_POINT('Ctrl Pts',(-0.985900301681989,3.06824349712394,
19.3135039820931));
#254586=CARTESIAN_POINT('Ctrl Pts',(-1.08127342630268,3.03759782235138,
19.3196750775263));
#254587=CARTESIAN_POINT('Ctrl Pts',(-1.17516559543678,3.0025174686337,19.3258461729595));
#254588=CARTESIAN_POINT('Ctrl Pts',(-1.26714708413827,2.96318339453701,
19.3320172683927));
#254589=CARTESIAN_POINT('Ctrl Pts',(-1.35918080956772,2.92382698243126,
19.3381918684206));
#254590=CARTESIAN_POINT('Ctrl Pts',(-1.4493013044587,2.8802122268692,19.3443664684484));
#254591=CARTESIAN_POINT('Ctrl Pts',(-1.53710260306726,2.83256653057679,
19.3505410684763));
#254592=CARTESIAN_POINT('Ctrl Pts',(-1.62504645148955,2.78484347910583,
19.3567256932771));
#254593=CARTESIAN_POINT('Ctrl Pts',(-1.71066321323486,2.73307663927585,
19.3629103180779));
#254594=CARTESIAN_POINT('Ctrl Pts',(-1.79357502569557,2.67753733675203,
19.3690949428787));
#254595=CARTESIAN_POINT('Ctrl Pts',(-1.84992566537771,2.63979030008943,
19.3732982952525));
#254596=CARTESIAN_POINT('Ctrl Pts',(-1.90502747139949,2.60030158584876,
19.3775016476262));
#254597=CARTESIAN_POINT('Ctrl Pts',(-1.95877093229023,2.55916666071494,
19.381705));
#254598=CARTESIAN_POINT('Ctrl Pts',(-2.03613542261648,2.49995234022197,
19.3877557866198));
#254599=CARTESIAN_POINT('Ctrl Pts',(-2.11097584776025,2.43710122137895,
19.3938065732395));
#254600=CARTESIAN_POINT('Ctrl Pts',(-2.18291996081745,2.37086018296414,
19.3998573598593));
#254601=CARTESIAN_POINT('Ctrl Pts',(-2.25476589126913,2.30470954413128,
19.4058998889307));
#254602=CARTESIAN_POINT('Ctrl Pts',(-2.32372302892345,2.23517847506401,
19.411942418002));
#254603=CARTESIAN_POINT('Ctrl Pts',(-2.38944943747474,2.16255611447464,
19.4179849470734));
#254604=CARTESIAN_POINT('Ctrl Pts',(-2.4557291860714,2.0893223579306,19.4240783472236));
#254605=CARTESIAN_POINT('Ctrl Pts',(-2.51872316734277,2.01294527951245,
19.4301717473738));
#254606=CARTESIAN_POINT('Ctrl Pts',(-2.57811608605867,1.93376188019765,
19.436265147524));
#254607=CARTESIAN_POINT('Ctrl Pts',(-2.63691201497651,1.85537439532161,
19.4422972996702));
#254608=CARTESIAN_POINT('Ctrl Pts',(-2.69217866538471,1.77423711730017,
19.4483294518163));
#254609=CARTESIAN_POINT('Ctrl Pts',(-2.74364938584352,1.69071156915084,
19.4543616039625));
#254610=CARTESIAN_POINT('Ctrl Pts',(-2.79510388599354,1.60721234296029,
19.4603918551566));
#254611=CARTESIAN_POINT('Ctrl Pts',(-2.84276459394218,1.52132672566836,
19.4664221063507));
#254612=CARTESIAN_POINT('Ctrl Pts',(-2.88640833827298,1.43344496484805,
19.4724523575449));
#254613=CARTESIAN_POINT('Ctrl Pts',(-2.93005099255805,1.34556539896172,
19.4784824581275));
#254614=CARTESIAN_POINT('Ctrl Pts',(-2.96967668238611,1.25569019436361,
19.4845125587101));
#254615=CARTESIAN_POINT('Ctrl Pts',(-3.0051089118833,1.16423279039011,19.4905426592928));
#254616=CARTESIAN_POINT('Ctrl Pts',(-3.04118880411217,1.07110364425051,
19.4966829835749));
#254617=CARTESIAN_POINT('Ctrl Pts',(-3.07292022257069,0.976334331643927,
19.502823307857));
#254618=CARTESIAN_POINT('Ctrl Pts',(-3.10016929488618,0.880379409996024,
19.5089636321391));
#254619=CARTESIAN_POINT('Ctrl Pts',(-3.12696636369791,0.786016174123127,
19.5150021016477));
#254620=CARTESIAN_POINT('Ctrl Pts',(-3.14942862080919,0.6905068241316,19.5210405711562));
#254621=CARTESIAN_POINT('Ctrl Pts',(-3.16748039468825,0.594294129001434,
19.5270790406648));
#254622=CARTESIAN_POINT('Ctrl Pts',(-3.18598890499804,0.495647111169271,
19.5332702923337));
#254623=CARTESIAN_POINT('Ctrl Pts',(-3.19986067498097,0.396261184100161,
19.5394615440026));
#254624=CARTESIAN_POINT('Ctrl Pts',(-3.20907084007098,0.296617440326984,
19.5456527956714));
#254625=CARTESIAN_POINT('Ctrl Pts',(-3.21828100516099,0.196973696553792,
19.5518440473403));
#254626=CARTESIAN_POINT('Ctrl Pts',(-3.22282962077333,0.0970726424224399,
19.5580352990092));
#254627=CARTESIAN_POINT('Ctrl Pts',(-3.22274894448647,-0.00260831580023724,
19.564226550678));
#254628=CARTESIAN_POINT('Origin',(0.,0.,0.));
#254629=CARTESIAN_POINT('',(-3.93722999530371,0.00274405186980325,0.404163522034968));
#254630=CARTESIAN_POINT('',(1.75148086551352,3.5285439479163,7.45444598572177E-5));
#254631=CARTESIAN_POINT('Ctrl Pts',(-3.93722999530371,0.00274405186980325,
0.404163522034968));
#254632=CARTESIAN_POINT('Ctrl Pts',(-3.93835497379214,0.1547293111658,0.396451338459333));
#254633=CARTESIAN_POINT('Ctrl Pts',(-3.86157235511925,1.60468070640351,
0.322814988217039));
#254634=CARTESIAN_POINT('Ctrl Pts',(-2.12592865623231,4.06914714944292,
0.188118662358656));
#254635=CARTESIAN_POINT('Ctrl Pts',(0.671429896126083,4.05739230139646,
0.0611345200759264));
#254636=CARTESIAN_POINT('Ctrl Pts',(1.75148086551352,3.5285439479163,7.45444598572177E-5));
#254637=CARTESIAN_POINT('',(-1.74869447533115,3.52286199445086,2.77555756156289E-16));
#254638=CARTESIAN_POINT('Origin',(0.,0.,0.));
#254639=CARTESIAN_POINT('',(-3.93488389043595,0.00402910871532618,0.220836477965015));
#254640=CARTESIAN_POINT('Ctrl Pts',(-1.74869447533115,3.52286199445086,
3.95516952522712E-15));
#254641=CARTESIAN_POINT('Ctrl Pts',(-2.91690893257059,2.9429783173172,0.0659716112048785));
#254642=CARTESIAN_POINT('Ctrl Pts',(-3.86227691191404,1.60239438884148,
0.139583770526549));
#254643=CARTESIAN_POINT('Ctrl Pts',(-3.93787086126692,0.15449063739856,
0.213195929848219));
#254644=CARTESIAN_POINT('Ctrl Pts',(-3.93673266199906,0.00403100175761811,
0.220836477965015));
#254645=CARTESIAN_POINT('',(-3.93299973577035,0.00144167622244941,1.470836477933));
#254646=CARTESIAN_POINT('Ctrl Pts',(-3.93299793819429,0.00402717760202628,
0.220836477965015));
#254647=CARTESIAN_POINT('Ctrl Pts',(-3.93311354600702,-0.108877028281689,
0.226575404348846));
#254648=CARTESIAN_POINT('Ctrl Pts',(-3.92836338289706,-0.222004398198187,
0.232314330732677));
#254649=CARTESIAN_POINT('Ctrl Pts',(-3.91871648337901,-0.334888224477394,
0.238053257116508));
#254650=CARTESIAN_POINT('Ctrl Pts',(-3.909081298676,-0.447634969081591,
0.243785214374049));
#254651=CARTESIAN_POINT('Ctrl Pts',(-3.89456122812118,-0.560138330773846,
0.24951717163159));
#254652=CARTESIAN_POINT('Ctrl Pts',(-3.87517729968192,-0.671929978517044,
0.255249128889131));
#254653=CARTESIAN_POINT('Ctrl Pts',(-3.85536874380315,-0.786170551992133,
0.26110665131997));
#254654=CARTESIAN_POINT('Ctrl Pts',(-3.83048071255231,-0.899667408140772,
0.266964173750808));
#254655=CARTESIAN_POINT('Ctrl Pts',(-3.80059184697523,-1.01192421292574,
0.272821696181647));
#254656=CARTESIAN_POINT('Ctrl Pts',(-3.7713872696243,-1.12161096333307,
0.278545114036871));
#254657=CARTESIAN_POINT('Ctrl Pts',(-3.73740849536641,-1.23011338996449,
0.284268531892095));
#254658=CARTESIAN_POINT('Ctrl Pts',(-3.69878062655764,-1.33697826332438,
0.289991949747319));
#254659=CARTESIAN_POINT('Ctrl Pts',(-3.66016258806189,-1.4438159409008,
0.295713911063759));
#254660=CARTESIAN_POINT('Ctrl Pts',(-3.6168979520197,-1.54901648634995,
0.301435872380199));
#254661=CARTESIAN_POINT('Ctrl Pts',(-3.5691613056908,-1.65214302466812,
0.30715783369664));
#254662=CARTESIAN_POINT('Ctrl Pts',(-3.52142416854057,-1.75527062331854,
0.312879853845464));
#254663=CARTESIAN_POINT('Ctrl Pts',(-3.46921511245753,-1.85632378025581,
0.318601873994288));
#254664=CARTESIAN_POINT('Ctrl Pts',(-3.41275596076645,-1.95488765719493,
0.324323894143112));
#254665=CARTESIAN_POINT('Ctrl Pts',(-3.35396036083763,-2.05753040159275,
0.330282708566958));
#254666=CARTESIAN_POINT('Ctrl Pts',(-3.29055555814702,-2.15747294469517,
0.336241522990803));
#254667=CARTESIAN_POINT('Ctrl Pts',(-3.22284284643409,-2.25427881753536,
0.342200337414648));
#254668=CARTESIAN_POINT('Ctrl Pts',(-3.15773097117648,-2.34736638938298,
0.347930274551024));
#254669=CARTESIAN_POINT('Ctrl Pts',(-3.08863633849219,-2.43755349830048,
0.353660211687401));
#254670=CARTESIAN_POINT('Ctrl Pts',(-3.01586797195248,-2.52448596267661,
0.359390148823777));
#254671=CARTESIAN_POINT('Ctrl Pts',(-2.94305066525653,-2.61147689323235,
0.365123939612942));
#254672=CARTESIAN_POINT('Ctrl Pts',(-2.86655500274261,-2.69520850910087,
0.370857730402108));
#254673=CARTESIAN_POINT('Ctrl Pts',(-2.78672642131459,-2.77536391357011,
0.376591521191273));
#254674=CARTESIAN_POINT('Ctrl Pts',(-2.70678384060799,-2.85563378403786,
0.382333500125608));
#254675=CARTESIAN_POINT('Ctrl Pts',(-2.62349916875116,-2.93231697145337,
0.388075479059943));
#254676=CARTESIAN_POINT('Ctrl Pts',(-2.53725013549212,-3.00513739285664,
0.393817457994278));
#254677=CARTESIAN_POINT('Ctrl Pts',(-2.52717514780255,-3.0136437473219,
0.394488194405937));
#254678=CARTESIAN_POINT('Ctrl Pts',(-2.51705974165276,-3.02209744311984,
0.395158930817596));
#254679=CARTESIAN_POINT('Ctrl Pts',(-2.50690454292716,-3.03049807996164,
0.395829667229255));
#254680=CARTESIAN_POINT('Ctrl Pts',(-2.41781056388444,-3.10419886937527,
0.401714197647443));
#254681=CARTESIAN_POINT('Ctrl Pts',(-2.32531925628814,-3.17408692819413,
0.407598728065632));
#254682=CARTESIAN_POINT('Ctrl Pts',(-2.22979024642192,-3.23983401688446,
0.413483258483821));
#254683=CARTESIAN_POINT('Ctrl Pts',(-2.13438351126278,-3.30549695097063,
0.419360256852487));
#254684=CARTESIAN_POINT('Ctrl Pts',(-2.03594714277588,-3.36702922541343,
0.425237255221152));
#254685=CARTESIAN_POINT('Ctrl Pts',(-1.9348744840283,-3.42414218908273,
0.431114253589818));
#254686=CARTESIAN_POINT('Ctrl Pts',(-1.83390449070715,-3.48119713976569,
0.43698528234661));
#254687=CARTESIAN_POINT('Ctrl Pts',(-1.73030389014374,-3.53384150821365,
0.442856311103402));
#254688=CARTESIAN_POINT('Ctrl Pts',(-1.62449517126266,-3.58182976124554,
0.448727339860194));
#254689=CARTESIAN_POINT('Ctrl Pts',(-1.51559829918762,-3.63121860846703,
0.454769721567848));
#254690=CARTESIAN_POINT('Ctrl Pts',(-1.40436279656774,-3.67567511612874,
0.460812103275502));
#254691=CARTESIAN_POINT('Ctrl Pts',(-1.29127707938659,-3.7149821674203,
0.466854484983155));
#254692=CARTESIAN_POINT('Ctrl Pts',(-1.18152407658287,-3.75313081269703,
0.472718793518591));
#254693=CARTESIAN_POINT('Ctrl Pts',(-1.07002880257866,-3.78642912584396,
0.478583102054027));
#254694=CARTESIAN_POINT('Ctrl Pts',(-0.957257541823985,-3.8147276440948,
0.484447410589463));
#254695=CARTESIAN_POINT('Ctrl Pts',(-0.844503572797165,-3.84302182320575,
0.490310819923927));
#254696=CARTESIAN_POINT('Ctrl Pts',(-0.730474404974104,-3.86631763193849,
0.496174229258391));
#254697=CARTESIAN_POINT('Ctrl Pts',(-0.615649723824761,-3.88451598240431,
0.502037638592855));
#254698=CARTESIAN_POINT('Ctrl Pts',(-0.50081517840818,-3.90271589623952,
0.507901551636417));
#254699=CARTESIAN_POINT('Ctrl Pts',(-0.385185390104271,-3.91581741691315,
0.513765464679979));
#254700=CARTESIAN_POINT('Ctrl Pts',(-0.269247752295546,-3.92377301176862,
0.519629377723542));
#254701=CARTESIAN_POINT('Ctrl Pts',(-0.153272417791312,-3.93173119335643,
0.525495197396811));
#254702=CARTESIAN_POINT('Ctrl Pts',(-0.036989444897966,-3.93454009371325,
0.531361017070082));
#254703=CARTESIAN_POINT('Ctrl Pts',(0.0791118554183913,-3.93220425643586,
0.537226836743351));
#254704=CARTESIAN_POINT('Ctrl Pts',(0.195341224038918,-3.92986584255753,
0.543099126848702));
#254705=CARTESIAN_POINT('Ctrl Pts',(0.311388108615128,-3.92237137231704,
0.548971416954052));
#254706=CARTESIAN_POINT('Ctrl Pts',(0.426766308745078,-3.90977742559856,
0.554843707059402));
#254707=CARTESIAN_POINT('Ctrl Pts',(0.542221028469673,-3.89717512649031,
0.560719891706858));
#254708=CARTESIAN_POINT('Ctrl Pts',(0.657005774981368,-3.87946667824872,
0.566596076354314));
#254709=CARTESIAN_POINT('Ctrl Pts',(0.770644217653579,-3.85675984341741,
0.57247226100177));
#254710=CARTESIAN_POINT('Ctrl Pts',(0.884443379880605,-3.83402089416866,
0.578356756373646));
#254711=CARTESIAN_POINT('Ctrl Pts',(0.997092604841083,-3.80626954806755,
0.584241251745521));
#254712=CARTESIAN_POINT('Ctrl Pts',(1.1081303468093,-3.77366348983058,0.590125747117397));
#254713=CARTESIAN_POINT('Ctrl Pts',(1.13089175721267,-3.7669796374754,0.591331998359559));
#254714=CARTESIAN_POINT('Ctrl Pts',(1.1535855204548,-3.76009195101654,0.59253824960172));
#254715=CARTESIAN_POINT('Ctrl Pts',(1.17620777064543,-3.75300203574063,
0.593744500843882));
#254716=CARTESIAN_POINT('Ctrl Pts',(1.28659360400096,-3.71840661753262,
0.599630433829332));
#254717=CARTESIAN_POINT('Ctrl Pts',(1.39562681385626,-3.67888213448853,
0.605516366814782));
#254718=CARTESIAN_POINT('Ctrl Pts',(1.50283619962322,-3.63455256628681,
0.611402299800233));
#254719=CARTESIAN_POINT('Ctrl Pts',(1.60991159789792,-3.59027840002246,
0.617280876700255));
#254720=CARTESIAN_POINT('Ctrl Pts',(1.71516732886334,-3.54121124835459,
0.623159453600278));
#254721=CARTESIAN_POINT('Ctrl Pts',(1.81814716568986,-3.48752489365939,
0.629038030500301));
#254722=CARTESIAN_POINT('Ctrl Pts',(1.92102546456795,-3.43389147362094,
0.634910811133243));
#254723=CARTESIAN_POINT('Ctrl Pts',(2.02163197087264,-3.37564810000452,
0.640783591766186));
#254724=CARTESIAN_POINT('Ctrl Pts',(2.11953087241314,-3.31301643232985,
0.646656372399129));
#254725=CARTESIAN_POINT('Ctrl Pts',(2.22024715141409,-3.24858232309515,
0.652698162484936));
#254726=CARTESIAN_POINT('Ctrl Pts',(2.31809720859455,-3.17950367824976,
0.658739952570744));
#254727=CARTESIAN_POINT('Ctrl Pts',(2.41263387155287,-3.10607256866864,
0.664781742656551));
#254728=CARTESIAN_POINT('Ctrl Pts',(2.50442748710302,-3.03477211410021,
0.670648225976528));
#254729=CARTESIAN_POINT('Ctrl Pts',(2.59309699683705,-2.95936856719085,
0.676514709296505));
#254730=CARTESIAN_POINT('Ctrl Pts',(2.6782635032127,-2.88017249611179,0.682381192616482));
#254731=CARTESIAN_POINT('Ctrl Pts',(2.76341919202161,-2.80098648425461,
0.688246930795235));
#254732=CARTESIAN_POINT('Ctrl Pts',(2.84507246129512,-2.71800918605741,
0.694112668973988));
#254733=CARTESIAN_POINT('Ctrl Pts',(2.92287945763673,-2.63158976212578,
0.699978407152741));
#254734=CARTESIAN_POINT('Ctrl Pts',(3.00069515605258,-2.54516067289053,
0.70584480136619));
#254735=CARTESIAN_POINT('Ctrl Pts',(3.07466345113915,-2.45528899800045,
0.711711195579639));
#254736=CARTESIAN_POINT('Ctrl Pts',(3.14447961111279,-2.36235835031351,
0.717577589793087));
#254737=CARTESIAN_POINT('Ctrl Pts',(3.21795039442107,-2.26456311950328,
0.723751068515206));
#254738=CARTESIAN_POINT('Ctrl Pts',(3.28682226938243,-2.16338040068169,
0.729924547237324));
#254739=CARTESIAN_POINT('Ctrl Pts',(3.35079154505351,-2.05929235942785,
0.736098025959443));
#254740=CARTESIAN_POINT('Ctrl Pts',(3.41167121663846,-1.96023158844089,
0.741973336461187));
#254741=CARTESIAN_POINT('Ctrl Pts',(3.46811063420051,-1.85853997033719,
0.74784864696293));
#254742=CARTESIAN_POINT('Ctrl Pts',(3.51989560504022,-1.75465778134043,
0.753723957464674));
#254743=CARTESIAN_POINT('Ctrl Pts',(3.57171659929356,-1.65070332830641,
0.759603355035252));
#254744=CARTESIAN_POINT('Ctrl Pts',(3.61887653269448,-1.54455564449925,
0.765482752605829));
#254745=CARTESIAN_POINT('Ctrl Pts',(3.66120966513167,-1.43667421078909,
0.771362150176407));
#254746=CARTESIAN_POINT('Ctrl Pts',(3.7036032251698,-1.32863878383888,0.777249940177917));
#254747=CARTESIAN_POINT('Ctrl Pts',(3.74115610293889,-1.21886505578006,
0.783137730179428));
#254748=CARTESIAN_POINT('Ctrl Pts',(3.77375259322463,-1.10782686604468,
0.789025520180939));
#254749=CARTESIAN_POINT('Ctrl Pts',(3.77861310973372,-1.09126977816137,
0.789903458273462));
#254750=CARTESIAN_POINT('Ctrl Pts',(3.78336351760962,-1.07468459181666,
0.790781396365985));
#254751=CARTESIAN_POINT('Ctrl Pts',(3.78800353131779,-1.05807289291615,
0.791659334458508));
#254752=CARTESIAN_POINT('Ctrl Pts',(3.81901775404746,-0.947038968875929,
0.797527542885656));
#254753=CARTESIAN_POINT('Ctrl Pts',(3.84519837414544,-0.83445237177865,
0.803395751312803));
#254754=CARTESIAN_POINT('Ctrl Pts',(3.86639062477172,-0.720772180843109,
0.809263959739951));
#254755=CARTESIAN_POINT('Ctrl Pts',(3.88755529218587,-0.607239952711398,
0.815124530279044));
#254756=CARTESIAN_POINT('Ctrl Pts',(3.9037444262341,-0.49261736447216,0.820985100818138));
#254757=CARTESIAN_POINT('Ctrl Pts',(3.91485306469716,-0.377378433182414,
0.826845671357231));
#254758=CARTESIAN_POINT('Ctrl Pts',(3.92595022710798,-0.262258552305652,
0.832700187489752));
#254759=CARTESIAN_POINT('Ctrl Pts',(3.93197729373393,-0.146524004434368,
0.838554703622273));
#254760=CARTESIAN_POINT('Ctrl Pts',(3.93288050677404,-0.0306581055645306,
0.844409219754794));
#254761=CARTESIAN_POINT('Ctrl Pts',(3.93381365302187,0.0890476825297482,
0.850457759268059));
#254762=CARTESIAN_POINT('Ctrl Pts',(3.92927733600448,0.208893237457599,
0.856506298781322));
#254763=CARTESIAN_POINT('Ctrl Pts',(3.91927053949092,0.328340430465874,
0.862554838294587));
#254764=CARTESIAN_POINT('Ctrl Pts',(3.90959602720176,0.443821277418104,
0.868402530887642));
#254765=CARTESIAN_POINT('Ctrl Pts',(3.89480861733269,0.558929353772634,
0.874250223480699));
#254766=CARTESIAN_POINT('Ctrl Pts',(3.87496032876677,0.673180102560742,
0.880097916073754));
#254767=CARTESIAN_POINT('Ctrl Pts',(3.85511512250948,0.787413108959298,
0.885944700558626));
#254768=CARTESIAN_POINT('Ctrl Pts',(3.83021067106616,0.900788644716794,
0.891791485043498));
#254769=CARTESIAN_POINT('Ctrl Pts',(3.80035047746741,1.01283031570604,0.89763826952837));
#254770=CARTESIAN_POINT('Ctrl Pts',(3.77048766277349,1.12488182159079,0.903485567237599));
#254771=CARTESIAN_POINT('Ctrl Pts',(3.73566834789256,1.23559882990257,0.909332864946827));
#254772=CARTESIAN_POINT('Ctrl Pts',(3.69604628257231,1.34451882734435,0.915180162656055));
#254773=CARTESIAN_POINT('Ctrl Pts',(3.65641110822163,1.45347486116001,0.921029394954077));
#254774=CARTESIAN_POINT('Ctrl Pts',(3.61197016544886,1.56063231309586,0.926878627252099));
#254775=CARTESIAN_POINT('Ctrl Pts',(3.56292556304311,1.66554808763179,0.932727859550121));
#254776=CARTESIAN_POINT('Ctrl Pts',(3.51382565579645,1.77058216978844,0.938583687698569));
#254777=CARTESIAN_POINT('Ctrl Pts',(3.46011190326251,1.8733691541328,0.944439515847018));
#254778=CARTESIAN_POINT('Ctrl Pts',(3.40203268499144,1.97348995696707,0.950295343995466));
#254779=CARTESIAN_POINT('Ctrl Pts',(3.34391430392436,2.07367827122274,0.956155120726732));
#254780=CARTESIAN_POINT('Ctrl Pts',(3.28142481884333,2.17119647665599,0.962014897457997));
#254781=CARTESIAN_POINT('Ctrl Pts',(3.21485531851645,2.2656553756047,0.967874674189263));
#254782=CARTESIAN_POINT('Ctrl Pts',(3.14818909663982,2.36025151775112,0.97374296482981));
#254783=CARTESIAN_POINT('Ctrl Pts',(3.07743128169455,2.45177915671903,0.979611255470357));
#254784=CARTESIAN_POINT('Ctrl Pts',(3.0029125123752,2.5398829585279,0.985479546110905));
#254785=CARTESIAN_POINT('Ctrl Pts',(2.9855805947781,2.56037454537093,0.986844420098315));
#254786=CARTESIAN_POINT('Ctrl Pts',(2.96804537837472,2.58068107986218,0.988209294085726));
#254787=CARTESIAN_POINT('Ctrl Pts',(2.9503112926361,2.60079839213729,0.989574168073137));
#254788=CARTESIAN_POINT('Ctrl Pts',(2.87394205037106,2.68743065034914,0.995451797951671));
#254789=CARTESIAN_POINT('Ctrl Pts',(2.79362831518194,2.77083868145239,1.0013294278302));
#254790=CARTESIAN_POINT('Ctrl Pts',(2.70967281965614,2.85064242065131,1.00720705770874));
#254791=CARTESIAN_POINT('Ctrl Pts',(2.62582492649507,2.93034387862374,1.01307715446666));
#254792=CARTESIAN_POINT('Ctrl Pts',(2.53834485178755,3.00644995003002,1.01894725122458));
#254793=CARTESIAN_POINT('Ctrl Pts',(2.44757487058002,3.07861433974852,1.0248173479825));
#254794=CARTESIAN_POINT('Ctrl Pts',(2.35689707581916,3.15070543895207,1.03068148304081));
#254795=CARTESIAN_POINT('Ctrl Pts',(2.2629363418411,3.21886256425645,1.03654561809912));
#254796=CARTESIAN_POINT('Ctrl Pts',(2.16607051905588,3.28277740739103,1.04240975315743));
#254797=CARTESIAN_POINT('Ctrl Pts',(2.06621762345819,3.34866320668695,1.04845472184619));
#254798=CARTESIAN_POINT('Ctrl Pts',(1.96327788442577,3.41004052912714,1.05449969053495));
#254799=CARTESIAN_POINT('Ctrl Pts',(1.85770083722228,3.46661745789518,1.06054465922372));
#254800=CARTESIAN_POINT('Ctrl Pts',(1.75539829892882,3.52143963350181,1.06640214110208));
#254801=CARTESIAN_POINT('Ctrl Pts',(1.65062002168364,3.57175458276345,1.07225962298044));
#254802=CARTESIAN_POINT('Ctrl Pts',(1.54380224754594,3.61734206572617,1.0781171048588));
#254803=CARTESIAN_POINT('Ctrl Pts',(1.43700018562714,3.66292284305852,1.08397372513862));
#254804=CARTESIAN_POINT('Ctrl Pts',(1.32815960264227,3.70377737499157,1.08983034541845));
#254805=CARTESIAN_POINT('Ctrl Pts',(1.21773786134816,3.73973307884924,1.09568696569828));
#254806=CARTESIAN_POINT('Ctrl Pts',(1.1073057625578,3.77569215533139,1.10154413532574));
#254807=CARTESIAN_POINT('Ctrl Pts',(0.99529260286013,3.80675136255577,1.1074013049532));
#254808=CARTESIAN_POINT('Ctrl Pts',(0.882171412714956,3.83278783636513,
1.11325847458067));
#254809=CARTESIAN_POINT('Ctrl Pts',(0.76901236190473,3.85883302435274,1.11911760455117));
#254810=CARTESIAN_POINT('Ctrl Pts',(0.654744944964708,3.87985204364202,
1.12497673452167));
#254811=CARTESIAN_POINT('Ctrl Pts',(0.539852207007587,3.8957731703205,1.13083586449217));
#254812=CARTESIAN_POINT('Ctrl Pts',(0.424830350794599,3.91171218941015,
1.13670157904457));
#254813=CARTESIAN_POINT('Ctrl Pts',(0.309182179743551,3.92254182454833,
1.14256729359697));
#254814=CARTESIAN_POINT('Ctrl Pts',(0.193395777696842,3.9282422370787,1.14843300814937));
#254815=CARTESIAN_POINT('Ctrl Pts',(0.0775313268123665,3.93394649212048,
1.15430267663932));
#254816=CARTESIAN_POINT('Ctrl Pts',(-0.0384711291623765,3.93451463764493,
1.16017234512928));
#254817=CARTESIAN_POINT('Ctrl Pts',(-0.154125307541816,3.92997892991491,
1.16604201361923));
#254818=CARTESIAN_POINT('Ctrl Pts',(-0.269945917752929,3.92543669508699,
1.17192012883971));
#254819=CARTESIAN_POINT('Ctrl Pts',(-0.385416840740004,3.91577598371688,
1.17779824406018));
#254820=CARTESIAN_POINT('Ctrl Pts',(-0.500058645391984,3.90108066452986,
1.18367635928065));
#254821=CARTESIAN_POINT('Ctrl Pts',(-0.524844833347922,3.8979034557922,
1.18494724008302));
#254822=CARTESIAN_POINT('Ctrl Pts',(-0.549592310496414,3.8944910933274,
1.18621812088539));
#254823=CARTESIAN_POINT('Ctrl Pts',(-0.574296314742032,3.89084473384299,
1.18748900168776));
#254824=CARTESIAN_POINT('Ctrl Pts',(-0.688538162859492,3.87398241297151,
1.19336609635453));
#254825=CARTESIAN_POINT('Ctrl Pts',(-0.802224297210271,3.85205664271962,
1.19924319102131));
#254826=CARTESIAN_POINT('Ctrl Pts',(-0.914871154585363,3.82511434737677,
1.20512028568808));
#254827=CARTESIAN_POINT('Ctrl Pts',(-1.02737392205874,3.79820651471472,
1.21098986279055));
#254828=CARTESIAN_POINT('Ctrl Pts',(-1.13883965865839,3.76629501342637,
1.21685943989303));
#254829=CARTESIAN_POINT('Ctrl Pts',(-1.2487915917321,3.72947832282468,1.22272901699551));
#254830=CARTESIAN_POINT('Ctrl Pts',(-1.35863214956261,3.69269892549975,
1.22859264854015));
#254831=CARTESIAN_POINT('Ctrl Pts',(-1.46696156508408,3.65102435259494,
1.23445628008479));
#254832=CARTESIAN_POINT('Ctrl Pts',(-1.57331555457698,3.60460360729528,
1.24031991162943));
#254833=CARTESIAN_POINT('Ctrl Pts',(-1.68296215310863,3.55674572394101,
1.2463650751158));
#254834=CARTESIAN_POINT('Ctrl Pts',(-1.79050858428811,3.50384311083602,
1.25241023860217));
#254835=CARTESIAN_POINT('Ctrl Pts',(-1.89546511648441,3.44611389715876,
1.25845540208855));
#254836=CARTESIAN_POINT('Ctrl Pts',(-1.99715512642981,3.39018136785224,
1.26431242424988));
#254837=CARTESIAN_POINT('Ctrl Pts',(-2.09641367033037,3.32971843360438,
1.27016944641122));
#254838=CARTESIAN_POINT('Ctrl Pts',(-2.19281853834584,3.26497103476996,
1.27602646857256));
#254839=CARTESIAN_POINT('Ctrl Pts',(-2.28920950689362,3.20023297109045,
1.28188264627975));
#254840=CARTESIAN_POINT('Ctrl Pts',(-2.38274727528615,3.13121190112845,
1.28773882398695));
#254841=CARTESIAN_POINT('Ctrl Pts',(-2.4730381082637,3.05819742905449,1.29359500169414));
#254842=CARTESIAN_POINT('Ctrl Pts',(-2.56333768435814,2.98517588678256,
1.2994517464716));
#254843=CARTESIAN_POINT('Ctrl Pts',(-2.65038937918525,2.9081604331004,1.30530849124905));
#254844=CARTESIAN_POINT('Ctrl Pts',(-2.7338326307723,2.82748088356484,1.3111652360265));
#254845=CARTESIAN_POINT('Ctrl Pts',(-2.81730407304,2.74677407704477,1.31702395946153));
#254846=CARTESIAN_POINT('Ctrl Pts',(-2.89716435146355,2.66240099972866,
1.32288268289656));
#254847=CARTESIAN_POINT('Ctrl Pts',(-2.97309034837575,2.57472770995206,
1.32874140633159));
#254848=CARTESIAN_POINT('Ctrl Pts',(-3.04910205755941,2.48695544647581,
1.33460674363425));
#254849=CARTESIAN_POINT('Ctrl Pts',(-3.12117035047973,2.39587584669275,
1.34047208093691));
#254850=CARTESIAN_POINT('Ctrl Pts',(-3.18901288686557,2.30188744455617,
1.34633741823958));
#254851=CARTESIAN_POINT('Ctrl Pts',(-3.25690135059727,2.20783541511315,
1.35220672619825));
#254852=CARTESIAN_POINT('Ctrl Pts',(-3.32055813548043,2.11087100616429,
1.35807603415693));
#254853=CARTESIAN_POINT('Ctrl Pts',(-3.37974558077294,2.01141960049259,
1.3639453421156));
#254854=CARTESIAN_POINT('Ctrl Pts',(-3.43901847831361,1.9118246112255,1.36982312392473));
#254855=CARTESIAN_POINT('Ctrl Pts',(-3.49380896468209,1.80973582166201,
1.37570090573386));
#254856=CARTESIAN_POINT('Ctrl Pts',(-3.54392640262637,1.70560096528107,
1.38157868754299));
#254857=CARTESIAN_POINT('Ctrl Pts',(-3.55479822534706,1.68301130898465,
1.38285373679612));
#254858=CARTESIAN_POINT('Ctrl Pts',(-3.56545033110821,1.66032543435367,
1.38412878604925));
#254859=CARTESIAN_POINT('Ctrl Pts',(-3.57588108174667,1.63754801126754,
1.38540383530239));
#254860=CARTESIAN_POINT('Ctrl Pts',(-3.6282167406232,1.52326367200564,1.3918013176194));
#254861=CARTESIAN_POINT('Ctrl Pts',(-3.67512622428012,1.40634521511715,
1.39819879993641));
#254862=CARTESIAN_POINT('Ctrl Pts',(-3.71636016386655,1.28730576493146,
1.40459628225342));
#254863=CARTESIAN_POINT('Ctrl Pts',(-3.75744538515146,1.1686956539024,1.41097069079398));
#254864=CARTESIAN_POINT('Ctrl Pts',(-3.7928957832422,1.0479800797706,1.41734509933454));
#254865=CARTESIAN_POINT('Ctrl Pts',(-3.82251035156653,0.925690883700762,
1.4237195078751));
#254866=CARTESIAN_POINT('Ctrl Pts',(-3.85205662684401,0.803683694165899,
1.43007921663086));
#254867=CARTESIAN_POINT('Ctrl Pts',(-3.8757938214186,0.680110397212712,
1.43643892538663));
#254868=CARTESIAN_POINT('Ctrl Pts',(-3.89356997535806,0.555519438895018,
1.44279863414239));
#254869=CARTESIAN_POINT('Ctrl Pts',(-3.91128399626355,0.431363963656041,
1.44913611379272));
#254870=CARTESIAN_POINT('Ctrl Pts',(-3.92307847021014,0.306198207414769,
1.45547359344305));
#254871=CARTESIAN_POINT('Ctrl Pts',(-3.9288521876697,0.180580971984852,
1.46181107309338));
#254872=CARTESIAN_POINT('Ctrl Pts',(-3.9315930321051,0.120949148444982,
1.46481954137325));
#254873=CARTESIAN_POINT('Ctrl Pts',(-3.9329778250335,0.0612157925789621,
1.46782800965313));
#254874=CARTESIAN_POINT('Ctrl Pts',(-3.93299973577035,0.0014416762224595,
1.470836477933));
#254875=CARTESIAN_POINT('',(-3.93299840952093,-0.00353704761472742,2.72083647800911));
#254876=CARTESIAN_POINT('Ctrl Pts',(-3.93299973577059,0.00144167558636852,
1.47083647796501));
#254877=CARTESIAN_POINT('Ctrl Pts',(-3.93304331884989,-0.117456251947492,
1.47682068426248));
#254878=CARTESIAN_POINT('Ctrl Pts',(-3.92769097363441,-0.236318755341996,
1.48280489055995));
#254879=CARTESIAN_POINT('Ctrl Pts',(-3.91697863997465,-0.354636904428063,
1.48878909685742));
#254880=CARTESIAN_POINT('Ctrl Pts',(-3.90626038729162,-0.473020429360419,
1.49477660968524));
#254881=CARTESIAN_POINT('Ctrl Pts',(-3.89017628169922,-0.590858615918335,
1.50076412251306));
#254882=CARTESIAN_POINT('Ctrl Pts',(-3.86881396591898,-0.707649275496164,
1.50675163534088));
#254883=CARTESIAN_POINT('Ctrl Pts',(-3.84743570814185,-0.824527092119618,
1.5127436164535));
#254884=CARTESIAN_POINT('Ctrl Pts',(-3.82077146341929,-0.940355444834012,
1.51873559756612));
#254885=CARTESIAN_POINT('Ctrl Pts',(-3.78895954349243,-1.05464428969091,
1.52472757867874));
#254886=CARTESIAN_POINT('Ctrl Pts',(-3.7570959412729,-1.16911881053159,
1.53072929448584));
#254887=CARTESIAN_POINT('Ctrl Pts',(-3.72006806543135,-1.28204845581664,
1.53673101029295));
#254888=CARTESIAN_POINT('Ctrl Pts',(-3.6780636878262,-1.39295962191815,
1.54273272610005));
#254889=CARTESIAN_POINT('Ctrl Pts',(-3.63601965285659,-1.50397550197536,
1.54874010827444));
#254890=CARTESIAN_POINT('Ctrl Pts',(-3.58898990357719,-1.61296875038297,
1.55474749044884));
#254891=CARTESIAN_POINT('Ctrl Pts',(-3.53720909265351,-1.71948853873742,
1.56075487262323));
#254892=CARTESIAN_POINT('Ctrl Pts',(-3.48533727340255,-1.826195542927,1.56677281318388));
#254893=CARTESIAN_POINT('Ctrl Pts',(-3.42869789966955,-1.93042006630803,
1.57279075374454));
#254894=CARTESIAN_POINT('Ctrl Pts',(-3.36757026993159,-2.03173804341821,
1.5788086943052));
#254895=CARTESIAN_POINT('Ctrl Pts',(-3.35230014801198,-2.05704800341098,
1.58031201917581));
#254896=CARTESIAN_POINT('Ctrl Pts',(-3.33675014438406,-2.08217673920702,
1.58181534404641));
#254897=CARTESIAN_POINT('Ctrl Pts',(-3.32092500819953,-2.10711795823465,
1.58331866891702));
#254898=CARTESIAN_POINT('Ctrl Pts',(-3.25906702428011,-2.20460928516867,
1.58919493087061));
#254899=CARTESIAN_POINT('Ctrl Pts',(-3.19281041116404,-2.29953508526944,
1.5950711928242));
#254900=CARTESIAN_POINT('Ctrl Pts',(-3.12239447932152,-2.39147270850046,
1.60094745477779));
#254901=CARTESIAN_POINT('Ctrl Pts',(-3.05206887796362,-2.48329239293772,
1.60681617858516));
#254902=CARTESIAN_POINT('Ctrl Pts',(-2.97759481769122,-2.57213119913305,
1.61268490239254));
#254903=CARTESIAN_POINT('Ctrl Pts',(-2.89925595724034,-2.65759362853059,
1.61855362619991));
#254904=CARTESIAN_POINT('Ctrl Pts',(-2.82099672069398,-2.74296919360205,
1.62441638501493));
#254905=CARTESIAN_POINT('Ctrl Pts',(-2.73888077494803,-2.8249749056687,
1.63027914382994));
#254906=CARTESIAN_POINT('Ctrl Pts',(-2.65323286853758,-2.90324720706174,
1.63614190264496));
#254907=CARTESIAN_POINT('Ctrl Pts',(-2.56491557514853,-2.98395902006552,
1.64218738597357));
#254908=CARTESIAN_POINT('Ctrl Pts',(-2.47284282112379,-3.06070053310228,
1.64823286930218));
#254909=CARTESIAN_POINT('Ctrl Pts',(-2.37741309954045,-3.13311282180095,
1.6542783526308));
#254910=CARTESIAN_POINT('Ctrl Pts',(-2.28497274721762,-3.20325677033967,
1.66013445908889));
#254911=CARTESIAN_POINT('Ctrl Pts',(-2.18938295969857,-3.26933841021361,
1.66599056554699));
#254912=CARTESIAN_POINT('Ctrl Pts',(-2.09103996362314,-3.33107203022254,
1.67184667200509));
#254913=CARTESIAN_POINT('Ctrl Pts',(-1.99271139055599,-3.39279659636341,
1.67770191960516));
#254914=CARTESIAN_POINT('Ctrl Pts',(-1.89163076130424,-3.45017419128729,
1.68355716720522));
#254915=CARTESIAN_POINT('Ctrl Pts',(-1.78822262322662,-3.50296286731397,
1.68941241480529));
#254916=CARTESIAN_POINT('Ctrl Pts',(-1.68480470781403,-3.55575653455873,
1.69526821602443));
#254917=CARTESIAN_POINT('Ctrl Pts',(-1.57905921369824,-3.6039602327234,
1.70112401724356));
#254918=CARTESIAN_POINT('Ctrl Pts',(-1.47143394316256,-3.64737866842875,
1.7069798184627));
#254919=CARTESIAN_POINT('Ctrl Pts',(-1.36377253625714,-3.69081168235201,
1.71283758583158));
#254920=CARTESIAN_POINT('Ctrl Pts',(-1.25423048040731,-3.72945608458083,
1.71869535320046));
#254921=CARTESIAN_POINT('Ctrl Pts',(-1.14327346905214,-3.76316552585207,
1.72455312056934));
#254922=CARTESIAN_POINT('Ctrl Pts',(-1.03219143968109,-3.79691294838662,
1.73041748802995));
#254923=CARTESIAN_POINT('Ctrl Pts',(-0.919691667906793,-3.82571419208598,
1.73628185549057));
#254924=CARTESIAN_POINT('Ctrl Pts',(-0.806252939139831,-3.84947336633576,
1.74214622295119));
#254925=CARTESIAN_POINT('Ctrl Pts',(-0.692737581551075,-3.87324859010892,
1.74801455184168));
#254926=CARTESIAN_POINT('Ctrl Pts',(-0.57828241022721,-3.89197489578581,
1.75388288073217));
#254927=CARTESIAN_POINT('Ctrl Pts',(-0.463372574453545,-3.90560812899148,
1.75975120962266));
#254928=CARTESIAN_POINT('Ctrl Pts',(-0.348296927444828,-3.91926103451866,
1.76562800632493));
#254929=CARTESIAN_POINT('Ctrl Pts',(-0.232765716647418,-3.92780617089726,
1.77150480302721));
#254930=CARTESIAN_POINT('Ctrl Pts',(-0.117265391300309,-3.93125143281413,
1.77738159972948));
#254931=CARTESIAN_POINT('Ctrl Pts',(-0.0920307808260116,-3.93200415660251,
1.7786655673302));
#254932=CARTESIAN_POINT('Ctrl Pts',(-0.0667976280864975,-3.93251364043545,
1.77994953493092));
#254933=CARTESIAN_POINT('Ctrl Pts',(-0.0415709710780869,-3.93278029571493,
1.78123350253164));
#254934=CARTESIAN_POINT('Ctrl Pts',(0.0738785598176377,-3.93400064080135,
1.7871095667735));
#254935=CARTESIAN_POINT('Ctrl Pts',(0.189572229615238,-3.93013503998305,
1.79298563101535));
#254936=CARTESIAN_POINT('Ctrl Pts',(0.30502526520211,-3.92115398672233,
1.7988616952572));
#254937=CARTESIAN_POINT('Ctrl Pts',(0.420330200777649,-3.91218445411225,
1.80473022184379));
#254938=CARTESIAN_POINT('Ctrl Pts',(0.535394708215583,-3.89811255072205,
1.81059874843039));
#254939=CARTESIAN_POINT('Ctrl Pts',(0.649732629574102,-3.87896075129238,
1.81646727501698));
#254940=CARTESIAN_POINT('Ctrl Pts',(0.763954347843103,-3.85982841608103,
1.82232983734507));
#254941=CARTESIAN_POINT('Ctrl Pts',(0.877450544192772,-3.8356265220567,
1.82819239967315));
#254942=CARTESIAN_POINT('Ctrl Pts',(0.989739467693193,-3.80642940116987,
1.83405496200124));
#254943=CARTESIAN_POINT('Ctrl Pts',(1.10553339503263,-3.77632091683234,
1.84010051925728));
#254944=CARTESIAN_POINT('Ctrl Pts',(1.22004299834067,-3.74090027531032,
1.84614607651332));
#254945=CARTESIAN_POINT('Ctrl Pts',(1.3327501787942,-3.70030619826576,1.85219163376937));
#254946=CARTESIAN_POINT('Ctrl Pts',(1.44192182779629,-3.66098552399427,
1.858047546872));
#254947=CARTESIAN_POINT('Ctrl Pts',(1.54940202900473,-3.61681128903568,
1.86390345997463));
#254948=CARTESIAN_POINT('Ctrl Pts',(1.65473538768409,-3.56796017308853,
1.86975937307727));
#254949=CARTESIAN_POINT('Ctrl Pts',(1.76005332475921,-3.51911620931603,
1.87561442882972));
#254950=CARTESIAN_POINT('Ctrl Pts',(1.86322466997484,-3.4655968997278,1.88146948458217));
#254951=CARTESIAN_POINT('Ctrl Pts',(1.96381530701981,-3.40762651121197,
1.88732454033462));
#254952=CARTESIAN_POINT('Ctrl Pts',(2.06441548497679,-3.34965062426814,
1.89318015143271));
#254953=CARTESIAN_POINT('Ctrl Pts',(2.16243411054512,-3.2872230252367,1.8990357625308));
#254954=CARTESIAN_POINT('Ctrl Pts',(2.25746352965753,-3.22061289388622,
1.90489137362889));
#254955=CARTESIAN_POINT('Ctrl Pts',(2.35252488857384,-3.15398037457891,
1.91074895282352));
#254956=CARTESIAN_POINT('Ctrl Pts',(2.44459470543798,-3.08316276437169,
1.91660653201814));
#254957=CARTESIAN_POINT('Ctrl Pts',(2.53329663046633,-3.00847090430802,
1.92246411121276));
#254958=CARTESIAN_POINT('Ctrl Pts',(2.62209855956728,-2.93369483535944,
1.9283282943427));
#254959=CARTESIAN_POINT('Ctrl Pts',(2.70752470251825,-2.85503606469215,
1.93419247747264));
#254960=CARTESIAN_POINT('Ctrl Pts',(2.78923389782364,-2.7728438944938,1.94005666060257));
#254961=CARTESIAN_POINT('Ctrl Pts',(2.8709983184397,-2.69059617255348,1.94592480719505));
#254962=CARTESIAN_POINT('Ctrl Pts',(2.94904051192503,-2.60481060020193,
1.95179295378754));
#254963=CARTESIAN_POINT('Ctrl Pts',(3.02305924146376,-2.51586999318338,
1.95766110038002));
#254964=CARTESIAN_POINT('Ctrl Pts',(3.09718483584109,-2.42680097780559,
1.96353771913275));
#254965=CARTESIAN_POINT('Ctrl Pts',(3.16727512500263,-2.33456816467696,
1.96941433788549));
#254966=CARTESIAN_POINT('Ctrl Pts',(3.23307181699572,-2.23958380645779,
1.97529095663822));
#254967=CARTESIAN_POINT('Ctrl Pts',(3.24746800988998,-2.21880140689576,
1.97657674980757));
#254968=CARTESIAN_POINT('Ctrl Pts',(3.26165883164836,-2.19788737725816,
1.97786254297692));
#254969=CARTESIAN_POINT('Ctrl Pts',(3.2756418733088,-2.17684618607425,1.97914833614627));
#254970=CARTESIAN_POINT('Ctrl Pts',(3.33954123599477,-2.08069266386818,
1.98502412240669));
#254971=CARTESIAN_POINT('Ctrl Pts',(3.39930873664199,-1.98156448329821,
1.99089990866711));
#254972=CARTESIAN_POINT('Ctrl Pts',(3.45465558287158,-1.87985206964117,
1.99677569492753));
#254973=CARTESIAN_POINT('Ctrl Pts',(3.50993138150432,-1.7782702220968,2.00264393856317));
#254974=CARTESIAN_POINT('Ctrl Pts',(3.56079761558454,-1.67411109801916,
2.00851218219882));
#254975=CARTESIAN_POINT('Ctrl Pts',(3.6070083295756,-1.5677946008238,2.01438042583447));
#254976=CARTESIAN_POINT('Ctrl Pts',(3.65317204055434,-1.46158624295794,
2.02024270061346));
#254977=CARTESIAN_POINT('Ctrl Pts',(3.69468948707016,-1.3532252532075,2.02610497539245));
#254978=CARTESIAN_POINT('Ctrl Pts',(3.73136060182487,-1.24315608800711,
2.03196725017144));
#254979=CARTESIAN_POINT('Ctrl Pts',(3.76917889277777,-1.12964364797537,
2.03801291348767));
#254980=CARTESIAN_POINT('Ctrl Pts',(3.80184243417943,-1.01431479296164,
2.0440585768039));
#254981=CARTESIAN_POINT('Ctrl Pts',(3.82918532724637,-0.897679636396601,
2.05010424012012));
#254982=CARTESIAN_POINT('Ctrl Pts',(3.85566868752297,-0.784710944141966,
2.05595985603183));
#254983=CARTESIAN_POINT('Ctrl Pts',(3.87716080328516,-0.670517280452859,
2.06181547194353));
#254984=CARTESIAN_POINT('Ctrl Pts',(3.8935617978487,-0.555576751073317,
2.06767108785523));
#254985=CARTESIAN_POINT('Ctrl Pts',(3.90996038245756,-0.440653111002933,
2.07352584334539));
#254986=CARTESIAN_POINT('Ctrl Pts',(3.92126927511692,-0.324983232003589,
2.07938059883555));
#254987=CARTESIAN_POINT('Ctrl Pts',(3.92744009748582,-0.209053296220209,
2.08523535432571));
#254988=CARTESIAN_POINT('Ctrl Pts',(3.93361150227453,-0.0931124186392676,
2.09109066240437));
#254989=CARTESIAN_POINT('Ctrl Pts',(3.93464385080627,0.0230881522979025,
2.09694597048303));
#254990=CARTESIAN_POINT('Ctrl Pts',(3.93054084405488,0.139059962664729,
2.10280127856169));
#254991=CARTESIAN_POINT('Ctrl Pts',(3.92643645990672,0.25507070526025,2.10865855229211));
#254992=CARTESIAN_POINT('Ctrl Pts',(3.91719330699798,0.370852122281178,
2.11451582602253));
#254993=CARTESIAN_POINT('Ctrl Pts',(3.90286707613669,0.485919320472276,
2.12037309975295));
#254994=CARTESIAN_POINT('Ctrl Pts',(3.88852469792352,0.601116212967287,
2.1262369753217));
#254995=CARTESIAN_POINT('Ctrl Pts',(3.86908785786984,0.715596870093928,
2.13210085089045));
#254996=CARTESIAN_POINT('Ctrl Pts',(3.84466366834342,0.828884960244852,
2.1379647264592));
#254997=CARTESIAN_POINT('Ctrl Pts',(3.82022297686574,0.942249592323194,
2.14383256389488));
#254998=CARTESIAN_POINT('Ctrl Pts',(3.7907883305828,1.05441965472114,2.14970040133056));
#254999=CARTESIAN_POINT('Ctrl Pts',(3.7565166938021,1.16493404499403,2.15556823876624));
#255000=CARTESIAN_POINT('Ctrl Pts',(3.72219557451284,1.27560799955317,2.16144454837726));
#255001=CARTESIAN_POINT('Ctrl Pts',(3.68302366650833,1.38462112443565,2.16732085798829));
#255002=CARTESIAN_POINT('Ctrl Pts',(3.63920601205468,1.49153229996037,2.17319716759931));
#255003=CARTESIAN_POINT('Ctrl Pts',(3.62959685494493,1.51497778774868,2.17448583498651));
#255004=CARTESIAN_POINT('Ctrl Pts',(3.61976444921045,1.53832228457782,2.1757745023737));
#255005=CARTESIAN_POINT('Ctrl Pts',(3.60971124706245,1.56156130613909,2.1770631697609));
#255006=CARTESIAN_POINT('Ctrl Pts',(3.56387118189431,1.6675253807822,2.18293916788961));
#255007=CARTESIAN_POINT('Ctrl Pts',(3.51328564673423,1.77164405858943,2.18881516601832));
#255008=CARTESIAN_POINT('Ctrl Pts',(3.45812483112943,1.87346247689299,2.19469116414703));
#255009=CARTESIAN_POINT('Ctrl Pts',(3.40303479650818,1.97515024434029,2.20055962234141));
#255010=CARTESIAN_POINT('Ctrl Pts',(3.3433813518564,2.07454326261412,2.2064280805358));
#255011=CARTESIAN_POINT('Ctrl Pts',(3.27938273845134,2.1712065435484,2.21229653873019));
#255012=CARTESIAN_POINT('Ctrl Pts',(3.21544919223906,2.26777154722322,2.21815903048123));
#255013=CARTESIAN_POINT('Ctrl Pts',(3.14717949124203,2.36161199188648,2.22402152223228));
#255014=CARTESIAN_POINT('Ctrl Pts',(3.07483745964873,2.45231800481523,2.22988401398333));
#255015=CARTESIAN_POINT('Ctrl Pts',(3.00023611825712,2.54585685197964,2.23592959687467));
#255016=CARTESIAN_POINT('Ctrl Pts',(2.921304114022,2.63606187505386,2.24197517976601));
#255017=CARTESIAN_POINT('Ctrl Pts',(2.83837889454358,2.72251616175361,2.24802076265735));
#255018=CARTESIAN_POINT('Ctrl Pts',(2.75805634838872,2.80625701257563,2.25387660016827));
#255019=CARTESIAN_POINT('Ctrl Pts',(2.67398780795631,2.886478728125,2.25973243767919));
#255020=CARTESIAN_POINT('Ctrl Pts',(2.58651988086599,2.96283713792793,2.26558827519011));
#255021=CARTESIAN_POINT('Ctrl Pts',(2.49906478584445,3.03918434549481,2.27144325361459));
#255022=CARTESIAN_POINT('Ctrl Pts',(2.40821160668983,3.11166910294655,2.27729823203907));
#255023=CARTESIAN_POINT('Ctrl Pts',(2.3143417713154,3.17998603228767,2.28315321046355));
#255024=CARTESIAN_POINT('Ctrl Pts',(2.22046305898802,3.24830942212981,2.28900874257355));
#255025=CARTESIAN_POINT('Ctrl Pts',(2.12356745708081,3.31246395746161,2.29486427468355));
#255026=CARTESIAN_POINT('Ctrl Pts',(2.02406666232136,3.37218670101157,2.30071980679354));
#255027=CARTESIAN_POINT('Ctrl Pts',(1.92453245139317,3.43192950174077,2.30657730541495));
#255028=CARTESIAN_POINT('Ctrl Pts',(1.82239166153794,3.48723733879669,2.31243480403637));
#255029=CARTESIAN_POINT('Ctrl Pts',(1.71808131839746,3.53789281682948,2.31829230265778));
#255030=CARTESIAN_POINT('Ctrl Pts',(1.61365340711978,3.58860538862702,2.32415640326305));
#255031=CARTESIAN_POINT('Ctrl Pts',(1.50705143347116,3.63465495520625,2.33002050386832));
#255032=CARTESIAN_POINT('Ctrl Pts',(1.39873324863807,3.67587191005813,2.33588460447359));
#255033=CARTESIAN_POINT('Ctrl Pts',(1.29034187601629,3.7171167141376,2.34175266729958));
#255034=CARTESIAN_POINT('Ctrl Pts',(1.18023237404171,3.75352227524243,2.34762073012557));
#255035=CARTESIAN_POINT('Ctrl Pts',(1.06887697324244,3.78496909050419,2.35348879295156));
#255036=CARTESIAN_POINT('Ctrl Pts',(0.957360822683537,3.81646130157035,
2.35936532676038));
#255037=CARTESIAN_POINT('Ctrl Pts',(0.844595584209227,3.84298038715884,
2.3652418605692));
#255038=CARTESIAN_POINT('Ctrl Pts',(0.731062914969777,3.8644580492426,2.37111839437802));
#255039=CARTESIAN_POINT('Ctrl Pts',(0.706207462988379,3.86916010550686,
2.37240493071052));
#255040=CARTESIAN_POINT('Ctrl Pts',(0.68131524305133,3.87362072737202,2.37369146704302));
#255041=CARTESIAN_POINT('Ctrl Pts',(0.656391326074888,3.87783953085396,
2.37497800337552));
#255042=CARTESIAN_POINT('Ctrl Pts',(0.542557172440594,3.89710792771827,
2.38085395676873));
#255043=CARTESIAN_POINT('Ctrl Pts',(0.427686078346322,3.91139145575735,
2.38672991016195));
#255044=CARTESIAN_POINT('Ctrl Pts',(0.312252207183927,3.92058510417881,
2.39260586355516));
#255045=CARTESIAN_POINT('Ctrl Pts',(0.196966462480855,3.92976695517396,
2.39847427683764));
#255046=CARTESIAN_POINT('Ctrl Pts',(0.0811197846539712,3.93387188323681,
2.40434269012011));
#255047=CARTESIAN_POINT('Ctrl Pts',(-0.0348041591618446,3.93284600137166,
2.41021110340259));
#255048=CARTESIAN_POINT('Ctrl Pts',(-0.150610240190929,3.93182116254638,
2.41607355012182));
#255049=CARTESIAN_POINT('Ctrl Pts',(-0.266493020612717,3.92567589398727,
2.42193599684104));
#255050=CARTESIAN_POINT('Ctrl Pts',(-0.381965069665893,3.91440821651947,
2.42779844356027));
#255051=CARTESIAN_POINT('Ctrl Pts',(-0.501044665878769,3.90278851725783,
2.43384404328651));
#255052=CARTESIAN_POINT('Ctrl Pts',(-0.619686999582292,3.88572104679525,
2.43988964301276));
#255053=CARTESIAN_POINT('Ctrl Pts',(-0.73735862085761,3.86326173902921,
2.445935242739));
#255054=CARTESIAN_POINT('Ctrl Pts',(-0.851335831634707,3.84150756221567,
2.45179103521304));
#255055=CARTESIAN_POINT('Ctrl Pts',(-0.964401936260121,3.81469513307558,
2.45764682768708));
#255056=CARTESIAN_POINT('Ctrl Pts',(-1.07607951783734,3.78292768517863,
2.46350262016112));
#255057=CARTESIAN_POINT('Ctrl Pts',(-1.18774071699334,3.75116489737286,
2.46935755362606));
#255058=CARTESIAN_POINT('Ctrl Pts',(-1.29801340122305,3.71444864907143,
2.475212487091));
#255059=CARTESIAN_POINT('Ctrl Pts',(-1.40643372264266,3.67293250466347,
2.48106742055595));
#255060=CARTESIAN_POINT('Ctrl Pts',(-1.51486429943933,3.63141243328215,
2.48692290783358));
#255061=CARTESIAN_POINT('Ctrl Pts',(-1.62144177963602,3.58509171085717,
2.49277839511122));
#255062=CARTESIAN_POINT('Ctrl Pts',(-1.72572142306456,3.53417240241277,
2.49863388238885));
#255063=CARTESIAN_POINT('Ctrl Pts',(-1.83003609100383,3.48323599164804,
2.504491336355));
#255064=CARTESIAN_POINT('Ctrl Pts',(-1.93205101681309,3.42769810459332,
2.51034879032115));
#255065=CARTESIAN_POINT('Ctrl Pts',(-2.03134585949666,3.36780685299881,
2.5162062442873));
#255066=CARTESIAN_POINT('Ctrl Pts',(-2.13075262648066,3.30784809249594,
2.52207030072564));
#255067=CARTESIAN_POINT('Ctrl Pts',(-2.2274328372074,3.24352638675588,2.52793435716398));
#255068=CARTESIAN_POINT('Ctrl Pts',(-2.32099488704266,3.17513334118771,
2.53379841360232));
#255069=CARTESIAN_POINT('Ctrl Pts',(-2.41462015853048,3.10669408114079,
2.53966643249487));
#255070=CARTESIAN_POINT('Ctrl Pts',(-2.50512275224329,3.03417826059038,
2.54553445138742));
#255071=CARTESIAN_POINT('Ctrl Pts',(-2.59214525227701,2.95791683302586,
2.55140247027998));
#255072=CARTESIAN_POINT('Ctrl Pts',(-2.67929338666174,2.88154530686666,
2.55727896082923));
#255073=CARTESIAN_POINT('Ctrl Pts',(-2.76295110388891,2.80141766650173,
2.56315545137848));
#255074=CARTESIAN_POINT('Ctrl Pts',(-2.84279879779158,2.717900659567,2.56903194192774));
#255075=CARTESIAN_POINT('Ctrl Pts',(-2.86028562741945,2.69961024189912,
2.57031890694854));
#255076=CARTESIAN_POINT('Ctrl Pts',(-2.87758987875138,2.68115738336707,
2.57160587196934));
#255077=CARTESIAN_POINT('Ctrl Pts',(-2.89470846482543,2.66254613174458,
2.57289283699015));
#255078=CARTESIAN_POINT('Ctrl Pts',(-2.97199921562884,2.5785159668074,2.57870350922005));
#255079=CARTESIAN_POINT('Ctrl Pts',(-3.04577010973515,2.49096272657869,
2.58451418144996));
#255080=CARTESIAN_POINT('Ctrl Pts',(-3.11567770475681,2.4002169568773,2.59032485367986));
#255081=CARTESIAN_POINT('Ctrl Pts',(-3.18547304992174,2.30961689666062,
2.59612619577725));
#255082=CARTESIAN_POINT('Ctrl Pts',(-3.251417184205,2.21583483950157,2.60192753787464));
#255083=CARTESIAN_POINT('Ctrl Pts',(-3.3132042719903,2.11923723355013,2.60772887997203));
#255084=CARTESIAN_POINT('Ctrl Pts',(-3.37493450249722,2.02272851796671,
2.61352488359928));
#255085=CARTESIAN_POINT('Ctrl Pts',(-3.43251506141284,1.92340975574695,
2.61932088722654));
#255086=CARTESIAN_POINT('Ctrl Pts',(-3.48568123427798,1.82167926183572,
2.6251168908538));
#255087=CARTESIAN_POINT('Ctrl Pts',(-3.53881202382018,1.7200164719311,2.63090903710602));
#255088=CARTESIAN_POINT('Ctrl Pts',(-3.58753407170129,1.61594551417336,
2.63670118335824));
#255089=CARTESIAN_POINT('Ctrl Pts',(-3.63162720055065,1.50989167698238,
2.64249332961046));
#255090=CARTESIAN_POINT('Ctrl Pts',(-3.67570221153748,1.40388141730318,
2.64828309587033));
#255091=CARTESIAN_POINT('Ctrl Pts',(-3.71515192401547,1.29589028846412,
2.65407286213019));
#255092=CARTESIAN_POINT('Ctrl Pts',(-3.74980351497563,1.18636528905577,
2.65986262839006));
#255093=CARTESIAN_POINT('Ctrl Pts',(-3.78445905022108,1.0768278227496,2.66565305368143));
#255094=CARTESIAN_POINT('Ctrl Pts',(-3.81431523614364,0.965756537495509,
2.67144347897279));
#255095=CARTESIAN_POINT('Ctrl Pts',(-3.83924868942866,0.85361496045954,
2.67723390426415));
#255096=CARTESIAN_POINT('Ctrl Pts',(-3.86418350428454,0.74146725957452,
2.68302464576019));
#255097=CARTESIAN_POINT('Ctrl Pts',(-3.88419496787494,0.628249565364137,
2.68881538725622));
#255098=CARTESIAN_POINT('Ctrl Pts',(-3.89921080241616,0.514435728076061,
2.69460612875226));
#255099=CARTESIAN_POINT('Ctrl Pts',(-3.91423736986617,0.40054053976273,
2.7004010093123));
#255100=CARTESIAN_POINT('Ctrl Pts',(-3.92426113293412,0.286048778251258,
2.70619588987235));
#255101=CARTESIAN_POINT('Ctrl Pts',(-3.92926170845107,0.171439279338812,
2.71199077043239));
#255102=CARTESIAN_POINT('Ctrl Pts',(-3.93180611686232,0.113123317095084,
2.71493933960993));
#255103=CARTESIAN_POINT('Ctrl Pts',(-3.93305085275237,0.0547768964339249,
2.71788790878747));
#255104=CARTESIAN_POINT('Ctrl Pts',(-3.93299840952171,-0.00353704674266808,
2.72083647796501));
#255105=CARTESIAN_POINT('',(-3.93299972773902,0.00146342229266634,3.97083647800159));
#255106=CARTESIAN_POINT('Ctrl Pts',(-3.93299840952093,-0.003537047614731,
2.7208364780091));
#255107=CARTESIAN_POINT('Ctrl Pts',(-3.93286543410983,-0.151398240717296,
2.7283128881572));
#255108=CARTESIAN_POINT('Ctrl Pts',(-3.92439064523477,-0.298892057261803,
2.73578929830529));
#255109=CARTESIAN_POINT('Ctrl Pts',(-3.9077192050117,-0.445218614595948,
2.74326570845338));
#255110=CARTESIAN_POINT('Ctrl Pts',(-3.89069193773564,-0.59466829428622,
2.75090169143706));
#255111=CARTESIAN_POINT('Ctrl Pts',(-3.86511439039472,-0.74290061369427,
2.75853767442075));
#255112=CARTESIAN_POINT('Ctrl Pts',(-3.83118937793492,-0.889087706808858,
2.76617365740444));
#255113=CARTESIAN_POINT('Ctrl Pts',(-3.82432674017123,-0.918659665462114,
2.76771832847122));
#255114=CARTESIAN_POINT('Ctrl Pts',(-3.81712267433492,-0.948148002712915,
2.769262999538));
#255115=CARTESIAN_POINT('Ctrl Pts',(-3.80957909485044,-0.977545968268768,
2.77080767060477));
#255116=CARTESIAN_POINT('Ctrl Pts',(-3.78088320660007,-1.08937626529343,
2.77668362225439));
#255117=CARTESIAN_POINT('Ctrl Pts',(-3.74721163719714,-1.20012642413732,
2.78255957390401));
#255118=CARTESIAN_POINT('Ctrl Pts',(-3.70866130388434,-1.30932056161619,
2.78843552555362));
#255119=CARTESIAN_POINT('Ctrl Pts',(-3.67016044042314,-1.41837457533184,
2.7943039368675));
#255120=CARTESIAN_POINT('Ctrl Pts',(-3.62679340000546,-1.52587615298419,
2.80017234818137));
#255121=CARTESIAN_POINT('Ctrl Pts',(-3.57870766956689,-1.63136152209838,
2.80604075949525));
#255122=CARTESIAN_POINT('Ctrl Pts',(-3.53067083093152,-1.73673963756663,
2.8119032040242));
#255123=CARTESIAN_POINT('Ctrl Pts',(-3.47792501593129,-1.84010524885018,
2.81776564855317));
#255124=CARTESIAN_POINT('Ctrl Pts',(-3.42066666284254,-1.94101225697255,
2.82362809308212));
#255125=CARTESIAN_POINT('Ctrl Pts',(-3.36161943019168,-2.0450718266823,
2.82967369354618));
#255126=CARTESIAN_POINT('Ctrl Pts',(-3.29777320981625,-2.14651622218016,
2.83571929401023));
#255127=CARTESIAN_POINT('Ctrl Pts',(-3.22939606394173,-2.24488085701618,
2.84176489447428));
#255128=CARTESIAN_POINT('Ctrl Pts',(-3.16316572142948,-2.34015718616036,
2.84762068421668));
#255129=CARTESIAN_POINT('Ctrl Pts',(-3.0926849631957,-2.43254388693036,
2.85347647395908));
#255130=CARTESIAN_POINT('Ctrl Pts',(-3.0182422722671,-2.52164680038659,
2.85933226370148));
#255131=CARTESIAN_POINT('Ctrl Pts',(-2.94381050413745,-2.6107366399843,
2.86518719423777));
#255132=CARTESIAN_POINT('Ctrl Pts',(-2.86541822382966,-2.69654333368181,
2.87104212477407));
#255133=CARTESIAN_POINT('Ctrl Pts',(-2.7833943755537,-2.77870558896333,
2.87689705531037));
#255134=CARTESIAN_POINT('Ctrl Pts',(-2.70136277144353,-2.86087561316624,
2.88275253946457));
#255135=CARTESIAN_POINT('Ctrl Pts',(-2.61569920837702,-2.93940022179111,
2.88860802361877));
#255136=CARTESIAN_POINT('Ctrl Pts',(-2.52676916708865,-3.01395530428873,
2.89446350777296));
#255137=CARTESIAN_POINT('Ctrl Pts',(-2.43780925968775,-3.08853542523736,
2.90032095842292));
#255138=CARTESIAN_POINT('Ctrl Pts',(-2.34558100880988,-3.15914310414153,
2.90617840907287));
#255139=CARTESIAN_POINT('Ctrl Pts',(-2.25048203780732,-3.22549524840863,
2.91203585972282));
#255140=CARTESIAN_POINT('Ctrl Pts',(-2.1552758763756,-3.29192218123278,
2.91789991257511));
#255141=CARTESIAN_POINT('Ctrl Pts',(-2.05719287534988,-3.35408376960859,
2.9237639654274));
#255142=CARTESIAN_POINT('Ctrl Pts',(-1.95665870430632,-3.41174086279458,
2.9296280182797));
#255143=CARTESIAN_POINT('Ctrl Pts',(-1.85605660315932,-3.46943691439902,
2.93549603342374));
#255144=CARTESIAN_POINT('Ctrl Pts',(-1.7530003998661,-3.52262222129955,
2.94136404856778));
#255145=CARTESIAN_POINT('Ctrl Pts',(-1.64793780546317,-3.57110486955021,
2.94723206371183));
#255146=CARTESIAN_POINT('Ctrl Pts',(-1.54272353587014,-3.61965751050314,
2.95310855030394));
#255147=CARTESIAN_POINT('Ctrl Pts',(-1.43549747518267,-3.6634937886144,
2.95898503689605));
#255148=CARTESIAN_POINT('Ctrl Pts',(-1.32672465644692,-3.70247088928135,
2.96486152348817));
#255149=CARTESIAN_POINT('Ctrl Pts',(-1.30290261297253,-3.71100715962338,
2.96614851706525));
#255150=CARTESIAN_POINT('Ctrl Pts',(-1.27900642578727,-3.71931055660903,
2.96743551064233));
#255151=CARTESIAN_POINT('Ctrl Pts',(-1.25504104861124,-3.72737990635524,
2.96872250421941));
#255152=CARTESIAN_POINT('Ctrl Pts',(-1.14562388076583,-3.76422161300141,
2.97459844730202));
#255153=CARTESIAN_POINT('Ctrl Pts',(-1.03440259986148,-3.79630210987866,
2.98047439038462));
#255154=CARTESIAN_POINT('Ctrl Pts',(-0.921829096808699,-3.82344348935313,
2.98635033346722));
#255155=CARTESIAN_POINT('Ctrl Pts',(-0.809400055451564,-3.85055003923099,
2.99221873615463));
#255156=CARTESIAN_POINT('Ctrl Pts',(-0.695622640555321,-3.8727299807493,
2.99808713884204));
#255157=CARTESIAN_POINT('Ctrl Pts',(-0.580966128939605,-3.88985441334569,
3.00395554152945));
#255158=CARTESIAN_POINT('Ctrl Pts',(-0.466426196970153,-3.90696143428123,
3.00981797738341));
#255159=CARTESIAN_POINT('Ctrl Pts',(-0.351009352101416,-3.91902311043383,
3.01568041323736));
#255160=CARTESIAN_POINT('Ctrl Pts',(-0.235196710299091,-3.92596122083045,
3.02154284909132));
#255161=CARTESIAN_POINT('Ctrl Pts',(-0.115765580824421,-3.93311610779436,
3.02758845278893));
#255162=CARTESIAN_POINT('Ctrl Pts',(0.00408605061782454,-3.93482189660319,
3.03363405648654));
#255163=CARTESIAN_POINT('Ctrl Pts',(0.123822550277072,-3.93105036549303,
3.03967966018416));
#255164=CARTESIAN_POINT('Ctrl Pts',(0.239799507270431,-3.92739725468215,
3.04553544118688));
#255165=CARTESIAN_POINT('Ctrl Pts',(0.355668011357442,-3.91860565406824,
3.0513912221896));
#255166=CARTESIAN_POINT('Ctrl Pts',(0.470940374846716,-3.90470282650796,
3.05724700319232));
#255167=CARTESIAN_POINT('Ctrl Pts',(0.586195824499152,-3.89080203890026,
3.06310192498021));
#255168=CARTESIAN_POINT('Ctrl Pts',(0.700854897804681,-3.87179156504165,
3.0689568467681));
#255169=CARTESIAN_POINT('Ctrl Pts',(0.814435433910154,-3.84775050178563,
3.07481176855599));
#255170=CARTESIAN_POINT('Ctrl Pts',(0.92802670975107,-3.82370716529981,
3.0806672439626));
#255171=CARTESIAN_POINT('Ctrl Pts',(1.04053884182932,-3.79463237929988,
3.08652271936921));
#255172=CARTESIAN_POINT('Ctrl Pts',(1.15150095299908,-3.76065613360783,
3.09237819477582));
#255173=CARTESIAN_POINT('Ctrl Pts',(1.26250032974675,-3.72666847731429,
3.09823563668859));
#255174=CARTESIAN_POINT('Ctrl Pts',(1.37194825600815,-3.68777620884512,
3.10409307860135));
#255175=CARTESIAN_POINT('Ctrl Pts',(1.47939074860313,-3.64415861522896,
3.10995052051412));
#255176=CARTESIAN_POINT('Ctrl Pts',(1.5869543458508,-3.60049185769824,3.11581456468873));
#255177=CARTESIAN_POINT('Ctrl Pts',(1.6925076152002,-3.55208929986645,3.12167860886333));
#255178=CARTESIAN_POINT('Ctrl Pts',(1.79561815070364,-3.49917768295119,
3.12754265303794));
#255179=CARTESIAN_POINT('Ctrl Pts',(1.89879835767266,-3.44623031382225,
3.13341065952881));
#255180=CARTESIAN_POINT('Ctrl Pts',(1.99953218650402,-3.388768022727,3.13927866601968));
#255181=CARTESIAN_POINT('Ctrl Pts',(2.09741484233863,-3.32706176364937,
3.14514667251055));
#255182=CARTESIAN_POINT('Ctrl Pts',(2.19543880983669,-3.265266420208,3.15102315055086));
#255183=CARTESIAN_POINT('Ctrl Pts',(2.29060305210702,-3.19921511592724,
3.15689962859117));
#255184=CARTESIAN_POINT('Ctrl Pts',(2.38253451786802,-3.12922007394293,
3.16277610663149));
#255185=CARTESIAN_POINT('Ctrl Pts',(2.40266951719116,-3.11388963064682,
3.164063183699));
#255186=CARTESIAN_POINT('Ctrl Pts',(2.42264957578162,-3.09837014727083,
3.16535026076652));
#255187=CARTESIAN_POINT('Ctrl Pts',(2.44247101039903,-3.08266513967384,
3.16663733783403));
#255188=CARTESIAN_POINT('Ctrl Pts',(2.53296252505151,-3.01096649865662,
3.17251327747019));
#255189=CARTESIAN_POINT('Ctrl Pts',(2.62044358809482,-2.93516163647177,
3.17838921710635));
#255190=CARTESIAN_POINT('Ctrl Pts',(2.70451887362864,-2.8555326407146,3.18426515674252));
#255191=CARTESIAN_POINT('Ctrl Pts',(2.78848626707818,-2.7760058312095,3.19013355590622));
#255192=CARTESIAN_POINT('Ctrl Pts',(2.86905627786566,-2.6926649289364,3.19600195506993));
#255193=CARTESIAN_POINT('Ctrl Pts',(2.94586521137948,-2.6058332940509,3.20187035423364));
#255194=CARTESIAN_POINT('Ctrl Pts',(3.02259604664626,-2.5190899483547,3.20773278649134));
#255195=CARTESIAN_POINT('Ctrl Pts',(3.09557313962486,-2.42886323749221,
3.21359521874903));
#255196=CARTESIAN_POINT('Ctrl Pts',(3.16446885071461,-2.33551405323473,
3.21945765100672));
#255197=CARTESIAN_POINT('Ctrl Pts',(3.23551722081132,-2.23924815675953,
3.22550325602513));
#255198=CARTESIAN_POINT('Ctrl Pts',(3.30222464492171,-2.1396617620172,3.23154886104355));
#255199=CARTESIAN_POINT('Ctrl Pts',(3.3642757222787,-2.03718871597261,3.23759446606196));
#255200=CARTESIAN_POINT('Ctrl Pts',(3.42437843919462,-1.93793325192166,
3.24345024331006));
#255201=CARTESIAN_POINT('Ctrl Pts',(3.48011261971374,-1.8359700828469,3.24930602055816));
#255202=CARTESIAN_POINT('Ctrl Pts',(3.53123551057275,-1.73172306356126,
3.25516179780626));
#255203=CARTESIAN_POINT('Ctrl Pts',(3.58235089974168,-1.62749134131413,
3.26101671578711));
#255204=CARTESIAN_POINT('Ctrl Pts',(3.62885616305942,-1.52097680574703,
3.26687163376796));
#255205=CARTESIAN_POINT('Ctrl Pts',(3.67055502879798,-1.41262690777355,
3.2727265517488));
#255206=CARTESIAN_POINT('Ctrl Pts',(3.71225783707682,-1.30426676554451,
3.27858202329986));
#255207=CARTESIAN_POINT('Ctrl Pts',(3.7491531961434,-1.19407130118298,3.28443749485092));
#255208=CARTESIAN_POINT('Ctrl Pts',(3.78109366206613,-1.08250622108299,
3.29029296640198));
#255209=CARTESIAN_POINT('Ctrl Pts',(3.81304485465657,-0.970903673729209,
3.29615040441457));
#255210=CARTESIAN_POINT('Ctrl Pts',(3.84003773168579,-0.857930992604897,
3.30200784242717));
#255211=CARTESIAN_POINT('Ctrl Pts',(3.8619753943248,-0.744066565321826,
3.30786528043976));
#255212=CARTESIAN_POINT('Ctrl Pts',(3.8839377840147,-0.630073795674539,
3.31372932066747));
#255213=CARTESIAN_POINT('Ctrl Pts',(3.90083350862215,-0.515187679243987,
3.31959336089518));
#255214=CARTESIAN_POINT('Ctrl Pts',(3.91261721947705,-0.399894353363076,
3.32545740112289));
#255215=CARTESIAN_POINT('Ctrl Pts',(3.92440889248932,-0.28452312472169,
3.33132540363478));
#255216=CARTESIAN_POINT('Ctrl Pts',(3.93108164995838,-0.168744549773994,
3.33719340614666));
#255217=CARTESIAN_POINT('Ctrl Pts',(3.93264226122829,-0.053045689752066,
3.34306140865855));
#255218=CARTESIAN_POINT('Ctrl Pts',(3.93420512552544,0.0628202026942429,
3.34893788270323));
#255219=CARTESIAN_POINT('Ctrl Pts',(3.93064112771776,0.178605739630143,
3.3548143567479));
#255220=CARTESIAN_POINT('Ctrl Pts',(3.92200893720495,0.293828004935673,
3.36069083079258));
#255221=CARTESIAN_POINT('Ctrl Pts',(3.92011824402597,0.319064930691254,
3.3619779443446));
#255222=CARTESIAN_POINT('Ctrl Pts',(3.91798460763643,0.344274871621692,
3.36326505789663));
#255223=CARTESIAN_POINT('Ctrl Pts',(3.91560897068264,0.369452823388364,
3.36455217144866));
#255224=CARTESIAN_POINT('Ctrl Pts',(3.90476368860647,0.484395465855034,
3.37042811537752));
#255225=CARTESIAN_POINT('Ctrl Pts',(3.88883501953614,0.599049782738696,
3.37630405930639));
#255226=CARTESIAN_POINT('Ctrl Pts',(3.86784422839489,0.712930589098507,
3.38218000323526));
#255227=CARTESIAN_POINT('Ctrl Pts',(3.84688037406965,0.826665255834172,
3.38804840675179));
#255228=CARTESIAN_POINT('Ctrl Pts',(3.82086739068328,0.93962798381804,3.39391681026832));
#255229=CARTESIAN_POINT('Ctrl Pts',(3.78987838490746,1.05133763730365,3.39978521378485));
#255230=CARTESIAN_POINT('Ctrl Pts',(3.75892088800736,1.16293370710045,3.40564765044983));
#255231=CARTESIAN_POINT('Ctrl Pts',(3.72299754243153,1.27327884132832,3.41151008711481));
#255232=CARTESIAN_POINT('Ctrl Pts',(3.68223256855608,1.38190170094146,3.41737252377979));
#255233=CARTESIAN_POINT('Ctrl Pts',(3.64019392861701,1.49391838708925,3.4234181271666));
#255234=CARTESIAN_POINT('Ctrl Pts',(3.59300622314532,1.60410296817546,3.42946373055342));
#255235=CARTESIAN_POINT('Ctrl Pts',(3.54086152279313,1.71195463619896,3.43550933394023));
#255236=CARTESIAN_POINT('Ctrl Pts',(3.49035407699754,1.81641994599784,3.44136511570326));
#255237=CARTESIAN_POINT('Ctrl Pts',(3.4351964574227,1.91869625234109,3.44722089746629));
#255238=CARTESIAN_POINT('Ctrl Pts',(3.37561192235501,2.01834911490919,3.45307667922932));
#255239=CARTESIAN_POINT('Ctrl Pts',(3.31603613029114,2.11798735513682,3.45893160175728));
#255240=CARTESIAN_POINT('Ctrl Pts',(3.25203492615573,2.21500256286955,3.46478652428524));
#255241=CARTESIAN_POINT('Ctrl Pts',(3.18387667346721,2.30898642874994,3.47064144681319));
#255242=CARTESIAN_POINT('Ctrl Pts',(3.11571197624547,2.40297918103984,3.47649692293872));
#255243=CARTESIAN_POINT('Ctrl Pts',(3.04338969143918,2.4939396875457,3.48235239906424));
#255244=CARTESIAN_POINT('Ctrl Pts',(2.96722008668919,2.58149064634142,3.48820787518976));
#255245=CARTESIAN_POINT('Ctrl Pts',(2.89102490138669,2.66907100796659,3.49406531779936));
#255246=CARTESIAN_POINT('Ctrl Pts',(2.81098009764579,2.75323923373456,3.49992276040895));
#255247=CARTESIAN_POINT('Ctrl Pts',(2.7274341076162,2.83365350539049,3.50578020301854));
#255248=CARTESIAN_POINT('Ctrl Pts',(2.64379394859512,2.91415841611672,3.51164424785361));
#255249=CARTESIAN_POINT('Ctrl Pts',(2.5566450243001,2.99090064118381,3.51750829268867));
#255250=CARTESIAN_POINT('Ctrl Pts',(2.46637034291811,3.06357737483061,3.52337233752374));
#255251=CARTESIAN_POINT('Ctrl Pts',(2.3760346635397,3.13630321565863,3.52924034465454));
#255252=CARTESIAN_POINT('Ctrl Pts',(2.28256935324666,3.20495785128986,3.53510835178535));
#255253=CARTESIAN_POINT('Ctrl Pts',(2.18638658096923,3.26928168235129,3.54097635891616));
#255254=CARTESIAN_POINT('Ctrl Pts',(2.09006495170927,3.33369837633271,3.54685283756161));
#255255=CARTESIAN_POINT('Ctrl Pts',(1.99101838274663,3.3937715751451,3.55272931620706));
#255256=CARTESIAN_POINT('Ctrl Pts',(1.889683833842,3.4492874638273,3.55860579485251));
#255257=CARTESIAN_POINT('Ctrl Pts',(1.86748947683889,3.46144658888462,3.55989286492277));
#255258=CARTESIAN_POINT('Ctrl Pts',(1.84518544034691,3.47338728338781,3.56117993499302));
#255259=CARTESIAN_POINT('Ctrl Pts',(1.82277643425848,3.48510761250093,3.56246700506328));
#255260=CARTESIAN_POINT('Ctrl Pts',(1.72047118090115,3.53861517256929,3.56834294749048));
#255261=CARTESIAN_POINT('Ctrl Pts',(1.6156390865796,3.58770243836325,3.57421888991769));
#255262=CARTESIAN_POINT('Ctrl Pts',(1.50869864076134,3.63212298957027,3.58009483234489));
#255263=CARTESIAN_POINT('Ctrl Pts',(1.40189542849687,3.67648653718004,3.58596323434662));
#255264=CARTESIAN_POINT('Ctrl Pts',(1.29298962315551,3.7161951230695,3.59183163634836));
#255265=CARTESIAN_POINT('Ctrl Pts',(1.18242455374738,3.75104801018266,3.59770003835009));
#255266=CARTESIAN_POINT('Ctrl Pts',(1.07197190448255,3.78586545964282,3.60356247348908));
#255267=CARTESIAN_POINT('Ctrl Pts',(0.959863738392177,3.81583690764605,
3.60942490862806));
#255268=CARTESIAN_POINT('Ctrl Pts',(0.84656300726491,3.84080982017212,3.61528734376705));
#255269=CARTESIAN_POINT('Ctrl Pts',(0.729722252198946,3.86656299869719,
3.62133294772167));
#255270=CARTESIAN_POINT('Ctrl Pts',(0.611613597500106,3.8869999823317,3.62737855167629));
#255271=CARTESIAN_POINT('Ctrl Pts',(0.492761664545086,3.90200909045004,
3.63342415563091));
#255272=CARTESIAN_POINT('Ctrl Pts',(0.377641520518336,3.916546933002,3.63927993584988));
#255273=CARTESIAN_POINT('Ctrl Pts',(0.261824515878091,3.92599260394204,
3.64513571606885));
#255274=CARTESIAN_POINT('Ctrl Pts',(0.145796597435225,3.93029672571631,
3.65099149628782));
#255275=CARTESIAN_POINT('Ctrl Pts',(0.0297857041741822,3.93460021593174,
3.65684641726771));
#255276=CARTESIAN_POINT('Ctrl Pts',(-0.0864356289817935,3.93376364185813,
3.66270133824759));
#255277=CARTESIAN_POINT('Ctrl Pts',(-0.202378803930732,3.92778968628917,
3.66855625922747));
#255278=CARTESIAN_POINT('Ctrl Pts',(-0.318332941553371,3.92181516587001,
3.67441173380258));
#255279=CARTESIAN_POINT('Ctrl Pts',(-0.434008456454422,3.9107023195692,
3.68026720837769));
#255280=CARTESIAN_POINT('Ctrl Pts',(-0.54891993244486,3.89450586182185,
3.6861226829528));
#255281=CARTESIAN_POINT('Ctrl Pts',(-0.663869999929264,3.87830396470914,
3.69198012401132));
#255282=CARTESIAN_POINT('Ctrl Pts',(-0.778055109781406,3.8570151188575,
3.69783756506984));
#255283=CARTESIAN_POINT('Ctrl Pts',(-0.890998818565252,3.83074537202818,
3.70369500612837));
#255284=CARTESIAN_POINT('Ctrl Pts',(-1.00406983219014,3.80444601517471,
3.7095590494192));
#255285=CARTESIAN_POINT('Ctrl Pts',(-1.11589624976747,3.77315464549148,
3.71542309271003));
#255286=CARTESIAN_POINT('Ctrl Pts',(-1.22601551456742,3.73702755649995,
3.72128713600086));
#255287=CARTESIAN_POINT('Ctrl Pts',(-1.33620918627586,3.70087605665706,
3.7271551415896));
#255288=CARTESIAN_POINT('Ctrl Pts',(-1.44469302312683,3.65988247666801,
3.73302314717833));
#255289=CARTESIAN_POINT('Ctrl Pts',(-1.55102482179837,3.61425109838336,
3.73889115276707));
#255290=CARTESIAN_POINT('Ctrl Pts',(-1.65751012969131,3.5685538429346,3.74476762988531));
#255291=CARTESIAN_POINT('Ctrl Pts',(-1.76183682894323,3.51820560597106,
3.75064410700355));
#255292=CARTESIAN_POINT('Ctrl Pts',(-1.86358761179898,3.46345639688872,
3.75652058412178));
#255293=CARTESIAN_POINT('Ctrl Pts',(-1.88587339436265,3.45146504964895,
3.75780766897383));
#255294=CARTESIAN_POINT('Ctrl Pts',(-1.90803572050762,3.43926274564896,
3.75909475382587));
#255295=CARTESIAN_POINT('Ctrl Pts',(-1.93007040218111,3.42685238121289,
3.76038183867792));
#255296=CARTESIAN_POINT('Ctrl Pts',(-2.03066556788191,3.37019521296542,
3.76625778078959));
#255297=CARTESIAN_POINT('Ctrl Pts',(-2.12892982139993,3.30901137172813,
3.77213372290126));
#255298=CARTESIAN_POINT('Ctrl Pts',(-2.224428569587,3.24351761808151,3.77800966501293));
#255299=CARTESIAN_POINT('Ctrl Pts',(-2.31980476686566,3.17810791076174,
3.78387806669022));
#255300=CARTESIAN_POINT('Ctrl Pts',(-2.41242217924012,3.10839952159439,
3.78974646836752));
#255301=CARTESIAN_POINT('Ctrl Pts',(-2.50187099775053,3.03465492447078,
3.79561487004482));
#255302=CARTESIAN_POINT('Ctrl Pts',(-2.59122886652548,2.96098530935043,
3.8014773048509));
#255303=CARTESIAN_POINT('Ctrl Pts',(-2.67742423332938,2.88328791058103,
3.80733973965698));
#255304=CARTESIAN_POINT('Ctrl Pts',(-2.76007702793749,2.80186791263467,
3.81320217446306));
#255305=CARTESIAN_POINT('Ctrl Pts',(-2.84531227379063,2.71790398164813,
3.81924777853929));
#255306=CARTESIAN_POINT('Ctrl Pts',(-2.92677956764456,2.62998125818639,
3.82529338261552));
#255307=CARTESIAN_POINT('Ctrl Pts',(-3.00409951337268,2.53847889763812,
3.83133898669175));
#255308=CARTESIAN_POINT('Ctrl Pts',(-3.07899171203542,2.44984959377923,
3.83719476655876));
#255309=CARTESIAN_POINT('Ctrl Pts',(-3.14999282527869,2.35786242231984,
3.84305054642577));
#255310=CARTESIAN_POINT('Ctrl Pts',(-3.21679677247992,2.26289803671371,
3.84890632629278));
#255311=CARTESIAN_POINT('Ctrl Pts',(-3.28359091723009,2.16794758566955,
3.85476124691422));
#255312=CARTESIAN_POINT('Ctrl Pts',(-3.34618888314999,2.07002112666861,
3.86061616753567));
#255313=CARTESIAN_POINT('Ctrl Pts',(-3.404326806816,1.96952989121616,3.86647108815711));
#255314=CARTESIAN_POINT('Ctrl Pts',(-3.46247022748581,1.86902915420832,
3.87232656236765));
#255315=CARTESIAN_POINT('Ctrl Pts',(-3.51615256089043,1.76596351596973,
3.8781820365782));
#255316=CARTESIAN_POINT('Ctrl Pts',(-3.56515531376704,1.66076987831506,
3.88403751078874));
#255317=CARTESIAN_POINT('Ctrl Pts',(-3.61417452352064,1.55554091287465,
3.88989495147694));
#255318=CARTESIAN_POINT('Ctrl Pts',(-3.65851085350462,1.44818290087696,
3.89575239216514));
#255319=CARTESIAN_POINT('Ctrl Pts',(-3.69799374892721,1.33915317753246,
3.90160983285335));
#255320=CARTESIAN_POINT('Ctrl Pts',(-3.73752114757169,1.23000056112453,
3.90747387576715));
#255321=CARTESIAN_POINT('Ctrl Pts',(-3.77218405240381,1.11917286085807,
3.91333791868094));
#255322=CARTESIAN_POINT('Ctrl Pts',(-3.80186161136825,1.00714313183601,
3.91920196159474));
#255323=CARTESIAN_POINT('Ctrl Pts',(-3.83155922325541,0.895037705095614,
3.92506996680205));
#255324=CARTESIAN_POINT('Ctrl Pts',(-3.85626469388085,0.78172903455963,
3.93093797200937));
#255325=CARTESIAN_POINT('Ctrl Pts',(-3.87590850276474,0.667699242320964,
3.93680597721668));
#255326=CARTESIAN_POINT('Ctrl Pts',(-3.89558067103686,0.553504827469349,
3.94268245395));
#255327=CARTESIAN_POINT('Ctrl Pts',(-3.91017654268165,0.438587621137512,
3.94855893068331));
#255328=CARTESIAN_POINT('Ctrl Pts',(-3.91967850662608,0.32343377172702,
3.95443540741663));
#255329=CARTESIAN_POINT('Ctrl Pts',(-3.92175966292067,0.298212337510988,
3.9557224957086));
#255330=CARTESIAN_POINT('Ctrl Pts',(-3.92359665559735,0.272979544951817,
3.95700958400057));
#255331=CARTESIAN_POINT('Ctrl Pts',(-3.92518963269511,0.247740483940024,
3.95829667229254));
#255332=CARTESIAN_POINT('Ctrl Pts',(-3.93036296938364,0.165774358689514,
3.9624766075167));
#255333=CARTESIAN_POINT('Ctrl Pts',(-3.93296914912035,0.0836445127446457,
3.96665654274086));
#255334=CARTESIAN_POINT('Ctrl Pts',(-3.93299972773875,0.00146342301184574,
3.97083647796501));
#255335=CARTESIAN_POINT('',(-3.93299929447449,0.00235577231090492,5.22083647792055));
#255336=CARTESIAN_POINT('Ctrl Pts',(-3.93299972773902,0.00146342229266634,
3.97083647800159));
#255337=CARTESIAN_POINT('Ctrl Pts',(-3.93304230994955,-0.112977790790186,
3.97665724357202));
#255338=CARTESIAN_POINT('Ctrl Pts',(-3.92808569945042,-0.22761977987397,
3.98247800914245));
#255339=CARTESIAN_POINT('Ctrl Pts',(-3.91810353637897,-0.34198490933754,
3.98829877471288));
#255340=CARTESIAN_POINT('Ctrl Pts',(-3.90813370529849,-0.45620875181412,
3.99411234929394));
#255341=CARTESIAN_POINT('Ctrl Pts',(-3.89315070054257,-0.570155998831521,
3.99992592387501));
#255342=CARTESIAN_POINT('Ctrl Pts',(-3.87318016355311,-0.683347949919138,
4.00573949845607));
#255343=CARTESIAN_POINT('Ctrl Pts',(-3.85322872710721,-0.79643164013262,
4.01154751272424));
#255344=CARTESIAN_POINT('Ctrl Pts',(-3.82829931666604,-0.908761058411598,
4.0173555269924));
#255345=CARTESIAN_POINT('Ctrl Pts',(-3.79846940238943,-1.01986234321661,
4.02316354126057));
#255346=CARTESIAN_POINT('Ctrl Pts',(-3.76865832275454,-1.13089347854432,
4.02896788834193));
#255347=CARTESIAN_POINT('Ctrl Pts',(-3.73395300014328,-1.24069761661006,
4.0347722354233));
#255348=CARTESIAN_POINT('Ctrl Pts',(-3.69448189796611,-1.34881151596534,
4.04057658250466));
#255349=CARTESIAN_POINT('Ctrl Pts',(-3.6550233510648,-1.45689102560877,
4.04637908329406));
#255350=CARTESIAN_POINT('Ctrl Pts',(-3.6108021815709,-1.56328096981285,
4.05218158408346));
#255351=CARTESIAN_POINT('Ctrl Pts',(-3.56199635662642,-1.66753439406212,
4.05798408487286));
#255352=CARTESIAN_POINT('Ctrl Pts',(-3.51319373768717,-1.77178097000948,
4.06378620450186));
#255353=CARTESIAN_POINT('Ctrl Pts',(-3.45980724086497,-1.87389092372813,
4.06958832413086));
#255354=CARTESIAN_POINT('Ctrl Pts',(-3.40206217040772,-1.97343912717892,
4.07539044375985));
#255355=CARTESIAN_POINT('Ctrl Pts',(-3.34430631778608,-2.07300591827859,
4.08119364676111));
#255356=CARTESIAN_POINT('Ctrl Pts',(-3.28219048585822,-2.17000964447472,
4.08699684976237));
#255357=CARTESIAN_POINT('Ctrl Pts',(-3.21598451503738,-2.26405225183514,
4.09280005276363));
#255358=CARTESIAN_POINT('Ctrl Pts',(-3.14970989622288,-2.35819237058668,
4.09860927302041));
#255359=CARTESIAN_POINT('Ctrl Pts',(-3.07933691406554,-2.44936489567792,
4.10441849327718));
#255360=CARTESIAN_POINT('Ctrl Pts',(-3.00517711848789,-2.53720308342017,
4.11022771353395));
#255361=CARTESIAN_POINT('Ctrl Pts',(-2.93097562625754,-2.62509065854786,
4.11604020004891));
#255362=CARTESIAN_POINT('Ctrl Pts',(-2.85298336717487,-2.70963985493228,
4.12185268656387));
#255363=CARTESIAN_POINT('Ctrl Pts',(-2.7715490370689,-2.79052054913101,
4.12766517307883));
#255364=CARTESIAN_POINT('Ctrl Pts',(-2.68998837512432,-2.8715267162942,
4.13348667670129));
#255365=CARTESIAN_POINT('Ctrl Pts',(-2.60497529118688,-2.94885273489322,
4.13930818032374));
#255366=CARTESIAN_POINT('Ctrl Pts',(-2.51689200387587,-3.02220840459848,
4.1451296839462));
#255367=CARTESIAN_POINT('Ctrl Pts',(-2.46100018330727,-3.06875505441162,
4.14882362459985));
#255368=CARTESIAN_POINT('Ctrl Pts',(-2.40387282263669,-3.113703957637,4.15251756525351));
#255369=CARTESIAN_POINT('Ctrl Pts',(-2.34561324049977,-3.15699026384184,
4.15621150590716));
#255370=CARTESIAN_POINT('Ctrl Pts',(-2.25293986429195,-3.22584568628788,
4.16208744835867));
#255371=CARTESIAN_POINT('Ctrl Pts',(-2.15707916056136,-3.29073060875942,
4.16796339081019));
#255372=CARTESIAN_POINT('Ctrl Pts',(-2.05840590930094,-3.35133616824021,
4.1738393332617));
#255373=CARTESIAN_POINT('Ctrl Pts',(-1.95985928259052,-3.41186395434676,
4.17970773528498));
#255374=CARTESIAN_POINT('Ctrl Pts',(-1.85850763472646,-3.46812308461244,
4.18557613730827));
#255375=CARTESIAN_POINT('Ctrl Pts',(-1.75475742700522,-3.51984593020348,
4.19144453933155));
#255376=CARTESIAN_POINT('Ctrl Pts',(-1.65111271027363,-3.57151618511265,
4.19730697448932));
#255377=CARTESIAN_POINT('Ctrl Pts',(-1.54507465203718,-3.61865914693874,
4.20316940964708));
#255378=CARTESIAN_POINT('Ctrl Pts',(-1.43707663663068,-3.66105172600037,
4.20903184480485));
#255379=CARTESIAN_POINT('Ctrl Pts',(-1.32570427845713,-3.7047688395175,
4.21507744875139));
#255380=CARTESIAN_POINT('Ctrl Pts',(-1.21224785479972,-3.74343361017472,
4.22112305269793));
#255381=CARTESIAN_POINT('Ctrl Pts',(-1.09720805204918,-3.77685364960286,
4.22716865664447));
#255382=CARTESIAN_POINT('Ctrl Pts',(-0.985780342155254,-3.80922434538819,
4.23302443687515));
#255383=CARTESIAN_POINT('Ctrl Pts',(-0.872867623950878,-3.83667461670365,
4.23888021710584));
#255384=CARTESIAN_POINT('Ctrl Pts',(-0.758942133632789,-3.85907966201747,
4.24473599733652));
#255385=CARTESIAN_POINT('Ctrl Pts',(-0.645033360051377,-3.88148141975061,
4.25059091832547));
#255386=CARTESIAN_POINT('Ctrl Pts',(-0.530112514754661,-3.89883934392723,
4.25644583931442));
#255387=CARTESIAN_POINT('Ctrl Pts',(-0.414662598033087,-3.91107963736261,
4.26230076030336));
#255388=CARTESIAN_POINT('Ctrl Pts',(-0.2992017653294,-3.92332108813815,
4.26815623488485));
#255389=CARTESIAN_POINT('Ctrl Pts',(-0.18321217223457,-3.93044390274308,
4.27401170946634));
#255390=CARTESIAN_POINT('Ctrl Pts',(-0.0671818172790369,-3.93242617266073,
4.27986718404783));
#255391=CARTESIAN_POINT('Ctrl Pts',(0.0488875048780162,-3.93440910829651,
4.28572462511006));
#255392=CARTESIAN_POINT('Ctrl Pts',(0.16499720364775,-3.9312480593145,4.29158206617229));
#255393=CARTESIAN_POINT('Ctrl Pts',(0.280660111039486,-3.92297322219657,
4.29743950723451));
#255394=CARTESIAN_POINT('Ctrl Pts',(0.39645338814494,-3.91468905807682,
4.30330355052499));
#255395=CARTESIAN_POINT('Ctrl Pts',(0.51179845682318,-3.90127963093733,
4.30916759381546));
#255396=CARTESIAN_POINT('Ctrl Pts',(0.626214003219102,-3.88282693693297,
4.31503163710594));
#255397=CARTESIAN_POINT('Ctrl Pts',(0.740706859448634,-3.86436177456441,
4.32089964269197));
#255398=CARTESIAN_POINT('Ctrl Pts',(0.854268539576944,-3.84084664319408,
4.326767648278));
#255399=CARTESIAN_POINT('Ctrl Pts',(0.966430324143622,-3.81241412081317,
4.33263565386403));
#255400=CARTESIAN_POINT('Ctrl Pts',(1.07875403450676,-3.78394055095028,
4.3385121309761));
#255401=CARTESIAN_POINT('Ctrl Pts',(1.18967342243987,-3.7505355412015,4.34438860808817));
#255402=CARTESIAN_POINT('Ctrl Pts',(1.2987372028215,-3.71238072912887,4.35026508520023));
#255403=CARTESIAN_POINT('Ctrl Pts',(1.32262470011469,-3.70402394040471,
4.35155216997408));
#255404=CARTESIAN_POINT('Ctrl Pts',(1.34642326815575,-3.69543947687454,
4.35283925474794));
#255405=CARTESIAN_POINT('Ctrl Pts',(1.37012831730859,-3.68662954392073,
4.35412633952179));
#255406=CARTESIAN_POINT('Ctrl Pts',(1.47834924184469,-3.64640945902591,
4.36000228195433));
#255407=CARTESIAN_POINT('Ctrl Pts',(1.58497621249439,-3.60135375242019,
4.36587822438687));
#255408=CARTESIAN_POINT('Ctrl Pts',(1.6895460737779,-3.55160851792279,4.37175416681941));
#255409=CARTESIAN_POINT('Ctrl Pts',(1.79398174354379,-3.50192712006463,
4.37762256882278));
#255410=CARTESIAN_POINT('Ctrl Pts',(1.89636518444536,-3.44756833804321,
4.38349097082616));
#255411=CARTESIAN_POINT('Ctrl Pts',(1.9962505675709,-3.38872729375984,4.38935937282953));
#255412=CARTESIAN_POINT('Ctrl Pts',(2.09603438936188,-3.32994607779966,
4.39522180796647));
#255413=CARTESIAN_POINT('Ctrl Pts',(2.19332485215691,-3.26669187327245,
4.40108424310342));
#255414=CARTESIAN_POINT('Ctrl Pts',(2.2876988169505,-3.19920663960978,4.40694667824036));
#255415=CARTESIAN_POINT('Ctrl Pts',(2.38502144848215,-3.12961286399652,
4.41299228219436));
#255416=CARTESIAN_POINT('Ctrl Pts',(2.4792419336473,-3.05551951225002,4.41903788614836));
#255417=CARTESIAN_POINT('Ctrl Pts',(2.5699262257194,-2.97724170909244,4.42508349010236));
#255418=CARTESIAN_POINT('Ctrl Pts',(2.65776315428894,-2.90142172254982,
4.43093927031009));
#255419=CARTESIAN_POINT('Ctrl Pts',(2.74228229737723,-2.82167641745144,
4.43679505051782));
#255420=CARTESIAN_POINT('Ctrl Pts',(2.823121786322,-2.73833386927052,4.44265083072554));
#255421=CARTESIAN_POINT('Ctrl Pts',(2.90394941335901,-2.65500355028145,
4.44850575169077));
#255422=CARTESIAN_POINT('Ctrl Pts',(2.98109817257947,-2.56807733400152,
4.45436067265599));
#255423=CARTESIAN_POINT('Ctrl Pts',(3.05424310828056,-2.47792010273147,
4.46021559362122));
#255424=CARTESIAN_POINT('Ctrl Pts',(3.12739495994839,-2.38775434695583,
4.46607106817827));
#255425=CARTESIAN_POINT('Ctrl Pts',(3.19654197547533,-2.29435728944028,
4.47192654273532));
#255426=CARTESIAN_POINT('Ctrl Pts',(3.26139999412125,-2.1981262653328,4.47778201729237));
#255427=CARTESIAN_POINT('Ctrl Pts',(3.32627979443366,-2.10186292336984,
4.48363945832938));
#255428=CARTESIAN_POINT('Ctrl Pts',(3.38686750309089,-2.00276406436294,
4.4894968993664));
#255429=CARTESIAN_POINT('Ctrl Pts',(3.44292311037051,-1.90125470573426,
4.49535434040341));
#255430=CARTESIAN_POINT('Ctrl Pts',(3.49904190084925,-1.7996309306122,4.50121838366777));
#255431=CARTESIAN_POINT('Ctrl Pts',(3.5506181945708,-1.69559159454111,4.50708242693213));
#255432=CARTESIAN_POINT('Ctrl Pts',(3.59745861284973,-1.58958501780599,
4.51294647019649));
#255433=CARTESIAN_POINT('Ctrl Pts',(3.64433068088722,-1.48350681313326,
4.51881447575582));
#255434=CARTESIAN_POINT('Ctrl Pts',(3.68646035188462,-1.37545910450063,
4.52468248131514));
#255435=CARTESIAN_POINT('Ctrl Pts',(3.7237035278962,-1.26590719894209,4.53055048687446));
#255436=CARTESIAN_POINT('Ctrl Pts',(3.7610004711561,-1.15619713542978,4.5364269639592));
#255437=CARTESIAN_POINT('Ctrl Pts',(3.79339672604397,-1.04497893597937,
4.54230344104394));
#255438=CARTESIAN_POINT('Ctrl Pts',(3.82079883474219,-0.932730006182235,
4.54817991812868));
#255439=CARTESIAN_POINT('Ctrl Pts',(3.82680053314686,-0.908144882814232,
4.54946700313126));
#255440=CARTESIAN_POINT('Ctrl Pts',(3.83256285342018,-0.883510338981573,
4.55075408813383));
#255441=CARTESIAN_POINT('Ctrl Pts',(3.83808514540956,-0.858831425011042,
4.55204117313641));
#255442=CARTESIAN_POINT('Ctrl Pts',(3.86329612230202,-0.746164523108877,
4.55791711564744));
#255443=CARTESIAN_POINT('Ctrl Pts',(3.88358348786856,-0.632200709728735,
4.56379305815847));
#255444=CARTESIAN_POINT('Ctrl Pts',(3.89881750983979,-0.517407986956778,
4.56966900066949));
#255445=CARTESIAN_POINT('Ctrl Pts',(3.91403198242897,-0.40276257438288,
4.57553740275257));
#255446=CARTESIAN_POINT('Ctrl Pts',(3.9242059540972,-0.287290773350273,
4.58140580483565));
#255447=CARTESIAN_POINT('Ctrl Pts',(3.92926024759816,-0.171472757733917,
4.58727420691872));
#255448=CARTESIAN_POINT('Ctrl Pts',(3.93430940200193,-0.0557725033907323,
4.59313664213648));
#255449=CARTESIAN_POINT('Ctrl Pts',(3.93424921494047,0.0602728553535137,
4.59899907735424));
#255450=CARTESIAN_POINT('Ctrl Pts',(3.92905214817471,0.176176663958865,
4.604861512572));
#255451=CARTESIAN_POINT('Ctrl Pts',(3.92369270179007,0.295701826130957,
4.61090711649612));
#255452=CARTESIAN_POINT('Ctrl Pts',(3.91287004200091,0.415076004530788,
4.61695272042025));
#255453=CARTESIAN_POINT('Ctrl Pts',(3.89661205092077,0.533763547480533,
4.62299832434438));
#255454=CARTESIAN_POINT('Ctrl Pts',(3.88086453835968,0.648724465113842,
4.62885410463515));
#255455=CARTESIAN_POINT('Ctrl Pts',(3.86001797510522,0.763040782344009,
4.63470988492592));
#255456=CARTESIAN_POINT('Ctrl Pts',(3.83415041616872,0.876230327136198,
4.64056566521669));
#255457=CARTESIAN_POINT('Ctrl Pts',(3.80828665288148,0.9894032631787,4.64642058626565));
#255458=CARTESIAN_POINT('Ctrl Pts',(3.77740345085058,1.10144935326724,4.65227550731462));
#255459=CARTESIAN_POINT('Ctrl Pts',(3.74162983822925,1.21189733627588,4.65813042836358));
#255460=CARTESIAN_POINT('Ctrl Pts',(3.70585284315408,1.32235576232275,4.66398590300495));
#255461=CARTESIAN_POINT('Ctrl Pts',(3.66518464547931,1.43121538821599,4.66984137764632));
#255462=CARTESIAN_POINT('Ctrl Pts',(3.61980370928726,1.53802149082195,4.67569685228768));
#255463=CARTESIAN_POINT('Ctrl Pts',(3.57440753253252,1.64486346278715,4.6815542934096));
#255464=CARTESIAN_POINT('Ctrl Pts',(3.5242956313901,1.74965016043284,4.68741173453152));
#255465=CARTESIAN_POINT('Ctrl Pts',(3.46969373282064,1.85194881150241,4.69326917565344));
#255466=CARTESIAN_POINT('Ctrl Pts',(3.41503028960123,1.9543627687213,4.69913321900299));
#255467=CARTESIAN_POINT('Ctrl Pts',(3.35586694238364,2.05428271775246,4.70499726235254));
#255468=CARTESIAN_POINT('Ctrl Pts',(3.29247435887988,2.15130230235514,4.71086130570208));
#255469=CARTESIAN_POINT('Ctrl Pts',(3.22903894142714,2.2483874424488,4.7167293113469));
#255470=CARTESIAN_POINT('Ctrl Pts',(3.16136883757253,2.34256798137124,4.72259731699172));
#255471=CARTESIAN_POINT('Ctrl Pts',(3.08977580182442,2.43346964116265,4.72846532263654));
#255472=CARTESIAN_POINT('Ctrl Pts',(3.01807940860798,2.52450253390604,4.73434179980657));
#255473=CARTESIAN_POINT('Ctrl Pts',(2.94244904960256,2.61224678938462,4.7402182769766));
#255474=CARTESIAN_POINT('Ctrl Pts',(2.86323420694151,2.69636401032947,4.74609475414663));
#255475=CARTESIAN_POINT('Ctrl Pts',(2.84588432714771,2.7147876241745,4.7473818383481));
#255476=CARTESIAN_POINT('Ctrl Pts',(2.82836262380406,2.73303739673917,4.74866892254958));
#255477=CARTESIAN_POINT('Ctrl Pts',(2.81067297833481,2.75111003212495,4.74995600675105));
#255478=CARTESIAN_POINT('Ctrl Pts',(2.72991420668571,2.83361727268861,4.75583194922262));
#255479=CARTESIAN_POINT('Ctrl Pts',(2.64538613112808,2.91270160876023,4.76170789169419));
#255480=CARTESIAN_POINT('Ctrl Pts',(2.55741059061983,2.98799934253432,4.76758383416576));
#255481=CARTESIAN_POINT('Ctrl Pts',(2.46954794659865,3.06320044888699,4.77345223620894));
#255482=CARTESIAN_POINT('Ctrl Pts',(2.3782469465681,3.13462435063305,4.77932063825213));
#255483=CARTESIAN_POINT('Ctrl Pts',(2.28386717217618,3.20194311939734,4.78518904029531));
#255484=CARTESIAN_POINT('Ctrl Pts',(2.18958336112032,3.26919343987733,4.7910514754728));
#255485=CARTESIAN_POINT('Ctrl Pts',(2.09222733662673,3.33234669175443,4.7969139106503));
#255486=CARTESIAN_POINT('Ctrl Pts',(1.99219224047247,3.39111472483626,4.80277634582779));
#255487=CARTESIAN_POINT('Ctrl Pts',(1.88903159936587,3.45171893478219,4.80882194976687));
#255488=CARTESIAN_POINT('Ctrl Pts',(1.78302206161625,3.50765910302015,4.81486755370595));
#255489=CARTESIAN_POINT('Ctrl Pts',(1.67462804574086,3.55866687235798,4.82091315764503));
#255490=CARTESIAN_POINT('Ctrl Pts',(1.56963745360849,3.60807306755133,4.82676893789484));
#255491=CARTESIAN_POINT('Ctrl Pts',(1.46241028418778,3.65285178513794,4.83262471814466));
#255492=CARTESIAN_POINT('Ctrl Pts',(1.35339343095619,3.69280587372863,4.83848049839448));
#255493=CARTESIAN_POINT('Ctrl Pts',(1.24439257420256,3.73275409969643,4.84433541940229));
#255494=CARTESIAN_POINT('Ctrl Pts',(1.13360294327495,3.76787896237897,4.85019034041011));
#255495=CARTESIAN_POINT('Ctrl Pts',(1.02149004340447,3.79803200239618,4.85604526141792));
#255496=CARTESIAN_POINT('Ctrl Pts',(0.909366543076926,3.82818789343238,
4.86190073601803));
#255497=CARTESIAN_POINT('Ctrl Pts',(0.795919923698388,3.85337092009224,
4.86775621061815));
#255498=CARTESIAN_POINT('Ctrl Pts',(0.681628745774486,3.87348309057028,
4.87361168521827));
#255499=CARTESIAN_POINT('Ctrl Pts',(0.567299184735177,3.89360201544332,
4.87946912629875));
#255500=CARTESIAN_POINT('Ctrl Pts',(0.452124907436328,3.9086466262942,4.88532656737923));
#255501=CARTESIAN_POINT('Ctrl Pts',(0.336591806513044,3.91857052453931,
4.89118400845971));
#255502=CARTESIAN_POINT('Ctrl Pts',(0.220928482197998,3.92850560852841,
4.89704805176794));
#255503=CARTESIAN_POINT('Ctrl Pts',(0.104905938474842,3.93330842463923,
4.90291209507617));
#255504=CARTESIAN_POINT('Ctrl Pts',(-0.0109876093889282,3.93298465194563,
4.9087761383844));
#255505=CARTESIAN_POINT('Ctrl Pts',(-0.126959465756043,3.93266066048097,
4.91464414398789));
#255506=CARTESIAN_POINT('Ctrl Pts',(-0.242801741441477,3.92720320185946,
4.92051214959137));
#255507=CARTESIAN_POINT('Ctrl Pts',(-0.358030746336293,3.91666988456748,
4.92638015519486));
#255508=CARTESIAN_POINT('Ctrl Pts',(-0.473426105103055,3.90612136053032,
4.93225663232384));
#255509=CARTESIAN_POINT('Ctrl Pts',(-0.588206018844008,3.89048240933832,
4.93813310945282));
#255510=CARTESIAN_POINT('Ctrl Pts',(-0.701896341120765,3.86986182263932,
4.9440095865818));
#255511=CARTESIAN_POINT('Ctrl Pts',(-0.726797154847766,3.86534543656484,
4.94529667117642));
#255512=CARTESIAN_POINT('Ctrl Pts',(-0.751645756990695,3.86059026576184,
4.94658375577104));
#255513=CARTESIAN_POINT('Ctrl Pts',(-0.776437269383352,3.85559777034801,
4.94787084036566));
#255514=CARTESIAN_POINT('Ctrl Pts',(-0.889618253164547,3.83280547218116,
4.95374678283829));
#255515=CARTESIAN_POINT('Ctrl Pts',(-1.00198150404016,3.80498771482945,
4.95962272531091));
#255516=CARTESIAN_POINT('Ctrl Pts',(-1.11304671264367,3.77221632670677,
4.96549866778354));
#255517=CARTESIAN_POINT('Ctrl Pts',(-1.22396939445008,3.73948699316666,
4.9713670698277));
#255518=CARTESIAN_POINT('Ctrl Pts',(-1.33359695434867,3.70181678663287,
4.97723547187186));
#255519=CARTESIAN_POINT('Ctrl Pts',(-1.44145852512785,3.65932867071766,
4.98310387391602));
#255520=CARTESIAN_POINT('Ctrl Pts',(-1.54921042456725,3.61688375581058,
4.98896630909441));
#255521=CARTESIAN_POINT('Ctrl Pts',(-1.65519952481822,3.56963082618071,
4.9948287442728));
#255522=CARTESIAN_POINT('Ctrl Pts',(-1.75897004084498,3.51774265622285,
5.00069117945119));
#255523=CARTESIAN_POINT('Ctrl Pts',(-1.86598281306738,3.46423326718497,
5.00673678338991));
#255524=CARTESIAN_POINT('Ctrl Pts',(-1.97063565652213,3.40579435146224,
5.01278238732862));
#255525=CARTESIAN_POINT('Ctrl Pts',(-2.07245056523527,3.3426692409893,5.01882799126733));
#255526=CARTESIAN_POINT('Ctrl Pts',(-2.17106862518289,3.2815261725772,5.02468377151782));
#255527=CARTESIAN_POINT('Ctrl Pts',(-2.26702392365972,3.21598702314574,
5.0305395517683));
#255528=CARTESIAN_POINT('Ctrl Pts',(-2.35990771750162,3.14631920899268,
5.03639533201879));
#255529=CARTESIAN_POINT('Ctrl Pts',(-2.4527778821325,3.07666161747696,5.04225025302719));
#255530=CARTESIAN_POINT('Ctrl Pts',(-2.54257710820565,3.0028768134861,5.0481051740356));
#255531=CARTESIAN_POINT('Ctrl Pts',(-2.62892735203609,2.92527434229962,
5.053960095044));
#255532=CARTESIAN_POINT('Ctrl Pts',(-2.71528576042096,2.8476645336747,5.0598155696446));
#255533=CARTESIAN_POINT('Ctrl Pts',(-2.79819423127799,2.76623661619892,
5.0656710442452));
#255534=CARTESIAN_POINT('Ctrl Pts',(-2.87730993582532,2.68133857116196,
5.0715265188458));
#255535=CARTESIAN_POINT('Ctrl Pts',(-2.95645221028981,2.59641201428862,
5.0773839599267));
#255536=CARTESIAN_POINT('Ctrl Pts',(-3.03179890437162,2.50801331428315,
5.08324140100761));
#255537=CARTESIAN_POINT('Ctrl Pts',(-3.10304646532606,2.41652470172093,
5.08909884208852));
#255538=CARTESIAN_POINT('Ctrl Pts',(-3.1743743331257,2.32493296756762,5.09496288539703));
#255539=CARTESIAN_POINT('Ctrl Pts',(-3.24159359235149,2.2302446953858,5.10082692870555));
#255540=CARTESIAN_POINT('Ctrl Pts',(-3.3044431009817,2.13287242759018,5.10669097201407));
#255541=CARTESIAN_POINT('Ctrl Pts',(-3.36733507660839,2.03543436599851,
5.11255897761779));
#255542=CARTESIAN_POINT('Ctrl Pts',(-3.42585121448078,1.93530905299102,
5.11842698322151));
#255543=CARTESIAN_POINT('Ctrl Pts',(-3.4797763885994,1.83293351907431,5.12429498882523));
#255544=CARTESIAN_POINT('Ctrl Pts',(-3.53377941344132,1.73041018759377,
5.13017146595432));
#255545=CARTESIAN_POINT('Ctrl Pts',(-3.58317807225354,1.6256305239824,5.13604794308341));
#255546=CARTESIAN_POINT('Ctrl Pts',(-3.62780536252005,1.51905143154232,
5.1419244202125));
#255547=CARTESIAN_POINT('Ctrl Pts',(-3.63757977264724,1.49570814194818,
5.14321150480177));
#255548=CARTESIAN_POINT('Ctrl Pts',(-3.64712548538044,1.47227858708217,
5.14449858939103));
#255549=CARTESIAN_POINT('Ctrl Pts',(-3.65644106839263,1.44876765334257,
5.1457856739803));
#255550=CARTESIAN_POINT('Ctrl Pts',(-3.70437574779256,1.32778874416156,
5.15240855384368));
#255551=CARTESIAN_POINT('Ctrl Pts',(-3.74634559922482,1.20431996042898,
5.15903143370706));
#255552=CARTESIAN_POINT('Ctrl Pts',(-3.78211649997361,1.07892714333608,
5.16565431357044));
#255553=CARTESIAN_POINT('Ctrl Pts',(-3.81777367070408,0.9539330002236,5.17225613664653));
#255554=CARTESIAN_POINT('Ctrl Pts',(-3.84727112473125,0.827027227948243,
5.17885795972262));
#255555=CARTESIAN_POINT('Ctrl Pts',(-3.87042347272765,0.698792631442877,
5.18545978279872));
#255556=CARTESIAN_POINT('Ctrl Pts',(-3.89343898965604,0.571315905232001,
5.19202258890329));
#255557=CARTESIAN_POINT('Ctrl Pts',(-3.91018408115724,0.442526219216769,
5.19858539500787));
#255558=CARTESIAN_POINT('Ctrl Pts',(-3.92052425525767,0.313015277480708,
5.20514820111245));
#255559=CARTESIAN_POINT('Ctrl Pts',(-3.92876359226008,0.209817373451253,
5.21037762671515));
#255560=CARTESIAN_POINT('Ctrl Pts',(-3.93293711707552,0.106161927577145,
5.21560705231785));
#255561=CARTESIAN_POINT('Ctrl Pts',(-3.93299929447449,0.00235577231090366,
5.22083647792055));
#255562=CARTESIAN_POINT('',(-3.93299863531357,-0.00327637323301094,6.4708364779999));
#255563=CARTESIAN_POINT('Ctrl Pts',(-3.93299929447502,0.00235577142831299,
5.22083647796501));
#255564=CARTESIAN_POINT('Ctrl Pts',(-3.93306949457354,-0.114844452091178,
5.22674065434008));
#255565=CARTESIAN_POINT('Ctrl Pts',(-3.92789664864031,-0.232061737731447,
5.23264483071515));
#255566=CARTESIAN_POINT('Ctrl Pts',(-3.91750276642645,-0.348799476836041,
5.23854900709023));
#255567=CARTESIAN_POINT('Ctrl Pts',(-3.90710756542916,-0.465552027710973,
5.24445393259154));
#255568=CARTESIAN_POINT('Ctrl Pts',(-3.89149004524592,-0.581824509508502,
5.25035885809286));
#255569=CARTESIAN_POINT('Ctrl Pts',(-3.87072410551644,-0.697125454257667,
5.25626378359418));
#255570=CARTESIAN_POINT('Ctrl Pts',(-3.84995084376558,-0.812467053848058,
5.26217079115831));
#255571=CARTESIAN_POINT('Ctrl Pts',(-3.82402562123884,-0.926836038212441,
5.26807779872244));
#255572=CARTESIAN_POINT('Ctrl Pts',(-3.79307334122479,-1.03975171463663,
5.27398480628656));
#255573=CARTESIAN_POINT('Ctrl Pts',(-3.76208114843012,-1.15281299515265,
5.27989943090174));
#255574=CARTESIAN_POINT('Ctrl Pts',(-3.72604905630204,-1.26441683501574,
5.28581405551692));
#255575=CARTESIAN_POINT('Ctrl Pts',(-3.68515184878624,-1.37409783181088,
5.29172868013209));
#255576=CARTESIAN_POINT('Ctrl Pts',(-3.64422778518474,-1.48385085313846,
5.29764718872066));
#255577=CARTESIAN_POINT('Ctrl Pts',(-3.59843239766944,-1.59167814466311,
5.30356569730922));
#255578=CARTESIAN_POINT('Ctrl Pts',(-3.54798787396473,-1.69713613072117,
5.30948420589778));
#255579=CARTESIAN_POINT('Ctrl Pts',(-3.49745156616804,-1.80278599817254,
5.31541348324571));
#255580=CARTESIAN_POINT('Ctrl Pts',(-3.44224940748687,-1.90605758935708,
5.32134276059362));
#255581=CARTESIAN_POINT('Ctrl Pts',(-3.3826490056056,-2.00653300617644,
5.32727203794154));
#255582=CARTESIAN_POINT('Ctrl Pts',(-3.32760332093607,-2.09932999976544,
5.33274819449267));
#255583=CARTESIAN_POINT('Ctrl Pts',(-3.26880657120879,-2.18974197557187,
5.3382243510438));
#255584=CARTESIAN_POINT('Ctrl Pts',(-3.2065003103526,-2.27746454631212,
5.34370050759492));
#255585=CARTESIAN_POINT('Ctrl Pts',(-3.13964539097391,-2.37159128917778,
5.34957645007164));
#255586=CARTESIAN_POINT('Ctrl Pts',(-3.06853203668357,-2.4629270359288,
5.35545239254837));
#255587=CARTESIAN_POINT('Ctrl Pts',(-2.9934212178758,-2.55106221256381,
5.36132833502509));
#255588=CARTESIAN_POINT('Ctrl Pts',(-2.91840678662658,-2.63908428785559,
5.36719673707344));
#255589=CARTESIAN_POINT('Ctrl Pts',(-2.83940535799492,-2.72391364977943,
5.37306513912178));
#255590=CARTESIAN_POINT('Ctrl Pts',(-2.75672077677496,-2.80517014794063,
5.37893354117013));
#255591=CARTESIAN_POINT('Ctrl Pts',(-2.67412026746886,-2.88634402623229,
5.38479597635278));
#255592=CARTESIAN_POINT('Ctrl Pts',(-2.58784434746087,-2.96395197928577,
5.39065841153543));
#255593=CARTESIAN_POINT('Ctrl Pts',(-2.49823623211291,-3.03764789410463,
5.39652084671807));
#255594=CARTESIAN_POINT('Ctrl Pts',(-2.40582835755744,-3.11364639965725,
5.40256645065522));
#255595=CARTESIAN_POINT('Ctrl Pts',(-2.30987692912422,-3.18548404916728,
5.40861205459237));
#255596=CARTESIAN_POINT('Ctrl Pts',(-2.21079865791848,-3.25282312678477,
5.41465765852951));
#255597=CARTESIAN_POINT('Ctrl Pts',(-2.11483130870848,-3.31804784960798,
5.42051343878446));
#255598=CARTESIAN_POINT('Ctrl Pts',(-2.01593090453599,-3.37905202558977,
5.42636921903941));
#255599=CARTESIAN_POINT('Ctrl Pts',(-1.91450798829165,-3.43557100971111,
5.43222499929437));
#255600=CARTESIAN_POINT('Ctrl Pts',(-1.8130999542368,-3.49208170057624,
5.4380799203073));
#255601=CARTESIAN_POINT('Ctrl Pts',(-1.70917050457927,-3.54410830737973,
5.44393484132023));
#255602=CARTESIAN_POINT('Ctrl Pts',(-1.60315618317904,-3.59143136539386,
5.44978976233316));
#255603=CARTESIAN_POINT('Ctrl Pts',(-1.49713183795337,-3.63875889787961,
5.45564523693834));
#255604=CARTESIAN_POINT('Ctrl Pts',(-1.38902260604292,-3.68138182924245,
5.46150071154352));
#255605=CARTESIAN_POINT('Ctrl Pts',(-1.27928582203951,-3.71912849812005,
5.4673561861487));
#255606=CARTESIAN_POINT('Ctrl Pts',(-1.16951218445099,-3.75688784369568,
5.47321362723424));
#255607=CARTESIAN_POINT('Ctrl Pts',(-1.05811029797793,-3.78976753620867,
5.47907106831979));
#255608=CARTESIAN_POINT('Ctrl Pts',(-0.945552811405881,-3.81764572489937,
5.48492850940534));
#255609=CARTESIAN_POINT('Ctrl Pts',(-0.832868455413806,-3.84555533655213,
5.49079255271857));
#255610=CARTESIAN_POINT('Ctrl Pts',(-0.719026300455215,-3.86845209334975,
5.4966565960318));
#255611=CARTESIAN_POINT('Ctrl Pts',(-0.604509437504849,-3.88626521739929,
5.50252063934503));
#255612=CARTESIAN_POINT('Ctrl Pts',(-0.4899151962689,-3.90409037765874,
5.50838864495347));
#255613=CARTESIAN_POINT('Ctrl Pts',(-0.374645748461646,-3.91682502002907,
5.51425665056191));
#255614=CARTESIAN_POINT('Ctrl Pts',(-0.259187840598699,-3.92445036448237,
5.52012465617036));
#255615=CARTESIAN_POINT('Ctrl Pts',(-0.143563248402915,-3.93208671749693,
5.52600113330421));
#255616=CARTESIAN_POINT('Ctrl Pts',(-0.0277500641979943,-3.93459904335077,
5.53187761043806));
#255617=CARTESIAN_POINT('Ctrl Pts',(0.0877663834234242,-3.93202060802595,
5.53775408757191));
#255618=CARTESIAN_POINT('Ctrl Pts',(0.113067159916258,-3.93145587099328,
5.53904117211779));
#255619=CARTESIAN_POINT('Ctrl Pts',(0.138353728543505,-3.93064712100273,
5.54032825666368));
#255620=CARTESIAN_POINT('Ctrl Pts',(0.163621042766362,-3.92959503694262,
5.54161534120956));
#255621=CARTESIAN_POINT('Ctrl Pts',(0.278974214713604,-3.92479194499473,
5.54749128368696));
#255622=CARTESIAN_POINT('Ctrl Pts',(0.394306017157791,-3.9148973433921,
5.55336722616436));
#255623=CARTESIAN_POINT('Ctrl Pts',(0.509130817813535,-3.89990702586004,
5.55924316864175));
#255624=CARTESIAN_POINT('Ctrl Pts',(0.623808267097234,-3.88493594497236,
5.56511157069077));
#255625=CARTESIAN_POINT('Ctrl Pts',(0.737979602885249,-3.8648822057332,
5.57097997273978));
#255626=CARTESIAN_POINT('Ctrl Pts',(0.851160518054364,-3.83979358462215,
5.5768483747888));
#255627=CARTESIAN_POINT('Ctrl Pts',(0.964226353289277,-3.81473047308454,
5.5827108099721));
#255628=CARTESIAN_POINT('Ctrl Pts',(1.07630337041335,-3.78464275157337,
5.58857324515541));
#255629=CARTESIAN_POINT('Ctrl Pts',(1.18691436524442,-3.74962975366588,
5.59443568033871));
#255630=CARTESIAN_POINT('Ctrl Pts',(1.30098134336964,-3.71352279275741,
5.60048128427561));
#255631=CARTESIAN_POINT('Ctrl Pts',(1.41348874002193,-3.67217777851635,
5.6065268882125));
#255632=CARTESIAN_POINT('Ctrl Pts',(1.52392636419819,-3.62576025634648,
5.61257249214939));
#255633=CARTESIAN_POINT('Ctrl Pts',(1.63089639827218,-3.58080018078186,
5.618428272405));
#255634=CARTESIAN_POINT('Ctrl Pts',(1.7359242839985,-3.53108154589111,5.62428405266061));
#255635=CARTESIAN_POINT('Ctrl Pts',(1.83856447186049,-3.47680452180049,
5.63013983291621));
#255636=CARTESIAN_POINT('Ctrl Pts',(1.94118959891774,-3.42253546199442,
5.63599475392979));
#255637=CARTESIAN_POINT('Ctrl Pts',(2.04142735999498,-3.36370953591843,
5.64184967494337));
#255638=CARTESIAN_POINT('Ctrl Pts',(2.13885593538562,-3.30057332711541,
5.64770459595695));
#255639=CARTESIAN_POINT('Ctrl Pts',(2.23629372280573,-3.23743114868168,
5.65356007056279));
#255640=CARTESIAN_POINT('Ctrl Pts',(2.33092145012147,-3.16997810183942,
5.65941554516862));
#255641=CARTESIAN_POINT('Ctrl Pts',(2.42234606505718,-3.09850424255026,
5.66527101977446));
#255642=CARTESIAN_POINT('Ctrl Pts',(2.51380138368802,-3.02700637975192,
5.67112846086063));
#255643=CARTESIAN_POINT('Ctrl Pts',(2.60205112588368,-2.95148527346462,
5.6769859019468));
#255644=CARTESIAN_POINT('Ctrl Pts',(2.68673567297893,-2.87227095232021,
5.68284334303296));
#255645=CARTESIAN_POINT('Ctrl Pts',(2.77151567244853,-2.79296734457871,
5.68870738634679));
#255646=CARTESIAN_POINT('Ctrl Pts',(2.85272215470362,-2.70996249556236,
5.69457142966062));
#255647=CARTESIAN_POINT('Ctrl Pts',(2.93003264682825,-2.62362300807883,
5.70043547297445));
#255648=CARTESIAN_POINT('Ctrl Pts',(3.00739537714036,-2.53722518157546,
5.70630347858351));
#255649=CARTESIAN_POINT('Ctrl Pts',(3.08085661454114,-2.44748854849365,
5.71217148419256));
#255650=CARTESIAN_POINT('Ctrl Pts',(3.15013550395417,-2.35481109788607,
5.71803948980162));
#255651=CARTESIAN_POINT('Ctrl Pts',(3.2195144099501,-2.26199985064868,5.72391596693605));
#255652=CARTESIAN_POINT('Ctrl Pts',(3.28469868691709,-2.16623965298586,
5.72979244407048));
#255653=CARTESIAN_POINT('Ctrl Pts',(3.34545190124147,-2.06795565147801,
5.73566892120491));
#255654=CARTESIAN_POINT('Ctrl Pts',(3.35875826168645,-2.04642917975824,
5.73695600574466));
#255655=CARTESIAN_POINT('Ctrl Pts',(3.37185223860402,-2.02478172281951,
5.73824309028442));
#255656=CARTESIAN_POINT('Ctrl Pts',(3.38473165277341,-2.00301788277433,
5.73953017482417));
#255657=CARTESIAN_POINT('Ctrl Pts',(3.4435301966768,-1.90365916291552,5.74540611730284));
#255658=CARTESIAN_POINT('Ctrl Pts',(3.49804702800377,-1.80154529067286,
5.7512820597815));
#255659=CARTESIAN_POINT('Ctrl Pts',(3.54801412104477,-1.69708125818031,
5.75715800226016));
#255660=CARTESIAN_POINT('Ctrl Pts',(3.59791709274918,-1.59275128138288,
5.76302640431046));
#255661=CARTESIAN_POINT('Ctrl Pts',(3.64328176091414,-1.48607751112254,
5.76889480636076));
#255662=CARTESIAN_POINT('Ctrl Pts',(3.68388441772059,-1.37749214040422,
5.77476320841106));
#255663=CARTESIAN_POINT('Ctrl Pts',(3.72444579061415,-1.26901717696806,
5.78062564359569));
#255664=CARTESIAN_POINT('Ctrl Pts',(3.76025463963724,-1.15863486366175,
5.78648807878032));
#255665=CARTESIAN_POINT('Ctrl Pts',(3.79113436472628,-1.0467995169045,5.79235051396495));
#255666=CARTESIAN_POINT('Ctrl Pts',(3.82297891083624,-0.931469932646011,
5.79839611790136));
#255667=CARTESIAN_POINT('Ctrl Pts',(3.84958106106959,-0.814595426852911,
5.80444172183777));
#255668=CARTESIAN_POINT('Ctrl Pts',(3.87080177877556,-0.696694042911201,
5.81048732577418));
#255669=CARTESIAN_POINT('Ctrl Pts',(3.89135619502379,-0.582494600867895,
5.81634310603113));
#255670=CARTESIAN_POINT('Ctrl Pts',(3.90686198668723,-0.467332237805583,
5.82219888628808));
#255671=CARTESIAN_POINT('Ctrl Pts',(3.91724436245317,-0.351689642765965,
5.82805466654503));
#255672=CARTESIAN_POINT('Ctrl Pts',(3.92762521477168,-0.236064016425919,
5.83390958755997));
#255673=CARTESIAN_POINT('Ctrl Pts',(3.93288410918128,-0.119958709227479,
5.83976450857491));
#255674=CARTESIAN_POINT('Ctrl Pts',(3.93299810406709,-0.00386178775522389,
5.84561942958985));
#255675=CARTESIAN_POINT('Ctrl Pts',(3.9331121097313,0.112246110868742,5.85147490419704));
#255676=CARTESIAN_POINT('Ctrl Pts',(3.92808024843203,0.228345209412011,
5.85733037880423));
#255677=CARTESIAN_POINT('Ctrl Pts',(3.91793170546246,0.343947890431156,
5.86318585341143));
#255678=CARTESIAN_POINT('Ctrl Pts',(3.9077797542447,0.459589395016366,5.86904329449901));
#255679=CARTESIAN_POINT('Ctrl Pts',(3.89250774048567,0.574733739618474,
5.87490073558659));
#255680=CARTESIAN_POINT('Ctrl Pts',(3.87219658268766,0.688899575425928,
5.88075817667417));
#255681=CARTESIAN_POINT('Ctrl Pts',(3.85186253112331,0.803194093507157,
5.8866222199894));
#255682=CARTESIAN_POINT('Ctrl Pts',(3.82647807142746,0.916507494885766,
5.89248626330463));
#255683=CARTESIAN_POINT('Ctrl Pts',(3.79617502691577,1.02836966360401,5.89835030661986));
#255684=CARTESIAN_POINT('Ctrl Pts',(3.76585150683773,1.14030741684832,5.90421831223029));
#255685=CARTESIAN_POINT('Ctrl Pts',(3.73060290922078,1.25079159258783,5.91008631784073));
#255686=CARTESIAN_POINT('Ctrl Pts',(3.69061004696455,1.35936988389633,5.91595432345117));
#255687=CARTESIAN_POINT('Ctrl Pts',(3.65055944779205,1.46810492756914,5.92183080058701));
#255688=CARTESIAN_POINT('Ctrl Pts',(3.60575107436815,1.57492821668222,5.92770727772284));
#255689=CARTESIAN_POINT('Ctrl Pts',(3.55641270968123,1.67940990780029,5.93358375485868));
#255690=CARTESIAN_POINT('Ctrl Pts',(3.54560646568609,1.70229381679102,5.9348708393854));
#255691=CARTESIAN_POINT('Ctrl Pts',(3.53458308155962,1.72506550124405,5.93615792391211));
#255692=CARTESIAN_POINT('Ctrl Pts',(3.52334523002941,1.74772062699648,5.93744500843882));
#255693=CARTESIAN_POINT('Ctrl Pts',(3.47204093120941,1.85114834521145,5.94332095091657));
#255694=CARTESIAN_POINT('Ctrl Pts',(3.41609396010992,1.95248572342226,5.94919689339432));
#255695=CARTESIAN_POINT('Ctrl Pts',(3.35569799034643,2.05128740004538,5.95507283587207));
#255696=CARTESIAN_POINT('Ctrl Pts',(3.29537952499783,2.14996228731208,5.96094123792146));
#255697=CARTESIAN_POINT('Ctrl Pts',(3.23062362848781,2.24610759526916,5.96680963997084));
#255698=CARTESIAN_POINT('Ctrl Pts',(3.16167092446085,2.33930031535476,5.97267804202023));
#255699=CARTESIAN_POINT('Ctrl Pts',(3.09278833006882,2.43239827907546,5.9785404772039));
#255700=CARTESIAN_POINT('Ctrl Pts',(3.0197176603111,2.52254929668518,5.98440291238758));
#255701=CARTESIAN_POINT('Ctrl Pts',(2.9427437500641,2.60935781782773,5.99026534757125));
#255702=CARTESIAN_POINT('Ctrl Pts',(2.86336482983094,2.69887862628374,5.99631095150801));
#255703=CARTESIAN_POINT('Ctrl Pts',(2.77983498318723,2.7848442544325,6.00235655544476));
#255704=CARTESIAN_POINT('Ctrl Pts',(2.6925129494124,2.86685594637166,6.00840215938152));
#255705=CARTESIAN_POINT('Ctrl Pts',(2.6079327078613,2.94629258354521,6.01425793963753));
#255706=CARTESIAN_POINT('Ctrl Pts',(2.51979518059038,3.0220195650233,6.02011371989354));
#255707=CARTESIAN_POINT('Ctrl Pts',(2.42846444742363,3.09371127088477,6.02596950014955));
#255708=CARTESIAN_POINT('Ctrl Pts',(2.33714711557994,3.16539245713605,6.03182442116354));
#255709=CARTESIAN_POINT('Ctrl Pts',(2.24263783413364,3.23303929037039,6.03767934217754));
#255710=CARTESIAN_POINT('Ctrl Pts',(2.14533343263872,3.29636670636059,6.04353426319153));
#255711=CARTESIAN_POINT('Ctrl Pts',(2.04801983085547,3.35970011006026,6.04938973779777));
#255712=CARTESIAN_POINT('Ctrl Pts',(1.94791092961559,3.41871305948063,6.055245212404));
#255713=CARTESIAN_POINT('Ctrl Pts',(1.84543157254559,3.47316445205981,6.06110068701024));
#255714=CARTESIAN_POINT('Ctrl Pts',(1.74291779919691,3.52763413138819,6.06695812809686));
#255715=CARTESIAN_POINT('Ctrl Pts',(1.63803235131246,3.57753901407749,6.07281556918348));
#255716=CARTESIAN_POINT('Ctrl Pts',(1.531222991558,3.6226847986161,6.07867301027011));
#255717=CARTESIAN_POINT('Ctrl Pts',(1.4242932413981,3.66788146932533,6.08453705358437));
#255718=CARTESIAN_POINT('Ctrl Pts',(1.31543563157924,3.70830817468893,6.09040109689863));
#255719=CARTESIAN_POINT('Ctrl Pts',(1.20511622930149,3.74381942324602,6.0962651402129));
#255720=CARTESIAN_POINT('Ctrl Pts',(1.09472228493422,3.77935466651859,6.10213314582239));
#255721=CARTESIAN_POINT('Ctrl Pts',(0.982864978407684,3.80996773064951,
6.10800115143189));
#255722=CARTESIAN_POINT('Ctrl Pts',(0.870022123119032,3.8355639096857,6.11386915704138));
#255723=CARTESIAN_POINT('Ctrl Pts',(0.757016358798775,3.86119704142686,
6.11974563417625));
#255724=CARTESIAN_POINT('Ctrl Pts',(0.643022610824618,3.88179876088044,
6.12562211131112));
#255725=CARTESIAN_POINT('Ctrl Pts',(0.528525435344543,3.89732598895626,
6.13149858844598));
#255726=CARTESIAN_POINT('Ctrl Pts',(0.503447903249601,3.90072681136767,
6.1327856729818));
#255727=CARTESIAN_POINT('Ctrl Pts',(0.478346225338373,3.90388440309693,
6.13407275751761));
#255728=CARTESIAN_POINT('Ctrl Pts',(0.453225492216509,3.90679864508079,
6.13535984205342));
#255729=CARTESIAN_POINT('Ctrl Pts',(0.338541507815882,3.92010306898418,
6.14123578453135));
#255730=CARTESIAN_POINT('Ctrl Pts',(0.223082003137737,3.92837534667247,
6.14711172700929));
#255731=CARTESIAN_POINT('Ctrl Pts',(0.107325971306983,3.93153534079029,
6.15298766948722));
#255732=CARTESIAN_POINT('Ctrl Pts',(-0.0082815141296696,3.93469127977833,
6.15885607153678));
#255733=CARTESIAN_POINT('Ctrl Pts',(-0.124184361059787,3.93274797094074,
6.16472447358634));
#255734=CARTESIAN_POINT('Ctrl Pts',(-0.239896751886397,3.92567682679488,
6.17059287563589));
#255735=CARTESIAN_POINT('Ctrl Pts',(-0.355491488828726,3.91861287243717,
6.17645531081975));
#255736=CARTESIAN_POINT('Ctrl Pts',(-0.47089574527979,3.9064314788922,6.18231774600361));
#255737=CARTESIAN_POINT('Ctrl Pts',(-0.585622652389425,3.88915609213726,
6.18818018118747));
#255738=CARTESIAN_POINT('Ctrl Pts',(-0.70393414232727,3.87134094486518,
6.19422578512416));
#255739=CARTESIAN_POINT('Ctrl Pts',(-0.821524813649213,3.84810824116936,
6.20027138906086));
#255740=CARTESIAN_POINT('Ctrl Pts',(-0.937864857330161,3.81954166221355,
6.20631699299755));
#255741=CARTESIAN_POINT('Ctrl Pts',(-1.05055198303728,3.79187203469783,
6.21217277325372));
#255742=CARTESIAN_POINT('Ctrl Pts',(-1.16206541246184,3.75919858223408,
6.2180285535099));
#255743=CARTESIAN_POINT('Ctrl Pts',(-1.27193376449624,3.72164929819219,
6.22388433376607));
#255744=CARTESIAN_POINT('Ctrl Pts',(-1.38178599510872,3.68410552390666,
6.22973925478023));
#255745=CARTESIAN_POINT('Ctrl Pts',(-1.48999323784757,3.64168747414375,
6.23559417579439));
#255746=CARTESIAN_POINT('Ctrl Pts',(-1.59610028723417,3.59457269687107,
6.24144909680856));
#255747=CARTESIAN_POINT('Ctrl Pts',(-1.70221736921331,3.54745346482027,
6.24730457141493));
#255748=CARTESIAN_POINT('Ctrl Pts',(-1.80623348582855,3.49563678997855,
6.25316004602132));
#255749=CARTESIAN_POINT('Ctrl Pts',(-1.90771504296155,3.43934765832973,
6.25901552062769));
#255750=CARTESIAN_POINT('Ctrl Pts',(-2.00923068127598,3.38303962275233,
6.26487296171447));
#255751=CARTESIAN_POINT('Ctrl Pts',(-2.10820970676538,3.32225634373593,
6.27073040280124));
#255752=CARTESIAN_POINT('Ctrl Pts',(-2.20424529295946,3.25726751871351,
6.27658784388801));
#255753=CARTESIAN_POINT('Ctrl Pts',(-2.30038912587654,3.19220544139348,
6.28245188720244));
#255754=CARTESIAN_POINT('Ctrl Pts',(-2.39358255570672,3.12292858841028,
6.28831593051687));
#255755=CARTESIAN_POINT('Ctrl Pts',(-2.48344972178239,3.04974859281531,
6.2941799738313));
#255756=CARTESIAN_POINT('Ctrl Pts',(-2.5733776105068,2.97651914998214,6.30004797944094));
#255757=CARTESIAN_POINT('Ctrl Pts',(-2.65997445261805,2.89938158678553,
6.30591598505058));
#255758=CARTESIAN_POINT('Ctrl Pts',(-2.7429005819761,2.81868504757009,6.31178399066022));
#255759=CARTESIAN_POINT('Ctrl Pts',(-2.82594643017179,2.73787200833286,
6.31766046779526));
#255760=CARTESIAN_POINT('Ctrl Pts',(-2.905310708314,2.65349003882839,6.3235369449303));
#255761=CARTESIAN_POINT('Ctrl Pts',(-2.98069337551666,2.56592205671784,
6.32941342206534));
#255762=CARTESIAN_POINT('Ctrl Pts',(-2.99720392475848,2.54674264141861,
6.33070050659958));
#255763=CARTESIAN_POINT('Ctrl Pts',(-3.01352363574769,2.52741050105189,
6.33198759113383));
#255764=CARTESIAN_POINT('Ctrl Pts',(-3.02964963604818,2.50792984008587,
6.33327467566807));
#255765=CARTESIAN_POINT('Ctrl Pts',(-3.10287633135138,2.41946993693054,
6.3391192090466));
#255766=CARTESIAN_POINT('Ctrl Pts',(-3.17235473525013,2.32764397398516,
6.34496374242514));
#255767=CARTESIAN_POINT('Ctrl Pts',(-3.23775741246485,2.23280450062896,
6.35080827580367));
#255768=CARTESIAN_POINT('Ctrl Pts',(-3.30308038054781,2.13808061232829,
6.35664568619121));
#255769=CARTESIAN_POINT('Ctrl Pts',(-3.36433725947034,2.04035085249035,
6.36248309657875));
#255770=CARTESIAN_POINT('Ctrl Pts',(-3.42123975304002,1.94000194644714,
6.36832050696628));
#255771=CARTESIAN_POINT('Ctrl Pts',(-3.47808699042986,1.83975048599639,
6.37415224883249));
#255772=CARTESIAN_POINT('Ctrl Pts',(-3.53058804355407,1.73688529573961,
6.37998399069871));
#255773=CARTESIAN_POINT('Ctrl Pts',(-3.57849741899204,1.63182266875641,
6.38581573256492));
#255774=CARTESIAN_POINT('Ctrl Pts',(-3.6263721341728,1.52683604981215,6.39164325543075));
#255775=CARTESIAN_POINT('Ctrl Pts',(-3.66966160474642,1.41965553356179,
6.39747077829659));
#255776=CARTESIAN_POINT('Ctrl Pts',(-3.7081662451842,1.31072197588828,6.40329830116242));
#255777=CARTESIAN_POINT('Ctrl Pts',(-3.74665800471865,1.20182485960497,
6.40912387455521));
#255778=CARTESIAN_POINT('Ctrl Pts',(-3.78036797210157,1.09117625864008,
6.414949447948));
#255779=CARTESIAN_POINT('Ctrl Pts',(-3.80914491256672,0.979236455135857,
6.42077502134078));
#255780=CARTESIAN_POINT('Ctrl Pts',(-3.83791529183902,0.867322174103,6.42659926649263));
#255781=CARTESIAN_POINT('Ctrl Pts',(-3.86175478097165,0.754117681054901,
6.43242351164447));
#255782=CARTESIAN_POINT('Ctrl Pts',(-3.88056245260592,0.640096907839084,
6.43824775679632));
#255783=CARTESIAN_POINT('Ctrl Pts',(-3.89937772268794,0.526030069331107,
6.44407435498916));
#255784=CARTESIAN_POINT('Ctrl Pts',(-3.91315704387449,0.411146703655898,
6.44990095318201));
#255785=CARTESIAN_POINT('Ctrl Pts',(-3.92185095594521,0.295929179621853,
6.45572755137486));
#255786=CARTESIAN_POINT('Ctrl Pts',(-3.92936567121646,0.196339158428675,
6.46076386023824));
#255787=CARTESIAN_POINT('Ctrl Pts',(-3.93308175351824,0.0964997606865402,
6.46580016910163));
#255788=CARTESIAN_POINT('Ctrl Pts',(-3.93299863531415,-0.00327637254193622,
6.47083647796501));
#255789=CARTESIAN_POINT('',(-3.93299999135599,0.000260756115896825,7.72083647799638));
#255790=CARTESIAN_POINT('Ctrl Pts',(-3.93299863531357,-0.00327637323301801,
6.47083647799989));
#255791=CARTESIAN_POINT('Ctrl Pts',(-3.93288302433106,-0.142057215378997,
6.47784159197612));
#255792=CARTESIAN_POINT('Ctrl Pts',(-3.92541801980143,-0.280523368869989,
6.48484670595235));
#255793=CARTESIAN_POINT('Ctrl Pts',(-3.91072617825782,-0.417982964591799,
6.49185181992859));
#255794=CARTESIAN_POINT('Ctrl Pts',(-3.89585191697551,-0.557149313239084,
6.49894391218167));
#255795=CARTESIAN_POINT('Ctrl Pts',(-3.87357031095842,-0.695283924055693,
6.50603600443474));
#255796=CARTESIAN_POINT('Ctrl Pts',(-3.84405778351081,-0.831690301151798,
6.51312809668782));
#255797=CARTESIAN_POINT('Ctrl Pts',(-3.81900462496335,-0.947485554484084,
6.51914856755278));
#255798=CARTESIAN_POINT('Ctrl Pts',(-3.78874151244498,-1.06203576112651,
6.52516903841774));
#255799=CARTESIAN_POINT('Ctrl Pts',(-3.7534032234113,-1.17492690942272,
6.53118950928269));
#255800=CARTESIAN_POINT('Ctrl Pts',(-3.71891327099915,-1.28510797474763,
6.53706545176065));
#255801=CARTESIAN_POINT('Ctrl Pts',(-3.67951076709477,-1.39395084536786,
6.54294139423859));
#255802=CARTESIAN_POINT('Ctrl Pts',(-3.63531731797249,-1.50098534224998,
6.54881733671654));
#255803=CARTESIAN_POINT('Ctrl Pts',(-3.59118058103526,-1.60788248483379,
6.55468573876613));
#255804=CARTESIAN_POINT('Ctrl Pts',(-3.54226528181998,-1.71297549068377,
6.56055414081572));
#255805=CARTESIAN_POINT('Ctrl Pts',(-3.48874289578739,-1.81580891260424,
6.56642254286531));
#255806=CARTESIAN_POINT('Ctrl Pts',(-3.43527493017229,-1.91853777570049,
6.5722849780492));
#255807=CARTESIAN_POINT('Ctrl Pts',(-3.37720938506593,-2.01901126089608,
6.57814741323308));
#255808=CARTESIAN_POINT('Ctrl Pts',(-3.31476569881553,-2.1167941236587,
6.58400984841696));
#255809=CARTESIAN_POINT('Ctrl Pts',(-3.25037099191042,-2.21763216135384,
6.59005545235365));
#255810=CARTESIAN_POINT('Ctrl Pts',(-3.18132023154694,-2.31560826556371,
6.59610105629033));
#255811=CARTESIAN_POINT('Ctrl Pts',(-3.10790534872448,-2.41027246247593,
6.60214666022701));
#255812=CARTESIAN_POINT('Ctrl Pts',(-3.03679559263627,-2.50196433330534,
6.60800244048321));
#255813=CARTESIAN_POINT('Ctrl Pts',(-2.96159194301872,-2.59054881570634,
6.61385822073942));
#255814=CARTESIAN_POINT('Ctrl Pts',(-2.88260304862656,-2.67564733551507,
6.61971400099562));
#255815=CARTESIAN_POINT('Ctrl Pts',(-2.80362574459031,-2.76073336847813,
6.6255689220098));
#255816=CARTESIAN_POINT('Ctrl Pts',(-2.72086458095177,-2.84233415352404,
6.63142384302398));
#255817=CARTESIAN_POINT('Ctrl Pts',(-2.63466689826601,-2.92010604861902,
6.63727876403816));
#255818=CARTESIAN_POINT('Ctrl Pts',(-2.54846106544974,-2.99788529717264,
6.64313423864461));
#255819=CARTESIAN_POINT('Ctrl Pts',(-2.45881837413144,-3.07183465958274,
6.64898971325106));
#255820=CARTESIAN_POINT('Ctrl Pts',(-2.36612071223765,-3.14164953091843,
6.65484518785751));
#255821=CARTESIAN_POINT('Ctrl Pts',(-2.27339191911294,-3.21148784861552,
6.66070262894432));
#255822=CARTESIAN_POINT('Ctrl Pts',(-2.17760644481216,-3.27718866602247,
6.66656007003113));
#255823=CARTESIAN_POINT('Ctrl Pts',(-2.0791761366056,-3.33849001690432,
6.67241751111794));
#255824=CARTESIAN_POINT('Ctrl Pts',(-1.98063488245983,-3.39986046373916,
6.67828155443241));
#255825=CARTESIAN_POINT('Ctrl Pts',(-1.87944319493971,-3.45682132837217,
6.68414559774688));
#255826=CARTESIAN_POINT('Ctrl Pts',(-1.77603863731821,-3.50915598951555,
6.69000964106134));
#255827=CARTESIAN_POINT('Ctrl Pts',(-1.67256420992241,-3.56152601284264,
6.69587764667101));
#255828=CARTESIAN_POINT('Ctrl Pts',(-1.56687431026887,-3.60926343873527,
6.70174565228068));
#255829=CARTESIAN_POINT('Ctrl Pts',(-1.45942604915193,-3.65219996810919,
6.70761365789035));
#255830=CARTESIAN_POINT('Ctrl Pts',(-1.35182266707329,-3.69519848411425,
6.71349013502542));
#255831=CARTESIAN_POINT('Ctrl Pts',(-1.24245624567729,-3.73338213629185,
6.7193666121605));
#255832=CARTESIAN_POINT('Ctrl Pts',(-1.13179863309566,-3.76663256160231,
6.72524308929557));
#255833=CARTESIAN_POINT('Ctrl Pts',(-1.10756205419988,-3.77391517449766,
6.72653017382948));
#255834=CARTESIAN_POINT('Ctrl Pts',(-1.08326357056531,-3.78096133023377,
6.72781725836339));
#255835=CARTESIAN_POINT('Ctrl Pts',(-1.05890819147291,-3.78777011472866,
6.72910434289731));
#255836=CARTESIAN_POINT('Ctrl Pts',(-0.947718286842929,-3.81885434034308,
6.73498028537528));
#255837=CARTESIAN_POINT('Ctrl Pts',(-0.834975074744924,-3.84508973484664,
6.74085622785326));
#255838=CARTESIAN_POINT('Ctrl Pts',(-0.721139110600009,-3.86632220374389,
6.74673217033124));
#255839=CARTESIAN_POINT('Ctrl Pts',(-0.60744922888121,-3.8875274256231,
6.75260057238086));
#255840=CARTESIAN_POINT('Ctrl Pts',(-0.492669786014068,-3.90374241471174,
6.75846897443047));
#255841=CARTESIAN_POINT('Ctrl Pts',(-0.377276143425831,-3.91486292373076,
6.76433737648009));
#255842=CARTESIAN_POINT('Ctrl Pts',(-0.261999830625348,-3.92597212565404,
6.77019981166401));
#255843=CARTESIAN_POINT('Ctrl Pts',(-0.14611096878662,-3.9319971117745,
6.77606224684794));
#255844=CARTESIAN_POINT('Ctrl Pts',(-0.0300940988899279,-3.93288486294883,
6.78192468203187));
#255845=CARTESIAN_POINT('Ctrl Pts',(0.0895476580527755,-3.93380035144907,
6.78797028596853));
#255846=CARTESIAN_POINT('Ctrl Pts',(0.209325114417832,-3.92925222550942,
6.7940158899052));
#255847=CARTESIAN_POINT('Ctrl Pts',(0.328701893396891,-3.91924024082185,
6.80006149384187));
#255848=CARTESIAN_POINT('Ctrl Pts',(0.444330405076032,-3.90954261873588,
6.80591727409811));
#255849=CARTESIAN_POINT('Ctrl Pts',(0.559582582987395,-3.89471916013571,
6.81177305435435));
#255850=CARTESIAN_POINT('Ctrl Pts',(0.673972825476779,-3.87482252890618,
6.81762883461058));
#255851=CARTESIAN_POINT('Ctrl Pts',(0.788346283029122,-3.85492881718879,
6.8234837556248));
#255852=CARTESIAN_POINT('Ctrl Pts',(0.901857650103256,-3.82996348378381,
6.82933867663902));
#255853=CARTESIAN_POINT('Ctrl Pts',(1.01402954805526,-3.80003066772767,
6.83519359765323));
#255854=CARTESIAN_POINT('Ctrl Pts',(1.12621205204158,-3.77009502147538,
6.8410490722597));
#255855=CARTESIAN_POINT('Ctrl Pts',(1.23705443631635,-3.73519106530982,
6.84690454686617));
#255856=CARTESIAN_POINT('Ctrl Pts',(1.34609324519494,-3.69547317338938,
6.85276002147263));
#255857=CARTESIAN_POINT('Ctrl Pts',(1.4551686732536,-3.65574194276273,6.85861746255948));
#255858=CARTESIAN_POINT('Ctrl Pts',(1.56243893386359,-3.6111937027998,6.86447490364634));
#255859=CARTESIAN_POINT('Ctrl Pts',(1.6674600136861,-3.56203117655615,6.87033234473319));
#255860=CARTESIAN_POINT('Ctrl Pts',(1.77259946825045,-3.51281323666256,
6.87619638804769));
#255861=CARTESIAN_POINT('Ctrl Pts',(1.87548430809016,-3.45897080493629,
6.88206043136219));
#255862=CARTESIAN_POINT('Ctrl Pts',(1.97569454297385,-3.4007528685371,6.88792447467668));
#255863=CARTESIAN_POINT('Ctrl Pts',(2.07597248924917,-3.3424955946641,6.89379248028639));
#255864=CARTESIAN_POINT('Ctrl Pts',(2.17357188544326,-3.27985715133792,
6.89966048589609));
#255865=CARTESIAN_POINT('Ctrl Pts',(2.26810262099788,-3.2131292380828,6.9055284915058));
#255866=CARTESIAN_POINT('Ctrl Pts',(2.36276982873405,-3.1463049910391,6.9114049686409));
#255867=CARTESIAN_POINT('Ctrl Pts',(2.45435920970812,-3.07537974366202,
6.917281445776));
#255868=CARTESIAN_POINT('Ctrl Pts',(2.54251450635903,-3.00068475267794,
6.9231579229111));
#255869=CARTESIAN_POINT('Ctrl Pts',(2.56182255712942,-2.984324820456,6.92444500744472));
#255870=CARTESIAN_POINT('Ctrl Pts',(2.58096601564204,-2.96778418523611,
6.92573209197833));
#255871=CARTESIAN_POINT('Ctrl Pts',(2.59994138699915,-2.95106655027787,
6.92701917651194));
#255872=CARTESIAN_POINT('Ctrl Pts',(2.68656987773229,-2.87474533063978,
6.93289511898994));
#255873=CARTESIAN_POINT('Ctrl Pts',(2.76997782474021,-2.79448050537409,
6.93877106146793));
#255874=CARTESIAN_POINT('Ctrl Pts',(2.84978515425914,-2.71057439937815,
6.94464700394593));
#255875=CARTESIAN_POINT('Ctrl Pts',(2.92949006932228,-2.62677596768023,
6.95051540599556));
#255876=CARTESIAN_POINT('Ctrl Pts',(3.00560327401114,-2.53934584444975,
6.95638380804519));
#255877=CARTESIAN_POINT('Ctrl Pts',(3.0777784356618,-2.44862592099634,6.96225221009482));
#255878=CARTESIAN_POINT('Ctrl Pts',(3.14988021115175,-2.35799823962083,
6.96811464527875));
#255879=CARTESIAN_POINT('Ctrl Pts',(3.21805165285137,-2.26408773279291,
6.97397708046269));
#255880=CARTESIAN_POINT('Ctrl Pts',(3.28198439175556,-2.16727189163541,
6.97983951564663));
#255881=CARTESIAN_POINT('Ctrl Pts',(3.34791467599305,-2.06743108963609,
6.98588511958329));
#255882=CARTESIAN_POINT('Ctrl Pts',(3.40933672327431,-1.96450074129025,
6.99193072351996));
#255883=CARTESIAN_POINT('Ctrl Pts',(3.46595819281448,-1.8589305542871,6.99797632745662));
#255884=CARTESIAN_POINT('Ctrl Pts',(3.52080182578924,-1.75667512651214,
7.00383210771287));
#255885=CARTESIAN_POINT('Ctrl Pts',(3.57114162729818,-1.65194354664113,
7.00968788796912));
#255886=CARTESIAN_POINT('Ctrl Pts',(3.61675728335841,-1.54517175526667,
7.01554366822537));
#255887=CARTESIAN_POINT('Ctrl Pts',(3.66236624605132,-1.43841563094344,
7.0213985892396));
#255888=CARTESIAN_POINT('Ctrl Pts',(3.70325227956609,-1.32962026987251,
7.02725351025383));
#255889=CARTESIAN_POINT('Ctrl Pts',(3.73924271899208,-1.21924275206569,
7.03310843126807));
#255890=CARTESIAN_POINT('Ctrl Pts',(3.77523656137231,-1.10885479788609,
7.03896390587455));
#255891=CARTESIAN_POINT('Ctrl Pts',(3.80633376152611,-0.996884782031934,
7.04481938048103));
#255892=CARTESIAN_POINT('Ctrl Pts',(3.8324113681037,-0.883805468205252,
7.05067485508751));
#255893=CARTESIAN_POINT('Ctrl Pts',(3.85849773248577,-0.770688178250771,
7.05653229617437));
#255894=CARTESIAN_POINT('Ctrl Pts',(3.87956105847857,-0.656461251507195,
7.06238973726123));
#255895=CARTESIAN_POINT('Ctrl Pts',(3.89552953249747,-0.541607479121249,
7.0682471783481));
#255896=CARTESIAN_POINT('Ctrl Pts',(3.9115160054171,-0.426624249052216,
7.07411122166261));
#255897=CARTESIAN_POINT('Ctrl Pts',(3.92239610774169,-0.31101317217588,
7.07997526497712));
#255898=CARTESIAN_POINT('Ctrl Pts',(3.92814991010467,-0.195262089880939,
7.08583930829163));
#255899=CARTESIAN_POINT('Ctrl Pts',(3.93390760027378,-0.0794327953467238,
7.09170731390136));
#255900=CARTESIAN_POINT('Ctrl Pts',(3.93453209092554,0.0365362812697187,
7.09757531951108));
#255901=CARTESIAN_POINT('Ctrl Pts',(3.93005554794925,0.152159094481161,
7.1034433251208));
#255902=CARTESIAN_POINT('Ctrl Pts',(3.92557254227506,0.267948830095802,
7.10931980225592));
#255903=CARTESIAN_POINT('Ctrl Pts',(3.91597384052081,0.383390894991611,
7.11519627939103));
#255904=CARTESIAN_POINT('Ctrl Pts',(3.90134322176381,0.49800609032178,7.12107275652615));
#255905=CARTESIAN_POINT('Ctrl Pts',(3.89813877755612,0.523109471449321,
7.12235984105962));
#255906=CARTESIAN_POINT('Ctrl Pts',(3.89469313932908,0.548173234023334,
7.12364692559309));
#255907=CARTESIAN_POINT('Ctrl Pts',(3.89100750939418,0.573192430025141,
7.12493401012656));
#255908=CARTESIAN_POINT('Ctrl Pts',(3.87418145878955,0.687412866001887,
7.13080995260454));
#255909=CARTESIAN_POINT('Ctrl Pts',(3.85229398329045,0.801080214942577,
7.13668589508252));
#255910=CARTESIAN_POINT('Ctrl Pts',(3.82539162642816,0.913711061798685,
7.1425618375605));
#255911=CARTESIAN_POINT('Ctrl Pts',(3.79852379258844,1.0261973727211,7.14843023961011));
#255912=CARTESIAN_POINT('Ctrl Pts',(3.76665397074647,1.13764942892371,7.15429864165973));
#255913=CARTESIAN_POINT('Ctrl Pts',(3.72988026440124,1.24759056313766,7.16016704370934));
#255914=CARTESIAN_POINT('Ctrl Pts',(3.69314394877411,1.35741991155773,7.16602947889326));
#255915=CARTESIAN_POINT('Ctrl Pts',(3.65151379696037,1.46574100468358,7.17189191407718));
#255916=CARTESIAN_POINT('Ctrl Pts',(3.60513844557973,1.57208962473612,7.1777543492611));
#255917=CARTESIAN_POINT('Ctrl Pts',(3.55731412035048,1.68176105237297,7.18379995319777));
#255918=CARTESIAN_POINT('Ctrl Pts',(3.50444330237383,1.78933428840002,7.18984555713445));
#255919=CARTESIAN_POINT('Ctrl Pts',(3.44674392353413,1.89431922483529,7.19589116107112));
#255920=CARTESIAN_POINT('Ctrl Pts',(3.39085622613519,1.99600777810795,7.20174694132735));
#255921=CARTESIAN_POINT('Ctrl Pts',(3.33043886805119,2.09526775131126,7.20760272158358));
#255922=CARTESIAN_POINT('Ctrl Pts',(3.26573746434136,2.19167694106529,7.21345850183982));
#255923=CARTESIAN_POINT('Ctrl Pts',(3.20104555452681,2.28807198431398,7.21931342285403));
#255924=CARTESIAN_POINT('Ctrl Pts',(3.13207107901831,2.38161673326005,7.22516834386825));
#255925=CARTESIAN_POINT('Ctrl Pts',(3.05910333369062,2.47191743264271,7.23102326488247));
#255926=CARTESIAN_POINT('Ctrl Pts',(2.98612868914464,2.56222667010249,7.23687873948893));
#255927=CARTESIAN_POINT('Ctrl Pts',(2.90916028363934,2.64929092718708,7.2427342140954));
#255928=CARTESIAN_POINT('Ctrl Pts',(2.82852764275017,2.73274959961541,7.24858968870186));
#255929=CARTESIAN_POINT('Ctrl Pts',(2.74786792250078,2.81623630048767,7.25444712978871));
#255930=CARTESIAN_POINT('Ctrl Pts',(2.66354180650745,2.896114712193,7.26030457087555));
#255931=CARTESIAN_POINT('Ctrl Pts',(2.57591508203623,2.97206165651695,7.26616201196239));
#255932=CARTESIAN_POINT('Ctrl Pts',(2.48818958890905,3.04809420460689,7.27202605527689));
#255933=CARTESIAN_POINT('Ctrl Pts',(2.39715637408173,3.12018617032596,7.27789009859139));
#255934=CARTESIAN_POINT('Ctrl Pts',(2.30321371885568,3.18805513836806,7.28375414190588));
#255935=CARTESIAN_POINT('Ctrl Pts',(2.20920758720002,3.25596996502212,7.28962214751559));
#255936=CARTESIAN_POINT('Ctrl Pts',(2.11228844462947,3.31965588594009,7.2954901531253));
#255937=CARTESIAN_POINT('Ctrl Pts',(2.01288143979719,3.37887515444415,7.301358158735));
#255938=CARTESIAN_POINT('Ctrl Pts',(1.91333092300844,3.43817991665259,7.3072346358701));
#255939=CARTESIAN_POINT('Ctrl Pts',(1.81128573836657,3.49300496306484,7.3131111130052));
#255940=CARTESIAN_POINT('Ctrl Pts',(1.70719340343905,3.54315956220634,7.3189875901403));
#255941=CARTESIAN_POINT('Ctrl Pts',(1.6843947723417,3.55414458050243,7.32027467467393));
#255942=CARTESIAN_POINT('Ctrl Pts',(1.66149800241855,3.56490573956675,7.32156175920757));
#255943=CARTESIAN_POINT('Ctrl Pts',(1.63850789823744,3.57544135281415,7.3228488437412));
#255944=CARTESIAN_POINT('Ctrl Pts',(1.53355089953154,3.62353971449461,7.32872478621919));
#255945=CARTESIAN_POINT('Ctrl Pts',(1.42630106718662,3.66709199642041,7.33460072869717));
#255946=CARTESIAN_POINT('Ctrl Pts',(1.3171891745337,3.70587394260669,7.34047667117515));
#255947=CARTESIAN_POINT('Ctrl Pts',(1.20821730204159,3.7446061210343,7.34634507322477));
#255948=CARTESIAN_POINT('Ctrl Pts',(1.09738850678137,3.77858000095999,7.35221347527439));
#255949=CARTESIAN_POINT('Ctrl Pts',(0.985155984923154,3.80761824312392,
7.358081877324));
#255950=CARTESIAN_POINT('Ctrl Pts',(0.87303757869263,3.83662695982432,7.36394431250793));
#255951=CARTESIAN_POINT('Ctrl Pts',(0.759518682182498,3.86070991834644,
7.36980674769186));
#255952=CARTESIAN_POINT('Ctrl Pts',(0.645069573305308,3.87973894039221,
7.37566918287579));
#255953=CARTESIAN_POINT('Ctrl Pts',(0.527044561263792,3.89936251438178,
7.38171478681246));
#255954=CARTESIAN_POINT('Ctrl Pts',(0.408030674305431,3.91361099549031,
7.38776039074913));
#255955=CARTESIAN_POINT('Ctrl Pts',(0.288557645005564,3.92240021995574,
7.3938059946858));
#255956=CARTESIAN_POINT('Ctrl Pts',(0.172835905133741,3.93091347481522,
7.39966177494204));
#255957=CARTESIAN_POINT('Ctrl Pts',(0.0566838666735855,3.93430514103444,
7.40551755519828));
#255958=CARTESIAN_POINT('Ctrl Pts',(-0.0594106094984069,3.93255125579808,
7.41137333545451));
#255959=CARTESIAN_POINT('Ctrl Pts',(-0.175488050664438,3.9307976279163,
7.41722825646874));
#255960=CARTESIAN_POINT('Ctrl Pts',(-0.291507533732658,3.92389995615897,
7.42308317748296));
#255961=CARTESIAN_POINT('Ctrl Pts',(-0.406981265669249,3.91188640548192,
7.42893809849719));
#255962=CARTESIAN_POINT('Ctrl Pts',(-0.522465915833852,3.89987171890424,
7.43479357310366));
#255963=CARTESIAN_POINT('Ctrl Pts',(-0.637404301724936,3.88274023454091,
7.44064904771013));
#255964=CARTESIAN_POINT('Ctrl Pts',(-0.751314521917127,3.86057191218561,
7.4465045223166));
#255965=CARTESIAN_POINT('Ctrl Pts',(-0.86526299728565,3.838396144905,7.45236196340345));
#255966=CARTESIAN_POINT('Ctrl Pts',(-0.978182215408448,3.81118025480984,
7.45821940449031));
#255967=CARTESIAN_POINT('Ctrl Pts',(-1.08960191300048,3.77905499711048,
7.46407684557716));
#255968=CARTESIAN_POINT('Ctrl Pts',(-1.20114719755051,3.74689352935602,
7.46994088889166));
#255969=CARTESIAN_POINT('Ctrl Pts',(-1.31118919133558,3.70981176393342,
7.47580493220616));
#255970=CARTESIAN_POINT('Ctrl Pts',(-1.41927411974641,3.6679899090671,7.48166897552066));
#255971=CARTESIAN_POINT('Ctrl Pts',(-1.52743208042712,3.62613979545058,
7.48753698113037));
#255972=CARTESIAN_POINT('Ctrl Pts',(-1.633629965518,3.57954338011618,7.49340498674008));
#255973=CARTESIAN_POINT('Ctrl Pts',(-1.73743682923334,3.52842773263441,
7.49927299234979));
#255974=CARTESIAN_POINT('Ctrl Pts',(-1.84139355689568,3.4772382904881,7.50514946948489));
#255975=CARTESIAN_POINT('Ctrl Pts',(-1.94295201401711,3.42151679365053,
7.51102594661999));
#255976=CARTESIAN_POINT('Ctrl Pts',(-2.04170850168642,3.36153467840827,
7.51690242375509));
#255977=CARTESIAN_POINT('Ctrl Pts',(-2.06333845870785,3.34839720657869,
7.51818950828867));
#255978=CARTESIAN_POINT('Ctrl Pts',(-2.08483412369737,3.33505550489099,
7.51947659282224));
#255979=CARTESIAN_POINT('Ctrl Pts',(-2.10619146538181,3.32151268417762,
7.52076367735582));
#255980=CARTESIAN_POINT('Ctrl Pts',(-2.20369439385821,3.25968548213652,
7.52663961983381));
#255981=CARTESIAN_POINT('Ctrl Pts',(-2.29863346627671,3.19345935189115,
7.53251556231179));
#255982=CARTESIAN_POINT('Ctrl Pts',(-2.39058598756845,3.12307342789781,
7.53839150478978));
#255983=CARTESIAN_POINT('Ctrl Pts',(-2.48242050882824,3.05277782814097,
7.54425990683939));
#255984=CARTESIAN_POINT('Ctrl Pts',(-2.57127577603329,2.97833329935637,
7.55012830888901));
#255985=CARTESIAN_POINT('Ctrl Pts',(-2.65675622902896,2.9000233343054,7.55599671093863));
#255986=CARTESIAN_POINT('Ctrl Pts',(-2.74214976732823,2.82179299315204,
7.56185914612255));
#255987=CARTESIAN_POINT('Ctrl Pts',(-2.82417501443411,2.73970531080422,
7.56772158130647));
#255988=CARTESIAN_POINT('Ctrl Pts',(-2.90246833628129,2.65408488125089,
7.5735840164904));
#255989=CARTESIAN_POINT('Ctrl Pts',(-2.98320789244257,2.5657892856959,7.57962962042706));
#255990=CARTESIAN_POINT('Ctrl Pts',(-3.05997813090029,2.47373682787979,
7.58567522436373));
#255991=CARTESIAN_POINT('Ctrl Pts',(-3.13241994927456,2.37832593674348,
7.5917208283004));
#255992=CARTESIAN_POINT('Ctrl Pts',(-3.20258719380562,2.28591081686481,
7.59757660855664));
#255993=CARTESIAN_POINT('Ctrl Pts',(-3.26869349911763,2.19034536371258,
7.60343238881288));
#255994=CARTESIAN_POINT('Ctrl Pts',(-3.33045305657604,2.09202567812714,
7.60928816906912));
#255995=CARTESIAN_POINT('Ctrl Pts',(-3.392203551808,1.99372041938172,7.61514309008334));
#255996=CARTESIAN_POINT('Ctrl Pts',(-3.44960834796533,1.89266208125359,
7.62099801109756));
#255997=CARTESIAN_POINT('Ctrl Pts',(-3.50242539112959,1.78927509890758,
7.62685293211179));
#255998=CARTESIAN_POINT('Ctrl Pts',(-3.55524742823067,1.68587834115526,
7.63270840671826));
#255999=CARTESIAN_POINT('Ctrl Pts',(-3.60348066223641,1.58015286908215,
7.63856388132473));
#256000=CARTESIAN_POINT('Ctrl Pts',(-3.64692968661997,1.47254638665475,
7.6444193559312));
#256001=CARTESIAN_POINT('Ctrl Pts',(-3.69039330275907,1.36490376607447,
7.65027679701805));
#256002=CARTESIAN_POINT('Ctrl Pts',(-3.72906935990102,1.25537926151467,
7.6561342381049));
#256003=CARTESIAN_POINT('Ctrl Pts',(-3.7628113905605,1.14443848199376,7.66199167919175));
#256004=CARTESIAN_POINT('Ctrl Pts',(-3.79659145362431,1.03337265532832,
7.66785572250625));
#256005=CARTESIAN_POINT('Ctrl Pts',(-3.8254262700917,0.920887762643375,
7.67371976582075));
#256006=CARTESIAN_POINT('Ctrl Pts',(-3.84921982752044,0.807462518897018,
7.67958380913525));
#256007=CARTESIAN_POINT('Ctrl Pts',(-3.8730294620983,0.693960634464899,
7.68545181474497));
#256008=CARTESIAN_POINT('Ctrl Pts',(-3.89179098811298,0.579517540040464,
7.69131982035469));
#256009=CARTESIAN_POINT('Ctrl Pts',(-3.90546012776368,0.464618327714394,
7.69718782596441));
#256010=CARTESIAN_POINT('Ctrl Pts',(-3.919149001285,0.349553237633885,7.70306430309951));
#256011=CARTESIAN_POINT('Ctrl Pts',(-3.92773078638208,0.234031125519982,
7.70894078023462));
#256012=CARTESIAN_POINT('Ctrl Pts',(-3.93121325401241,0.11853839663663,
7.71481725736972));
#256013=CARTESIAN_POINT('Ctrl Pts',(-3.9319759950429,0.0932428153438174,
7.71610434190329));
#256014=CARTESIAN_POINT('Ctrl Pts',(-3.93249431380678,0.0679486270207419,
7.71739142643687));
#256015=CARTESIAN_POINT('Ctrl Pts',(-3.93276862363217,0.0426609068621461,
7.71867851097045));
#256016=CARTESIAN_POINT('Ctrl Pts',(-3.93292192916729,0.0285281740471575,
7.71939783330197));
#256017=CARTESIAN_POINT('Ctrl Pts',(-3.93299905428545,0.0143946133687574,
7.72011715563349));
#256018=CARTESIAN_POINT('Ctrl Pts',(-3.93299999135595,0.00026075673218739,
7.72083647796501));
#256019=CARTESIAN_POINT('',(-3.9329988040277,0.00306716754010798,8.97083647792409));
#256020=CARTESIAN_POINT('Ctrl Pts',(-3.93299999135599,0.000260756115881105,
7.72083647799638));
#256021=CARTESIAN_POINT('Ctrl Pts',(-3.93300763141371,-0.114974688434713,
7.72670122042153));
#256022=CARTESIAN_POINT('Ctrl Pts',(-3.927946446357,-0.230403984016668,
7.73256596284667));
#256023=CARTESIAN_POINT('Ctrl Pts',(-3.91779128489456,-0.345543699123907,
7.73843070527182));
#256024=CARTESIAN_POINT('Ctrl Pts',(-3.90764915179362,-0.460535698034116,
7.74428792364285));
#256025=CARTESIAN_POINT('Ctrl Pts',(-3.89242607403925,-0.57523844606433,
7.75014514201388));
#256026=CARTESIAN_POINT('Ctrl Pts',(-3.8721488925929,-0.689167580194828,
7.75600236038491));
#256027=CARTESIAN_POINT('Ctrl Pts',(-3.85189226461298,-0.802981232859575,
7.76185364173054));
#256028=CARTESIAN_POINT('Ctrl Pts',(-3.82659179463562,-0.916022425562077,
7.76770492307617));
#256029=CARTESIAN_POINT('Ctrl Pts',(-3.79632613907405,-1.02781167817023,
7.77355620442181));
#256030=CARTESIAN_POINT('Ctrl Pts',(-3.76549875443117,-1.14167573381843,
7.77951608526194));
#256031=CARTESIAN_POINT('Ctrl Pts',(-3.72952007097172,-1.25424047765321,
7.78547596610208));
#256032=CARTESIAN_POINT('Ctrl Pts',(-3.688527897781,-1.3650095044692,7.79143584694221));
#256033=CARTESIAN_POINT('Ctrl Pts',(-3.64832754556203,-1.47363887311081,
7.79728060437534));
#256034=CARTESIAN_POINT('Ctrl Pts',(-3.6033058045945,-1.58054087155183,
7.80312536180847));
#256035=CARTESIAN_POINT('Ctrl Pts',(-3.55364279889051,-1.6852631420326,
7.8089701192416));
#256036=CARTESIAN_POINT('Ctrl Pts',(-3.50398670115038,-1.78997084598345,
7.81481406368783));
#256037=CARTESIAN_POINT('Ctrl Pts',(-3.44969079993109,-1.89249905036668,
7.82065800813405));
#256038=CARTESIAN_POINT('Ctrl Pts',(-3.39098260860229,-1.99241711199157,
7.82650195258028));
#256039=CARTESIAN_POINT('Ctrl Pts',(-3.3322682701429,-2.09234563568928,
7.83234650892561));
#256040=CARTESIAN_POINT('Ctrl Pts',(-3.26914093330697,-2.18966311598395,
7.83819106527095));
#256041=CARTESIAN_POINT('Ctrl Pts',(-3.20187276557864,-2.28396580382583,
7.84403562161628));
#256042=CARTESIAN_POINT('Ctrl Pts',(-3.13228058454925,-2.38152650668836,
7.85008209853034));
#256043=CARTESIAN_POINT('Ctrl Pts',(-3.05825654802452,-2.47585994134154,
7.85612857544441));
#256044=CARTESIAN_POINT('Ctrl Pts',(-2.98014815975296,-2.56655526843298,
7.86217505235848));
#256045=CARTESIAN_POINT('Ctrl Pts',(-2.90453498716516,-2.65435328311519,
7.86802837122177));
#256046=CARTESIAN_POINT('Ctrl Pts',(-2.82509477184531,-2.73874182604679,
7.87388169008506));
#256047=CARTESIAN_POINT('Ctrl Pts',(-2.74218029393698,-2.81938579047702,
7.87973500894835));
#256048=CARTESIAN_POINT('Ctrl Pts',(-2.6551615806433,-2.90402160073174,
7.88587806488781));
#256049=CARTESIAN_POINT('Ctrl Pts',(-2.56431624269091,-2.98453227656997,
7.89202112082726));
#256050=CARTESIAN_POINT('Ctrl Pts',(-2.47009000278943,-3.06057909195624,
7.89816417676671));
#256051=CARTESIAN_POINT('Ctrl Pts',(-2.37586376288796,-3.13662590734251,
7.90430723270616));
#256052=CARTESIAN_POINT('Ctrl Pts',(-2.27825708356548,-3.20820861392727,
7.91045028864561));
#256053=CARTESIAN_POINT('Ctrl Pts',(-2.1777479311858,-3.27504243456722,
7.91659334458507));
#256054=CARTESIAN_POINT('Ctrl Pts',(-2.08160913581824,-3.33897017501681,
7.92246928706305));
#256055=CARTESIAN_POINT('Ctrl Pts',(-1.98249445764508,-3.39876656595813,
7.92834522954104));
#256056=CARTESIAN_POINT('Ctrl Pts',(-1.88079427711241,-3.45414271378315,
7.93422117201903));
#256057=CARTESIAN_POINT('Ctrl Pts',(-1.77922460550304,-3.50944779898672,
7.94008957406865));
#256058=CARTESIAN_POINT('Ctrl Pts',(-1.67507638916764,-3.56034372623259,
7.94595797611827));
#256059=CARTESIAN_POINT('Ctrl Pts',(-1.56876949590573,-3.60658443249506,
7.9518263781679));
#256060=CARTESIAN_POINT('Ctrl Pts',(-1.46257069321916,-3.65277812219641,
7.95768881335183));
#256061=CARTESIAN_POINT('Ctrl Pts',(-1.3542179558431,-3.69432584246097,
7.96355124853576));
#256062=CARTESIAN_POINT('Ctrl Pts',(-1.24415571475198,-3.73102741311961,
7.9694136837197));
#256063=CARTESIAN_POINT('Ctrl Pts',(-1.13065463590979,-3.76887570535554,
7.97545928765636));
#256064=CARTESIAN_POINT('Ctrl Pts',(-1.01533586459138,-3.80156982538415,
7.98150489159303));
#256065=CARTESIAN_POINT('Ctrl Pts',(-0.898709440783336,-3.82894376310842,
7.9875504955297));
#256066=CARTESIAN_POINT('Ctrl Pts',(-0.785744926891016,-3.85545819669366,
7.99340627578594));
#256067=CARTESIAN_POINT('Ctrl Pts',(-0.671554081155232,-3.87698144431913,
7.99926205604218));
#256068=CARTESIAN_POINT('Ctrl Pts',(-0.556615006701356,-3.89341350672066,
8.00511783629842));
#256069=CARTESIAN_POINT('Ctrl Pts',(-0.441692797716789,-3.90984315798006,
8.01097275731265));
#256070=CARTESIAN_POINT('Ctrl Pts',(-0.326022986827634,-3.92118305109915,
8.01682767832687));
#256071=CARTESIAN_POINT('Ctrl Pts',(-0.210091766155291,-3.92738468319488,
8.02268259934109));
#256072=CARTESIAN_POINT('Ctrl Pts',(-0.0941495839985609,-3.93358690166496,
8.02853807394757));
#256073=CARTESIAN_POINT('Ctrl Pts',(0.0220536448866986,-3.9346498712754,
8.03439354855404));
#256074=CARTESIAN_POINT('Ctrl Pts',(0.138029443514754,-3.93057716788807,
8.04024902316051));
#256075=CARTESIAN_POINT('Ctrl Pts',(0.254044191015066,-3.92650309673949,
8.04610646424737));
#256076=CARTESIAN_POINT('Ctrl Pts',(0.369830944103958,-3.91728993744105,
8.05196390533422));
#256077=CARTESIAN_POINT('Ctrl Pts',(0.484904773060254,-3.90299325659978,
8.05782134642107));
#256078=CARTESIAN_POINT('Ctrl Pts',(0.600108307736879,-3.88868046122315,
8.06368538973557));
#256079=CARTESIAN_POINT('Ctrl Pts',(0.714596904617967,-3.86927275895671,
8.06954943305008));
#256080=CARTESIAN_POINT('Ctrl Pts',(0.827894182077904,-3.84487714020638,
8.07541347636458));
#256081=CARTESIAN_POINT('Ctrl Pts',(0.941268013757286,-3.82046503749815,
8.08128148197429));
#256082=CARTESIAN_POINT('Ctrl Pts',(1.05344852485709,-3.79105841155848,
8.08714948758399));
#256083=CARTESIAN_POINT('Ctrl Pts',(1.16397454940685,-3.75681410883385,
8.09301749319369));
#256084=CARTESIAN_POINT('Ctrl Pts',(1.27466013822565,-3.72252036827633,
8.09889397032881));
#256085=CARTESIAN_POINT('Ctrl Pts',(1.3836860868475,-3.68337515209494,8.10477044746393));
#256086=CARTESIAN_POINT('Ctrl Pts',(1.49061119890961,-3.63958339012657,
8.11064692459905));
#256087=CARTESIAN_POINT('Ctrl Pts',(1.514030273777,-3.62999198047235,8.1119340091326));
#256088=CARTESIAN_POINT('Ctrl Pts',(1.53734866471534,-3.62017784468314,
8.11322109366616));
#256089=CARTESIAN_POINT('Ctrl Pts',(1.56056190337424,-3.61014342453828,
8.11450817819971));
#256090=CARTESIAN_POINT('Ctrl Pts',(1.66653758059776,-3.5643331657449,8.12038412067769));
#256091=CARTESIAN_POINT('Ctrl Pts',(1.77066924225063,-3.51377701042851,
8.12626006315568));
#256092=CARTESIAN_POINT('Ctrl Pts',(1.87250198377017,-3.45864501225216,
8.13213600563367));
#256093=CARTESIAN_POINT('Ctrl Pts',(1.97420404625462,-3.40358376338707,
8.13800440768328));
#256094=CARTESIAN_POINT('Ctrl Pts',(2.07361269589383,-3.34395854428528,
8.14387280973289));
#256095=CARTESIAN_POINT('Ctrl Pts',(2.17029288846745,-3.27998746617538,
8.1497412117825));
#256096=CARTESIAN_POINT('Ctrl Pts',(2.266874778689,-3.21608143248953,8.15560364696642));
#256097=CARTESIAN_POINT('Ctrl Pts',(2.36073338795434,-3.1478385557713,8.16146608215034));
#256098=CARTESIAN_POINT('Ctrl Pts',(2.45145877416057,-3.07552253748711,
8.16732851733426));
#256099=CARTESIAN_POINT('Ctrl Pts',(2.54501882809664,-3.00094704264456,
8.17337412127093));
#256100=CARTESIAN_POINT('Ctrl Pts',(2.63524625568776,-2.92203990853658,
8.1794197252076));
#256101=CARTESIAN_POINT('Ctrl Pts',(2.72172403835726,-2.83913847126699,
8.18546532914427));
#256102=CARTESIAN_POINT('Ctrl Pts',(2.80548653713557,-2.75884002554304,
8.19132110940051));
#256103=CARTESIAN_POINT('Ctrl Pts',(2.88573101786577,-2.67479466427583,
8.19717688965675));
#256104=CARTESIAN_POINT('Ctrl Pts',(2.96211321729066,-2.5873488918103,8.20303266991299));
#256105=CARTESIAN_POINT('Ctrl Pts',(3.0384842088505,-2.49991595061205,8.20888759092721));
#256106=CARTESIAN_POINT('Ctrl Pts',(3.11099377455895,-2.40908390115884,
8.21474251194144));
#256107=CARTESIAN_POINT('Ctrl Pts',(3.17933643375411,-2.31523407909518,
8.22059743295566));
#256108=CARTESIAN_POINT('Ctrl Pts',(3.24768555485803,-2.22137538337933,
8.22645290756213));
#256109=CARTESIAN_POINT('Ctrl Pts',(3.31186674324788,-2.12449868151264,
8.23230838216859));
#256110=CARTESIAN_POINT('Ctrl Pts',(3.37161695046699,-2.02501558989645,
8.23816385677505));
#256111=CARTESIAN_POINT('Ctrl Pts',(3.43138722396919,-1.9254990882559,8.2440212978619));
#256112=CARTESIAN_POINT('Ctrl Pts',(3.48672334486547,-1.82337480995101,
8.24987873894876));
#256113=CARTESIAN_POINT('Ctrl Pts',(3.5374077995522,-1.71907971300554,8.25573618003562));
#256114=CARTESIAN_POINT('Ctrl Pts',(3.58814938333396,-1.61466705961125,
8.26160022335013));
#256115=CARTESIAN_POINT('Ctrl Pts',(3.63422865567289,-1.50807907537374,
8.26746426666464));
#256116=CARTESIAN_POINT('Ctrl Pts',(3.67547588602648,-1.39977355712911,
8.27332830997915));
#256117=CARTESIAN_POINT('Ctrl Pts',(3.71675098686027,-1.29139485756354,
8.27919631558887));
#256118=CARTESIAN_POINT('Ctrl Pts',(3.7531874149327,-1.18129670394983,8.28506432119859));
#256119=CARTESIAN_POINT('Ctrl Pts',(3.78466553940226,-1.06995128620932,
8.2909323268083));
#256120=CARTESIAN_POINT('Ctrl Pts',(3.81618910822688,-0.958445121258386,
8.2968088039434));
#256121=CARTESIAN_POINT('Ctrl Pts',(3.84273999392077,-0.845688498873854,
8.3026852810785));
#256122=CARTESIAN_POINT('Ctrl Pts',(3.86424976790761,-0.732163049618011,
8.3085617582136));
#256123=CARTESIAN_POINT('Ctrl Pts',(3.86896090636399,-0.707298348106351,
8.30984884274717));
#256124=CARTESIAN_POINT('Ctrl Pts',(3.87343041490796,-0.682396779669048,
8.31113592728075));
#256125=CARTESIAN_POINT('Ctrl Pts',(3.87765790770314,-0.657463421664869,
8.31242301181432));
#256126=CARTESIAN_POINT('Ctrl Pts',(3.89695773132982,-0.543634862938722,
8.31829895429231));
#256127=CARTESIAN_POINT('Ctrl Pts',(3.91127299793002,-0.428767979368567,
8.32417489677029));
#256128=CARTESIAN_POINT('Ctrl Pts',(3.92049856335526,-0.313336902916516,
8.33005083924827));
#256129=CARTESIAN_POINT('Ctrl Pts',(3.92971228987715,-0.198053955852254,
8.3359192412979));
#256130=CARTESIAN_POINT('Ctrl Pts',(3.93384927191079,-0.0822086635191154,
8.34178764334753));
#256131=CARTESIAN_POINT('Ctrl Pts',(3.93285548640346,0.0337153239081983,
8.34765604539716));
#256132=CARTESIAN_POINT('Ctrl Pts',(3.93186271135597,0.149521442304274,
8.35351848058109));
#256133=CARTESIAN_POINT('Ctrl Pts',(3.92574954930698,0.265405686297156,
8.35938091576501));
#256134=CARTESIAN_POINT('Ctrl Pts',(3.91451388395261,0.380880627417861,
8.36524335094894));
#256135=CARTESIAN_POINT('Ctrl Pts',(3.90292716605019,0.499963523300396,
8.37128895488561));
#256136=CARTESIAN_POINT('Ctrl Pts',(3.88589254737316,0.618610673579545,
8.37733455882228));
#256137=CARTESIAN_POINT('Ctrl Pts',(3.86346581227279,0.7362886101247,8.38338016275894));
#256138=CARTESIAN_POINT('Ctrl Pts',(3.84174324592732,0.850271620694905,
8.38923594301519));
#256139=CARTESIAN_POINT('Ctrl Pts',(3.81496219345816,0.963344936144892,
8.39509172327143));
#256140=CARTESIAN_POINT('Ctrl Pts',(3.78322575425377,1.07503111227119,8.40094750352767));
#256141=CARTESIAN_POINT('Ctrl Pts',(3.75149397186385,1.1867009002388,8.40680242454189));
#256142=CARTESIAN_POINT('Ctrl Pts',(3.71480836139263,1.29698355667858,8.41265734555611));
#256143=CARTESIAN_POINT('Ctrl Pts',(3.67332235685453,1.40541519225911,8.41851226657032));
#256144=CARTESIAN_POINT('Ctrl Pts',(3.6318324297476,1.51385708022616,8.42436774117679));
#256145=CARTESIAN_POINT('Ctrl Pts',(3.58554135379455,1.62044721389172,8.43022321578326));
#256146=CARTESIAN_POINT('Ctrl Pts',(3.53465106900056,1.72474079803698,8.43607869038973));
#256147=CARTESIAN_POINT('Ctrl Pts',(3.48374369340638,1.82906940774389,8.44193613147658));
#256148=CARTESIAN_POINT('Ctrl Pts',(3.42823421850167,1.93109956353574,8.44779357256343));
#256149=CARTESIAN_POINT('Ctrl Pts',(3.36837063784763,2.03041085647363,8.45365101365027));
#256150=CARTESIAN_POINT('Ctrl Pts',(3.30843958182644,2.12983408835467,8.45951505696478));
#256151=CARTESIAN_POINT('Ctrl Pts',(3.24414483793516,2.22653198714789,8.46537910027928));
#256152=CARTESIAN_POINT('Ctrl Pts',(3.17577790141848,2.32011286812992,8.47124314359379));
#256153=CARTESIAN_POINT('Ctrl Pts',(3.1073647698161,2.41375698109275,8.47711114920348));
#256154=CARTESIAN_POINT('Ctrl Pts',(3.03487422388538,2.50427956098514,8.48297915481317));
#256155=CARTESIAN_POINT('Ctrl Pts',(2.95863711649576,2.59132310082971,8.48884716042286));
#256156=CARTESIAN_POINT('Ctrl Pts',(2.88228994707891,2.67849230373757,8.49472363755797));
#256157=CARTESIAN_POINT('Ctrl Pts',(2.8021857063234,2.76217214620715,8.50060011469308));
#256158=CARTESIAN_POINT('Ctrl Pts',(2.71869105178692,2.84204292102243,8.50647659182819));
#256159=CARTESIAN_POINT('Ctrl Pts',(2.70040378953428,2.85953646972297,8.50776367636178));
#256160=CARTESIAN_POINT('Ctrl Pts',(2.68195400531168,2.8768474511919,8.50905076089537));
#256161=CARTESIAN_POINT('Ctrl Pts',(2.66334574718046,2.89397277647454,8.51033784542896));
#256162=CARTESIAN_POINT('Ctrl Pts',(2.57839324286485,2.97215522964777,8.51621378790694));
#256163=CARTESIAN_POINT('Ctrl Pts',(2.48985510842656,3.04672282682729,8.52208973038492));
#256164=CARTESIAN_POINT('Ctrl Pts',(2.39807171558815,3.1173291527999,8.5279656728629));
#256165=CARTESIAN_POINT('Ctrl Pts',(2.30640610574387,3.18784487170056,8.53383407491252));
#256166=CARTESIAN_POINT('Ctrl Pts',(2.21150384384635,3.25440917942465,8.53970247696214));
#256167=CARTESIAN_POINT('Ctrl Pts',(2.1137411271544,3.31671335019716,8.54557087901176));
#256168=CARTESIAN_POINT('Ctrl Pts',(2.01607781350173,3.37895417142145,8.55143331419569));
#256169=CARTESIAN_POINT('Ctrl Pts',(1.91556017639965,3.43694325132007,8.55729574937962));
#256170=CARTESIAN_POINT('Ctrl Pts',(1.81259585267499,3.49041333868432,8.56315818456356));
#256171=CARTESIAN_POINT('Ctrl Pts',(1.70641446195327,3.5455540712504,8.56920378850023));
#256172=CARTESIAN_POINT('Ctrl Pts',(1.59763133453854,3.59588850968678,8.5752493924369));
#256173=CARTESIAN_POINT('Ctrl Pts',(1.48672425454009,3.64117288671689,8.58129499637356));
#256174=CARTESIAN_POINT('Ctrl Pts',(1.37929950489814,3.68503539635306,8.58715077662979));
#256175=CARTESIAN_POINT('Ctrl Pts',(1.2698825971241,3.72416006544192,8.59300655688602));
#256176=CARTESIAN_POINT('Ctrl Pts',(1.15893009997142,3.75837332144908,8.59886233714225));
#256177=CARTESIAN_POINT('Ctrl Pts',(1.04799388332157,3.79258155720862,8.60471725815646));
#256178=CARTESIAN_POINT('Ctrl Pts',(0.935522919670791,3.82187969132178,
8.61057217917068));
#256179=CARTESIAN_POINT('Ctrl Pts',(0.821989824359372,3.84614374778812,
8.61642710018489));
#256180=CARTESIAN_POINT('Ctrl Pts',(0.70844599431038,3.8704100984602,8.62228257479135));
#256181=CARTESIAN_POINT('Ctrl Pts',(0.593840236625425,3.8896413390112,8.6281380493978));
#256182=CARTESIAN_POINT('Ctrl Pts',(0.478655571701212,3.90376457329068,
8.63399352400426));
#256183=CARTESIAN_POINT('Ctrl Pts',(0.363432223596314,3.91789255066356,
8.63985096509108));
#256184=CARTESIAN_POINT('Ctrl Pts',(0.24762999111753,3.92690906040524,8.64570840617791));
#256185=CARTESIAN_POINT('Ctrl Pts',(0.131736525648879,3.93079311180453,
8.65156584726473));
#256186=CARTESIAN_POINT('Ctrl Pts',(0.0157124306043185,3.93468154112095,
8.65742989057923));
#256187=CARTESIAN_POINT('Ctrl Pts',(-0.100402689938917,3.93342595190847,
8.66329393389373));
#256188=CARTESIAN_POINT('Ctrl Pts',(-0.216121581555738,3.92705748137022,
8.66915797720823));
#256189=CARTESIAN_POINT('Ctrl Pts',(-0.331918663660945,3.92068470769863,
8.67502598281794));
#256190=CARTESIAN_POINT('Ctrl Pts',(-0.447318574030938,3.90919221421752,
8.68089398842765));
#256191=CARTESIAN_POINT('Ctrl Pts',(-0.561841285935853,3.8926627608127,
8.68676199403737));
#256192=CARTESIAN_POINT('Ctrl Pts',(-0.676529332048938,3.87610944415801,
8.69263847117247));
#256193=CARTESIAN_POINT('Ctrl Pts',(-0.790337248512992,3.85450473233834,
8.69851494830757));
#256194=CARTESIAN_POINT('Ctrl Pts',(-0.902797209048255,3.82798200091572,
8.70439142544266));
#256195=CARTESIAN_POINT('Ctrl Pts',(-0.927428543865126,3.8221729087302,
8.7056785099763));
#256196=CARTESIAN_POINT('Ctrl Pts',(-0.951995282899111,3.81612808031578,
8.70696559450994));
#256197=CARTESIAN_POINT('Ctrl Pts',(-0.976492630786821,3.80984922825288,
8.70825267904357));
#256198=CARTESIAN_POINT('Ctrl Pts',(-1.08833066728694,3.78118430952744,
8.71412862152157));
#256199=CARTESIAN_POINT('Ctrl Pts',(-1.19908995043581,3.74754342673066,
8.72000456399956));
#256200=CARTESIAN_POINT('Ctrl Pts',(-1.30829457137154,3.70902336397599,
8.72588050647755));
#256201=CARTESIAN_POINT('Ctrl Pts',(-1.41735905315022,3.67055273291274,
8.73174890852714));
#256202=CARTESIAN_POINT('Ctrl Pts',(-1.52487245456459,3.62721550997189,
8.73761731057673));
#256203=CARTESIAN_POINT('Ctrl Pts',(-1.63037096332379,3.57915905234046,
8.74348571262632));
#256204=CARTESIAN_POINT('Ctrl Pts',(-1.73576220345629,3.53115145748704,
8.74934814781025));
#256205=CARTESIAN_POINT('Ctrl Pts',(-1.83914225263862,3.47843434274131,
8.75521058299418));
#256206=CARTESIAN_POINT('Ctrl Pts',(-1.94006495841097,3.4212040215611,8.76107301817811));
#256207=CARTESIAN_POINT('Ctrl Pts',(-2.04414094188438,3.36218556861985,
8.76711862211478));
#256208=CARTESIAN_POINT('Ctrl Pts',(-2.14560307951632,3.29836739620784,
8.77316422605145));
#256209=CARTESIAN_POINT('Ctrl Pts',(-2.24398670852152,3.23001743833973,
8.77920982998812));
#256210=CARTESIAN_POINT('Ctrl Pts',(-2.33928122637291,3.16381357550133,
8.78506561024436));
#256211=CARTESIAN_POINT('Ctrl Pts',(-2.43168730305447,3.09335850875303,
8.7909213905006));
#256212=CARTESIAN_POINT('Ctrl Pts',(-2.52081070056782,3.0189406108605,8.79677717075683));
#256213=CARTESIAN_POINT('Ctrl Pts',(-2.60992102064913,2.94453363260333,
8.80263209177105));
#256214=CARTESIAN_POINT('Ctrl Pts',(-2.69574930261961,2.86616524394409,
8.80848701278526));
#256215=CARTESIAN_POINT('Ctrl Pts',(-2.77793416366369,2.78416428795969,
8.81434193379948));
#256216=CARTESIAN_POINT('Ctrl Pts',(-2.86012679541967,2.70215557865192,
8.82019740840597));
#256217=CARTESIAN_POINT('Ctrl Pts',(-2.93867502922724,2.61651391079365,
8.82605288301246));
#256218=CARTESIAN_POINT('Ctrl Pts',(-3.01325465410107,2.52760467429901,
8.83190835761895));
#256219=CARTESIAN_POINT('Ctrl Pts',(-3.0878593255131,2.4386655788638,8.83776579870582));
#256220=CARTESIAN_POINT('Ctrl Pts',(-3.15849247261472,2.34645704875029,
8.84362323979268));
#256221=CARTESIAN_POINT('Ctrl Pts',(-3.22487089347209,2.25137662785162,
8.84948068087954));
#256222=CARTESIAN_POINT('Ctrl Pts',(-3.29132413291297,2.15618903684676,
8.85534472419405));
#256223=CARTESIAN_POINT('Ctrl Pts',(-3.35351283797005,2.05812343285433,
8.86120876750855));
#256224=CARTESIAN_POINT('Ctrl Pts',(-3.41119774079782,1.95760541815144,
8.86707281082306));
#256225=CARTESIAN_POINT('Ctrl Pts',(-3.46892162093227,1.85701948409192,
8.87294081643279));
#256226=CARTESIAN_POINT('Ctrl Pts',(-3.5221354501389,1.75397820546516,8.87880882204251));
#256227=CARTESIAN_POINT('Ctrl Pts',(-3.57064719127853,1.64892923905629,
8.88467682765224));
#256228=CARTESIAN_POINT('Ctrl Pts',(-3.6192289678737,1.54372861550123,8.89055330478734));
#256229=CARTESIAN_POINT('Ctrl Pts',(-3.66309495360247,1.43651490033964,
8.89642978192244));
#256230=CARTESIAN_POINT('Ctrl Pts',(-3.70210220588523,1.32775308592361,
8.90230625905754));
#256231=CARTESIAN_POINT('Ctrl Pts',(-3.71064569715652,1.30393173072083,
8.9035933435911));
#256232=CARTESIAN_POINT('Ctrl Pts',(-3.71895630268983,1.28003615680195,
8.90488042812465));
#256233=CARTESIAN_POINT('Ctrl Pts',(-3.72703284698822,1.25607131862442,
8.90616751265821));
#256234=CARTESIAN_POINT('Ctrl Pts',(-3.77057278820299,1.12687898005475,
8.9131060723762));
#256235=CARTESIAN_POINT('Ctrl Pts',(-3.8074234076311,0.995326044578603,
8.9200446320942));
#256236=CARTESIAN_POINT('Ctrl Pts',(-3.83736273983174,0.862053480331147,
8.9269831918122));
#256237=CARTESIAN_POINT('Ctrl Pts',(-3.86714814939447,0.729466090506162,
8.93388607934459));
#256238=CARTESIAN_POINT('Ctrl Pts',(-3.89009306797262,0.595176783475139,
8.94078896687699));
#256239=CARTESIAN_POINT('Ctrl Pts',(-3.90602587688562,0.459837850877824,
8.94769185440938));
#256240=CARTESIAN_POINT('Ctrl Pts',(-3.92181433051305,0.325725123299988,
8.95453220003178));
#256241=CARTESIAN_POINT('Ctrl Pts',(-3.93071707851339,0.190581796902268,
8.96137254565419));
#256242=CARTESIAN_POINT('Ctrl Pts',(-3.93261454488523,0.0550621590310676,
8.96821289127659));
#256243=CARTESIAN_POINT('Ctrl Pts',(-3.93285713337963,0.0377361576845521,
8.96908742015909));
#256244=CARTESIAN_POINT('Ctrl Pts',(-3.93298528379372,0.0204040307365112,
8.96996194904159));
#256245=CARTESIAN_POINT('Ctrl Pts',(-3.9329988040277,0.00306716754012942,
8.97083647792409));
#256246=CARTESIAN_POINT('',(-3.93299908398399,-0.00268428409338097,10.2208364780097));
#256247=CARTESIAN_POINT('Ctrl Pts',(-3.93299880402833,0.00306716672873387,
8.97083647796502));
#256248=CARTESIAN_POINT('Ctrl Pts',(-3.93308917252479,-0.112811499136198,
8.97668178221734));
#256249=CARTESIAN_POINT('Ctrl Pts',(-3.9280540123563,-0.228756031444991,
8.98252708646965));
#256250=CARTESIAN_POINT('Ctrl Pts',(-3.91790260917037,-0.344279167327913,
8.98837239072197));
#256251=CARTESIAN_POINT('Ctrl Pts',(-3.90775321798013,-0.459779406666684,
8.99421653644213));
#256252=CARTESIAN_POINT('Ctrl Pts',(-3.89248963587196,-0.574858003416339,
9.0000606821623));
#256253=CARTESIAN_POINT('Ctrl Pts',(-3.87217315440355,-0.689031249158154,
9.00590482788247));
#256254=CARTESIAN_POINT('Ctrl Pts',(-3.85185576317811,-0.803209607493564,
9.01174923529916));
#256255=CARTESIAN_POINT('Ctrl Pts',(-3.82648509527511,-0.916482126613162,
9.01759364271585));
#256256=CARTESIAN_POINT('Ctrl Pts',(-3.79617372817084,-1.02837445784379,
9.02343805013255));
#256257=CARTESIAN_POINT('Ctrl Pts',(-3.76585363871364,-1.1402989870416,
9.02928413932704));
#256258=CARTESIAN_POINT('Ctrl Pts',(-3.73059013125671,-1.25084213917707,
9.03513022852153));
#256259=CARTESIAN_POINT('Ctrl Pts',(-3.69054568544134,-1.35954460892989,
9.04097631771602));
#256260=CARTESIAN_POINT('Ctrl Pts',(-3.65045510954265,-1.46837230089229,
9.04682914144201));
#256261=CARTESIAN_POINT('Ctrl Pts',(-3.60557274235956,-1.57535468796528,
9.052681965168));
#256262=CARTESIAN_POINT('Ctrl Pts',(-3.55610934335194,-1.68005218315533,
9.05853478889398));
#256263=CARTESIAN_POINT('Ctrl Pts',(-3.50661459556593,-1.78481603323892,
9.06439132200666));
#256264=CARTESIAN_POINT('Ctrl Pts',(-3.45253322725666,-1.88729174216262,
9.07024785511933));
#256265=CARTESIAN_POINT('Ctrl Pts',(-3.39412122504588,-1.98706570341623,
9.07610438823201));
#256266=CARTESIAN_POINT('Ctrl Pts',(-3.33561524295534,-2.08700019237866,
9.08197034400196));
#256267=CARTESIAN_POINT('Ctrl Pts',(-3.27276493769432,-2.18422390633897,
9.08783629977193));
#256268=CARTESIAN_POINT('Ctrl Pts',(-3.20586891361158,-2.27835324494226,
9.09370225554188));
#256269=CARTESIAN_POINT('Ctrl Pts',(-3.16641033676859,-2.33387537486531,
9.09716228578553));
#256270=CARTESIAN_POINT('Ctrl Pts',(-3.12554492914801,-2.38832153375116,
9.10062231602918));
#256271=CARTESIAN_POINT('Ctrl Pts',(-3.0833401164466,-2.4416188740897,9.10408234627284));
#256272=CARTESIAN_POINT('Ctrl Pts',(-3.01166645053495,-2.5321302523164,
9.10995828875082));
#256273=CARTESIAN_POINT('Ctrl Pts',(-2.93588572830932,-2.61963230908041,
9.11583423122881));
#256274=CARTESIAN_POINT('Ctrl Pts',(-2.85627992874342,-2.70372964045178,
9.1217101737068));
#256275=CARTESIAN_POINT('Ctrl Pts',(-2.7767762850157,-2.78771905213108,
9.12757857575642));
#256276=CARTESIAN_POINT('Ctrl Pts',(-2.69345760701673,-2.86831213044786,
9.13344697780604));
#256277=CARTESIAN_POINT('Ctrl Pts',(-2.60664715498583,-2.94514509140115,
9.13931537985567));
#256278=CARTESIAN_POINT('Ctrl Pts',(-2.51992496996597,-3.02189993024294,
9.14517781503959));
#256279=CARTESIAN_POINT('Ctrl Pts',(-2.42971838034013,-3.0949019846257,
9.15104025022351));
#256280=CARTESIAN_POINT('Ctrl Pts',(-2.33638818789035,-3.16382351522433,
9.15690268540744));
#256281=CARTESIAN_POINT('Ctrl Pts',(-2.24014194188808,-3.23489846337059,
9.16294828934411));
#256282=CARTESIAN_POINT('Ctrl Pts',(-2.14057400087049,-3.30163338394711,
9.16899389328077));
#256283=CARTESIAN_POINT('Ctrl Pts',(-2.03811812430678,-3.36371275696546,
9.17503949721744));
#256284=CARTESIAN_POINT('Ctrl Pts',(-1.93887922189066,-3.42384292272702,
9.18089527747368));
#256285=CARTESIAN_POINT('Ctrl Pts',(-1.8369314058288,-3.47960529568957,
9.18675105772992));
#256286=CARTESIAN_POINT('Ctrl Pts',(-1.73269846431591,-3.53075700548158,
9.19260683798616));
#256287=CARTESIAN_POINT('Ctrl Pts',(-1.62848081731874,-3.58190120957897,
9.19846175900038));
#256288=CARTESIAN_POINT('Ctrl Pts',(-1.52197908206302,-3.62843591398964,
9.2043166800146));
#256289=CARTESIAN_POINT('Ctrl Pts',(-1.4136406556621,-3.67016472336859,
9.21017160102882));
#256290=CARTESIAN_POINT('Ctrl Pts',(-1.30529198568751,-3.71189747827405,
9.2160270756353));
#256291=CARTESIAN_POINT('Ctrl Pts',(-1.19510666453686,-3.74882328646736,
9.22188255024179));
#256292=CARTESIAN_POINT('Ctrl Pts',(-1.08355035827497,-3.7807945753614,
9.22773802484827));
#256293=CARTESIAN_POINT('Ctrl Pts',(-0.971956587366361,-3.81277660137182,
9.23359546593513));
#256294=CARTESIAN_POINT('Ctrl Pts',(-0.85899131235982,-3.83980068577578,
9.23945290702199));
#256295=CARTESIAN_POINT('Ctrl Pts',(-0.745132894489018,-3.86176979758639,
9.24531034810885));
#256296=CARTESIAN_POINT('Ctrl Pts',(-0.631146140851378,-3.88376367192983,
9.25117439142336));
#256297=CARTESIAN_POINT('Ctrl Pts',(-0.516264640558031,-3.9006911234041,
9.25703843473786));
#256298=CARTESIAN_POINT('Ctrl Pts',(-0.400974518798198,-3.91250666903899,
9.26290247805236));
#256299=CARTESIAN_POINT('Ctrl Pts',(-0.285606496267014,-3.92433019835977,
9.26877048366208));
#256300=CARTESIAN_POINT('Ctrl Pts',(-0.169829713505279,-3.93103492006655,
9.2746384892718));
#256301=CARTESIAN_POINT('Ctrl Pts',(-0.0541312339993148,-3.93262746894563,
9.28050649488151));
#256302=CARTESIAN_POINT('Ctrl Pts',(0.0617342771478512,-3.9342223169565,
9.28638297201663));
#256303=CARTESIAN_POINT('Ctrl Pts',(0.177520848519057,-3.93069027606435,
9.29225944915174));
#256304=CARTESIAN_POINT('Ctrl Pts',(0.292745547399449,-3.92208988225382,
9.29813592628685));
#256305=CARTESIAN_POINT('Ctrl Pts',(0.317982423915861,-3.92020619690947,
9.29942301082039));
#256306=CARTESIAN_POINT('Ctrl Pts',(0.343192383916798,-3.91807957188955,
9.30071009535392));
#256307=CARTESIAN_POINT('Ctrl Pts',(0.368370423145139,-3.91571094839135,
9.30199717988746));
#256308=CARTESIAN_POINT('Ctrl Pts',(0.483316028005758,-3.90489744308944,
9.30787312236544));
#256309=CARTESIAN_POINT('Ctrl Pts',(0.597974713552378,-3.88900047395475,
9.31374906484342));
#256310=CARTESIAN_POINT('Ctrl Pts',(0.71186128919564,-3.86804117156795,
9.31962500732141));
#256311=CARTESIAN_POINT('Ctrl Pts',(0.825601717464484,-3.84710876565245,
9.32549340937103));
#256312=CARTESIAN_POINT('Ctrl Pts',(0.938571604011507,-3.82112701995287,
9.33136181142064));
#256313=CARTESIAN_POINT('Ctrl Pts',(1.0502897930848,-3.79016890791715,9.33723021347026));
#256314=CARTESIAN_POINT('Ctrl Pts',(1.16189438949284,-3.75924227342763,
9.34309264865419));
#256315=CARTESIAN_POINT('Ctrl Pts',(1.27224942454752,-3.7233494469283,9.34895508383811));
#256316=CARTESIAN_POINT('Ctrl Pts',(1.38088352504515,-3.68261451828166,
9.35481751902204));
#256317=CARTESIAN_POINT('Ctrl Pts',(1.49291184178044,-3.64060684787513,
9.36086312295871));
#256318=CARTESIAN_POINT('Ctrl Pts',(1.60310947734438,-3.59344960432805,
9.36690872689538));
#256319=CARTESIAN_POINT('Ctrl Pts',(1.71097557030186,-3.5413347198239,9.37295433083205));
#256320=CARTESIAN_POINT('Ctrl Pts',(1.8154548157296,-3.49085617128971,9.37881011108829));
#256321=CARTESIAN_POINT('Ctrl Pts',(1.91774634485568,-3.43572684599689,
9.38466589134452));
#256322=CARTESIAN_POINT('Ctrl Pts',(2.0174156557983,-3.37616988194313,9.39052167160076));
#256323=CARTESIAN_POINT('Ctrl Pts',(2.11707034186477,-3.31662165692063,
9.39637659261497));
#256324=CARTESIAN_POINT('Ctrl Pts',(2.21410322061805,-3.2526472966825,9.40223151362919));
#256325=CARTESIAN_POINT('Ctrl Pts',(2.30810590865885,-3.18451505168591,
9.4080864346434));
#256326=CARTESIAN_POINT('Ctrl Pts',(2.40211748480592,-3.1163763646753,9.41394190924986));
#256327=CARTESIAN_POINT('Ctrl Pts',(2.49309796646332,-3.04407925363265,
9.41979738385633));
#256328=CARTESIAN_POINT('Ctrl Pts',(2.58066996607157,-2.96793388171235,
9.4256528584628));
#256329=CARTESIAN_POINT('Ctrl Pts',(2.66827137552787,-2.89176293741929,
9.43151029954964));
#256330=CARTESIAN_POINT('Ctrl Pts',(2.75246171542831,-2.81174143304379,
9.43736774063648));
#256331=CARTESIAN_POINT('Ctrl Pts',(2.83289907132974,-2.72821770605996,
9.44322518172332));
#256332=CARTESIAN_POINT('Ctrl Pts',(2.91342709237467,-2.64459983512266,
9.44908922503783));
#256333=CARTESIAN_POINT('Ctrl Pts',(2.9901933999685,-2.5574721601767,9.45495326835233));
#256334=CARTESIAN_POINT('Ctrl Pts',(3.06289508260059,-2.46721760551864,
9.46081731166684));
#256335=CARTESIAN_POINT('Ctrl Pts',(3.1356458892776,-2.37690206645641,9.46668531727654));
#256336=CARTESIAN_POINT('Ctrl Pts',(3.20432635828969,-2.28345577227626,
9.47255332288623));
#256337=CARTESIAN_POINT('Ctrl Pts',(3.26867677645263,-2.18729081995953,
9.47842132849593));
#256338=CARTESIAN_POINT('Ctrl Pts',(3.33312009606093,-2.09098703617414,
9.48429780563103));
#256339=CARTESIAN_POINT('Ctrl Pts',(3.393220676276,-1.99195711301693,9.49017428276613));
#256340=CARTESIAN_POINT('Ctrl Pts',(3.44876458147198,-1.89063795095317,
9.49605075990123));
#256341=CARTESIAN_POINT('Ctrl Pts',(3.46092998255685,-1.86844670891249,
9.49733784443485));
#256342=CARTESIAN_POINT('Ctrl Pts',(3.47287697851214,-1.84614572451827,
9.49862492896847));
#256343=CARTESIAN_POINT('Ctrl Pts',(3.48460363313516,-1.82373970728863,
9.49991201350209));
#256344=CARTESIAN_POINT('Ctrl Pts',(3.53813947031149,-1.72144924775539,
9.50578795598008));
#256345=CARTESIAN_POINT('Ctrl Pts',(3.58725571182295,-1.61663072544782,
9.51166389845806));
#256346=CARTESIAN_POINT('Ctrl Pts',(3.63170582167591,-1.50970256170059,
9.51753984093605));
#256347=CARTESIAN_POINT('Ctrl Pts',(3.67609888997846,-1.40291161579743,
9.52340824298567));
#256348=CARTESIAN_POINT('Ctrl Pts',(3.71583757790152,-1.29401679012507,
9.52927664503529));
#256349=CARTESIAN_POINT('Ctrl Pts',(3.75072102583942,-1.18346135818881,
9.53514504708491));
#256350=CARTESIAN_POINT('Ctrl Pts',(3.78556900503359,-1.07301833665102,
9.54100748226885));
#256351=CARTESIAN_POINT('Ctrl Pts',(3.81557144053061,-0.96091845877266,
9.54686991745278));
#256352=CARTESIAN_POINT('Ctrl Pts',(3.84057567033391,-0.847624634162565,
9.55273235263672));
#256353=CARTESIAN_POINT('Ctrl Pts',(3.86636114435439,-0.730791002647243,
9.55877795657339));
#256354=CARTESIAN_POINT('Ctrl Pts',(3.88683077421347,-0.612688002023787,
9.56482356051005));
#256355=CARTESIAN_POINT('Ctrl Pts',(3.90187273426225,-0.49384022276529,
9.57086916444672));
#256356=CARTESIAN_POINT('Ctrl Pts',(3.91644239737474,-0.378724100940102,
9.57672494470296));
#256357=CARTESIAN_POINT('Ctrl Pts',(3.92592008163983,-0.262909710905088,
9.58258072495921));
#256358=CARTESIAN_POINT('Ctrl Pts',(3.9302562751658,-0.146882985807825,
9.58843650521545));
#256359=CARTESIAN_POINT('Ctrl Pts',(3.93459183242479,-0.0308732857752303,
9.59429142622967));
#256360=CARTESIAN_POINT('Ctrl Pts',(3.93378738369546,0.0853482750012756,
9.60014634724389));
#256361=CARTESIAN_POINT('Ctrl Pts',(3.92784547669866,0.201293097690658,
9.60600126825812));
#256362=CARTESIAN_POINT('Ctrl Pts',(3.92190300788495,0.317248883150332,
9.61185674286458));
#256363=CARTESIAN_POINT('Ctrl Pts',(3.91082213629431,0.432927466269691,
9.61771221747104));
#256364=CARTESIAN_POINT('Ctrl Pts',(3.89465744216663,0.547843415745872,
9.62356769207751));
#256365=CARTESIAN_POINT('Ctrl Pts',(3.87848731934938,0.662797958158712,
9.62942513316436));
#256366=CARTESIAN_POINT('Ctrl Pts',(3.85723003645407,0.776988949130067,
9.6352825742512));
#256367=CARTESIAN_POINT('Ctrl Pts',(3.83099150952541,0.889939915918046,
9.64114001533805));
#256368=CARTESIAN_POINT('Ctrl Pts',(3.80472340778318,1.00301819563767,9.64700405865256));
#256369=CARTESIAN_POINT('Ctrl Pts',(3.77346294928052,1.11485325926834,9.65286810196706));
#256370=CARTESIAN_POINT('Ctrl Pts',(3.73736629965948,1.22498250688309,9.65873214528157));
#256371=CARTESIAN_POINT('Ctrl Pts',(3.70124525977146,1.33518616810079,9.66460015089129));
#256372=CARTESIAN_POINT('Ctrl Pts',(3.66028166719039,1.44368133298243,9.67046815650101));
#256373=CARTESIAN_POINT('Ctrl Pts',(3.61467968151267,1.55002574174092,9.67633616211073));
#256374=CARTESIAN_POINT('Ctrl Pts',(3.56901186113656,1.65652367785073,9.68221263924583));
#256375=CARTESIAN_POINT('Ctrl Pts',(3.51869246263513,1.76086429102316,9.68808911638094));
#256376=CARTESIAN_POINT('Ctrl Pts',(3.46397138003121,1.86263020439503,9.69396559351605));
#256377=CARTESIAN_POINT('Ctrl Pts',(3.45198619614305,1.88491929531337,9.69525267804961));
#256378=CARTESIAN_POINT('Ctrl Pts',(3.43979002147693,1.90708498819124,9.69653976258316));
#256379=CARTESIAN_POINT('Ctrl Pts',(3.42738575119693,1.92912309417835,9.69782684711672));
#256380=CARTESIAN_POINT('Ctrl Pts',(3.37075638712148,2.02973392410271,9.70370278959469));
#256381=CARTESIAN_POINT('Ctrl Pts',(3.30959970541971,2.12801509260485,9.70957873207267));
#256382=CARTESIAN_POINT('Ctrl Pts',(3.24413234661948,2.22353194661493,9.71545467455064));
#256383=CARTESIAN_POINT('Ctrl Pts',(3.17874900020217,2.31892622658718,9.72132307660025));
#256384=CARTESIAN_POINT('Ctrl Pts',(3.109066209097,2.41156290938507,9.72719147864986));
#256385=CARTESIAN_POINT('Ctrl Pts',(3.035346333988,2.50103211349746,9.73305988069947));
#256386=CARTESIAN_POINT('Ctrl Pts',(2.96170141567097,2.59041034723707,9.73892231588341));
#256387=CARTESIAN_POINT('Ctrl Pts',(2.88402783933348,2.67662719185028,9.74478475106736));
#256388=CARTESIAN_POINT('Ctrl Pts',(2.80263068445487,2.75930249276009,9.7506471862513));
#256389=CARTESIAN_POINT('Ctrl Pts',(2.71869031760603,2.84456094065125,9.75669279018797));
#256390=CARTESIAN_POINT('Ctrl Pts',(2.63079011730429,2.92605253095204,9.76273839412464));
#256391=CARTESIAN_POINT('Ctrl Pts',(2.53930913402945,3.00339776284038,9.76878399806131));
#256392=CARTESIAN_POINT('Ctrl Pts',(2.45070052828989,3.07831446041935,9.77463977831754));
#256393=CARTESIAN_POINT('Ctrl Pts',(2.35873297926471,3.14934100027928,9.78049555857378));
#256394=CARTESIAN_POINT('Ctrl Pts',(2.26378705585266,3.2161711965867,9.78635133883001));
#256395=CARTESIAN_POINT('Ctrl Pts',(2.16885506423521,3.28299158663247,9.79220625984422));
#256396=CARTESIAN_POINT('Ctrl Pts',(2.07094590469007,3.34561661999916,9.79806118085843));
#256397=CARTESIAN_POINT('Ctrl Pts',(1.97047073583236,3.40378231960099,9.80391610187263));
#256398=CARTESIAN_POINT('Ctrl Pts',(1.86998606688478,3.46195351886387,9.8097715764791));
#256399=CARTESIAN_POINT('Ctrl Pts',(1.76693526355375,3.51566433938033,9.81562705108557));
#256400=CARTESIAN_POINT('Ctrl Pts',(1.66175516730063,3.56469616712977,9.82148252569204));
#256401=CARTESIAN_POINT('Ctrl Pts',(1.55653974776288,3.61374446154229,9.82733996677889));
#256402=CARTESIAN_POINT('Ctrl Pts',(1.44919398724795,3.65811046423124,9.83319740786574));
#256403=CARTESIAN_POINT('Ctrl Pts',(1.34017517386066,3.69762349399821,9.83905484895259));
#256404=CARTESIAN_POINT('Ctrl Pts',(1.23103347967719,3.73718106096391,9.8449188922671));
#256405=CARTESIAN_POINT('Ctrl Pts',(1.12021535705179,3.77187459668523,9.8507829355816));
#256406=CARTESIAN_POINT('Ctrl Pts',(1.00819382771782,3.80158311835368,9.85664697889611));
#256407=CARTESIAN_POINT('Ctrl Pts',(0.896096606178859,3.83131171387334,
9.86251498450582));
#256408=CARTESIAN_POINT('Ctrl Pts',(0.782794761012432,3.85604850027893,
9.86838299011553));
#256409=CARTESIAN_POINT('Ctrl Pts',(0.668770395129177,3.8757238238294,9.87425099572524));
#256410=CARTESIAN_POINT('Ctrl Pts',(0.554581414489975,3.89542755226122,
9.88012747286034));
#256411=CARTESIAN_POINT('Ctrl Pts',(0.439668239311621,3.91005518341447,
9.88600394999545));
#256412=CARTESIAN_POINT('Ctrl Pts',(0.324517013160983,3.91958897183991,
9.89188042713056));
#256413=CARTESIAN_POINT('Ctrl Pts',(0.299296228872053,3.9216770922132,9.89316751166415));
#256414=CARTESIAN_POINT('Ctrl Pts',(0.274064018824445,3.92352105354648,
9.89445459619775));
#256415=CARTESIAN_POINT('Ctrl Pts',(0.248825472904327,3.92512100247036,
9.89574168073135));
#256416=CARTESIAN_POINT('Ctrl Pts',(0.133603636122442,3.93242526850652,
9.90161762320934));
#256417=CARTESIAN_POINT('Ctrl Pts',(0.0178698172299948,3.93466378666596,
9.90749356568732));
#256418=CARTESIAN_POINT('Ctrl Pts',(-0.0978934626551561,3.93178151350878,
9.91336950816531));
#256419=CARTESIAN_POINT('Ctrl Pts',(-0.213508186844968,3.92890293909004,
9.91923791021493));
#256420=CARTESIAN_POINT('Ctrl Pts',(-0.329151887914362,3.92091665215585,
9.92510631226454));
#256421=CARTESIAN_POINT('Ctrl Pts',(-0.44433791846337,3.90781944493545,
9.93097471431415));
#256422=CARTESIAN_POINT('Ctrl Pts',(-0.559406830319615,3.8947355546753,
9.93683714949805));
#256423=CARTESIAN_POINT('Ctrl Pts',(-0.674018589574355,3.87655112736964,
9.94269958468195));
#256424=CARTESIAN_POINT('Ctrl Pts',(-0.787688213129598,3.85331497270814,
9.94856201986584));
#256425=CARTESIAN_POINT('Ctrl Pts',(-0.90490938523454,3.82935281642185,
9.95460762380252));
#256426=CARTESIAN_POINT('Ctrl Pts',(-1.02112813411794,3.80001807744511,
9.96065322773919));
#256427=CARTESIAN_POINT('Ctrl Pts',(-1.13581973689763,3.7654219584628,9.96669883167586));
#256428=CARTESIAN_POINT('Ctrl Pts',(-1.2469101804907,3.73191211021587,9.97255461193209));
#256429=CARTESIAN_POINT('Ctrl Pts',(-1.35656752040787,3.69346647014502,
9.97841039218833));
#256430=CARTESIAN_POINT('Ctrl Pts',(-1.46432769352019,3.650237445152,9.98426617244456));
#256431=CARTESIAN_POINT('Ctrl Pts',(-1.57207205455225,3.60701476332635,
9.99012109345879));
#256432=CARTESIAN_POINT('Ctrl Pts',(-1.67791941934211,3.55901024589167,
9.99597601447301));
#256433=CARTESIAN_POINT('Ctrl Pts',(-1.7814244631935,3.50642494314876,10.0018309354872));
#256434=CARTESIAN_POINT('Ctrl Pts',(-1.88493929361403,3.4538346683805,10.0076864100937));
#256435=CARTESIAN_POINT('Ctrl Pts',(-1.98611099482549,3.39666293426557,
10.0135418847002));
#256436=CARTESIAN_POINT('Ctrl Pts',(-2.0845182984925,3.33515703726975,10.0193973593066));
#256437=CARTESIAN_POINT('Ctrl Pts',(-2.18295865089524,3.2736304843667,10.0252548003935));
#256438=CARTESIAN_POINT('Ctrl Pts',(-2.27863240985213,3.20776709284905,
10.0311122414804));
#256439=CARTESIAN_POINT('Ctrl Pts',(-2.3711473704363,3.13785741353444,10.0369696825672));
#256440=CARTESIAN_POINT('Ctrl Pts',(-2.46376660946253,3.06786893537045,
10.0428337258817));
#256441=CARTESIAN_POINT('Ctrl Pts',(-2.55321961437504,2.99382531555611,
10.0486977691962));
#256442=CARTESIAN_POINT('Ctrl Pts',(-2.63914729130462,2.91605736822846,
10.0545618125107));
#256443=CARTESIAN_POINT('Ctrl Pts',(-2.72513302899599,2.83823687361423,
10.0604298181205));
#256444=CARTESIAN_POINT('Ctrl Pts',(-2.80758840271163,2.75668732999067,
10.0662978237302));
#256445=CARTESIAN_POINT('Ctrl Pts',(-2.88619242046907,2.67177512377574,
10.0721658293399));
#256446=CARTESIAN_POINT('Ctrl Pts',(-2.96490991731583,2.58674033146271,
10.078042306475));
#256447=CARTESIAN_POINT('Ctrl Pts',(-3.03976469645951,2.49833350218984,
10.0839187836101));
#256448=CARTESIAN_POINT('Ctrl Pts',(-3.11047709888341,2.40695268281739,
10.0897952607452));
#256449=CARTESIAN_POINT('Ctrl Pts',(-3.12596475201316,2.38693816790007,
10.0910823452788));
#256450=CARTESIAN_POINT('Ctrl Pts',(-3.14125386036989,2.36678109016191,
10.0923694298124));
#256451=CARTESIAN_POINT('Ctrl Pts',(-3.15634177473762,2.34648579817697,
10.093656514346));
#256452=CARTESIAN_POINT('Ctrl Pts',(-3.22550845453863,2.25344722916221,
10.0995568238018));
#256453=CARTESIAN_POINT('Ctrl Pts',(-3.290673072617,2.1571930683664,10.1054571332576));
#256454=CARTESIAN_POINT('Ctrl Pts',(-3.35152387932836,2.05810026147701,
10.1113574427134));
#256455=CARTESIAN_POINT('Ctrl Pts',(-3.41229617600891,1.95913530464819,
10.1172501395589));
#256456=CARTESIAN_POINT('Ctrl Pts',(-3.4687655170211,1.85733932833455,10.1231428364044));
#256457=CARTESIAN_POINT('Ctrl Pts',(-3.52066119802542,1.75312113920237,
10.12903553325));
#256458=CARTESIAN_POINT('Ctrl Pts',(-3.57250208611494,1.64901298655582,
10.134922008421));
#256459=CARTESIAN_POINT('Ctrl Pts',(-3.61977873792708,1.54248807032957,
10.140808483592));
#256460=CARTESIAN_POINT('Ctrl Pts',(-3.66226482118138,1.43398234979978,
10.1466949587629));
#256461=CARTESIAN_POINT('Ctrl Pts',(-3.7068583267162,1.32009445808609,10.1528734186965));
#256462=CARTESIAN_POINT('Ctrl Pts',(-3.74617356237532,1.20402459394112,
10.15905187863));
#256463=CARTESIAN_POINT('Ctrl Pts',(-3.78000422930493,1.08630429734804,
10.1652303385635));
#256464=CARTESIAN_POINT('Ctrl Pts',(-3.81219018328193,0.97430709504086,
10.1711084262607));
#256465=CARTESIAN_POINT('Ctrl Pts',(-3.83941215511248,0.860816597138284,
10.176986513958));
#256466=CARTESIAN_POINT('Ctrl Pts',(-3.86154281169423,0.746308323317278,
10.1828646016552));
#256467=CARTESIAN_POINT('Ctrl Pts',(-3.88366644224654,0.631836403523942,
10.1887408231802));
#256468=CARTESIAN_POINT('Ctrl Pts',(-3.90070189906821,0.516347751439844,
10.1946170447052));
#256469=CARTESIAN_POINT('Ctrl Pts',(-3.91257278780409,0.400328839998983,
10.2004932662302));
#256470=CARTESIAN_POINT('Ctrl Pts',(-3.92444388921092,0.28430785004045,
10.2063695930297));
#256471=CARTESIAN_POINT('Ctrl Pts',(-3.93115019501299,0.167756987342149,
10.2122459198291));
#256472=CARTESIAN_POINT('Ctrl Pts',(-3.93266713851748,0.051168130948575,
10.2181222466286));
#256473=CARTESIAN_POINT('Ctrl Pts',(-3.9329006934652,0.0332176244332676,
10.2190269904074));
#256474=CARTESIAN_POINT('Ctrl Pts',(-3.93301133525525,0.0152662207290025,
10.2199317341862));
#256475=CARTESIAN_POINT('Ctrl Pts',(-3.9329990839846,-0.00268428320635572,
10.220836477965));
#256476=CARTESIAN_POINT('',(-3.93299987808706,-0.000979268682662659,11.4708364779372));
#256477=CARTESIAN_POINT('Ctrl Pts',(-3.93299908398399,-0.0026842840933697,
10.2208364780097));
#256478=CARTESIAN_POINT('Ctrl Pts',(-3.93290870171559,-0.135111913380411,
10.227511113673));
#256479=CARTESIAN_POINT('Ctrl Pts',(-3.9261258777171,-0.267278679899612,
10.2341857493362));
#256480=CARTESIAN_POINT('Ctrl Pts',(-3.9127534874604,-0.39855883676877,
10.2408603849995));
#256481=CARTESIAN_POINT('Ctrl Pts',(-3.8993178403376,-0.530460002383905,
10.2475665944148));
#256482=CARTESIAN_POINT('Ctrl Pts',(-3.87923025223139,-0.661465984719606,
10.2542728038301));
#256483=CARTESIAN_POINT('Ctrl Pts',(-3.8526446301691,-0.790960399532857,
10.2609790132454));
#256484=CARTESIAN_POINT('Ctrl Pts',(-3.82590297900647,-0.921214807736393,
10.2677245809206));
#256485=CARTESIAN_POINT('Ctrl Pts',(-3.79258689461957,-1.04993969128303,
10.2744701485958));
#256486=CARTESIAN_POINT('Ctrl Pts',(-3.75290144432354,-1.17652868609069,
10.281215716271));
#256487=CARTESIAN_POINT('Ctrl Pts',(-3.73259339779128,-1.24130746969652,
10.2846675935009));
#256488=CARTESIAN_POINT('Ctrl Pts',(-3.71061822050571,-1.30552729526668,
10.2881194707308));
#256489=CARTESIAN_POINT('Ctrl Pts',(-3.68700813042917,-1.36910921629693,
10.2915713479607));
#256490=CARTESIAN_POINT('Ctrl Pts',(-3.64681796086312,-1.47734125519457,
10.2974472904387));
#256491=CARTESIAN_POINT('Ctrl Pts',(-3.60179172910044,-1.58398067685562,
10.3033232329166));
#256492=CARTESIAN_POINT('Ctrl Pts',(-3.55207540094065,-1.68856428543076,
10.3091991753946));
#256493=CARTESIAN_POINT('Ctrl Pts',(-3.50242287231812,-1.7930136848622,
10.3150675774443));
#256494=CARTESIAN_POINT('Ctrl Pts',(-3.44809239237427,-1.89541214835226,
10.3209359794939));
#256495=CARTESIAN_POINT('Ctrl Pts',(-3.38927895977792,-1.99531379306783,
10.3268043815435));
#256496=CARTESIAN_POINT('Ctrl Pts',(-3.33052532742177,-2.09511385992801,
10.3326668167274));
#256497=CARTESIAN_POINT('Ctrl Pts',(-3.2672980174054,-2.19242180422965,
10.3385292519114));
#256498=CARTESIAN_POINT('Ctrl Pts',(-3.19983887219756,-2.28681442009916,
10.3443916870953));
#256499=CARTESIAN_POINT('Ctrl Pts',(-3.1302720009169,-2.38415628439061,
10.350437291032));
#256500=CARTESIAN_POINT('Ctrl Pts',(-3.0562046962359,-2.47839724618601,
10.3564828949686));
#256501=CARTESIAN_POINT('Ctrl Pts',(-2.97795196288579,-2.56910317168164,
10.3625284989053));
#256502=CARTESIAN_POINT('Ctrl Pts',(-2.90215625814747,-2.65696105539444,
10.3683842791615));
#256503=CARTESIAN_POINT('Ctrl Pts',(-2.82243431786652,-2.7415022387079,
10.3742400594178));
#256504=CARTESIAN_POINT('Ctrl Pts',(-2.73911411748493,-2.82236476228619,
10.380095839674));
#256505=CARTESIAN_POINT('Ctrl Pts',(-2.65580614300898,-2.90321542058356,
10.3859507606882));
#256506=CARTESIAN_POINT('Ctrl Pts',(-2.56890125444077,-2.98038820510011,
10.3918056817024));
#256507=CARTESIAN_POINT('Ctrl Pts',(-2.47876424425139,-3.05355805928442,
10.3976606027167));
#256508=CARTESIAN_POINT('Ctrl Pts',(-2.38861871146198,-3.12673483179673,
10.4035160773231));
#256509=CARTESIAN_POINT('Ctrl Pts',(-2.29524077002123,-3.19590766143401,
10.4093715519296));
#256510=CARTESIAN_POINT('Ctrl Pts',(-2.19902767652229,-3.26079227763575,
10.415227026536));
#256511=CARTESIAN_POINT('Ctrl Pts',(-2.10278227118321,-3.32569868444073,
10.4210844676229));
#256512=CARTESIAN_POINT('Ctrl Pts',(-2.00370016247812,-3.38631378346408,
10.4269419087097));
#256513=CARTESIAN_POINT('Ctrl Pts',(-1.90220630147709,-3.44239744750964,
10.4327993497965));
#256514=CARTESIAN_POINT('Ctrl Pts',(-1.80059804144638,-3.49854432638103,
10.438663393111));
#256515=CARTESIAN_POINT('Ctrl Pts',(-1.69657296491896,-3.55014937629392,
10.4445274364255));
#256516=CARTESIAN_POINT('Ctrl Pts',(-1.59057933871619,-3.59701909464617,
10.45039147974));
#256517=CARTESIAN_POINT('Ctrl Pts',(-1.48451409332259,-3.64392048255652,
10.4562594853497));
#256518=CARTESIAN_POINT('Ctrl Pts',(-1.37647803315502,-3.68608001793417,
10.4621274909594));
#256519=CARTESIAN_POINT('Ctrl Pts',(-1.26693642540508,-3.72335347421942,
10.4679954965691));
#256520=CARTESIAN_POINT('Ctrl Pts',(-1.15723667456969,-3.76068074146748,
10.4738719737042));
#256521=CARTESIAN_POINT('Ctrl Pts',(-1.04602743321664,-3.79310773732621,
10.4797484508393));
#256522=CARTESIAN_POINT('Ctrl Pts',(-0.933786081092086,-3.82054087201782,
10.4856249279744));
#256523=CARTESIAN_POINT('Ctrl Pts',(-0.909202626579218,-3.82654936359487,
10.486912012508));
#256524=CARTESIAN_POINT('Ctrl Pts',(-0.884569685472442,-3.8323184908851,
10.4881990970416));
#256525=CARTESIAN_POINT('Ctrl Pts',(-0.859892307913054,-3.83784760234066,
10.4894861815751));
#256526=CARTESIAN_POINT('Ctrl Pts',(-0.747232379785504,-3.86308972126895,
10.4953621240531));
#256527=CARTESIAN_POINT('Ctrl Pts',(-0.633274179249711,-3.88340858761525,
10.5012380665311));
#256528=CARTESIAN_POINT('Ctrl Pts',(-0.518485672507367,-3.89867433974737,
10.5071140090091));
#256529=CARTESIAN_POINT('Ctrl Pts',(-0.403844470561764,-3.91392050177784,
10.5129824110587));
#256530=CARTESIAN_POINT('Ctrl Pts',(-0.288375486892729,-3.92412639157176,
10.5188508131083));
#256531=CARTESIAN_POINT('Ctrl Pts',(-0.17255887346522,-3.92921269915341,
10.5247192151579));
#256532=CARTESIAN_POINT('Ctrl Pts',(-0.0568600198931209,-3.93429383508629,
10.5305816503419));
#256533=CARTESIAN_POINT('Ctrl Pts',(0.0591853503974699,-3.93426572520224,
10.5364440855258));
#256534=CARTESIAN_POINT('Ctrl Pts',(0.175090590502344,-3.92910069673934,
10.5423065207097));
#256535=CARTESIAN_POINT('Ctrl Pts',(0.294617229838071,-3.92377428963569,
10.5483521246464));
#256536=CARTESIAN_POINT('Ctrl Pts',(0.41399439555861,-3.91298462757559,
10.5543977285831));
#256537=CARTESIAN_POINT('Ctrl Pts',(0.532686428291837,-3.89675944460441,
10.5604433325198));
#256538=CARTESIAN_POINT('Ctrl Pts',(0.647651693819147,-3.88104371014814,
10.566299112776));
#256539=CARTESIAN_POINT('Ctrl Pts',(0.761973768459893,-3.86022874706799,
10.5721548930322));
#256540=CARTESIAN_POINT('Ctrl Pts',(0.875170458626114,-3.83439247708788,
10.5780106732885));
#256541=CARTESIAN_POINT('Ctrl Pts',(0.988350538990038,-3.80855999816683,
10.5838655943027));
#256542=CARTESIAN_POINT('Ctrl Pts',(1.10040516093316,-3.77770776926417,
10.5897205153169));
#256543=CARTESIAN_POINT('Ctrl Pts',(1.21086302768579,-3.74196468825984,
10.5955754363312));
#256544=CARTESIAN_POINT('Ctrl Pts',(1.32133133840838,-3.7062182276894,10.6014309109376));
#256545=CARTESIAN_POINT('Ctrl Pts',(1.43020220108577,-3.66558012281681,
10.6072863855441));
#256546=CARTESIAN_POINT('Ctrl Pts',(1.53702084327476,-3.62022871202068,
10.6131418601506));
#256547=CARTESIAN_POINT('Ctrl Pts',(1.64387535903125,-3.57486207057883,
10.6189993012375));
#256548=CARTESIAN_POINT('Ctrl Pts',(1.74867590409265,-3.52477913685943,
10.6248567423243));
#256549=CARTESIAN_POINT('Ctrl Pts',(1.85098964382749,-3.47020551818526,
10.6307141834112));
#256550=CARTESIAN_POINT('Ctrl Pts',(1.95341870671994,-3.41557038673631,
10.6365782267257));
#256551=CARTESIAN_POINT('Ctrl Pts',(2.05335500541286,-3.35643466211395,
10.6424422700402));
#256552=CARTESIAN_POINT('Ctrl Pts',(2.15039210886709,-3.29306889969253,
10.6483063133547));
#256553=CARTESIAN_POINT('Ctrl Pts',(2.2474947796491,-3.22966032144533,10.6541743189644));
#256554=CARTESIAN_POINT('Ctrl Pts',(2.34169401995645,-3.16201625411257,
10.6600423245741));
#256555=CARTESIAN_POINT('Ctrl Pts',(2.43261546567258,-3.09044834873042,
10.6659103301838));
#256556=CARTESIAN_POINT('Ctrl Pts',(2.52366817290881,-3.01877712215735,
10.6717868073189));
#256557=CARTESIAN_POINT('Ctrl Pts',(2.61143333047028,-2.94317102094232,
10.6776632844541));
#256558=CARTESIAN_POINT('Ctrl Pts',(2.69557244450134,-2.86397943366308,
10.6835397615892));
#256559=CARTESIAN_POINT('Ctrl Pts',(2.71400085830244,-2.84663464275632,
10.6848268461227));
#256560=CARTESIAN_POINT('Ctrl Pts',(2.73225547823554,-2.82911798016423,
10.6861139306563));
#256561=CARTESIAN_POINT('Ctrl Pts',(2.75033300732677,-2.8114333264029,10.6874010151899));
#256562=CARTESIAN_POINT('Ctrl Pts',(2.83286256798328,-2.73069736420806,
10.6932769576679));
#256563=CARTESIAN_POINT('Ctrl Pts',(2.91197026617098,-2.64619115209094,
10.6991529001459));
#256564=CARTESIAN_POINT('Ctrl Pts',(2.98729231513605,-2.55823642846573,
10.7050288426239));
#256565=CARTESIAN_POINT('Ctrl Pts',(3.06251770547715,-2.47039457461337,
10.7108972446735));
#256566=CARTESIAN_POINT('Ctrl Pts',(3.13396684176829,-2.37911332079149,
10.7167656467231));
#256567=CARTESIAN_POINT('Ctrl Pts',(3.2013116962519,-2.28475215799018,10.7226340487727));
#256568=CARTESIAN_POINT('Ctrl Pts',(3.2685880759278,-2.19048693960107,10.7284964839566));
#256569=CARTESIAN_POINT('Ctrl Pts',(3.33176823636123,-2.09314837538507,
10.7343589191406));
#256570=CARTESIAN_POINT('Ctrl Pts',(3.39056391869926,-1.99312952745543,
10.7402213543245));
#256571=CARTESIAN_POINT('Ctrl Pts',(3.4511966416975,-1.88998564239505,10.7462669582611));
#256572=CARTESIAN_POINT('Ctrl Pts',(3.50716611065423,-1.7839915715819,10.7523125621978));
#256573=CARTESIAN_POINT('Ctrl Pts',(3.55820384001509,-1.67561165933575,
10.7583581661345));
#256574=CARTESIAN_POINT('Ctrl Pts',(3.60763905460163,-1.57063472784105,
10.7642139463907));
#256575=CARTESIAN_POINT('Ctrl Pts',(3.65244740997755,-1.46341994002382,
10.7700697266469));
#256576=CARTESIAN_POINT('Ctrl Pts',(3.69243163123173,-1.35441413484922,
10.7759255069032));
#256577=CARTESIAN_POINT('Ctrl Pts',(3.73240998544149,-1.24542432453163,
10.7817804279174));
#256578=CARTESIAN_POINT('Ctrl Pts',(3.76756547098869,-1.1346444068434,10.7876353489316));
#256579=CARTESIAN_POINT('Ctrl Pts',(3.79774949982489,-1.02253984596191,
10.7934902699458));
#256580=CARTESIAN_POINT('Ctrl Pts',(3.82793638260982,-0.910424685412919,
10.7993457445523));
#256581=CARTESIAN_POINT('Ctrl Pts',(3.85315076693146,-0.796985031274626,
10.8052012191588));
#256582=CARTESIAN_POINT('Ctrl Pts',(3.87329452870525,-0.682699416948595,
10.8110566937652));
#256583=CARTESIAN_POINT('Ctrl Pts',(3.89344505548359,-0.568375421375381,
10.8169141348521));
#256584=CARTESIAN_POINT('Ctrl Pts',(3.90852150191746,-0.453205306944438,
10.8227715759389));
#256585=CARTESIAN_POINT('Ctrl Pts',(3.91847733511552,-0.33767495344781,
10.8286290170258));
#256586=CARTESIAN_POINT('Ctrl Pts',(3.92844439005294,-0.222014379658201,
10.8344930603403));
#256587=CARTESIAN_POINT('Ctrl Pts',(3.93327927659204,-0.105993167825182,
10.8403571036548));
#256588=CARTESIAN_POINT('Ctrl Pts',(3.93298753885493,0.0099004652317022,
10.8462211469692));
#256589=CARTESIAN_POINT('Ctrl Pts',(3.93269560399257,0.125872406848457,
10.852089152579));
#256590=CARTESIAN_POINT('Ctrl Pts',(3.92727016634025,0.241716186768103,
10.8579571581887));
#256591=CARTESIAN_POINT('Ctrl Pts',(3.91676870068147,0.356948098975225,
10.8638251637984));
#256592=CARTESIAN_POINT('Ctrl Pts',(3.90625207426127,0.47234636924939,10.8697016409335));
#256593=CARTESIAN_POINT('Ctrl Pts',(3.89064485074995,0.587130601602925,
10.8755781180686));
#256594=CARTESIAN_POINT('Ctrl Pts',(3.87005569072855,0.70082661954263,10.8814545952037));
#256595=CARTESIAN_POINT('Ctrl Pts',(3.86554618804285,0.725728679545069,
10.8827416797373));
#256596=CARTESIAN_POINT('Ctrl Pts',(3.86079788622815,0.750578593974643,
10.8840287642709));
#256597=CARTESIAN_POINT('Ctrl Pts',(3.85581224405347,0.775371484262431,
10.8853158488044));
#256598=CARTESIAN_POINT('Ctrl Pts',(3.83305123196016,0.888558764034425,
10.8911917912824));
#256599=CARTESIAN_POINT('Ctrl Pts',(3.80526453482832,1.00092970005197,10.8970677337604));
#256600=CARTESIAN_POINT('Ctrl Pts',(3.77252384830424,1.11200396311155,10.9029436762384));
#256601=CARTESIAN_POINT('Ctrl Pts',(3.73982517696364,1.22293568775675,10.908812078288));
#256602=CARTESIAN_POINT('Ctrl Pts',(3.70218527481469,1.33257365628167,10.9146804803376));
#256603=CARTESIAN_POINT('Ctrl Pts',(3.65972697531004,1.4404469675028,10.9205488823872));
#256604=CARTESIAN_POINT('Ctrl Pts',(3.61731184649622,1.54821059544829,10.9264113175712));
#256605=CARTESIAN_POINT('Ctrl Pts',(3.5700882158666,1.65421275328576,10.9322737527551));
#256606=CARTESIAN_POINT('Ctrl Pts',(3.5182287318234,1.75799760823851,10.938136187939));
#256607=CARTESIAN_POINT('Ctrl Pts',(3.46474892504538,1.86502516726193,10.9441817918757));
#256608=CARTESIAN_POINT('Ctrl Pts',(3.40633893945029,1.96969416021409,10.9502273958124));
#256609=CARTESIAN_POINT('Ctrl Pts',(3.34324197483432,2.07152651387953,10.956272999749));
#256610=CARTESIAN_POINT('Ctrl Pts',(3.2821261684571,2.17016147116209,10.9621287800053));
#256611=CARTESIAN_POINT('Ctrl Pts',(3.21661354518778,2.26613488222249,10.9679845602615));
#256612=CARTESIAN_POINT('Ctrl Pts',(3.14697140833103,2.35903792999329,10.9738403405178));
#256613=CARTESIAN_POINT('Ctrl Pts',(3.07733949034308,2.45192734572894,10.979695261532));
#256614=CARTESIAN_POINT('Ctrl Pts',(3.00357951117047,2.54174696385068,10.9855501825462));
#256615=CARTESIAN_POINT('Ctrl Pts',(2.92600091158385,2.62811865512394,10.9914051035604));
#256616=CARTESIAN_POINT('Ctrl Pts',(2.84841497681519,2.71449851298027,10.9972605781669));
#256617=CARTESIAN_POINT('Ctrl Pts',(2.76700997971318,2.79742948882504,11.0031160527734));
#256618=CARTESIAN_POINT('Ctrl Pts',(2.68213380679111,2.87656865770108,11.0089715273798));
#256619=CARTESIAN_POINT('Ctrl Pts',(2.59722912937711,2.95573440437538,11.0148289684667));
#256620=CARTESIAN_POINT('Ctrl Pts',(2.50885125979425,3.03110553056513,11.0206864095535));
#256621=CARTESIAN_POINT('Ctrl Pts',(2.41738234469678,3.10237837788176,11.0265438506404));
#256622=CARTESIAN_POINT('Ctrl Pts',(2.32581033020973,3.1737315605456,11.0324078939549));
#256623=CARTESIAN_POINT('Ctrl Pts',(2.23114064211733,3.24097699072152,11.0382719372694));
#256624=CARTESIAN_POINT('Ctrl Pts',(2.13378575063507,3.30385341236362,11.0441359805839));
#256625=CARTESIAN_POINT('Ctrl Pts',(2.03636507709774,3.36677231918718,11.0500039861936));
#256626=CARTESIAN_POINT('Ctrl Pts',(1.93625594268604,3.42531613121839,11.0558719918033));
#256627=CARTESIAN_POINT('Ctrl Pts',(1.83389531842599,3.47926960166286,11.0617399974131));
#256628=CARTESIAN_POINT('Ctrl Pts',(1.73138691812661,3.53330096368164,11.0676164745482));
#256629=CARTESIAN_POINT('Ctrl Pts',(1.62662091305287,3.58272858352748,11.0734929516833));
#256630=CARTESIAN_POINT('Ctrl Pts',(1.52005416032774,3.62738533239444,11.0793694288184));
#256631=CARTESIAN_POINT('Ctrl Pts',(1.49671357445081,3.63716619420415,11.080656513352));
#256632=CARTESIAN_POINT('Ctrl Pts',(1.47328666009692,3.64671838249366,11.0819435978855));
#256633=CARTESIAN_POINT('Ctrl Pts',(1.44977830326759,3.65604046358551,11.0832306824191));
#256634=CARTESIAN_POINT('Ctrl Pts',(1.34245531951811,3.69859867234487,11.0891066248971));
#256635=CARTESIAN_POINT('Ctrl Pts',(1.23307975206688,3.73649739321613,11.0949825673751));
#256636=CARTESIAN_POINT('Ctrl Pts',(1.12209348527102,3.76953514512232,11.1008585098531));
#256637=CARTESIAN_POINT('Ctrl Pts',(1.0112496439664,3.80253050062955,11.1067269119027));
#256638=CARTESIAN_POINT('Ctrl Pts',(0.898799605987272,3.83067717600267,
11.1125953139523));
#256639=CARTESIAN_POINT('Ctrl Pts',(0.785205200775825,3.85382171262172,
11.1184637160019));
#256640=CARTESIAN_POINT('Ctrl Pts',(0.671726295926075,3.87694271637094,
11.1243261511859));
#256641=CARTESIAN_POINT('Ctrl Pts',(0.557105740426479,3.89507161631037,
11.1301885863698));
#256642=CARTESIAN_POINT('Ctrl Pts',(0.441819857916594,3.9081049388611,11.1360510215537));
#256643=CARTESIAN_POINT('Ctrl Pts',(0.32293192768335,3.92154548082847,11.1420966254904));
#256644=CARTESIAN_POINT('Ctrl Pts',(0.203336839629667,3.92956666629365,
11.1481422294271));
#256645=CARTESIAN_POINT('Ctrl Pts',(0.0835679952731944,3.93211207751839,
11.1541878333637));
#256646=CARTESIAN_POINT('Ctrl Pts',(-0.032440271467795,3.93457756631819,
11.16004361362));
#256647=CARTESIAN_POINT('Ctrl Pts',(-0.148611103168792,3.93190599372951,
11.1658993938762));
#256648=CARTESIAN_POINT('Ctrl Pts',(-0.264456053159735,3.92409887693304,
11.1717551741325));
#256649=CARTESIAN_POINT('Ctrl Pts',(-0.380284004758634,3.916292905706,11.1776100951467));
#256650=CARTESIAN_POINT('Ctrl Pts',(-0.495785758013729,3.90335291644478,
11.1834650161609));
#256651=CARTESIAN_POINT('Ctrl Pts',(-0.610475653048774,3.8853324796,11.1893199371751));
#256652=CARTESIAN_POINT('Ctrl Pts',(-0.725176392198759,3.86731033889379,
11.1951754117816));
#256653=CARTESIAN_POINT('Ctrl Pts',(-0.839064712756267,3.84420685975501,
11.2010308863881));
#256654=CARTESIAN_POINT('Ctrl Pts',(-0.951663540110443,3.81612702964989,
11.2068863609945));
#256655=CARTESIAN_POINT('Ctrl Pts',(-1.06430018222756,3.78803776932116,
11.2127438020814));
#256656=CARTESIAN_POINT('Ctrl Pts',(-1.1756460697404,3.75496893461153,11.2186012431682));
#256657=CARTESIAN_POINT('Ctrl Pts',(-1.28523839988161,3.7170756321966,11.2244586842551));
#256658=CARTESIAN_POINT('Ctrl Pts',(-1.39495425725982,3.67913961826215,
11.2303227275696));
#256659=CARTESIAN_POINT('Ctrl Pts',(-1.50291222204019,3.63636841809741,
11.2361867708841));
#256660=CARTESIAN_POINT('Ctrl Pts',(-1.60866853720992,3.58896566400278,
11.2420508141986));
#256661=CARTESIAN_POINT('Ctrl Pts',(-1.71449631122097,3.54153088018134,
11.2479188198083));
#256662=CARTESIAN_POINT('Ctrl Pts',(-1.8181191054644,3.48945849562897,11.253786825418));
#256663=CARTESIAN_POINT('Ctrl Pts',(-1.91911840501449,3.43299774942173,
11.2596548310277));
#256664=CARTESIAN_POINT('Ctrl Pts',(-2.02026351528604,3.37645549193494,
11.2655313081628));
#256665=CARTESIAN_POINT('Ctrl Pts',(-2.1187772227289,3.3155124458296,11.2714077852979));
#256666=CARTESIAN_POINT('Ctrl Pts',(-2.21427053641827,3.25046073527276,
11.277284262433));
#256667=CARTESIAN_POINT('Ctrl Pts',(-2.23518578279538,3.23621290470764,
11.2785713469666));
#256668=CARTESIAN_POINT('Ctrl Pts',(-2.25595626709445,3.2217681271305,11.2798584315002));
#256669=CARTESIAN_POINT('Ctrl Pts',(-2.27657812579469,3.20712971941472,
11.2811455160338));
#256670=CARTESIAN_POINT('Ctrl Pts',(-2.37011177574112,3.14073494273801,
11.2869832882718));
#256671=CARTESIAN_POINT('Ctrl Pts',(-2.46090272053026,3.07012825322945,
11.2928210605097));
#256672=CARTESIAN_POINT('Ctrl Pts',(-2.54854429308361,2.99556521981929,
11.2986588327477));
#256673=CARTESIAN_POINT('Ctrl Pts',(-2.636073061497,2.92109815706108,11.3044890911443));
#256674=CARTESIAN_POINT('Ctrl Pts',(-2.72046020090262,2.84268514339137,
11.3103193495408));
#256675=CARTESIAN_POINT('Ctrl Pts',(-2.80132819023628,2.76062481525243,
11.3161496079374));
#256676=CARTESIAN_POINT('Ctrl Pts',(-2.88211438511873,2.67864748756351,
11.3219739692814));
#256677=CARTESIAN_POINT('Ctrl Pts',(-2.95938821612785,2.59303047806507,
11.3277983306253));
#256678=CARTESIAN_POINT('Ctrl Pts',(-3.03280600594098,2.50411196441539,
11.3336226919693));
#256679=CARTESIAN_POINT('Ctrl Pts',(-3.1061713577615,2.4152569600102,11.3394428933159));
#256680=CARTESIAN_POINT('Ctrl Pts',(-3.17568588015654,2.32310546307272,
11.3452630946624));
#256681=CARTESIAN_POINT('Ctrl Pts',(-3.24104398157485,2.22803117336751,
11.3510832960089));
#256682=CARTESIAN_POINT('Ctrl Pts',(-3.30637760077524,2.13299249714294,
11.3569013171906));
#256683=CARTESIAN_POINT('Ctrl Pts',(-3.36755765655974,2.03503354879621,
11.3627193383723));
#256684=CARTESIAN_POINT('Ctrl Pts',(-3.424320368447,1.9345591265813,11.3685373595539));
#256685=CARTESIAN_POINT('Ctrl Pts',(-3.48107597672475,1.83409727830865,
11.3743546526352));
#256686=CARTESIAN_POINT('Ctrl Pts',(-3.53341513437636,1.7311209466672,11.3801719457165));
#256687=CARTESIAN_POINT('Ctrl Pts',(-3.58111914101488,1.62606109905405,
11.3859892387978));
#256688=CARTESIAN_POINT('Ctrl Pts',(-3.62882907721868,1.52098819259598,
11.3918072549634));
#256689=CARTESIAN_POINT('Ctrl Pts',(-3.67190254461371,1.41383163693878,
11.397625271129));
#256690=CARTESIAN_POINT('Ctrl Pts',(-3.71016859552723,1.30504329152848,
11.4034432872947));
#256691=CARTESIAN_POINT('Ctrl Pts',(-3.74847237718387,1.19614767962433,
11.4092670400876));
#256692=CARTESIAN_POINT('Ctrl Pts',(-3.78195913607339,1.08561746027754,
11.4150907928806));
#256693=CARTESIAN_POINT('Ctrl Pts',(-3.81050750947591,0.973920695040244,
11.4209145456735));
#256694=CARTESIAN_POINT('Ctrl Pts',(-3.83907020804644,0.862167881953742,
11.4267412207428));
#256695=CARTESIAN_POINT('Ctrl Pts',(-3.86268950016671,0.749247767014327,
11.4325678958121));
#256696=CARTESIAN_POINT('Ctrl Pts',(-3.8812953413101,0.63563784777536,11.4383945708815));
#256697=CARTESIAN_POINT('Ctrl Pts',(-3.89993071618738,0.521847591345708,
11.4442304948458));
#256698=CARTESIAN_POINT('Ctrl Pts',(-3.91353669293783,0.407365759236058,
11.4500664188101));
#256699=CARTESIAN_POINT('Ctrl Pts',(-3.92209517684827,0.292674603858209,
11.4559023427744));
#256700=CARTESIAN_POINT('Ctrl Pts',(-3.92939556642889,0.194843010731158,
11.4608803878287));
#256701=CARTESIAN_POINT('Ctrl Pts',(-3.9330242386882,0.0968592949186528,
11.4658584328829));
#256702=CARTESIAN_POINT('Ctrl Pts',(-3.93299987808706,-0.000979268682664797,
11.4708364779372));
#256703=CARTESIAN_POINT('',(-3.93299846730095,0.00347220511500596,12.7208364779205));
#256704=CARTESIAN_POINT('Ctrl Pts',(-3.93299987808693,-0.000979269229120141,
11.470836477965));
#256705=CARTESIAN_POINT('Ctrl Pts',(-3.932986463278,-0.0548566303192047,
11.4735777685261));
#256706=CARTESIAN_POINT('Ctrl Pts',(-3.93186601489811,-0.108718747047242,
11.4763190590872));
#256707=CARTESIAN_POINT('Ctrl Pts',(-3.92964011457576,-0.1625348267819,
11.4790603496483));
#256708=CARTESIAN_POINT('Ctrl Pts',(-3.9248689084726,-0.277889321994402,
11.4849362921262));
#256709=CARTESIAN_POINT('Ctrl Pts',(-3.91500618700124,-0.393223855087732,
11.4908122346041));
#256710=CARTESIAN_POINT('Ctrl Pts',(-3.90004760964988,-0.508052794957657,
11.496688177082));
#256711=CARTESIAN_POINT('Ctrl Pts',(-3.8851082282116,-0.622734378144019,
11.5025565791315));
#256712=CARTESIAN_POINT('Ctrl Pts',(-3.86508604871629,-0.736911252790357,
11.5084249811811));
#256713=CARTESIAN_POINT('Ctrl Pts',(-3.84002871377076,-0.850099098585613,
11.5142933832306));
#256714=CARTESIAN_POINT('Ctrl Pts',(-3.81499685658747,-0.96317185740017,
11.5201558184145));
#256715=CARTESIAN_POINT('Ctrl Pts',(-3.78494011629482,-1.07525718703231,
11.5260182535983));
#256716=CARTESIAN_POINT('Ctrl Pts',(-3.74995769455867,-1.18587785586047,
11.5318806887822));
#256717=CARTESIAN_POINT('Ctrl Pts',(-3.7138822651629,-1.29995481022693,
11.5379262927189));
#256718=CARTESIAN_POINT('Ctrl Pts',(-3.6725683515392,-1.41247363107052,
11.5439718966556));
#256719=CARTESIAN_POINT('Ctrl Pts',(-3.62618135805924,-1.52292408164808,
11.5500175005923));
#256720=CARTESIAN_POINT('Ctrl Pts',(-3.58125085261957,-1.62990653940605,
11.5558732808485));
#256721=CARTESIAN_POINT('Ctrl Pts',(-3.53156125119061,-1.73494816424003,
11.5617290611047));
#256722=CARTESIAN_POINT('Ctrl Pts',(-3.47731260073327,-1.83760335131975,
11.5675848413608));
#256723=CARTESIAN_POINT('Ctrl Pts',(-3.42307191039701,-1.94024347539402,
11.573439762375));
#256724=CARTESIAN_POINT('Ctrl Pts',(-3.364273694054,-2.04049749317739,11.5792946833892));
#256725=CARTESIAN_POINT('Ctrl Pts',(-3.30116441863936,-2.13794351681926,
11.5851496044034));
#256726=CARTESIAN_POINT('Ctrl Pts',(-3.23804917614063,-2.23539875414029,
11.5910050790098));
#256727=CARTESIAN_POINT('Ctrl Pts',(-3.17062228864709,-2.330045123064,11.5968605536162));
#256728=CARTESIAN_POINT('Ctrl Pts',(-3.09917370346276,-2.4214894911531,
11.6027160282227));
#256729=CARTESIAN_POINT('Ctrl Pts',(-3.02770112325666,-2.51296456957184,
11.6085734693095));
#256730=CARTESIAN_POINT('Ctrl Pts',(-2.95220441363665,-2.60123518377285,
11.6144309103963));
#256731=CARTESIAN_POINT('Ctrl Pts',(-2.87301350381704,-2.68594162387885,
11.6202883514831));
#256732=CARTESIAN_POINT('Ctrl Pts',(-2.79373333378863,-2.77074354103578,
11.6261523947976));
#256733=CARTESIAN_POINT('Ctrl Pts',(-2.71075093484285,-2.85197296420257,
11.632016438112));
#256734=CARTESIAN_POINT('Ctrl Pts',(-2.6244328206362,-2.92930731914006,
11.6378804814265));
#256735=CARTESIAN_POINT('Ctrl Pts',(-2.53805638185176,-3.00669392838873,
11.6437484870362));
#256736=CARTESIAN_POINT('Ctrl Pts',(-2.4483400581743,-3.08017996777959,
11.6496164926458));
#256737=CARTESIAN_POINT('Ctrl Pts',(-2.35568176100807,-3.14948447223572,
11.6554844982555));
#256738=CARTESIAN_POINT('Ctrl Pts',(-2.26288969486313,-3.21888903025493,
11.6613609753906));
#256739=CARTESIAN_POINT('Ctrl Pts',(-2.16714751893534,-3.28409977454673,
11.6672374525256));
#256740=CARTESIAN_POINT('Ctrl Pts',(-2.06888031443449,-3.3448801539884,
11.6731139296607));
#256741=CARTESIAN_POINT('Ctrl Pts',(-2.04735752174451,-3.35819246416336,
11.6744010141948));
#256742=CARTESIAN_POINT('Ctrl Pts',(-2.02571368513469,-3.37129242426332,
11.675688098729));
#256743=CARTESIAN_POINT('Ctrl Pts',(-2.00395340611494,-3.38417785379556,
11.6769751832631));
#256744=CARTESIAN_POINT('Ctrl Pts',(-1.90461094302503,-3.44300385995762,
11.6828511257411));
#256745=CARTESIAN_POINT('Ctrl Pts',(-1.80251214411554,-3.49754891528115,
11.6887270682191));
#256746=CARTESIAN_POINT('Ctrl Pts',(-1.69806192741774,-3.5475448821198,
11.6946030106971));
#256747=CARTESIAN_POINT('Ctrl Pts',(-1.59374574868561,-3.59747669056893,
11.7004714127467));
#256748=CARTESIAN_POINT('Ctrl Pts',(-1.48708452211269,-3.64287084351938,
11.7063398147964));
#256749=CARTESIAN_POINT('Ctrl Pts',(-1.37851037885044,-3.68350351369476,
11.712208216846));
#256750=CARTESIAN_POINT('Ctrl Pts',(-1.27004663145496,-3.72409486944012,
11.7180706520299));
#256751=CARTESIAN_POINT('Ctrl Pts',(-1.15967422058035,-3.75993422872318,
11.7239330872139));
#256752=CARTESIAN_POINT('Ctrl Pts',(-1.04784741381294,-3.79084486590595,
11.7297955223978));
#256753=CARTESIAN_POINT('Ctrl Pts',(-0.932526636353501,-3.82272128994709,
11.7358411263345));
#256754=CARTESIAN_POINT('Ctrl Pts',(-0.815659488326674,-3.84935574535524,
11.7418867302711));
#256755=CARTESIAN_POINT('Ctrl Pts',(-0.697763974666621,-3.87060905228847,
11.7479323342078));
#256756=CARTESIAN_POINT('Ctrl Pts',(-0.583570218604554,-3.89119503450356,
11.753788114464));
#256757=CARTESIAN_POINT('Ctrl Pts',(-0.468412146030773,-3.90673265849635,
11.7596438947203));
#256758=CARTESIAN_POINT('Ctrl Pts',(-0.35277242529478,-3.91714699953316,
11.7654996749765));
#256759=CARTESIAN_POINT('Ctrl Pts',(-0.237149672836769,-3.92755981243212,
11.7713545959907));
#256760=CARTESIAN_POINT('Ctrl Pts',(-0.121045823738458,-3.93285080021131,
11.777209517005));
#256761=CARTESIAN_POINT('Ctrl Pts',(-0.00494893822420919,-3.9329968863464,
11.7830644380192));
#256762=CARTESIAN_POINT('Ctrl Pts',(0.111158924438277,-3.93314298629416,
11.7889199126257));
#256763=CARTESIAN_POINT('Ctrl Pts',(0.227259409429624,-3.92814321704365,
11.7947753872321));
#256764=CARTESIAN_POINT('Ctrl Pts',(0.342864891257786,-3.91802662910078,
11.8006308618386));
#256765=CARTESIAN_POINT('Ctrl Pts',(0.458509197592445,-3.90790664364138,
11.8064883029255));
#256766=CARTESIAN_POINT('Ctrl Pts',(0.573657759239503,-3.89266645841358,
11.8123457440123));
#256767=CARTESIAN_POINT('Ctrl Pts',(0.687829205038584,-3.87238685886315,
11.8182031850992));
#256768=CARTESIAN_POINT('Ctrl Pts',(0.802129339434854,-3.85208440111731,
11.8240672284137));
#256769=CARTESIAN_POINT('Ctrl Pts',(0.915449753188868,-3.82673126423591,
11.8299312717282));
#256770=CARTESIAN_POINT('Ctrl Pts',(1.02732029392263,-3.7964591415811,11.8357953150427));
#256771=CARTESIAN_POINT('Ctrl Pts',(1.13926642483947,-3.76616656425362,
11.8416633206524));
#256772=CARTESIAN_POINT('Ctrl Pts',(1.24976033968641,-3.73094850778175,
11.8475313262621));
#256773=CARTESIAN_POINT('Ctrl Pts',(1.35834968157471,-3.69098566003254,
11.8533993318718));
#256774=CARTESIAN_POINT('Ctrl Pts',(1.46709579178068,-3.65096511869848,
11.8592758090069));
#256775=CARTESIAN_POINT('Ctrl Pts',(1.57393146263382,-3.60618627485286,
11.865152286142));
#256776=CARTESIAN_POINT('Ctrl Pts',(1.6784267877521,-3.556876792659,11.8710287632771));
#256777=CARTESIAN_POINT('Ctrl Pts',(1.70131368302734,-3.54607687454046,
11.8723158478106));
#256778=CARTESIAN_POINT('Ctrl Pts',(1.72408841378939,-3.53505978527574,
11.8736029323441));
#256779=CARTESIAN_POINT('Ctrl Pts',(1.74674664513664,-3.52382819639435,
11.8748900168775));
#256780=CARTESIAN_POINT('Ctrl Pts',(1.85018854082262,-3.47255248878723,
11.8807659593555));
#256781=CARTESIAN_POINT('Ctrl Pts',(1.95154137990094,-3.41663353127061,
11.8866419018335));
#256782=CARTESIAN_POINT('Ctrl Pts',(2.05035974727023,-3.35626487434677,
11.8925178443115));
#256783=CARTESIAN_POINT('Ctrl Pts',(2.14905130386437,-3.29597368678803,
11.8983862463611));
#256784=CARTESIAN_POINT('Ctrl Pts',(2.24521450782985,-3.23124436901653,
11.9042546484107));
#256785=CARTESIAN_POINT('Ctrl Pts',(2.33842628410832,-3.16231742774051,
11.9101230504604));
#256786=CARTESIAN_POINT('Ctrl Pts',(2.43154328464627,-3.09346056990418,
11.9159854856443));
#256787=CARTESIAN_POINT('Ctrl Pts',(2.52171449684375,-3.02041482227373,
11.9218479208282));
#256788=CARTESIAN_POINT('Ctrl Pts',(2.60854429162626,-2.94346491037757,
11.9277103560122));
#256789=CARTESIAN_POINT('Ctrl Pts',(2.69808703840084,-2.86411073831598,
11.9337559599488));
#256790=CARTESIAN_POINT('Ctrl Pts',(2.78407575239366,-2.78060465728777,
11.9398015638855));
#256791=CARTESIAN_POINT('Ctrl Pts',(2.86611157855576,-2.69330529633545,
11.9458471678222));
#256792=CARTESIAN_POINT('Ctrl Pts',(2.9455715921751,-2.60874701570664,11.9517029480784));
#256793=CARTESIAN_POINT('Ctrl Pts',(3.02132293353721,-2.5206304240791,11.9575587283347));
#256794=CARTESIAN_POINT('Ctrl Pts',(3.09303988209523,-2.42931951125584,
11.9634145085909));
#256795=CARTESIAN_POINT('Ctrl Pts',(3.16474630733907,-2.33802199684736,
11.9692694296052));
#256796=CARTESIAN_POINT('Ctrl Pts',(3.2324192620312,-2.24353141779136,11.9751243506194));
#256797=CARTESIAN_POINT('Ctrl Pts',(3.2957735722646,-2.14624452482988,11.9809792716336));
#256798=CARTESIAN_POINT('Ctrl Pts',(3.35913387275045,-2.04894843323539,
11.9868347462401));
#256799=CARTESIAN_POINT('Ctrl Pts',(3.41817449179202,-1.94885584804075,
11.9926902208466));
#256800=CARTESIAN_POINT('Ctrl Pts',(3.47265420940231,-1.84639154621126,
11.9985456954531));
#256801=CARTESIAN_POINT('Ctrl Pts',(3.52715222327429,-1.74389283315933,
12.0044031365399));
#256802=CARTESIAN_POINT('Ctrl Pts',(3.57708609625411,-1.63902118387141,
12.0102605776268));
#256803=CARTESIAN_POINT('Ctrl Pts',(3.62226140306803,-1.5322243072878,12.0161180187137));
#256804=CARTESIAN_POINT('Ctrl Pts',(3.66748762932876,-1.425307054369,12.0219820620282));
#256805=CARTESIAN_POINT('Ctrl Pts',(3.70794442332027,-1.31646062336182,
12.0278461053427));
#256806=CARTESIAN_POINT('Ctrl Pts',(3.74348616475801,-1.20615104123213,
12.0337101486572));
#256807=CARTESIAN_POINT('Ctrl Pts',(3.77905192151493,-1.09576692364876,
12.0395781542669));
#256808=CARTESIAN_POINT('Ctrl Pts',(3.80969590381713,-0.983918083384415,
12.0454461598766));
#256809=CARTESIAN_POINT('Ctrl Pts',(3.83532327363904,-0.871082307639612,
12.0513141654864));
#256810=CARTESIAN_POINT('Ctrl Pts',(3.86098764119555,-0.758083633083303,
12.0571906426215));
#256811=CARTESIAN_POINT('Ctrl Pts',(3.88162086975249,-0.64409558413927,
12.0630671197566));
#256812=CARTESIAN_POINT('Ctrl Pts',(3.89717974628138,-0.529602705029176,
12.0689435968917));
#256813=CARTESIAN_POINT('Ctrl Pts',(3.90058750043051,-0.50452611398427,
12.0702306814252));
#256814=CARTESIAN_POINT('Ctrl Pts',(3.90375203058196,-0.479425309890811,
12.0715177659588));
#256815=CARTESIAN_POINT('Ctrl Pts',(3.90667321626538,-0.454305383321326,
12.0728048504923));
#256816=CARTESIAN_POINT('Ctrl Pts',(3.92000934034745,-0.339625080879565,
12.0786807929703));
#256817=CARTESIAN_POINT('Ctrl Pts',(3.92831353277412,-0.224167867215506,
12.0845567354483));
#256818=CARTESIAN_POINT('Ctrl Pts',(3.93150552379089,-0.108412713284382,
12.0904326779263));
#256819=CARTESIAN_POINT('Ctrl Pts',(3.93469341861719,0.00719389537941079,
12.0963010799759));
#256820=CARTESIAN_POINT('Ctrl Pts',(3.93278214745572,0.123097275047859,
12.1021694820255));
#256821=CARTESIAN_POINT('Ctrl Pts',(3.92574298853633,0.238811616044628,
12.1080378840751));
#256822=CARTESIAN_POINT('Ctrl Pts',(3.91871098688318,0.354408301174369,
12.113900319259));
#256823=CARTESIAN_POINT('Ctrl Pts',(3.90656149358598,0.469815920371005,
12.1197627544429));
#256824=CARTESIAN_POINT('Ctrl Pts',(3.88931782004195,0.584547598322071,
12.1256251896269));
#256825=CARTESIAN_POINT('Ctrl Pts',(3.87153537684389,0.702864008162148,
12.1316707935635));
#256826=CARTESIAN_POINT('Ctrl Pts',(3.84833517818206,0.820461096922471,
12.1377163975002));
#256827=CARTESIAN_POINT('Ctrl Pts',(3.81980075876842,0.936809032467246,
12.1437620014369));
#256828=CARTESIAN_POINT('Ctrl Pts',(3.79216228102892,1.04950380224599,12.1496177816931));
#256829=CARTESIAN_POINT('Ctrl Pts',(3.75951965410202,1.16102625893289,12.1554735619493));
#256830=CARTESIAN_POINT('Ctrl Pts',(3.72200074105462,1.27090498605871,12.1613293422055));
#256831=CARTESIAN_POINT('Ctrl Pts',(3.68448733330713,1.38076759024019,12.1671842632198));
#256832=CARTESIAN_POINT('Ctrl Pts',(3.64209919556459,1.48898655394699,12.173039184234));
#256833=CARTESIAN_POINT('Ctrl Pts',(3.59501374996098,1.59510662264047,12.1788941052482));
#256834=CARTESIAN_POINT('Ctrl Pts',(3.54792385235234,1.70123672515805,12.1847495798546));
#256835=CARTESIAN_POINT('Ctrl Pts',(3.49613593138806,1.80526716084839,12.1906050544611));
#256836=CARTESIAN_POINT('Ctrl Pts',(3.43987485319026,1.90676427341957,12.1964605290676));
#256837=CARTESIAN_POINT('Ctrl Pts',(3.38359488048542,2.00829547239596,12.2023179701544));
#256838=CARTESIAN_POINT('Ctrl Pts',(3.32283896334772,2.10729129568078,12.2081754112412));
#256839=CARTESIAN_POINT('Ctrl Pts',(3.25787668674578,2.20334484227012,12.2140328523281));
#256840=CARTESIAN_POINT('Ctrl Pts',(3.19284118777035,2.29950665582656,12.2198968956426));
#256841=CARTESIAN_POINT('Ctrl Pts',(3.12359009774898,2.39271923144746,12.2257609389571));
#256842=CARTESIAN_POINT('Ctrl Pts',(3.05043494582662,2.48260662233866,12.2316249822715));
#256843=CARTESIAN_POINT('Ctrl Pts',(2.97723036345287,2.57255474954424,12.2374929878812));
#256844=CARTESIAN_POINT('Ctrl Pts',(2.90011674010459,2.6591729105376,12.2433609934909));
#256845=CARTESIAN_POINT('Ctrl Pts',(2.81944312622333,2.74212134268198,12.2492289991006));
#256846=CARTESIAN_POINT('Ctrl Pts',(2.73865304541716,2.82518952586208,12.2551054762357));
#256847=CARTESIAN_POINT('Ctrl Pts',(2.65429301682881,2.90457712564489,12.2609819533708));
#256848=CARTESIAN_POINT('Ctrl Pts',(2.56674587516822,2.97998399531053,12.2668584305059));
#256849=CARTESIAN_POINT('Ctrl Pts',(2.54757102441917,2.99649984544414,12.2681455150396));
#256850=CARTESIAN_POINT('Ctrl Pts',(2.52824339585754,3.01282489954851,12.2694325995732));
#256851=CARTESIAN_POINT('Ctrl Pts',(2.50876719315735,3.02895628402547,12.2707196841068));
#256852=CARTESIAN_POINT('Ctrl Pts',(2.41985225108104,3.10260108729945,12.2765956265848));
#256853=CARTESIAN_POINT('Ctrl Pts',(2.32754511504253,3.17244892502778,12.2824715690628));
#256854=CARTESIAN_POINT('Ctrl Pts',(2.23220376281934,3.23817160775262,12.2883475115408));
#256855=CARTESIAN_POINT('Ctrl Pts',(2.1369847594175,3.30380995044472,12.2942159135904));
#256856=CARTESIAN_POINT('Ctrl Pts',(2.03873962015154,3.3653334336578,12.30008431564));
#256857=CARTESIAN_POINT('Ctrl Pts',(1.93786013364157,3.42245337476534,12.3059527176896));
#256858=CARTESIAN_POINT('Ctrl Pts',(1.83708321923592,3.47951523753842,12.3118151528736));
#256859=CARTESIAN_POINT('Ctrl Pts',(1.73367764265923,3.53218226222067,12.3176775880575));
#256860=CARTESIAN_POINT('Ctrl Pts',(1.62806442594008,3.5802088242152,12.3235400232414));
#256861=CARTESIAN_POINT('Ctrl Pts',(1.51915137893325,3.6297359512792,12.3295856271781));
#256862=CARTESIAN_POINT('Ctrl Pts',(1.40789083876213,3.67432761758209,12.3356312311148));
#256863=CARTESIAN_POINT('Ctrl Pts',(1.29477265429651,3.71376530945158,12.3416768350514));
#256864=CARTESIAN_POINT('Ctrl Pts',(1.185206225838,3.75196471183061,12.3475326153077));
#256865=CARTESIAN_POINT('Ctrl Pts',(1.07389748232933,3.78532881015082,12.3533883955639));
#256866=CARTESIAN_POINT('Ctrl Pts',(0.961311424728222,3.81370808330777,
12.3592441758202));
#256867=CARTESIAN_POINT('Ctrl Pts',(0.848741887328872,3.84208319226065,
12.3650990968344));
#256868=CARTESIAN_POINT('Ctrl Pts',(0.734895808662076,3.86547482963971,
12.3709540178486));
#256869=CARTESIAN_POINT('Ctrl Pts',(0.620251627416566,3.88378384036587,
12.3768089388628));
#256870=CARTESIAN_POINT('Ctrl Pts',(0.505596606378347,3.90209458223861,
12.3826644134693));
#256871=CARTESIAN_POINT('Ctrl Pts',(0.390143740363369,3.91532167703186,
12.3885198880758));
#256872=CARTESIAN_POINT('Ctrl Pts',(0.27437919456943,3.92341752272014,12.3943753626822));
#256873=CARTESIAN_POINT('Ctrl Pts',(0.1585757708495,3.93151608728653,12.4002328037691));
#256874=CARTESIAN_POINT('Ctrl Pts',(0.0424608707332888,3.93447994729295,
12.406090244856));
#256875=CARTESIAN_POINT('Ctrl Pts',(-0.0734774233447359,3.93231357705087,
12.4119476859428));
#256876=CARTESIAN_POINT('Ctrl Pts',(-0.189546397526822,3.93014476497979,
12.4178117292573));
#256877=CARTESIAN_POINT('Ctrl Pts',(-0.305437955469581,3.92283418903382,
12.4236757725718));
#256878=CARTESIAN_POINT('Ctrl Pts',(-0.420667130208069,3.91043835977023,
12.4295398158863));
#256879=CARTESIAN_POINT('Ctrl Pts',(-0.535974164536327,3.89803415472696,
12.435407821496));
#256880=CARTESIAN_POINT('Ctrl Pts',(-0.650617517431927,3.88053791636966,
12.4412758271057));
#256881=CARTESIAN_POINT('Ctrl Pts',(-0.76412213248344,3.85805733065865,
12.4471438327155));
#256882=CARTESIAN_POINT('Ctrl Pts',(-0.877790611936774,3.83554429016394,
12.4530203098506));
#256883=CARTESIAN_POINT('Ctrl Pts',(-0.990316673393825,3.80803263961904,
12.4588967869857));
#256884=CARTESIAN_POINT('Ctrl Pts',(-1.10124008445549,3.77567997536715,
12.4647732641208));
#256885=CARTESIAN_POINT('Ctrl Pts',(-1.12553487936497,3.76859399292889,
12.4660603486543));
#256886=CARTESIAN_POINT('Ctrl Pts',(-1.14975287015872,3.76127596456289,
12.4673474331879));
#256887=CARTESIAN_POINT('Ctrl Pts',(-1.17388935733151,3.75372785064978,
12.4686345177215));
#256888=CARTESIAN_POINT('Ctrl Pts',(-1.28407995208228,3.71926835555517,
12.4745104601995));
#256889=CARTESIAN_POINT('Ctrl Pts',(-1.39293371009581,3.67989593925522,
12.4803864026774));
#256890=CARTESIAN_POINT('Ctrl Pts',(-1.49998041874247,3.63573207805377,
12.4862623451554));
#256891=CARTESIAN_POINT('Ctrl Pts',(-1.60688975741978,3.59162489106806,
12.4921307472051));
#256892=CARTESIAN_POINT('Ctrl Pts',(-1.71199628031148,3.54273864329141,
12.4979991492547));
#256893=CARTESIAN_POINT('Ctrl Pts',(-1.81484449284045,3.48924468428436,
12.5038675513043));
#256894=CARTESIAN_POINT('Ctrl Pts',(-1.91758813150674,3.43580511679065,
12.5097299864882));
#256895=CARTESIAN_POINT('Ctrl Pts',(-2.01807766321097,3.37776734655479,
12.5155924216722));
#256896=CARTESIAN_POINT('Ctrl Pts',(-2.11587778278081,3.31535069160633,
12.5214548568561));
#256897=CARTESIAN_POINT('Ctrl Pts',(-2.21673361646199,3.25098386058296,
12.5275004607928));
#256898=CARTESIAN_POINT('Ctrl Pts',(-2.31472880378298,3.18196018518997,
12.5335460647294));
#256899=CARTESIAN_POINT('Ctrl Pts',(-2.40941329025367,3.10857147203486,
12.5395916686661));
#256900=CARTESIAN_POINT('Ctrl Pts',(-2.50112481357806,3.03748706392165,
12.5454474489223));
#256901=CARTESIAN_POINT('Ctrl Pts',(-2.58973008021745,2.96230790349821,
12.5513032291786));
#256902=CARTESIAN_POINT('Ctrl Pts',(-2.67485043070648,2.88334253486286,
12.5571590094348));
#256903=CARTESIAN_POINT('Ctrl Pts',(-2.75995829114658,2.80438875313136,
12.5630139304491));
#256904=CARTESIAN_POINT('Ctrl Pts',(-2.84158194972849,2.72165014855775,
12.5688688514633));
#256905=CARTESIAN_POINT('Ctrl Pts',(-2.9193776684205,2.63547396669511,12.5747237724775));
#256906=CARTESIAN_POINT('Ctrl Pts',(-2.99718074282344,2.5492896367352,12.580579247084));
#256907=CARTESIAN_POINT('Ctrl Pts',(-3.07115488123778,2.4596673897561,12.5864347216904));
#256908=CARTESIAN_POINT('Ctrl Pts',(-3.14099537318366,2.36698902947158,
12.5922901962969));
#256909=CARTESIAN_POINT('Ctrl Pts',(-3.21085932009554,2.27427954443796,
12.5981476373838));
#256910=CARTESIAN_POINT('Ctrl Pts',(-3.27658661179615,2.17851223466658,
12.6040050784706));
#256911=CARTESIAN_POINT('Ctrl Pts',(-3.33791516821867,2.08009887499987,
12.6098625195575));
#256912=CARTESIAN_POINT('Ctrl Pts',(-3.39931285125894,1.98157458849757,
12.615726562872));
#256913=CARTESIAN_POINT('Ctrl Pts',(-3.45630168489255,1.88039864983544,
12.6215906061865));
#256914=CARTESIAN_POINT('Ctrl Pts',(-3.50866492688975,1.77700856239178,
12.627454649501));
#256915=CARTESIAN_POINT('Ctrl Pts',(-3.56106355038251,1.67354861495132,
12.6333226551107));
#256916=CARTESIAN_POINT('Ctrl Pts',(-3.60883018901355,1.56787191480564,
12.6391906607204));
#256917=CARTESIAN_POINT('Ctrl Pts',(-3.65179641735151,1.46043552621082,
12.6450586663301));
#256918=CARTESIAN_POINT('Ctrl Pts',(-3.69482467519638,1.35284403379454,
12.6509351434652));
#256919=CARTESIAN_POINT('Ctrl Pts',(-3.73303855673301,1.24348817121452,
12.6568116206003));
#256920=CARTESIAN_POINT('Ctrl Pts',(-3.76631956849907,1.13283975386679,
12.6626880977354));
#256921=CARTESIAN_POINT('Ctrl Pts',(-3.77360888053423,1.10860518894691,
12.663975182269));
#256922=CARTESIAN_POINT('Ctrl Pts',(-3.78066175253088,1.08430865392967,
12.6652622668025));
#256923=CARTESIAN_POINT('Ctrl Pts',(-3.78747726902243,1.05995515784319,
12.6665493513361));
#256924=CARTESIAN_POINT('Ctrl Pts',(-3.82661172756583,0.920118230712979,
12.6739397459427));
#256925=CARTESIAN_POINT('Ctrl Pts',(-3.85802042500415,0.778031742465942,
12.6813301405493));
#256926=CARTESIAN_POINT('Ctrl Pts',(-3.88148939352243,0.634451801142437,
12.6887205351559));
#256927=CARTESIAN_POINT('Ctrl Pts',(-3.90458226727896,0.493172756161358,
12.6959924972589));
#256928=CARTESIAN_POINT('Ctrl Pts',(-3.91998784976489,0.350447625091903,
12.7032644593619));
#256929=CARTESIAN_POINT('Ctrl Pts',(-3.92754791774603,0.207017762061202,
12.7105364214649));
#256930=CARTESIAN_POINT('Ctrl Pts',(-3.93111729493799,0.139299418386965,
12.7139697736168));
#256931=CARTESIAN_POINT('Ctrl Pts',(-3.93293847653105,0.0714242984524084,
12.7174031257686));
#256932=CARTESIAN_POINT('Ctrl Pts',(-3.93299846730095,0.0034722051150112,
12.7208364779205));
#256933=CARTESIAN_POINT('',(-3.93299957516998,-0.0018280352083959,13.9708364780037));
#256934=CARTESIAN_POINT('Ctrl Pts',(-3.93299846730173,0.00347220423347139,
12.720836477965));
#256935=CARTESIAN_POINT('Ctrl Pts',(-3.93310303389525,-0.114971361987911,
12.7268209657561));
#256936=CARTESIAN_POINT('Ctrl Pts',(-3.92785234975832,-0.23353116451013,
12.7328054535471));
#256937=CARTESIAN_POINT('Ctrl Pts',(-3.91724514225673,-0.35168095692834,
12.7387899413382));
#256938=CARTESIAN_POINT('Ctrl Pts',(-3.90695911630223,-0.466253225939748,
12.7445932214885));
#256939=CARTESIAN_POINT('Ctrl Pts',(-3.89163632232622,-0.580439506551743,
12.7503965016387));
#256940=CARTESIAN_POINT('Ctrl Pts',(-3.87132845003179,-0.69376150943566,
12.7561997817889));
#256941=CARTESIAN_POINT('Ctrl Pts',(-3.85102457356454,-0.80706121480204,
12.7620019200714));
#256942=CARTESIAN_POINT('Ctrl Pts',(-3.82573764262538,-0.919496566210199,
12.7678040583539));
#256943=CARTESIAN_POINT('Ctrl Pts',(-3.79557082352466,-1.03059745953906,
12.7736061966364));
#256944=CARTESIAN_POINT('Ctrl Pts',(-3.76540233153998,-1.14170451390536,
12.7794086566731));
#256945=CARTESIAN_POINT('Ctrl Pts',(-3.73035352440218,-1.25147655692455,
12.7852111167099));
#256946=CARTESIAN_POINT('Ctrl Pts',(-3.69057778123338,-1.35945748027165,
12.7910135767467));
#256947=CARTESIAN_POINT('Ctrl Pts',(-3.650789799573,-1.46747162797899,12.7968178221268));
#256948=CARTESIAN_POINT('Ctrl Pts',(-3.60627213698255,-1.57369316595428,
12.802622067507));
#256949=CARTESIAN_POINT('Ctrl Pts',(-3.5572264497822,-1.6776856037321,12.8084263128871));
#256950=CARTESIAN_POINT('Ctrl Pts',(-3.50812621746861,-1.78179369447795,
12.8142370133347));
#256951=CARTESIAN_POINT('Ctrl Pts',(-3.45448809157378,-1.88366735725365,
12.8200477137823));
#256952=CARTESIAN_POINT('Ctrl Pts',(-3.39655984729305,-1.98289440055607,
12.82585841423));
#256953=CARTESIAN_POINT('Ctrl Pts',(-3.33859279959578,-2.08218791140539,
12.8316730069936));
#256954=CARTESIAN_POINT('Ctrl Pts',(-3.27633014163088,-2.17883092171571,
12.8374875997572));
#256955=CARTESIAN_POINT('Ctrl Pts',(-3.21006212263405,-2.27244145553416,
12.8433021925207));
#256956=CARTESIAN_POINT('Ctrl Pts',(-3.14369783785791,-2.3661879748721,
12.8491252319878));
#256957=CARTESIAN_POINT('Ctrl Pts',(-3.07331684109543,-2.45689289848686,
12.8549482714548));
#256958=CARTESIAN_POINT('Ctrl Pts',(-2.99924858950895,-2.54420850134744,
12.8607713109218));
#256959=CARTESIAN_POINT('Ctrl Pts',(-2.98359097494738,-2.5626665319546,
12.8620022689315));
#256960=CARTESIAN_POINT('Ctrl Pts',(-2.96776871131024,-2.5809732386353,
12.8632332269411));
#256961=CARTESIAN_POINT('Ctrl Pts',(-2.95178510743871,-2.59912556054974,
12.8644641849508));
#256962=CARTESIAN_POINT('Ctrl Pts',(-2.87548783636751,-2.68577514451157,
12.8703401274288));
#256963=CARTESIAN_POINT('Ctrl Pts',(-2.79524606960399,-2.76920527495376,
12.8762160699067));
#256964=CARTESIAN_POINT('Ctrl Pts',(-2.71136202697481,-2.84903579455911,
12.8820920123847));
#256965=CARTESIAN_POINT('Ctrl Pts',(-2.62758563033063,-2.92876386994925,
12.8879604144343));
#256966=CARTESIAN_POINT('Ctrl Pts',(-2.54017654948023,-3.00490123896631,
12.8938288164839));
#256967=CARTESIAN_POINT('Ctrl Pts',(-2.44947657998768,-3.07710147445479,
12.8996972185335));
#256968=CARTESIAN_POINT('Ctrl Pts',(-2.3588688322841,-3.14922829828814,
12.9055596537174));
#256969=CARTESIAN_POINT('Ctrl Pts',(-2.2649771728396,-3.21742569591253,
12.9114220889013));
#256970=CARTESIAN_POINT('Ctrl Pts',(-2.1681790075239,-3.28138519398937,
12.9172845240853));
#256971=CARTESIAN_POINT('Ctrl Pts',(-2.06835643363839,-3.34734307347637,
12.9233301280219));
#256972=CARTESIAN_POINT('Ctrl Pts',(-1.96544306736774,-3.40879357018475,
12.9293757319586));
#256973=CARTESIAN_POINT('Ctrl Pts',(-1.8598885355758,-3.46544421903364,
12.9354213358953));
#256974=CARTESIAN_POINT('Ctrl Pts',(-1.75764827146028,-3.52031611512659,
12.9412771161515));
#256975=CARTESIAN_POINT('Ctrl Pts',(-1.65293061040441,-3.57068486437814,
12.9471328964077));
#256976=CARTESIAN_POINT('Ctrl Pts',(-1.54617143208549,-3.61633003231214,
12.952988676664));
#256977=CARTESIAN_POINT('Ctrl Pts',(-1.43942791896704,-3.6619685025484,
12.9588435976782));
#256978=CARTESIAN_POINT('Ctrl Pts',(-1.33064386367743,-3.70288460746818,
12.9646985186924));
#256979=CARTESIAN_POINT('Ctrl Pts',(-1.22027629848336,-3.73890555582242,
12.9705534397066));
#256980=CARTESIAN_POINT('Ctrl Pts',(-1.10989829785761,-3.77492991001554,
12.9764089143131));
#256981=CARTESIAN_POINT('Ctrl Pts',(-0.997936882098993,-3.80605805947923,
12.9822643889195));
#256982=CARTESIAN_POINT('Ctrl Pts',(-0.884864780905563,-3.83216692218814,
12.988119863526));
#256983=CARTESIAN_POINT('Ctrl Pts',(-0.77175470600656,-3.85828455319848,
12.9939773046128));
#256984=CARTESIAN_POINT('Ctrl Pts',(-0.65753360590397,-3.87937945273476,
12.9998347456997));
#256985=CARTESIAN_POINT('Ctrl Pts',(-0.542684251875529,-3.89537967376305,
13.0056921867865));
#256986=CARTESIAN_POINT('Ctrl Pts',(-0.427705445144124,-3.91139792947579,
13.011556230101));
#256987=CARTESIAN_POINT('Ctrl Pts',(-0.312097380138019,-3.92230998833659,
13.0174202734155));
#256988=CARTESIAN_POINT('Ctrl Pts',(-0.196347892718441,-3.92809578613162,
13.02328431673));
#256989=CARTESIAN_POINT('Ctrl Pts',(-0.080520194137626,-3.93388549335187,
13.0291523223397));
#256990=CARTESIAN_POINT('Ctrl Pts',(0.035448705427454,-3.93454203988918,
13.0350203279494));
#256991=CARTESIAN_POINT('Ctrl Pts',(0.151072751616917,-3.93009745728002,
13.0408883335591));
#256992=CARTESIAN_POINT('Ctrl Pts',(0.266863721990182,-3.92564645811351,
13.0467648106942));
#256993=CARTESIAN_POINT('Ctrl Pts',(0.38230843572701,-3.91607966696002,
13.0526412878293));
#256994=CARTESIAN_POINT('Ctrl Pts',(0.496927670840884,-3.90148073043462,
13.0585177649644));
#256995=CARTESIAN_POINT('Ctrl Pts',(0.522031936778244,-3.89828322536863,
13.059804849498));
#256996=CARTESIAN_POINT('Ctrl Pts',(0.547096650833877,-3.89484451534116,
13.0610919340317));
#256997=CARTESIAN_POINT('Ctrl Pts',(0.572116864656961,-3.89116580129594,
13.0623790185654));
#256998=CARTESIAN_POINT('Ctrl Pts',(0.686341947289151,-3.87437132388793,
13.0682549610434));
#256999=CARTESIAN_POINT('Ctrl Pts',(0.800015341973993,-3.85251526889571,
13.0741309035213));
#257000=CARTESIAN_POINT('Ctrl Pts',(0.912653620815972,-3.82564404622431,
13.0800068459993));
#257001=CARTESIAN_POINT('Ctrl Pts',(1.02514735418691,-3.79880730662188,
13.085875248049));
#257002=CARTESIAN_POINT('Ctrl Pts',(1.13660821551571,-3.76696829332194,
13.0917436500986));
#257003=CARTESIAN_POINT('Ctrl Pts',(1.2465595104342,-3.73022497806044,13.0976120521482));
#257004=CARTESIAN_POINT('Ctrl Pts',(1.35639900922763,-3.69351902261604,
13.1034744873321));
#257005=CARTESIAN_POINT('Ctrl Pts',(1.46473160552755,-3.65191881426347,
13.1093369225161));
#257006=CARTESIAN_POINT('Ctrl Pts',(1.57109304048681,-3.60557286129873,
13.1151993577));
#257007=CARTESIAN_POINT('Ctrl Pts',(1.68077768342519,-3.5577788530238,13.1212449616367));
#257008=CARTESIAN_POINT('Ctrl Pts',(1.78836552977401,-3.50493777221692,
13.1272905655733));
#257009=CARTESIAN_POINT('Ctrl Pts',(1.89336641132977,-3.44726741527956,
13.13333616951));
#257010=CARTESIAN_POINT('Ctrl Pts',(1.99507040906837,-3.39140782853479,
13.1391919497663));
#257011=CARTESIAN_POINT('Ctrl Pts',(2.0943470789089,-3.3310179099754,13.1450477300225));
#257012=CARTESIAN_POINT('Ctrl Pts',(2.19077414959522,-3.26634315794672,
13.1509035102788));
#257013=CARTESIAN_POINT('Ctrl Pts',(2.28718707115254,-3.20167789590257,
13.156758431293));
#257014=CARTESIAN_POINT('Ctrl Pts',(2.38075088229321,-3.13272928045617,
13.1626133523072));
#257015=CARTESIAN_POINT('Ctrl Pts',(2.47107174780495,-3.05978649863029,
13.1684682733215));
#257016=CARTESIAN_POINT('Ctrl Pts',(2.5614011533005,-2.9868368199465,13.1743237479279));
#257017=CARTESIAN_POINT('Ctrl Pts',(2.64848668249115,-2.90989248348584,
13.1801792225344));
#257018=CARTESIAN_POINT('Ctrl Pts',(2.7319676400229,-2.82928291513374,13.1860346971409));
#257019=CARTESIAN_POINT('Ctrl Pts',(2.81547663348299,-2.74864627516978,
13.1918921382278));
#257020=CARTESIAN_POINT('Ctrl Pts',(2.89537835137074,-2.66434224220679,
13.1977495793147));
#257021=CARTESIAN_POINT('Ctrl Pts',(2.97134951437397,-2.57673651416469,
13.2036070204015));
#257022=CARTESIAN_POINT('Ctrl Pts',(3.04740630844109,-2.48903204113306,
13.2094710637161));
#257023=CARTESIAN_POINT('Ctrl Pts',(3.11952343460079,-2.3980187572808,13.2153351070306));
#257024=CARTESIAN_POINT('Ctrl Pts',(3.18741836746576,-2.30409486582951,
13.2211991503451));
#257025=CARTESIAN_POINT('Ctrl Pts',(3.25535917648669,-2.21010751062753,
13.2270671559548));
#257026=CARTESIAN_POINT('Ctrl Pts',(3.31907188514095,-2.11320597567742,
13.2329351615645));
#257027=CARTESIAN_POINT('Ctrl Pts',(3.37831862924121,-2.0138153438987,13.2388031671742));
#257028=CARTESIAN_POINT('Ctrl Pts',(3.43765090671206,-1.91428122380055,
13.2446796443093));
#257029=CARTESIAN_POINT('Ctrl Pts',(3.49250415812827,-1.81225119767171,
13.2505561214444));
#257030=CARTESIAN_POINT('Ctrl Pts',(3.54268752832076,-1.70817273034097,
13.2564325985795));
#257031=CARTESIAN_POINT('Ctrl Pts',(3.55367884814176,-1.6853771365711,13.257719683113));
#257032=CARTESIAN_POINT('Ctrl Pts',(3.56444633586689,-1.66248334210052,
13.2590067676465));
#257033=CARTESIAN_POINT('Ctrl Pts',(3.57498830358303,-1.63949615103072,
13.26029385218));
#257034=CARTESIAN_POINT('Ctrl Pts',(3.62311567540152,-1.53455245157456,
13.266169794658));
#257035=CARTESIAN_POINT('Ctrl Pts',(3.66669760141889,-1.42731466194993,
13.272045737136));
#257036=CARTESIAN_POINT('Ctrl Pts',(3.70550970658548,-1.31821349348304,
13.277921679614));
#257037=CARTESIAN_POINT('Ctrl Pts',(3.74427200529127,-1.20925233141488,
13.2837900816636));
#257038=CARTESIAN_POINT('Ctrl Pts',(3.77827651896329,-1.09843293137146,
13.2896584837132));
#257039=CARTESIAN_POINT('Ctrl Pts',(3.80734578307702,-0.986208440485887,
13.2955268857628));
#257040=CARTESIAN_POINT('Ctrl Pts',(3.83638549018477,-0.874098057062291,
13.3013893209467));
#257041=CARTESIAN_POINT('Ctrl Pts',(3.86049982642276,-0.76058582184569,
13.3072517561307));
#257042=CARTESIAN_POINT('Ctrl Pts',(3.87956048350467,-0.64614197729991,
13.3131141913146));
#257043=CARTESIAN_POINT('Ctrl Pts',(3.89921668095069,-0.528122394071141,
13.3191597952513));
#257044=CARTESIAN_POINT('Ctrl Pts',(3.91349805906358,-0.40911245019233,
13.325205399188));
#257045=CARTESIAN_POINT('Ctrl Pts',(3.92232030765702,-0.289641854954211,
13.3312510031246));
#257046=CARTESIAN_POINT('Ctrl Pts',(3.93086554973213,-0.173922472718091,
13.3371067833809));
#257047=CARTESIAN_POINT('Ctrl Pts',(3.9342893223048,-0.0577713762121623,
13.3429625636371));
#257048=CARTESIAN_POINT('Ctrl Pts',(3.93256752770725,0.058323580329461,
13.3488183438933));
#257049=CARTESIAN_POINT('Ctrl Pts',(3.9308459857555,0.174401501794627,13.3546732649075));
#257050=CARTESIAN_POINT('Ctrl Pts',(3.92398038410408,0.290422887069137,
13.3605281859218));
#257051=CARTESIAN_POINT('Ctrl Pts',(3.91199875287312,0.405899935352512,
13.366383106936));
#257052=CARTESIAN_POINT('Ctrl Pts',(3.90001598875952,0.521387902177801,
13.3722385815425));
#257053=CARTESIAN_POINT('Ctrl Pts',(3.88291627605861,0.636331019124076,
13.3780940561489));
#257054=CARTESIAN_POINT('Ctrl Pts',(3.86077944135489,0.750247362682064,
13.3839495307554));
#257055=CARTESIAN_POINT('Ctrl Pts',(3.83863517230056,0.86420196347287,13.3898069718423));
#257056=CARTESIAN_POINT('Ctrl Pts',(3.81145049611926,0.977128700236576,
13.3956644129291));
#257057=CARTESIAN_POINT('Ctrl Pts',(3.77935603802724,1.08855727356306,13.401521854016));
#257058=CARTESIAN_POINT('Ctrl Pts',(3.74722540459602,1.20011144385162,13.4073858973305));
#257059=CARTESIAN_POINT('Ctrl Pts',(3.71017405814841,1.31016368349018,13.413249940645));
#257060=CARTESIAN_POINT('Ctrl Pts',(3.66838208147061,1.41826016807402,13.4191139839595));
#257061=CARTESIAN_POINT('Ctrl Pts',(3.62656186623101,1.52642969273642,13.4249819895692));
#257062=CARTESIAN_POINT('Ctrl Pts',(3.57999480765519,1.6326404538458,13.4308499951789));
#257063=CARTESIAN_POINT('Ctrl Pts',(3.52890785618393,1.73646144286688,13.4367180007887));
#257064=CARTESIAN_POINT('Ctrl Pts',(3.4777471514762,1.84043231622699,13.4425944779238));
#257065=CARTESIAN_POINT('Ctrl Pts',(3.42205372932586,1.94200617187811,13.4484709550589));
#257066=CARTESIAN_POINT('Ctrl Pts',(3.36209891441958,2.04077923589463,13.4543474321939));
#257067=CARTESIAN_POINT('Ctrl Pts',(3.34896742199554,2.06241282351991,13.4556345167275));
#257068=CARTESIAN_POINT('Ctrl Pts',(3.33563166260049,2.08391217557118,13.4569216012611));
#257069=CARTESIAN_POINT('Ctrl Pts',(3.32209474595243,2.10527325991551,13.4582086857947));
#257070=CARTESIAN_POINT('Ctrl Pts',(3.26029449781206,2.20279327480133,13.4640846282726));
#257071=CARTESIAN_POINT('Ctrl Pts',(3.19409461294023,2.29775064966901,13.4699605707506));
#257072=CARTESIAN_POINT('Ctrl Pts',(3.1237341089437,2.38972262336483,13.4758365132285));
#257073=CARTESIAN_POINT('Ctrl Pts',(3.05346389656304,2.48157657206584,13.4817049152781));
#257074=CARTESIAN_POINT('Ctrl Pts',(2.97904393179451,2.57045241366354,13.4875733173277));
#257075=CARTESIAN_POINT('Ctrl Pts',(2.90075759804885,2.65595450965597,13.4934417193773));
#257076=CARTESIAN_POINT('Ctrl Pts',(2.82255086417264,2.74136966894625,13.4993041545612));
#257077=CARTESIAN_POINT('Ctrl Pts',(2.74048585819392,2.82341760340935,13.5051665897451));
#257078=CARTESIAN_POINT('Ctrl Pts',(2.65488707357435,2.90173458927033,13.511029024929));
#257079=CARTESIAN_POINT('Ctrl Pts',(2.56661379923745,2.98249854881566,13.5170746288656));
#257080=CARTESIAN_POINT('Ctrl Pts',(2.47458256559311,3.05929422927242,13.5231202328023));
#257081=CARTESIAN_POINT('Ctrl Pts',(2.37919170230479,3.13176241814158,13.529165836739));
#257082=CARTESIAN_POINT('Ctrl Pts',(2.28679598142782,3.2019552051696,13.5350216169952));
#257083=CARTESIAN_POINT('Ctrl Pts',(2.19124880488206,3.26808792394175,13.5408773972514));
#257084=CARTESIAN_POINT('Ctrl Pts',(2.09294619449014,3.32987465634508,13.5467331775076));
#257085=CARTESIAN_POINT('Ctrl Pts',(1.99465800843295,3.39165232253433,13.5525880985218));
#257086=CARTESIAN_POINT('Ctrl Pts',(1.89361554186998,3.449085050815,13.558443019536));
#257087=CARTESIAN_POINT('Ctrl Pts',(1.79024316304185,3.50193066995649,13.5642979405501));
#257088=CARTESIAN_POINT('Ctrl Pts',(1.68686101018808,3.55478128573676,13.5701534151566));
#257089=CARTESIAN_POINT('Ctrl Pts',(1.58114887467595,3.60304374229499,13.576008889763));
#257090=CARTESIAN_POINT('Ctrl Pts',(1.47355440644105,3.64652250935849,13.5818643643694));
#257091=CARTESIAN_POINT('Ctrl Pts',(1.36592380408785,3.69001587816629,13.5877218054563));
#257092=CARTESIAN_POINT('Ctrl Pts',(1.25640999446082,3.72872220834599,13.5935792465431));
#257093=CARTESIAN_POINT('Ctrl Pts',(1.14547854607439,3.76249490371526,13.5994366876299));
#257094=CARTESIAN_POINT('Ctrl Pts',(1.03442206106119,3.79630566605262,13.6053007309444));
#257095=CARTESIAN_POINT('Ctrl Pts',(0.921945143128858,3.82517157423755,
13.6111647742588));
#257096=CARTESIAN_POINT('Ctrl Pts',(0.808526480677646,3.84899648350619,
13.6170288175733));
#257097=CARTESIAN_POINT('Ctrl Pts',(0.695031181987774,3.87283749110815,
13.622896823183));
#257098=CARTESIAN_POINT('Ctrl Pts',(0.580593277954821,3.89163065050699,
13.6287648287926));
#257099=CARTESIAN_POINT('Ctrl Pts',(0.465697848411778,3.90533154981554,
13.6346328344023));
#257100=CARTESIAN_POINT('Ctrl Pts',(0.350636546575094,3.91905222884555,
13.6405093115374));
#257101=CARTESIAN_POINT('Ctrl Pts',(0.23511681103267,3.92766594597547,13.6463857886725));
#257102=CARTESIAN_POINT('Ctrl Pts',(0.119625049177905,3.93118033771146,
13.6522622658075));
#257103=CARTESIAN_POINT('Ctrl Pts',(0.0943296796800673,3.93195007086034,
13.6535493503414));
#257104=CARTESIAN_POINT('Ctrl Pts',(0.0690356355892736,3.93247538136678,
13.6548364348754));
#257105=CARTESIAN_POINT('Ctrl Pts',(0.0437479922143117,3.93275668115601,
13.6561235194093));
#257106=CARTESIAN_POINT('Ctrl Pts',(-0.071697989741531,3.93404090246163,
13.6619994618873));
#257107=CARTESIAN_POINT('Ctrl Pts',(-0.187391021699671,3.93023956642023,
13.6678754043654));
#257108=CARTESIAN_POINT('Ctrl Pts',(-0.302846368279034,3.92132287337069,
13.6737513468435));
#257109=CARTESIAN_POINT('Ctrl Pts',(-0.418153554325276,3.91241762285748,
13.6796197488932));
#257110=CARTESIAN_POINT('Ctrl Pts',(-0.533223253743708,3.89841010158475,
13.6854881509429));
#257111=CARTESIAN_POINT('Ctrl Pts',(-0.647569314295453,3.87932249022725,
13.6913565529926));
#257112=CARTESIAN_POINT('Ctrl Pts',(-0.76179911021818,3.86025428674477,
13.6972189881766));
#257113=CARTESIAN_POINT('Ctrl Pts',(-0.875306326089624,3.83611633526808,
13.7030814233607));
#257114=CARTESIAN_POINT('Ctrl Pts',(-0.987609184996774,3.8069826763081,
13.7089438585447));
#257115=CARTESIAN_POINT('Ctrl Pts',(-1.1034208885967,3.77693875125501,13.7149894624813));
#257116=CARTESIAN_POINT('Ctrl Pts',(-1.2179512936038,3.74158184483587,13.7210350664179));
#257117=CARTESIAN_POINT('Ctrl Pts',(-1.3306821919086,3.70105037849221,13.7270806703546));
#257118=CARTESIAN_POINT('Ctrl Pts',(-1.43987349446358,3.66179154465801,
13.7329364506109));
#257119=CARTESIAN_POINT('Ctrl Pts',(-1.54737618777003,3.61767839049213,
13.7387922308672));
#257120=CARTESIAN_POINT('Ctrl Pts',(-1.65273479015303,3.5688873214796,13.7446480111236));
#257121=CARTESIAN_POINT('Ctrl Pts',(-1.75807793284761,3.52010341177544,
13.7505029321379));
#257122=CARTESIAN_POINT('Ctrl Pts',(-1.86127723576311,3.46664312553191,
13.7563578531522));
#257123=CARTESIAN_POINT('Ctrl Pts',(-1.96189846744296,3.40873046799611,
13.7622127741665));
#257124=CARTESIAN_POINT('Ctrl Pts',(-2.06252921302292,3.35081233472491,
13.7680682487731));
#257125=CARTESIAN_POINT('Ctrl Pts',(-2.16058104503836,3.28844119920087,
13.7739237233797));
#257126=CARTESIAN_POINT('Ctrl Pts',(-2.25564616789749,3.22188599507328,
13.7797791979862));
#257127=CARTESIAN_POINT('Ctrl Pts',(-2.35074321706692,3.15530843929838,
13.7856366390732));
#257128=CARTESIAN_POINT('Ctrl Pts',(-2.44285122459867,3.08454425736946,
13.7914940801601));
#257129=CARTESIAN_POINT('Ctrl Pts',(-2.53159367494086,3.00990406242449,
13.7973515212471));
#257130=CARTESIAN_POINT('Ctrl Pts',(-2.62043615153184,2.93517973661902,
13.8032155645617));
#257131=CARTESIAN_POINT('Ctrl Pts',(-2.70590518348767,2.85657094385367,
13.8090796078763));
#257132=CARTESIAN_POINT('Ctrl Pts',(-2.78765942141966,2.77442677866442,
13.8149436511909));
#257133=CARTESIAN_POINT('Ctrl Pts',(-2.86946890014818,2.69222710920737,
13.8208116568007));
#257134=CARTESIAN_POINT('Ctrl Pts',(-2.94755830943711,2.60648761494094,
13.8266796624105));
#257135=CARTESIAN_POINT('Ctrl Pts',(-3.02162620540612,2.51759092681933,
13.8325476680203));
#257136=CARTESIAN_POINT('Ctrl Pts',(-3.09580103175368,2.42856590028081,
13.8384241451554));
#257137=CARTESIAN_POINT('Ctrl Pts',(-3.16594250952575,2.3363749109216,13.8443006222906));
#257138=CARTESIAN_POINT('Ctrl Pts',(-3.2317921229849,2.241430051064,13.8501770994258));
#257139=CARTESIAN_POINT('Ctrl Pts',(-3.24621471274706,2.22063492878737,
13.8514641839585));
#257140=CARTESIAN_POINT('Ctrl Pts',(-3.26043159178119,2.19970779408334,
13.8527512684912));
#257141=CARTESIAN_POINT('Ctrl Pts',(-3.27444034130428,2.17865312779228,
13.8540383530239));
#257142=CARTESIAN_POINT('Ctrl Pts',(-3.33950682555402,2.080860451126,13.8600164787186));
#257143=CARTESIAN_POINT('Ctrl Pts',(-3.40028894269776,1.98000000849237,
13.8659946044133));
#257144=CARTESIAN_POINT('Ctrl Pts',(-3.45649071384092,1.87647567134015,
13.871972730108));
#257145=CARTESIAN_POINT('Ctrl Pts',(-3.51261348722497,1.7730968490086,13.8779424528908));
#257146=CARTESIAN_POINT('Ctrl Pts',(-3.56416853833148,1.66706192514992,
13.8839121756736));
#257147=CARTESIAN_POINT('Ctrl Pts',(-3.61090274354847,1.55880414954353,
13.8898818984564));
#257148=CARTESIAN_POINT('Ctrl Pts',(-3.65758107040856,1.45067581374669,
13.8958444834629));
#257149=CARTESIAN_POINT('Ctrl Pts',(-3.69944986724521,1.34033027461661,
13.9018070684694));
#257150=CARTESIAN_POINT('Ctrl Pts',(-3.7363018239388,1.22822541922549,13.9077696534759));
#257151=CARTESIAN_POINT('Ctrl Pts',(-3.77311019821721,1.11625314296421,
13.9137251869205));
#257152=CARTESIAN_POINT('Ctrl Pts',(-3.80491342872528,1.00252606756105,
13.9196807203651));
#257153=CARTESIAN_POINT('Ctrl Pts',(-3.8315525277421,0.887521395321316,
13.9256362538097));
#257154=CARTESIAN_POINT('Ctrl Pts',(-3.85817311045603,0.772596660520337,
13.9315876476825));
#257155=CARTESIAN_POINT('Ctrl Pts',(-3.87963661635611,0.656396478575151,
13.9375390415554));
#257156=CARTESIAN_POINT('Ctrl Pts',(-3.89583407870534,0.539412487061738,
13.9434904354282));
#257157=CARTESIAN_POINT('Ctrl Pts',(-3.91202327786513,0.422488175321747,
13.9494387931776));
#257158=CARTESIAN_POINT('Ctrl Pts',(-3.92295172834644,0.30478123960899,
13.9553871509271));
#257159=CARTESIAN_POINT('Ctrl Pts',(-3.9285617780135,0.18679228124146,13.9613355086765));
#257160=CARTESIAN_POINT('Ctrl Pts',(-3.93154864777034,0.123973291695202,
13.9645024984393));
#257161=CARTESIAN_POINT('Ctrl Pts',(-3.93302881188282,0.0610744882110394,
13.9676694882022));
#257162=CARTESIAN_POINT('Ctrl Pts',(-3.93299957517034,-0.00182803443963738,
13.970836477965));
#257163=CARTESIAN_POINT('',(-3.93299944805027,-0.00208365934259914,15.2208364779214));
#257164=CARTESIAN_POINT('Ctrl Pts',(-3.93299957516998,-0.00182803520836979,
13.9708364780037));
#257165=CARTESIAN_POINT('Ctrl Pts',(-3.93294033855577,-0.129275021723806,
13.9772531252953));
#257166=CARTESIAN_POINT('Ctrl Pts',(-3.92668218850876,-0.256517553615144,
13.9836697725869));
#257167=CARTESIAN_POINT('Ctrl Pts',(-3.91430926981101,-0.382977728166544,
13.9900864198786));
#257168=CARTESIAN_POINT('Ctrl Pts',(-3.90187435879248,-0.510071509055871,
13.9965352166465));
#257169=CARTESIAN_POINT('Ctrl Pts',(-3.88326334398951,-0.636374811774402,
14.0029840134145));
#257170=CARTESIAN_POINT('Ctrl Pts',(-3.85861196357145,-0.76131643525099,
14.0094328101825));
#257171=CARTESIAN_POINT('Ctrl Pts',(-3.83389603093612,-0.886585231433034,
14.0158984937991));
#257172=CARTESIAN_POINT('Ctrl Pts',(-3.80310818328694,-1.01048496215025,
14.0223641774157));
#257173=CARTESIAN_POINT('Ctrl Pts',(-3.76643400785372,-1.13245921095772,
14.0288298610324));
#257174=CARTESIAN_POINT('Ctrl Pts',(-3.72963590519998,-1.25484562798578,
14.0353173931075));
#257175=CARTESIAN_POINT('Ctrl Pts',(-3.68691176032944,-1.37529328987783,
14.0418049251826));
#257176=CARTESIAN_POINT('Ctrl Pts',(-3.63849613831945,-1.49326315545334,
14.0482924572577));
#257177=CARTESIAN_POINT('Ctrl Pts',(-3.62938961995291,-1.51545216600326,
14.0495127003846));
#257178=CARTESIAN_POINT('Ctrl Pts',(-3.62008187839841,-1.53755358814958,
14.0507329435116));
#257179=CARTESIAN_POINT('Ctrl Pts',(-3.61057465360002,-1.55956393609915,
14.0519531866386));
#257180=CARTESIAN_POINT('Ctrl Pts',(-3.56479369011491,-1.66555227203757,
14.0578291291163));
#257181=CARTESIAN_POINT('Ctrl Pts',(-3.51426632056984,-1.76969790432598,
14.0637050715941));
#257182=CARTESIAN_POINT('Ctrl Pts',(-3.45916247287764,-1.87154588141329,
14.0695810140719));
#257183=CARTESIAN_POINT('Ctrl Pts',(-3.40412933837196,-1.97326315991416,
14.0754494161213));
#257184=CARTESIAN_POINT('Ctrl Pts',(-3.34453159986428,-2.07268828721999,
14.0813178181706));
#257185=CARTESIAN_POINT('Ctrl Pts',(-3.28058724832085,-2.16938615883724,
14.08718622022));
#257186=CARTESIAN_POINT('Ctrl Pts',(-3.21670791402643,-2.26598571012682,
14.0930486554037));
#257187=CARTESIAN_POINT('Ctrl Pts',(-3.14849098410243,-2.35986317934484,
14.0989110905874));
#257188=CARTESIAN_POINT('Ctrl Pts',(-3.07620004668988,-2.45060855151229,
14.1047735257711));
#257189=CARTESIAN_POINT('Ctrl Pts',(-3.00165041635399,-2.54418921586542,
14.1108191297079));
#257190=CARTESIAN_POINT('Ctrl Pts',(-2.92276822572093,-2.63443845134279,
14.1168647336446));
#257191=CARTESIAN_POINT('Ctrl Pts',(-2.83989069561032,-2.72093914613796,
14.1229103375814));
#257192=CARTESIAN_POINT('Ctrl Pts',(-2.7596154063976,-2.8047238376281,14.1287661178374));
#257193=CARTESIAN_POINT('Ctrl Pts',(-2.67559222934242,-2.88499154691874,
14.1346218980934));
#257194=CARTESIAN_POINT('Ctrl Pts',(-2.58816757361598,-2.96139791498589,
14.1404776783494));
#257195=CARTESIAN_POINT('Ctrl Pts',(-2.5007557460584,-3.03779307164153,
14.1463325993634));
#257196=CARTESIAN_POINT('Ctrl Pts',(-2.40994374300934,-3.11032774216744,
14.1521875203774));
#257197=CARTESIAN_POINT('Ctrl Pts',(-2.31611281565845,-3.17869634050544,
14.1580424413914));
#257198=CARTESIAN_POINT('Ctrl Pts',(-2.22227301644156,-3.24707140320504,
14.1638979159976));
#257199=CARTESIAN_POINT('Ctrl Pts',(-2.12541405909878,-3.31127936758053,
14.1697533906038));
#257200=CARTESIAN_POINT('Ctrl Pts',(-2.02594748730443,-3.37105707140726,
14.1756088652101));
#257201=CARTESIAN_POINT('Ctrl Pts',(-1.92644751103389,-3.43085485075129,
14.1814663062967));
#257202=CARTESIAN_POINT('Ctrl Pts',(-1.82433853252037,-3.48621919849487,
14.1873237473833));
#257203=CARTESIAN_POINT('Ctrl Pts',(-1.72005744964628,-3.53693248025974,
14.1931811884699));
#257204=CARTESIAN_POINT('Ctrl Pts',(-1.61565882611948,-3.58770292361208,
14.1990452317842));
#257205=CARTESIAN_POINT('Ctrl Pts',(-1.50908358308714,-3.63381165700011,
14.2049092750985));
#257206=CARTESIAN_POINT('Ctrl Pts',(-1.40078947045128,-3.67508882334466,
14.2107733184127));
#257207=CARTESIAN_POINT('Ctrl Pts',(-1.29242218420112,-3.71639388039698,
14.2166413240222));
#257208=CARTESIAN_POINT('Ctrl Pts',(-1.18233410647362,-3.75286074016077,
14.2225093296317));
#257209=CARTESIAN_POINT('Ctrl Pts',(-1.07099739410399,-3.78436964127746,
14.2283773352412));
#257210=CARTESIAN_POINT('Ctrl Pts',(-0.959499947091306,-3.81592403118095,
14.234253812376));
#257211=CARTESIAN_POINT('Ctrl Pts',(-0.846750668155043,-3.84250608379267,
14.2401302895109));
#257212=CARTESIAN_POINT('Ctrl Pts',(-0.733231168924177,-3.8640472374077,
14.2460067666458));
#257213=CARTESIAN_POINT('Ctrl Pts',(-0.708367770562164,-3.86876524873735,
14.2472938511816));
#257214=CARTESIAN_POINT('Ctrl Pts',(-0.683467438484994,-3.87324164035368,
14.2485809357174));
#257215=CARTESIAN_POINT('Ctrl Pts',(-0.658535249944616,-3.87747602501684,
14.2498680202532));
#257216=CARTESIAN_POINT('Ctrl Pts',(-0.544712030366906,-3.89680731214034,
14.2557439627319));
#257217=CARTESIAN_POINT('Ctrl Pts',(-0.429849108164953,-3.91115432943795,
14.2616199052106));
#257218=CARTESIAN_POINT('Ctrl Pts',(-0.314420586219157,-3.92041180170675,
14.2674958476893));
#257219=CARTESIAN_POINT('Ctrl Pts',(-0.199140190383127,-3.92965739412706,
14.2733642497396));
#257220=CARTESIAN_POINT('Ctrl Pts',(-0.0832960459976697,-3.93382639769409,
14.2792326517899));
#257221=CARTESIAN_POINT('Ctrl Pts',(0.032628211713834,-3.93286465566772,
14.2851010538403));
#257222=CARTESIAN_POINT('Ctrl Pts',(0.148434600119379,-3.93190389152007,
14.2909634890249));
#257223=CARTESIAN_POINT('Ctrl Pts',(0.264320529484257,-3.92582276216068,
14.2968259242096));
#257224=CARTESIAN_POINT('Ctrl Pts',(0.379798571942981,-3.91461901655194,
14.3026883593942));
#257225=CARTESIAN_POINT('Ctrl Pts',(0.498884666043312,-3.903065215713,14.3087339633306));
#257226=CARTESIAN_POINT('Ctrl Pts',(0.617536520453047,-3.88606339386041,
14.314779567267));
#257227=CARTESIAN_POINT('Ctrl Pts',(0.735220651642348,-3.86366918788327,
14.3208251712034));
#257228=CARTESIAN_POINT('Ctrl Pts',(0.849209662372347,-3.84197812928752,
14.3266809514604));
#257229=CARTESIAN_POINT('Ctrl Pts',(0.962290376271785,-3.81522833330441,
14.3325367317173));
#257230=CARTESIAN_POINT('Ctrl Pts',(1.07398532065683,-3.78352276734443,
14.3383925119743));
#257231=CARTESIAN_POINT('Ctrl Pts',(1.18566387559669,-3.75182185366874,
14.3442474329892));
#257232=CARTESIAN_POINT('Ctrl Pts',(1.29595666838717,-3.71516672867222,
14.3501023540042));
#257233=CARTESIAN_POINT('Ctrl Pts',(1.40439976730262,-3.6737106981362,14.3559572750191));
#257234=CARTESIAN_POINT('Ctrl Pts',(1.51285311968827,-3.63225074786552,
14.3618127496263));
#257235=CARTESIAN_POINT('Ctrl Pts',(1.61945604496533,-3.58598913707341,
14.3676682242335));
#257236=CARTESIAN_POINT('Ctrl Pts',(1.72376369211206,-3.53512768280811,
14.3735236988406));
#257237=CARTESIAN_POINT('Ctrl Pts',(1.82810636954325,-3.48424914742497,
14.3793811399282));
#257238=CARTESIAN_POINT('Ctrl Pts',(1.93015186524843,-3.42876787757276,
14.3852385810157));
#257239=CARTESIAN_POINT('Ctrl Pts',(2.02947970175482,-3.36893175059471,
14.3910960221033));
#257240=CARTESIAN_POINT('Ctrl Pts',(2.12891949585127,-3.30902817919414,
14.3969600654185));
#257241=CARTESIAN_POINT('Ctrl Pts',(2.22563516316399,-3.24476016675888,
14.4028241087337));
#257242=CARTESIAN_POINT('Ctrl Pts',(2.31923493841007,-3.17641910025394,
14.4086881520489));
#257243=CARTESIAN_POINT('Ctrl Pts',(2.41289795840394,-3.10803185614329,
14.4145561576593));
#257244=CARTESIAN_POINT('Ctrl Pts',(2.50344057251542,-3.03556633501209,
14.4204241632697));
#257245=CARTESIAN_POINT('Ctrl Pts',(2.59050518232709,-2.95935329089591,
14.4262921688801));
#257246=CARTESIAN_POINT('Ctrl Pts',(2.67769548561984,-2.88303021949265,
14.4321686460159));
#257247=CARTESIAN_POINT('Ctrl Pts',(2.76139746712784,-2.80294911237236,
14.4380451231517));
#257248=CARTESIAN_POINT('Ctrl Pts',(2.84129131829658,-2.71947653870602,
14.4439216002875));
#257249=CARTESIAN_POINT('Ctrl Pts',(2.85878992115806,-2.70119411277405,
14.4452086848142));
#257250=CARTESIAN_POINT('Ctrl Pts',(2.87610600172078,-2.68274911441523,
14.446495769341));
#257251=CARTESIAN_POINT('Ctrl Pts',(2.89323646991126,-2.66414559083684,
14.4477828538678));
#257252=CARTESIAN_POINT('Ctrl Pts',(2.97144240246882,-2.57921470079195,
14.4536587963451));
#257253=CARTESIAN_POINT('Ctrl Pts',(3.04603447030337,-2.49069718155165,
14.4595347388224));
#257254=CARTESIAN_POINT('Ctrl Pts',(3.11666616413018,-2.39893330907011,
14.4654106812997));
#257255=CARTESIAN_POINT('Ctrl Pts',(3.1872072183312,-2.30728719453281,14.4712790833487));
#257256=CARTESIAN_POINT('Ctrl Pts',(3.25379775617551,-2.21240333582628,
14.4771474853976));
#257257=CARTESIAN_POINT('Ctrl Pts',(3.31612894791232,-2.11465784485764,
14.4830158874466));
#257258=CARTESIAN_POINT('Ctrl Pts',(3.37839676262653,-2.0170117394136,14.4888783226298));
#257259=CARTESIAN_POINT('Ctrl Pts',(3.43641362516404,-1.91651013537292,
14.4947407578131));
#257260=CARTESIAN_POINT('Ctrl Pts',(3.48991217164834,-1.81356059567381,
14.5006031929963));
#257261=CARTESIAN_POINT('Ctrl Pts',(3.54508225253357,-1.70739445088026,
14.5066487969333));
#257262=CARTESIAN_POINT('Ctrl Pts',(3.59544675863839,-1.59862524094772,
14.5126944008702));
#257263=CARTESIAN_POINT('Ctrl Pts',(3.64076179062746,-1.48773068258577,
14.5187400048071));
#257264=CARTESIAN_POINT('Ctrl Pts',(3.68465399269227,-1.38031806143427,
14.5245957850627));
#257265=CARTESIAN_POINT('Ctrl Pts',(3.7238089050595,-1.27091197260396,14.5304515653183));
#257266=CARTESIAN_POINT('Ctrl Pts',(3.75805282899773,-1.15996893685224,
14.5363073455739));
#257267=CARTESIAN_POINT('Ctrl Pts',(3.79229172818833,-1.04904218021499,
14.5421622665874));
#257268=CARTESIAN_POINT('Ctrl Pts',(3.82162095015235,-0.936579319396514,
14.548017187601));
#257269=CARTESIAN_POINT('Ctrl Pts',(3.84591638825488,-0.823052935449811,
14.5538721086146));
#257270=CARTESIAN_POINT('Ctrl Pts',(3.87021412353039,-0.709515817399792,
14.5597275832204));
#257271=CARTESIAN_POINT('Ctrl Pts',(3.88947704241376,-0.594915379960817,
14.5655830578263));
#257272=CARTESIAN_POINT('Ctrl Pts',(3.90363211524196,-0.479734623361267,
14.5714385324321));
#257273=CARTESIAN_POINT('Ctrl Pts',(3.91779194185614,-0.364515184893195,
14.5772959735183));
#257274=CARTESIAN_POINT('Ctrl Pts',(3.92684046104926,-0.248715449173139,
14.5831534146045));
#257275=CARTESIAN_POINT('Ctrl Pts',(3.93075654731549,-0.1328230617642,14.5890108556908));
#257276=CARTESIAN_POINT('Ctrl Pts',(3.934677047607,-0.0168000459946449,
14.5948748990047));
#257277=CARTESIAN_POINT('Ctrl Pts',(3.93345355472821,0.0993154171680395,
14.6007389423185));
#257278=CARTESIAN_POINT('Ctrl Pts',(3.92711707119533,0.215036064710605,
14.6066029856324));
#257279=CARTESIAN_POINT('Ctrl Pts',(3.92077630614251,0.330834903928005,
14.6124709912415));
#257280=CARTESIAN_POINT('Ctrl Pts',(3.90931571169151,0.446237986606797,
14.6183389968506));
#257281=CARTESIAN_POINT('Ctrl Pts',(3.89281791503712,0.56076526315925,14.6242070024597));
#257282=CARTESIAN_POINT('Ctrl Pts',(3.87629630083501,0.675457880510334,
14.6300834795943));
#257283=CARTESIAN_POINT('Ctrl Pts',(3.8547230483785,0.789271764541383,14.6359599567288));
#257284=CARTESIAN_POINT('Ctrl Pts',(3.8282314039091,0.901739052123255,14.6418364338633));
#257285=CARTESIAN_POINT('Ctrl Pts',(3.82242912045815,0.926371991851243,
14.643123518403));
#257286=CARTESIAN_POINT('Ctrl Pts',(3.81639108292966,0.950940400959883,
14.6444106029427));
#257287=CARTESIAN_POINT('Ctrl Pts',(3.8101190025785,0.975439483612509,14.6456976874824));
#257288=CARTESIAN_POINT('Ctrl Pts',(3.7814849989708,1.08728543930576,14.6515736299591));
#257289=CARTESIAN_POINT('Ctrl Pts',(3.74787473329744,1.19805401713487,14.6574495724358));
#257290=CARTESIAN_POINT('Ctrl Pts',(3.70938485811833,1.30726928150343,14.6633255149126));
#257291=CARTESIAN_POINT('Ctrl Pts',(3.6709443758916,1.41634439305701,14.6691939169609));
#257292=CARTESIAN_POINT('Ctrl Pts',(3.62763687322898,1.52386976951915,14.6750623190093));
#257293=CARTESIAN_POINT('Ctrl Pts',(3.57960957910569,1.62938155788469,14.6809307210576));
#257294=CARTESIAN_POINT('Ctrl Pts',(3.53163111810794,1.73478606412035,14.6867931562403));
#257295=CARTESIAN_POINT('Ctrl Pts',(3.4789425814707,1.83818068127895,14.692655591423));
#257296=CARTESIAN_POINT('Ctrl Pts',(3.4217401593197,1.93911920265331,14.6985180266056));
#257297=CARTESIAN_POINT('Ctrl Pts',(3.36275047708099,2.04321149590971,14.7045636305428));
#257298=CARTESIAN_POINT('Ctrl Pts',(3.29896035304039,2.1446912701522,14.7106092344799));
#257299=CARTESIAN_POINT('Ctrl Pts',(3.23063759276133,2.24309378855127,14.716654838417));
#257300=CARTESIAN_POINT('Ctrl Pts',(3.16446007356457,2.33840660266718,14.722510618672));
#257301=CARTESIAN_POINT('Ctrl Pts',(3.09403055220544,2.43083215083332,14.7283663989269));
#257302=CARTESIAN_POINT('Ctrl Pts',(3.01963729246406,2.51997611535513,14.7342221791819));
#257303=CARTESIAN_POINT('Ctrl Pts',(2.94525494874276,2.60910699942705,14.7400771001948));
#257304=CARTESIAN_POINT('Ctrl Pts',(2.86691028755852,2.69495694051926,14.7459320212078));
#257305=CARTESIAN_POINT('Ctrl Pts',(2.78493205208289,2.77716446493206,14.7517869422207));
#257306=CARTESIAN_POINT('Ctrl Pts',(2.70294606543257,2.8593797621992,14.7576424168259));
#257307=CARTESIAN_POINT('Ctrl Pts',(2.6173261129955,2.93795166587313,14.7634978914311));
#257308=CARTESIAN_POINT('Ctrl Pts',(2.52843749505405,3.01255586398075,14.7693533660362));
#257309=CARTESIAN_POINT('Ctrl Pts',(2.43951902509637,3.08718511687923,14.7752108071218));
#257310=CARTESIAN_POINT('Ctrl Pts',(2.34733002278658,3.15784374935065,14.7810682482074));
#257311=CARTESIAN_POINT('Ctrl Pts',(2.25226795372043,3.22424844958387,14.7869256892929));
#257312=CARTESIAN_POINT('Ctrl Pts',(2.15709873523312,3.29072799802166,14.7927897326061));
#257313=CARTESIAN_POINT('Ctrl Pts',(2.05905032507611,3.35294380777436,14.7986537759194));
#257314=CARTESIAN_POINT('Ctrl Pts',(1.95854825937223,3.41065649336165,14.8045178192326));
#257315=CARTESIAN_POINT('Ctrl Pts',(1.85797828508849,3.46840817502819,14.810385824841));
#257316=CARTESIAN_POINT('Ctrl Pts',(1.75495171967396,3.52165048464205,14.8162538304495));
#257317=CARTESIAN_POINT('Ctrl Pts',(1.64991616681404,3.5701912613312,14.8221218360579));
#257318=CARTESIAN_POINT('Ctrl Pts',(1.5447289761722,3.61880211539424,14.8279983131917));
#257319=CARTESIAN_POINT('Ctrl Pts',(1.43752739047302,3.66269773522737,14.8338747903256));
#257320=CARTESIAN_POINT('Ctrl Pts',(1.32877636253884,3.70173504972439,14.8397512674594));
#257321=CARTESIAN_POINT('Ctrl Pts',(1.30495736959239,3.71028512540014,14.8410383520053));
#257322=CARTESIAN_POINT('Ctrl Pts',(1.2810640935575,3.71860233585773,14.8423254365511));
#257323=CARTESIAN_POINT('Ctrl Pts',(1.25710148856665,3.72668550423074,14.843612521097));
#257324=CARTESIAN_POINT('Ctrl Pts',(1.14770472118026,3.76358768955593,14.8494884635801));
#257325=CARTESIAN_POINT('Ctrl Pts',(1.03650120846817,3.7957296649438,14.8553644060631));
#257326=CARTESIAN_POINT('Ctrl Pts',(0.923942742723827,3.82293327278517,
14.8612403485462));
#257327=CARTESIAN_POINT('Ctrl Pts',(0.811528720028424,3.85010197101729,
14.8671087506009));
#257328=CARTESIAN_POINT('Ctrl Pts',(0.697763599842017,3.87234480866924,
14.8729771526556));
#257329=CARTESIAN_POINT('Ctrl Pts',(0.583116587485802,3.88953262557327,
14.8788455547103));
#257330=CARTESIAN_POINT('Ctrl Pts',(0.468586145759477,3.90670296627272,
14.8847079898993));
#257331=CARTESIAN_POINT('Ctrl Pts',(0.35317600131364,3.91882844920775,14.8905704250883));
#257332=CARTESIAN_POINT('Ctrl Pts',(0.237367226659337,3.92583058723986,
14.8964328602773));
#257333=CARTESIAN_POINT('Ctrl Pts',(0.11794006692834,3.93305150344172,14.9024784642121));
#257334=CARTESIAN_POINT('Ctrl Pts',(-0.00191060819045115,3.93482355446359,
14.9085240681468));
#257335=CARTESIAN_POINT('Ctrl Pts',(-0.121649180496793,3.93111822219638,
14.9145696720816));
#257336=CARTESIAN_POINT('Ctrl Pts',(-0.237628125825234,3.9275292322814,
14.9204254523429));
#257337=CARTESIAN_POINT('Ctrl Pts',(-0.353501459878626,3.91880169457394,
14.9262812326042));
#257338=CARTESIAN_POINT('Ctrl Pts',(-0.468781480055529,3.90496260212015,
14.9321370128655));
#257339=CARTESIAN_POINT('Ctrl Pts',(-0.584044584734466,3.89112554033168,
14.9379919338848));
#257340=CARTESIAN_POINT('Ctrl Pts',(-0.698714138941152,3.87217846440888,
14.943846854904));
#257341=CARTESIAN_POINT('Ctrl Pts',(-0.812307938231669,3.84820020444439,
14.9497017759233));
#257342=CARTESIAN_POINT('Ctrl Pts',(-0.925912477999098,3.82421967729674,
14.9555572505348));
#257343=CARTESIAN_POINT('Ctrl Pts',(-1.0384406567731,3.79520710570084,14.9614127251463));
#257344=CARTESIAN_POINT('Ctrl Pts',(-1.14942152565754,3.76129221895283,
14.9672681997578));
#257345=CARTESIAN_POINT('Ctrl Pts',(-1.26043966593545,3.72736594235807,
14.9731256408496));
#257346=CARTESIAN_POINT('Ctrl Pts',(-1.3699090685031,3.68853419738089,14.9789830819414));
#257347=CARTESIAN_POINT('Ctrl Pts',(-1.47737565115394,3.64497601986316,
14.9848405230333));
#257348=CARTESIAN_POINT('Ctrl Pts',(-1.58496336499929,3.60136874565003,
14.9907045663527));
#257349=CARTESIAN_POINT('Ctrl Pts',(-1.69054337051291,3.55302456109311,
14.9965686096721));
#257350=CARTESIAN_POINT('Ctrl Pts',(-1.79368313646694,3.50016996815214,
15.0024326529916));
#257351=CARTESIAN_POINT('Ctrl Pts',(-1.89689259327681,3.44727966171324,
15.0083006586062));
#257352=CARTESIAN_POINT('Ctrl Pts',(-1.99765816949556,3.38987308202568,
15.0141686642208));
#257353=CARTESIAN_POINT('Ctrl Pts',(-2.09557492052084,3.32822095908371,
15.0200366698354));
#257354=CARTESIAN_POINT('Ctrl Pts',(-2.1936330320506,3.26647983017382,15.0259131469753));
#257355=CARTESIAN_POINT('Ctrl Pts',(-2.28883377281264,3.2004811604603,15.0317896241152));
#257356=CARTESIAN_POINT('Ctrl Pts',(-2.38080391894879,3.13053696664296,
15.0376661012551));
#257357=CARTESIAN_POINT('Ctrl Pts',(-2.40094750930153,3.11521756956682,
15.0389531857406));
#257358=CARTESIAN_POINT('Ctrl Pts',(-2.4209362616762,3.09970904455408,15.0402402702261));
#257359=CARTESIAN_POINT('Ctrl Pts',(-2.44076649082374,3.08401490548797,
15.0415273547117));
#257360=CARTESIAN_POINT('Ctrl Pts',(-2.53021382122752,3.01322405218999,
15.0473329493106));
#257361=CARTESIAN_POINT('Ctrl Pts',(-2.6167437016043,2.93840781332431,15.0531385439095));
#257362=CARTESIAN_POINT('Ctrl Pts',(-2.69996564784677,2.85983819480183,
15.0589441385085));
#257363=CARTESIAN_POINT('Ctrl Pts',(-2.78308030073049,2.78136987165451,
15.0647422482819));
#257364=CARTESIAN_POINT('Ctrl Pts',(-2.86289519146216,2.69915807542079,
15.0705403580554));
#257365=CARTESIAN_POINT('Ctrl Pts',(-2.93905099343468,2.61351645450925,
15.0763384678288));
#257366=CARTESIAN_POINT('Ctrl Pts',(-3.01813108930501,2.5245862953256,15.0823592182494));
#257367=CARTESIAN_POINT('Ctrl Pts',(-3.09326507449529,2.43195788925591,
15.0883799686699));
#257368=CARTESIAN_POINT('Ctrl Pts',(-3.16409036142845,2.33602679452005,
15.0944007190904));
#257369=CARTESIAN_POINT('Ctrl Pts',(-3.23217814387143,2.24380358172803,
15.1001887583985));
#257370=CARTESIAN_POINT('Ctrl Pts',(-3.29628383170549,2.14852861894465,
15.1059767977066));
#257371=CARTESIAN_POINT('Ctrl Pts',(-3.35612529732445,2.05058820553003,
15.1117648370147));
#257372=CARTESIAN_POINT('Ctrl Pts',(-3.41594578615709,1.95268212408076,
15.1175508473874));
#257373=CARTESIAN_POINT('Ctrl Pts',(-3.47150480282969,1.85211280996971,
15.1233368577602));
#257374=CARTESIAN_POINT('Ctrl Pts',(-3.52256370317595,1.74929527440833,
15.129122868133));
#257375=CARTESIAN_POINT('Ctrl Pts',(-3.57361774512906,1.64648752221494,
15.1349083279511));
#257376=CARTESIAN_POINT('Ctrl Pts',(-3.620172334303,1.54143235359451,15.1406937877693));
#257377=CARTESIAN_POINT('Ctrl Pts',(-3.66203532518342,1.43456832430831,
15.1464792475874));
#257378=CARTESIAN_POINT('Ctrl Pts',(-3.70390502428713,1.32768717088085,
15.1522656344811));
#257379=CARTESIAN_POINT('Ctrl Pts',(-3.74108147791742,1.21899697566816,
15.1580520213748));
#257380=CARTESIAN_POINT('Ctrl Pts',(-3.77342142421475,1.10895435220624,
15.1638384082686));
#257381=CARTESIAN_POINT('Ctrl Pts',(-3.80579112984675,0.998810467127175,
15.1696301198163));
#257382=CARTESIAN_POINT('Ctrl Pts',(-3.83331532668721,0.887312076957398,
15.175421831364));
#257383=CARTESIAN_POINT('Ctrl Pts',(-3.85590123032483,0.774928836719529,
15.1812135429117));
#257384=CARTESIAN_POINT('Ctrl Pts',(-3.87849950850775,0.662484023054278,
15.1870084276686));
#257385=CARTESIAN_POINT('Ctrl Pts',(-3.89615404312042,0.549153812219911,
15.1928033124255));
#257386=CARTESIAN_POINT('Ctrl Pts',(-3.9088238041303,0.435414134203678,
15.1985981971824));
#257387=CARTESIAN_POINT('Ctrl Pts',(-3.92151034391662,0.321523828829201,
15.2044007562021));
#257388=CARTESIAN_POINT('Ctrl Pts',(-3.92919891029343,0.207223395534366,
15.2102033152218));
#257389=CARTESIAN_POINT('Ctrl Pts',(-3.93190054507825,0.0929898038138043,
15.2160058742415));
#257390=CARTESIAN_POINT('Ctrl Pts',(-3.93265024458662,0.0612901573504407,
15.2176160754681));
#257391=CARTESIAN_POINT('Ctrl Pts',(-3.93301623138631,0.0295956320002337,
15.2192262766947));
#257392=CARTESIAN_POINT('Ctrl Pts',(-3.93299944805027,-0.0020836593426039,
15.2208364779214));
#257393=CARTESIAN_POINT('',(-3.93299842594645,0.00351873595700912,16.4708364780091));
#257394=CARTESIAN_POINT('Ctrl Pts',(-3.93299944804982,-0.00208366020134649,
15.220836477965));
#257395=CARTESIAN_POINT('Ctrl Pts',(-3.93293480477982,-0.124100649844272,
15.2270383814188));
#257396=CARTESIAN_POINT('Ctrl Pts',(-3.92719245864474,-0.2459628104,15.2332402848725));
#257397=CARTESIAN_POINT('Ctrl Pts',(-3.9158126229022,-0.367288037267423,
15.2394421883262));
#257398=CARTESIAN_POINT('Ctrl Pts',(-3.9050308910257,-0.482236626643941,
15.245318130798));
#257399=CARTESIAN_POINT('Ctrl Pts',(-3.88916561621277,-0.596899701881591,
15.2511940732698));
#257400=CARTESIAN_POINT('Ctrl Pts',(-3.868237794927,-0.710792066569598,
15.2570700157417));
#257401=CARTESIAN_POINT('Ctrl Pts',(-3.84733682971402,-0.824538276452734,
15.2629384177851));
#257402=CARTESIAN_POINT('Ctrl Pts',(-3.82138631192933,-0.937515340376091,
15.2688068198285));
#257403=CARTESIAN_POINT('Ctrl Pts',(-3.79045908201708,-1.04924208243579,
15.2746752218719));
#257404=CARTESIAN_POINT('Ctrl Pts',(-3.75956329825118,-1.1608552231322,
15.2805376570495));
#257405=CARTESIAN_POINT('Ctrl Pts',(-3.72370097727427,-1.27122017527289,
15.2864000922272));
#257406=CARTESIAN_POINT('Ctrl Pts',(-3.68299607864721,-1.37986553137226,
15.2922625274048));
#257407=CARTESIAN_POINT('Ctrl Pts',(-3.64101937647165,-1.49190545554763,
15.2983081313438));
#257408=CARTESIAN_POINT('Ctrl Pts',(-3.59389259531413,-1.60211612205712,
15.3043537352828));
#257409=CARTESIAN_POINT('Ctrl Pts',(-3.54180752890365,-1.70999661642982,
15.3103993392218));
#257410=CARTESIAN_POINT('Ctrl Pts',(-3.49135786229038,-1.81448981093368,
15.3162551194716));
#257411=CARTESIAN_POINT('Ctrl Pts',(-3.43625681438112,-1.91679657478375,
15.3221108997215));
#257412=CARTESIAN_POINT('Ctrl Pts',(-3.37672740306017,-2.01648234443611,
15.3279666799713));
#257413=CARTESIAN_POINT('Ctrl Pts',(-3.31720672672778,-2.11615348679687,
15.3338216009791));
#257414=CARTESIAN_POINT('Ctrl Pts',(-3.25325919064256,-2.21320404541458,
15.3396765219869));
#257415=CARTESIAN_POINT('Ctrl Pts',(-3.1851529323662,-2.30722556275692,
15.3455314429947));
#257416=CARTESIAN_POINT('Ctrl Pts',(-3.11704023453342,-2.40125596998517,
15.3513869175948));
#257417=CARTESIAN_POINT('Ctrl Pts',(-3.04476827498617,-2.49225643230999,
15.3572423921948));
#257418=CARTESIAN_POINT('Ctrl Pts',(-2.9686471125496,-2.57984947645224,
15.3630978667948));
#257419=CARTESIAN_POINT('Ctrl Pts',(-2.8925003858707,-2.66747193751004,
15.3689553078752));
#257420=CARTESIAN_POINT('Ctrl Pts',(-2.81250215638256,-2.7516843935142,
15.3748127489556));
#257421=CARTESIAN_POINT('Ctrl Pts',(-2.72900066703397,-2.83214483374847,
15.380670190036));
#257422=CARTESIAN_POINT('Ctrl Pts',(-2.64540505879733,-2.91269596514558,
15.386534233344));
#257423=CARTESIAN_POINT('Ctrl Pts',(-2.55829860688726,-2.98948635341672,
15.392398276652));
#257424=CARTESIAN_POINT('Ctrl Pts',(-2.46806415185481,-3.06221298121623,
15.3982623199601));
#257425=CARTESIAN_POINT('Ctrl Pts',(-2.37776872599902,-3.13498874991623,
15.4041303255633));
#257426=CARTESIAN_POINT('Ctrl Pts',(-2.28434142003608,-3.20369504651285,
15.4099983311666));
#257427=CARTESIAN_POINT('Ctrl Pts',(-2.18819425914149,-3.26807204392134,
15.4158663367698));
#257428=CARTESIAN_POINT('Ctrl Pts',(-2.09190829246281,-3.33254198114751,
15.4217428138985));
#257429=CARTESIAN_POINT('Ctrl Pts',(-1.99289498611017,-3.39266993270988,
15.4276192910271));
#257430=CARTESIAN_POINT('Ctrl Pts',(-1.89159118139578,-3.4482418422242,
15.4334957681558));
#257431=CARTESIAN_POINT('Ctrl Pts',(-1.86940330188646,-3.46041337749755,
15.4347828527509));
#257432=CARTESIAN_POINT('Ctrl Pts',(-1.84710561964617,-3.4723665379636,
15.436069937346));
#257433=CARTESIAN_POINT('Ctrl Pts',(-1.82470284365832,-3.48409938611763,
15.437357021941));
#257434=CARTESIAN_POINT('Ctrl Pts',(-1.722427185683,-3.53766349645506,15.4432329644538));
#257435=CARTESIAN_POINT('Ctrl Pts',(-1.61762224335903,-3.58680871003884,
15.4491089069666));
#257436=CARTESIAN_POINT('Ctrl Pts',(-1.51070636986404,-3.6312883752261,
15.4549848494793));
#257437=CARTESIAN_POINT('Ctrl Pts',(-1.40392769843921,-3.67571096093635,
15.4608532515638));
#257438=CARTESIAN_POINT('Ctrl Pts',(-1.2950438607618,-3.71547974793598,
15.4667216536482));
#257439=CARTESIAN_POINT('Ctrl Pts',(-1.18449807480459,-3.75039375409892,
15.4725900557327));
#257440=CARTESIAN_POINT('Ctrl Pts',(-1.07406468943663,-3.78527226044763,
15.4784524909515));
#257441=CARTESIAN_POINT('Ctrl Pts',(-0.961973108392244,-3.81530568121076,
15.4843149261704));
#257442=CARTESIAN_POINT('Ctrl Pts',(-0.848686199069306,-3.8403412264419,
15.4901773613892));
#257443=CARTESIAN_POINT('Ctrl Pts',(-0.731859699853181,-3.86615899411516,
15.4962229653128));
#257444=CARTESIAN_POINT('Ctrl Pts',(-0.613762362204732,-3.88666126873163,
15.5022685692364));
#257445=CARTESIAN_POINT('Ctrl Pts',(-0.494918745659073,-3.90173607964394,
15.50831417316));
#257446=CARTESIAN_POINT('Ctrl Pts',(-0.379806654910923,-3.91633756226612,
15.514169953451));
#257447=CARTESIAN_POINT('Ctrl Pts',(-0.263994888467731,-3.92584725919359,
15.520025733742));
#257448=CARTESIAN_POINT('Ctrl Pts',(-0.147969365777272,-3.93021552421638,
15.525881514033));
#257449=CARTESIAN_POINT('Ctrl Pts',(-0.0319608679768984,-3.93458314826614,
15.5317364350819));
#257450=CARTESIAN_POINT('Ctrl Pts',(0.0842609113420141,-3.93381082503105,
15.5375913561308));
#257451=CARTESIAN_POINT('Ctrl Pts',(0.200207372658188,-3.92790096717487,
15.5434462771797));
#257452=CARTESIAN_POINT('Ctrl Pts',(0.316164796896931,-3.92199055053223,
15.5493017518207));
#257453=CARTESIAN_POINT('Ctrl Pts',(0.431846439140856,-3.91094165463097,
15.5551572264617));
#257454=CARTESIAN_POINT('Ctrl Pts',(0.546766853014029,-3.8948087255275,
15.5610127011027));
#257455=CARTESIAN_POINT('Ctrl Pts',(0.661725861319464,-3.87867037840282,
15.5668701422239));
#257456=CARTESIAN_POINT('Ctrl Pts',(0.775922724378473,-3.85744466028164,
15.5727275833451));
#257457=CARTESIAN_POINT('Ctrl Pts',(0.888880940185533,-3.83123735549951,
15.5785850244663));
#257458=CARTESIAN_POINT('Ctrl Pts',(1.00196647708577,-3.80500051109806,
15.5844490678148));
#257459=CARTESIAN_POINT('Ctrl Pts',(1.11381017790052,-3.7737709664274,15.5903131111632));
#257460=CARTESIAN_POINT('Ctrl Pts',(1.22394939954868,-3.73770475925325,
15.5961771545116));
#257461=CARTESIAN_POINT('Ctrl Pts',(1.33416304153472,-3.70161418238334,
15.602045160155));
#257462=CARTESIAN_POINT('Ctrl Pts',(1.4426695257927,-3.66068058069492,15.6079131657985));
#257463=CARTESIAN_POINT('Ctrl Pts',(1.549026536114,-3.6151079915287,15.6137811714419));
#257464=CARTESIAN_POINT('Ctrl Pts',(1.6555370919682,-3.569469610108,15.6196576486102));
#257465=CARTESIAN_POINT('Ctrl Pts',(1.75989161071668,-3.51917905436695,
15.6255341257784));
#257466=CARTESIAN_POINT('Ctrl Pts',(1.86167264643179,-3.46448610294913,
15.6314106029467));
#257467=CARTESIAN_POINT('Ctrl Pts',(1.8839650436415,-3.45250708358652,15.6326976871496));
#257468=CARTESIAN_POINT('Ctrl Pts',(1.90613410120014,-3.44031703945303,
15.6339847713526));
#257469=CARTESIAN_POINT('Ctrl Pts',(1.92817562946053,-3.42791886455244,
15.6352718555555));
#257470=CARTESIAN_POINT('Ctrl Pts',(2.02880210811891,-3.37131731372989,
15.6411477979834));
#257471=CARTESIAN_POINT('Ctrl Pts',(2.12710017692677,-3.31018780155748,
15.6470237404112));
#257472=CARTESIAN_POINT('Ctrl Pts',(2.22263512295192,-3.24474684840289,
15.652899682839));
#257473=CARTESIAN_POINT('Ctrl Pts',(2.31804747172299,-3.17938987374513,
15.6587680848386));
#257474=CARTESIAN_POINT('Ctrl Pts',(2.41070341192378,-3.10973269237195,
15.6646364868382));
#257475=CARTESIAN_POINT('Ctrl Pts',(2.50019298954164,-3.03603755165295,
15.6705048888378));
#257476=CARTESIAN_POINT('Ctrl Pts',(2.58959157607271,-2.96241734257543,
15.6763673239718));
#257477=CARTESIAN_POINT('Ctrl Pts',(2.6758298872504,-2.88476760181817,15.6822297591059));
#257478=CARTESIAN_POINT('Ctrl Pts',(2.75852768418662,-2.80339330376171,
15.6880921942399));
#257479=CARTESIAN_POINT('Ctrl Pts',(2.84380933197121,-2.71947650691013,
15.6941377981954));
#257480=CARTESIAN_POINT('Ctrl Pts',(2.92532521685751,-2.63159883548661,
15.7001834021508));
#257481=CARTESIAN_POINT('Ctrl Pts',(3.00269573325262,-2.54013923506301,
15.7062290061062));
#257482=CARTESIAN_POINT('Ctrl Pts',(3.07763692057785,-2.45155134180103,
15.7120847863133));
#257483=CARTESIAN_POINT('Ctrl Pts',(3.1486888788664,-2.35960343011601,15.7179405665204));
#257484=CARTESIAN_POINT('Ctrl Pts',(3.21554531710447,-2.26467598425195,
15.7237963467274));
#257485=CARTESIAN_POINT('Ctrl Pts',(3.2823919452343,-2.16976246746553,15.7296512676928));
#257486=CARTESIAN_POINT('Ctrl Pts',(3.34504403985302,-2.07187062323162,
15.7355061886582));
#257487=CARTESIAN_POINT('Ctrl Pts',(3.40323751023743,-1.97141153717658,
15.7413611096237));
#257488=CARTESIAN_POINT('Ctrl Pts',(3.46143648291255,-1.87094295254563,
15.7472165841817));
#257489=CARTESIAN_POINT('Ctrl Pts',(3.5151757864058,-1.7679070007335,15.7530720587398));
#257490=CARTESIAN_POINT('Ctrl Pts',(3.56423668595832,-1.66274046275083,
15.7589275332978));
#257491=CARTESIAN_POINT('Ctrl Pts',(3.61331406194108,-1.55753860602876,
15.7647849743367));
#257492=CARTESIAN_POINT('Ctrl Pts',(3.6577097353157,-1.45020511416891,15.7706424153756));
#257493=CARTESIAN_POINT('Ctrl Pts',(3.69725289849194,-1.34119722807383,
15.7764998564144));
#257494=CARTESIAN_POINT('Ctrl Pts',(3.73684063283831,-1.23206647348149,
15.7823638996819));
#257495=CARTESIAN_POINT('Ctrl Pts',(3.77156479959599,-1.12125794602727,
15.7882279429493));
#257496=CARTESIAN_POINT('Ctrl Pts',(3.8013042852138,-1.00924463397891,15.7940919862167));
#257497=CARTESIAN_POINT('Ctrl Pts',(3.83106386560749,-0.897155635268339,
15.7999599917798));
#257498=CARTESIAN_POINT('Ctrl Pts',(3.85583197013601,-0.783860633166325,
15.8058279973429));
#257499=CARTESIAN_POINT('Ctrl Pts',(3.87553881180354,-0.669841711305314,
15.811696002906));
#257500=CARTESIAN_POINT('Ctrl Pts',(3.8952741038582,-0.555658182526408,
15.8175724799956));
#257501=CARTESIAN_POINT('Ctrl Pts',(3.90993349909001,-0.440749056120797,
15.8234489570851));
#257502=CARTESIAN_POINT('Ctrl Pts',(3.9194991176761,-0.3256004707249,15.8293254341746));
#257503=CARTESIAN_POINT('Ctrl Pts',(3.92159421036448,-0.300380255516758,
15.8306125191732));
#257504=CARTESIAN_POINT('Ctrl Pts',(3.9234451470044,-0.275148547052067,
15.8318996041717));
#257505=CARTESIAN_POINT('Ctrl Pts',(3.92505207281976,-0.249910435262891,
15.8331866891702));
#257506=CARTESIAN_POINT('Ctrl Pts',(3.93238818786376,-0.134690622494353,
15.8390626316252));
#257507=CARTESIAN_POINT('Ctrl Pts',(3.93465869679811,-0.0189574273576847,
15.8449385740802));
#257508=CARTESIAN_POINT('Ctrl Pts',(3.93180842280314,0.0968066442672893,
15.8508145165352));
#257509=CARTESIAN_POINT('Ctrl Pts',(3.92896180648326,0.212422159170078,
15.8566829185614));
#257510=CARTESIAN_POINT('Ctrl Pts',(3.92100748590174,0.328068062832801,
15.8625513205875));
#257511=CARTESIAN_POINT('Ctrl Pts',(3.9079421187654,0.443257708764739,15.8684197226136));
#257512=CARTESIAN_POINT('Ctrl Pts',(3.89489003621609,0.558330232318181,
15.8742821577735));
#257513=CARTESIAN_POINT('Ctrl Pts',(3.8767372904962,0.672947013189608,15.8801445929335));
#257514=CARTESIAN_POINT('Ctrl Pts',(3.85353255723104,0.786623054811122,
15.8860070280934));
#257515=CARTESIAN_POINT('Ctrl Pts',(3.82960280395371,0.90385084616139,15.8920526320389));
#257516=CARTESIAN_POINT('Ctrl Pts',(3.80030019108715,1.02007769942268,15.8980982359843));
#257517=CARTESIAN_POINT('Ctrl Pts',(3.76573577626643,1.13477886098881,15.9041438399298));
#257518=CARTESIAN_POINT('Ctrl Pts',(3.73225663690586,1.24587856259837,15.909999620161));
#257519=CARTESIAN_POINT('Ctrl Pts',(3.69384130981319,1.35554652495435,15.9158554003922));
#257520=CARTESIAN_POINT('Ctrl Pts',(3.65064207360499,1.46331864282018,15.9217111806233));
#257521=CARTESIAN_POINT('Ctrl Pts',(3.60744917619579,1.57107494684637,15.9275661016122));
#257522=CARTESIAN_POINT('Ctrl Pts',(3.55947391903185,1.676935576517,15.933421022601));
#257523=CARTESIAN_POINT('Ctrl Pts',(3.50691722930669,1.78045515158116,15.9392759435898));
#257524=CARTESIAN_POINT('Ctrl Pts',(3.4543555702644,1.88398451458289,15.9451314181705));
#257525=CARTESIAN_POINT('Ctrl Pts',(3.39721180439954,1.98517201489416,15.9509868927512));
#257526=CARTESIAN_POINT('Ctrl Pts',(3.33573311171859,2.08359631584052,15.956842367332));
#257527=CARTESIAN_POINT('Ctrl Pts',(3.27423377226964,2.18205367122606,15.9626998083928));
#257528=CARTESIAN_POINT('Ctrl Pts',(3.20839682966444,2.27774563208528,15.9685572494536));
#257529=CARTESIAN_POINT('Ctrl Pts',(3.13851272629348,2.37027991319462,15.9744146905145));
#257530=CARTESIAN_POINT('Ctrl Pts',(3.06854985290432,2.46291849451896,15.9802787338026));
#257531=CARTESIAN_POINT('Ctrl Pts',(2.99453096284138,2.55239196280046,15.9861427770908));
#257532=CARTESIAN_POINT('Ctrl Pts',(2.91678677096562,2.63834113274231,15.992006820379));
#257533=CARTESIAN_POINT('Ctrl Pts',(2.83899004785703,2.72434837796604,15.9978748259622));
#257534=CARTESIAN_POINT('Ctrl Pts',(2.75746330004798,2.80682629016288,16.0037428315454));
#257535=CARTESIAN_POINT('Ctrl Pts',(2.67257282521114,2.88545377608843,16.0096108371286));
#257536=CARTESIAN_POINT('Ctrl Pts',(2.58755979565011,2.96419477498312,16.0154873142371));
#257537=CARTESIAN_POINT('Ctrl Pts',(2.4991736615527,3.0390739884535,16.0213637913456));
#257538=CARTESIAN_POINT('Ctrl Pts',(2.40781239245791,3.10981164746775,16.0272402684541));
#257539=CARTESIAN_POINT('Ctrl Pts',(2.38780215563081,3.12530483537434,16.028527353231));
#257540=CARTESIAN_POINT('Ctrl Pts',(2.36764930105252,3.14059951784754,16.0298144380079));
#257541=CARTESIAN_POINT('Ctrl Pts',(2.34735817656715,3.15569304446794,16.0311015227848));
#257542=CARTESIAN_POINT('Ctrl Pts',(2.25472287612864,3.2245996925034,16.0369774654948));
#257543=CARTESIAN_POINT('Ctrl Pts',(2.1588980534314,3.28953760282234,16.0428534082048));
#257544=CARTESIAN_POINT('Ctrl Pts',(2.06025831770452,3.35019770526,16.0487293509148));
#257545=CARTESIAN_POINT('Ctrl Pts',(1.96174516350281,3.41077996433943,16.0545977531972));
#257546=CARTESIAN_POINT('Ctrl Pts',(1.86042462856527,3.46709511852478,16.0604661554796));
#257547=CARTESIAN_POINT('Ctrl Pts',(1.75670302621306,3.51887531431477,16.0663345577619));
#257548=CARTESIAN_POINT('Ctrl Pts',(1.65308688575583,3.5706028611151,16.072196993179));
#257549=CARTESIAN_POINT('Ctrl Pts',(1.54707490120607,3.61780443822545,16.0780594285962));
#257550=CARTESIAN_POINT('Ctrl Pts',(1.43910033353993,3.66025671640737,16.0839218640133));
#257551=CARTESIAN_POINT('Ctrl Pts',(1.32775216243419,3.70403539167324,16.0899674678627));
#257552=CARTESIAN_POINT('Ctrl Pts',(1.2143171332307,3.74276287715576,16.0960130717121));
#257553=CARTESIAN_POINT('Ctrl Pts',(1.09929582583472,3.7762465077511,16.1020586755615));
#257554=CARTESIAN_POINT('Ctrl Pts',(0.987886023861116,3.80867879997971,
16.1079144560506));
#257555=CARTESIAN_POINT('Ctrl Pts',(0.874988493563392,3.83619148904333,
16.1137702365396));
#257556=CARTESIAN_POINT('Ctrl Pts',(0.761075402106802,3.85865951235762,
16.1196260170287));
#257557=CARTESIAN_POINT('Ctrl Pts',(0.647179025582752,3.88112423884721,
16.1254809382752));
#257558=CARTESIAN_POINT('Ctrl Pts',(0.532267789068168,3.89854569164663,
16.1313358595217));
#257559=CARTESIAN_POINT('Ctrl Pts',(0.416824652016948,3.91084980656007,
16.1371907807682));
#257560=CARTESIAN_POINT('Ctrl Pts',(0.301370599646478,3.92315508484576,
16.1430462556062));
#257561=CARTESIAN_POINT('Ctrl Pts',(0.185384957217368,3.93034201964616,
16.1489017304441));
#257562=CARTESIAN_POINT('Ctrl Pts',(0.0693557111087275,3.93238843266234,
16.1547572052821));
#257563=CARTESIAN_POINT('Ctrl Pts',(-0.0467125017996223,3.93443553293772,
16.1606146465994));
#257564=CARTESIAN_POINT('Ctrl Pts',(-0.162823935041237,3.93133867128822,
16.1664720879166));
#257565=CARTESIAN_POINT('Ctrl Pts',(-0.27849140397048,3.92312777486466,
16.1723295292339));
#257566=CARTESIAN_POINT('Ctrl Pts',(-0.394289247684611,3.91490762351519,
16.1781935727762));
#257567=CARTESIAN_POINT('Ctrl Pts',(-0.509641716381478,3.90156196173147,
16.1840576163185));
#257568=CARTESIAN_POINT('Ctrl Pts',(-0.624067450912624,3.88317251956585,
16.1899216598607));
#257569=CARTESIAN_POINT('Ctrl Pts',(-0.738570502125945,3.86477065178059,
16.1957896656969));
#257570=CARTESIAN_POINT('Ctrl Pts',(-0.852145169060522,3.84131830056579,
16.2016576715331));
#257571=CARTESIAN_POINT('Ctrl Pts',(-0.964322658995429,3.81294778476548,
16.2075256773693));
#257572=CARTESIAN_POINT('Ctrl Pts',(-1.07666209731249,3.78453631102309,
16.2134021547272));
#257573=CARTESIAN_POINT('Ctrl Pts',(-1.18759993953065,3.75119262138117,
16.2192786320852));
#257574=CARTESIAN_POINT('Ctrl Pts',(-1.29668480014169,3.71309810388596,
16.2251551094432));
#257575=CARTESIAN_POINT('Ctrl Pts',(-1.32057686791984,3.70475453733719,
16.2264421917619));
#257576=CARTESIAN_POINT('Ctrl Pts',(-1.34438013266287,3.69618324772217,
16.2277292740806));
#257577=CARTESIAN_POINT('Ctrl Pts',(-1.36809000354252,3.68738643787263,
16.2290163563994));
#257578=CARTESIAN_POINT('Ctrl Pts',(-1.47633314070521,3.64722618984889,
16.2348922984774));
#257579=CARTESIAN_POINT('Ctrl Pts',(-1.58298499780571,3.6022294401552,16.2407682405554));
#257580=CARTESIAN_POINT('Ctrl Pts',(-1.68758233870674,3.55254202650512,
16.2466441826334));
#257581=CARTESIAN_POINT('Ctrl Pts',(-1.79204545284052,3.50291837528771,
16.2525125842835));
#257582=CARTESIAN_POINT('Ctrl Pts',(-1.89445892456106,3.44861620653612,
16.2583809859336));
#257583=CARTESIAN_POINT('Ctrl Pts',(-1.99437681718968,3.3898303956181,16.2642493875837));
#257584=CARTESIAN_POINT('Ctrl Pts',(-2.09419311545055,3.33110435685035,
16.270111822369));
#257585=CARTESIAN_POINT('Ctrl Pts',(-2.19151852827018,3.26790395220451,
16.2759742571543));
#257586=CARTESIAN_POINT('Ctrl Pts',(-2.28592978297765,3.20047090711597,
16.2818366919396));
#257587=CARTESIAN_POINT('Ctrl Pts',(-2.38329087750043,3.13093094498788,
16.287882296026));
#257588=CARTESIAN_POINT('Ctrl Pts',(-2.47755231355264,3.05688969211424,
16.2939279001124));
#257589=CARTESIAN_POINT('Ctrl Pts',(-2.568279870193,2.97866203325611,16.2999735041989));
#257590=CARTESIAN_POINT('Ctrl Pts',(-2.65615869777351,2.90289062267937,
16.3058292840612));
#257591=CARTESIAN_POINT('Ctrl Pts',(-2.74072191081018,2.82319206033073,
16.3116850639235));
#257592=CARTESIAN_POINT('Ctrl Pts',(-2.82160745935929,2.7398942215509,16.3175408437858));
#257593=CARTESIAN_POINT('Ctrl Pts',(-2.9024811392813,2.65660860536218,16.3233957644085));
#257594=CARTESIAN_POINT('Ctrl Pts',(-2.97967794029489,2.56972505896492,
16.3292506850312));
#257595=CARTESIAN_POINT('Ctrl Pts',(-3.05287270506265,2.47960828492798,
16.3351056056539));
#257596=CARTESIAN_POINT('Ctrl Pts',(-3.12607439054958,2.38948299016025,
16.3409610798717));
#257597=CARTESIAN_POINT('Ctrl Pts',(-3.19527302732344,2.29612418043976,
16.3468165540895));
#257598=CARTESIAN_POINT('Ctrl Pts',(-3.2601842350632,2.19992903372935,16.3526720283073));
#257599=CARTESIAN_POINT('Ctrl Pts',(-3.32511724237395,2.10370158115063,
16.3585294690086));
#257600=CARTESIAN_POINT('Ctrl Pts',(-3.38575972672887,2.00463623941591,
16.36438690971));
#257601=CARTESIAN_POINT('Ctrl Pts',(-3.44187144351535,1.90315789316429,
16.3702443504114));
#257602=CARTESIAN_POINT('Ctrl Pts',(-3.49804640681553,1.80156516524725,
16.3761083933471));
#257603=CARTESIAN_POINT('Ctrl Pts',(-3.54968020995711,1.69755436573442,
16.3819724362829));
#257604=CARTESIAN_POINT('Ctrl Pts',(-3.59657922647575,1.59157370790143,
16.3878364792186));
#257605=CARTESIAN_POINT('Ctrl Pts',(-3.64350993237871,1.48552143957325,
16.393704484453));
#257606=CARTESIAN_POINT('Ctrl Pts',(-3.68569933130791,1.37749704602172,
16.3995724896874));
#257607=CARTESIAN_POINT('Ctrl Pts',(-3.72300306814158,1.26796575450931,
16.4054404949218));
#257608=CARTESIAN_POINT('Ctrl Pts',(-3.76036065970673,1.15827633464857,
16.4113169716894));
#257609=CARTESIAN_POINT('Ctrl Pts',(-3.7928183979578,1.04707606996503,16.417193448457));
#257610=CARTESIAN_POINT('Ctrl Pts',(-3.82028256120574,0.934842314268731,
16.4230699252246));
#257611=CARTESIAN_POINT('Ctrl Pts',(-3.82629786656153,0.91026045078191,
16.4243570134878));
#257612=CARTESIAN_POINT('Ctrl Pts',(-3.83207381993411,0.885629034250463,
16.4256441017509));
#257613=CARTESIAN_POINT('Ctrl Pts',(-3.83760976837449,0.860953114679714,
16.426931190014));
#257614=CARTESIAN_POINT('Ctrl Pts',(-3.8719651963883,0.707817335396848,
16.4349187044658));
#257615=CARTESIAN_POINT('Ctrl Pts',(-3.89716537352266,0.552558641249351,
16.4429062189176));
#257616=CARTESIAN_POINT('Ctrl Pts',(-3.91300312232185,0.39610044773955,
16.4508937333694));
#257617=CARTESIAN_POINT('Ctrl Pts',(-3.92618403448921,0.265888652321806,
16.4575413149013));
#257618=CARTESIAN_POINT('Ctrl Pts',(-3.93288093123125,0.13484612770825,
16.4641888964331));
#257619=CARTESIAN_POINT('Ctrl Pts',(-3.93299842594567,0.00351873682833392,
16.470836477965));
#257620=CARTESIAN_POINT('',(-3.93299991974386,-0.00079454059141139,17.720836478003));
#257621=CARTESIAN_POINT('Ctrl Pts',(-3.93299842594645,0.0035187359570327,
16.4708364780091));
#257622=CARTESIAN_POINT('Ctrl Pts',(-3.93310067614775,-0.110769430492911,
16.476621561376));
#257623=CARTESIAN_POINT('Ctrl Pts',(-3.92821711002783,-0.225203848643301,
16.482406644743));
#257624=CARTESIAN_POINT('Ctrl Pts',(-3.91833624616476,-0.339308210910733,
16.4881917281099));
#257625=CARTESIAN_POINT('Ctrl Pts',(-3.90846305116049,-0.453324013083181,
16.4939723214861));
#257626=CARTESIAN_POINT('Ctrl Pts',(-3.89360030670427,-0.567009847050024,
16.4997529148622));
#257627=CARTESIAN_POINT('Ctrl Pts',(-3.87378859678277,-0.679890364276321,
16.5055335082384));
#257628=CARTESIAN_POINT('Ctrl Pts',(-3.85398502950259,-0.792724487447362,
16.5113117257824));
#257629=CARTESIAN_POINT('Ctrl Pts',(-3.82923661124358,-0.904753533642884,
16.5170899433263));
#257630=CARTESIAN_POINT('Ctrl Pts',(-3.79963558588898,-1.01550894355793,
16.5228681608703));
#257631=CARTESIAN_POINT('Ctrl Pts',(-3.77003912510385,-1.12624727464689,
16.5286454873953));
#257632=CARTESIAN_POINT('Ctrl Pts',(-3.73559165424352,-1.23571194940489,
16.5344228139203));
#257633=CARTESIAN_POINT('Ctrl Pts',(-3.69643597277664,-1.34344709578114,
16.5402001404453));
#257634=CARTESIAN_POINT('Ctrl Pts',(-3.65727627383656,-1.45119329605937,
16.5459780597387));
#257635=CARTESIAN_POINT('Ctrl Pts',(-3.61340755033825,-1.55720921625382,
16.5517559790322));
#257636=CARTESIAN_POINT('Ctrl Pts',(-3.56502136312672,-1.66105739830089,
16.5575338983257));
#257637=CARTESIAN_POINT('Ctrl Pts',(-3.51658769134419,-1.76500749344872,
16.5633174878741));
#257638=CARTESIAN_POINT('Ctrl Pts',(-3.46362788203505,-1.8667852161216,
16.5691010774226));
#257639=CARTESIAN_POINT('Ctrl Pts',(-3.40638025669218,-1.96597623251598,
16.5748846669711));
#257640=CARTESIAN_POINT('Ctrl Pts',(-3.34910430852904,-2.06521632289924,
16.5806711179058));
#257641=CARTESIAN_POINT('Ctrl Pts',(-3.28753654943814,-2.16186680105467,
16.5864575688405));
#257642=CARTESIAN_POINT('Ctrl Pts',(-3.22195851665732,-2.25554257706197,
16.5922440197752));
#257643=CARTESIAN_POINT('Ctrl Pts',(-3.15627465627497,-2.3493695238543,
16.5980398086878));
#257644=CARTESIAN_POINT('Ctrl Pts',(-3.08656785431739,-2.44021184282936,
16.6038355976004));
#257645=CARTESIAN_POINT('Ctrl Pts',(-3.01315999384475,-2.52771751813638,
16.6096313865131));
#257646=CARTESIAN_POINT('Ctrl Pts',(-2.94892519766469,-2.60428846274304,
16.6147029322183));
#257647=CARTESIAN_POINT('Ctrl Pts',(-2.88185724592194,-2.67830497406639,
16.6197744779234));
#257648=CARTESIAN_POINT('Ctrl Pts',(-2.81219345753973,-2.74955577455172,
16.6248460236286));
#257649=CARTESIAN_POINT('Ctrl Pts',(-2.73148029001437,-2.83210767029901,
16.6307219676107));
#257650=CARTESIAN_POINT('Ctrl Pts',(-2.64699592537828,-2.91123874359358,
16.6365979115928));
#257651=CARTESIAN_POINT('Ctrl Pts',(-2.55906200173616,-2.98658511870499,
16.6424738555749));
#257652=CARTESIAN_POINT('Ctrl Pts',(-2.4712409210588,-3.06183480407484,
16.6483422591345));
#257653=CARTESIAN_POINT('Ctrl Pts',(-2.37997939550461,-3.13330918391156,
16.654210662694));
#257654=CARTESIAN_POINT('Ctrl Pts',(-2.28563682562428,-3.20068013105811,
16.6600790662536));
#257655=CARTESIAN_POINT('Ctrl Pts',(-2.19139018116286,-3.26798257692961,
16.6659415029514));
#257656=CARTESIAN_POINT('Ctrl Pts',(-2.09406905775236,-3.33118965085894,
16.6718039396492));
#257657=CARTESIAN_POINT('Ctrl Pts',(-1.99406643804611,-3.39001298532293,
16.6776663763471));
#257658=CARTESIAN_POINT('Ctrl Pts',(-1.89093932453771,-3.45067420307932,
16.6837119797177));
#257659=CARTESIAN_POINT('Ctrl Pts',(-1.78496073760388,-3.5066729555298,
16.6897575830884));
#257660=CARTESIAN_POINT('Ctrl Pts',(-1.67659494708285,-3.55774062902515,
16.6958031864591));
#257661=CARTESIAN_POINT('Ctrl Pts',(-1.57163165694161,-3.60720486496306,
16.7016589682295));
#257662=CARTESIAN_POINT('Ctrl Pts',(-1.46442923095247,-3.65204285809281,
16.70751475));
#257663=CARTESIAN_POINT('Ctrl Pts',(-1.35543445374064,-3.69205720995935,
16.7133705317705));
#257664=CARTESIAN_POINT('Ctrl Pts',(-1.24645566980974,-3.73206569034482,
16.7192254542964));
#257665=CARTESIAN_POINT('Ctrl Pts',(-1.13568544499393,-3.76725179467923,
16.7250803768224));
#257666=CARTESIAN_POINT('Ctrl Pts',(-1.02358920258385,-3.79746680622145,
16.7309352993484));
#257667=CARTESIAN_POINT('Ctrl Pts',(-0.911482361374219,-3.82768467461992,
16.7367907754625));
#257668=CARTESIAN_POINT('Ctrl Pts',(-0.798049651887935,-3.85293040843941,
16.7426462515766));
#257669=CARTESIAN_POINT('Ctrl Pts',(-0.68376958058739,-3.87310575128841,
16.7485017276907));
#257670=CARTESIAN_POINT('Ctrl Pts',(-0.569451130022772,-3.89328786972655,
16.7543591702794));
#257671=CARTESIAN_POINT('Ctrl Pts',(-0.454285158019641,-3.90839613945071,
16.7602166128682));
#257672=CARTESIAN_POINT('Ctrl Pts',(-0.338757531693442,-3.91838389322958,
16.766074055457));
#257673=CARTESIAN_POINT('Ctrl Pts',(-0.223099688497213,-3.92838290469699,
16.7719381002574));
#257674=CARTESIAN_POINT('Ctrl Pts',(-0.107079788808458,-3.93324984519266,
16.7778021450578));
#257675=CARTESIAN_POINT('Ctrl Pts',(0.00881394883159336,-3.93299012385055,
16.7836661898582));
#257676=CARTESIAN_POINT('Ctrl Pts',(0.124785994932083,-3.93273022701684,
16.7895341969462));
#257677=CARTESIAN_POINT('Ctrl Pts',(0.240631297964359,-3.92733678968229,
16.7954022040342));
#257678=CARTESIAN_POINT('Ctrl Pts',(0.355866135827682,-3.91686715288776,
16.8012702111222));
#257679=CARTESIAN_POINT('Ctrl Pts',(0.471267335504422,-3.9063824013259,
16.8071466897135));
#257680=CARTESIAN_POINT('Ctrl Pts',(0.586055903834923,-3.89080688065476,
16.8130231683047));
#257681=CARTESIAN_POINT('Ctrl Pts',(0.699757634082706,-3.87024912034651,
16.818899646896));
#257682=CARTESIAN_POINT('Ctrl Pts',(0.724660660077218,-3.86574654647864,
16.8201867170117));
#257683=CARTESIAN_POINT('Ctrl Pts',(0.749511607663112,-3.86100516442516,
16.8214737871275));
#257684=CARTESIAN_POINT('Ctrl Pts',(0.77430559803329,-3.85602643155546,
16.8227608572433));
#257685=CARTESIAN_POINT('Ctrl Pts',(0.887499108740622,-3.83329671988012,
16.8286367966446));
#257686=CARTESIAN_POINT('Ctrl Pts',(0.999877666872273,-3.8055411024948,
16.8345127360458));
#257687=CARTESIAN_POINT('Ctrl Pts',(1.11096092379942,-3.7728311419663,16.8403886754471));
#257688=CARTESIAN_POINT('Ctrl Pts',(1.22190163071379,-3.74016315720823,
16.846257074421));
#257689=CARTESIAN_POINT('Ctrl Pts',(1.33154994972937,-3.70255358869003,
16.8521254733948));
#257690=CARTESIAN_POINT('Ctrl Pts',(1.43943494607293,-3.66012513939401,
16.8579938723687));
#257691=CARTESIAN_POINT('Ctrl Pts',(1.54721024728521,-3.61773983042772,
16.8638563044814));
#257692=CARTESIAN_POINT('Ctrl Pts',(1.65322541027905,-3.57054553709331,
16.869718736594));
#257693=CARTESIAN_POINT('Ctrl Pts',(1.75702455489567,-3.51871478149248,
16.8755811687067));
#257694=CARTESIAN_POINT('Ctrl Pts',(1.86406692654826,-3.46526456256678,
16.8816267737963));
#257695=CARTESIAN_POINT('Ctrl Pts',(1.96875209481662,-3.40688351012709,
16.887672378886));
#257696=CARTESIAN_POINT('Ctrl Pts',(2.07060191860303,-3.34381469203625,
16.8937179839756));
#257697=CARTESIAN_POINT('Ctrl Pts',(2.16925372742428,-3.28272619179566,
16.8995737611909));
#257698=CARTESIAN_POINT('Ctrl Pts',(2.26524520844887,-3.21724014283959,
16.9054295384062));
#257699=CARTESIAN_POINT('Ctrl Pts',(2.35816747105485,-3.14762373521022,
16.9112853156215));
#257700=CARTESIAN_POINT('Ctrl Pts',(2.45107609905883,-3.07801754248507,
16.9171402336112));
#257701=CARTESIAN_POINT('Ctrl Pts',(2.5409160739004,-3.00428244362256,16.9229951516008));
#257702=CARTESIAN_POINT('Ctrl Pts',(2.62730918114217,-2.92672777461213,
16.9288500695905));
#257703=CARTESIAN_POINT('Ctrl Pts',(2.71371045728507,-2.84916577241917,
16.9347055411919));
#257704=CARTESIAN_POINT('Ctrl Pts',(2.7966639107643,-2.76778375787002,16.9405610127934));
#257705=CARTESIAN_POINT('Ctrl Pts',(2.87582652079642,-2.68292952242208,
16.9464164843949));
#257706=CARTESIAN_POINT('Ctrl Pts',(2.95501571682069,-2.59804678950498,
16.9522739224995));
#257707=CARTESIAN_POINT('Ctrl Pts',(3.03041125641113,-2.50968981853689,
16.9581313606042));
#257708=CARTESIAN_POINT('Ctrl Pts',(3.1017093758898,-2.41824067195912,16.9639887987088));
#257709=CARTESIAN_POINT('Ctrl Pts',(3.17308785983102,-2.32668844746613,
16.9698528390895));
#257710=CARTESIAN_POINT('Ctrl Pts',(3.24035945181504,-2.23203741660605,
16.9757168794701));
#257711=CARTESIAN_POINT('Ctrl Pts',(3.30326278213121,-2.1346999770897,16.9815809198508));
#257712=CARTESIAN_POINT('Ctrl Pts',(3.36620861609834,-2.03729676686562,
16.9874489225515));
#257713=CARTESIAN_POINT('Ctrl Pts',(3.42478010300587,-1.93720388879762,
16.9933169252522));
#257714=CARTESIAN_POINT('Ctrl Pts',(3.47876187563326,-1.83485825410044,
16.9991849279529));
#257715=CARTESIAN_POINT('Ctrl Pts',(3.53282158126532,-1.7323648639214,17.0050614022368));
#257716=CARTESIAN_POINT('Ctrl Pts',(3.58227817363852,-1.62761259844179,
17.0109378765208));
#257717=CARTESIAN_POINT('Ctrl Pts',(3.62696439803191,-1.52105826824912,
17.0168143508047));
#257718=CARTESIAN_POINT('Ctrl Pts',(3.63675193954838,-1.49771986934259,
17.0181014641558));
#257719=CARTESIAN_POINT('Ctrl Pts',(3.64631082119755,-1.47429507487814,
17.0193885775068));
#257720=CARTESIAN_POINT('Ctrl Pts',(3.65563960785821,-1.45078877079272,
17.0206756908579));
#257721=CARTESIAN_POINT('Ctrl Pts',(3.69822748261985,-1.3434775447015,17.0265516342354));
#257722=CARTESIAN_POINT('Ctrl Pts',(3.73615643626882,-1.23411244653244,
17.0324275776128));
#257723=CARTESIAN_POINT('Ctrl Pts',(3.76922486550075,-1.12313530497926,
17.0383035209903));
#257724=CARTESIAN_POINT('Ctrl Pts',(3.80225085884139,-1.01230057762671,
17.044171923916));
#257725=CARTESIAN_POINT('Ctrl Pts',(3.83042861538971,-0.899858312969997,
17.0500403268418));
#257726=CARTESIAN_POINT('Ctrl Pts',(3.85360454877944,-0.78627029806956,
17.0559087297675));
#257727=CARTESIAN_POINT('Ctrl Pts',(3.87675691728429,-0.672797777481723,
17.0617711658035));
#257728=CARTESIAN_POINT('Ctrl Pts',(3.89491749686474,-0.558182226016013,
17.0676336018395));
#257729=CARTESIAN_POINT('Ctrl Pts',(3.90798268218396,-0.442899938756253,
17.0734960378755));
#257730=CARTESIAN_POINT('Ctrl Pts',(3.92145607976527,-0.3240157398426,17.0795416414837));
#257731=CARTESIAN_POINT('Ctrl Pts',(3.92951031765096,-0.204422885091915,
17.0855872450919));
#257732=CARTESIAN_POINT('Ctrl Pts',(3.93208883058094,-0.08465476017675,
17.0916328487001));
#257733=CARTESIAN_POINT('Ctrl Pts',(3.93458638220943,0.0313528316190549,
17.097488629744));
#257734=CARTESIAN_POINT('Ctrl Pts',(3.93194691662088,0.147524408656614,
17.1033444107879));
#257735=CARTESIAN_POINT('Ctrl Pts',(3.92417181586921,0.263371523779159,
17.1092001918318));
#257736=CARTESIAN_POINT('Ctrl Pts',(3.91639785602221,0.379201639698823,
17.1150551136086));
#257737=CARTESIAN_POINT('Ctrl Pts',(3.90348978714195,0.494706976650673,
17.1209100353854));
#257738=CARTESIAN_POINT('Ctrl Pts',(3.88550104532099,0.609401859867114,
17.1267649571623));
#257739=CARTESIAN_POINT('Ctrl Pts',(3.86751060271479,0.724107587164066,
17.1326204325056));
#257740=CARTESIAN_POINT('Ctrl Pts',(3.84443859620843,0.838002300606692,
17.1384759078489));
#257741=CARTESIAN_POINT('Ctrl Pts',(3.81638988128393,0.950608896462505,
17.1443313831922));
#257742=CARTESIAN_POINT('Ctrl Pts',(3.78833174671346,1.06325330917618,17.1501888249894));
#257743=CARTESIAN_POINT('Ctrl Pts',(3.75529368000615,1.17460834380498,17.1560462667867));
#257744=CARTESIAN_POINT('Ctrl Pts',(3.71743065980171,1.28421115458722,17.1619037085839));
#257745=CARTESIAN_POINT('Ctrl Pts',(3.67952496248891,1.39393750361356,17.1677677525665));
#257746=CARTESIAN_POINT('Ctrl Pts',(3.63678359202403,1.50190729655567,17.173631796549));
#257747=CARTESIAN_POINT('Ctrl Pts',(3.58941005794056,1.60767671997674,17.1794958405316));
#257748=CARTESIAN_POINT('Ctrl Pts',(3.54200451407092,1.71351761065672,17.1853638467855));
#257749=CARTESIAN_POINT('Ctrl Pts',(3.48996075889787,1.81715480334818,17.1912318530394));
#257750=CARTESIAN_POINT('Ctrl Pts',(3.43352791571731,1.9181697140738,17.1970998592932));
#257751=CARTESIAN_POINT('Ctrl Pts',(3.37701360192753,2.01933045736522,17.2029763370332));
#257752=CARTESIAN_POINT('Ctrl Pts',(3.31609777103728,2.11786101402561,17.2088528147731));
#257753=CARTESIAN_POINT('Ctrl Pts',(3.25107243960499,2.21337231220616,17.2147292925131));
#257754=CARTESIAN_POINT('Ctrl Pts',(3.23683046796727,2.23429137820409,17.2160163698329));
#257755=CARTESIAN_POINT('Ctrl Pts',(3.22239151149396,2.25506573819467,17.2173034471527));
#257756=CARTESIAN_POINT('Ctrl Pts',(3.20775888593271,2.27569152780418,17.2185905244726));
#257757=CARTESIAN_POINT('Ctrl Pts',(3.14095590324228,2.36985537150351,17.2244664763692));
#257758=CARTESIAN_POINT('Ctrl Pts',(3.06989293192811,2.46123056080213,17.2303424282658));
#257759=CARTESIAN_POINT('Ctrl Pts',(2.99483071752197,2.54940737689896,17.2362183801624));
#257760=CARTESIAN_POINT('Ctrl Pts',(2.91986482756885,2.63747103907879,17.2420867916759));
#257761=CARTESIAN_POINT('Ctrl Pts',(2.84091016594796,2.72234417899121,17.2479552031894));
#257762=CARTESIAN_POINT('Ctrl Pts',(2.75827036878138,2.80364647783964,17.2538236147029));
#257763=CARTESIAN_POINT('Ctrl Pts',(2.67571459738447,2.88486611084824,17.2596860593843));
#257764=CARTESIAN_POINT('Ctrl Pts',(2.58948143612544,2.96252183701393,17.2655485040657));
#257765=CARTESIAN_POINT('Ctrl Pts',(2.49991391043687,3.03626735324876,17.2714109487471));
#257766=CARTESIAN_POINT('Ctrl Pts',(2.40754809760837,3.11231684213573,17.2774565491362));
#257767=CARTESIAN_POINT('Ctrl Pts',(2.31163643951869,3.18420743762803,17.2835021495254));
#257768=CARTESIAN_POINT('Ctrl Pts',(2.21259545924414,3.25160119537009,17.2895477499146));
#257769=CARTESIAN_POINT('Ctrl Pts',(2.11666401779078,3.31687902589269,17.2954035396915));
#257770=CARTESIAN_POINT('Ctrl Pts',(2.01779718218882,3.37793791755644,17.3012593294684));
#257771=CARTESIAN_POINT('Ctrl Pts',(1.9164053502428,3.4345129980189,17.3071151192452));
#257772=CARTESIAN_POINT('Ctrl Pts',(1.81502839603622,3.49107977693191,17.3129700497723));
#257773=CARTESIAN_POINT('Ctrl Pts',(1.71112754257285,3.54316385185117,17.3188249802993));
#257774=CARTESIAN_POINT('Ctrl Pts',(1.60513921357111,3.59054551636048,17.3246799108264));
#257775=CARTESIAN_POINT('Ctrl Pts',(1.49914086354589,3.63793166072881,17.3305353949276));
#257776=CARTESIAN_POINT('Ctrl Pts',(1.39105502246991,3.68061434239041,17.3363908790287));
#257777=CARTESIAN_POINT('Ctrl Pts',(1.28133893120599,3.71842164679799,17.3422463631299));
#257778=CARTESIAN_POINT('Ctrl Pts',(1.17158599389743,3.75624164806352,17.3481038136831));
#257779=CARTESIAN_POINT('Ctrl Pts',(1.06020210774935,3.78918288192592,17.3539612642363));
#257780=CARTESIAN_POINT('Ctrl Pts',(0.947659855360323,3.81712323596428,
17.3598187147895));
#257781=CARTESIAN_POINT('Ctrl Pts',(0.83499075264517,3.84509508255719,17.365682767481));
#257782=CARTESIAN_POINT('Ctrl Pts',(0.72116107858175,3.86805469964639,17.3715468201724));
#257783=CARTESIAN_POINT('Ctrl Pts',(0.606653886206962,3.88593104189331,
17.3774108728639));
#257784=CARTESIAN_POINT('Ctrl Pts',(0.492069323007804,3.90381946292155,
17.3832788878095));
#257785=CARTESIAN_POINT('Ctrl Pts',(0.376806739120909,3.91661772430358,
17.389146902755));
#257786=CARTESIAN_POINT('Ctrl Pts',(0.261352871919692,3.92430677653255,
17.3950149177006));
#257787=CARTESIAN_POINT('Ctrl Pts',(0.145732329050413,3.93200692910791,
17.4008914040411));
#257788=CARTESIAN_POINT('Ctrl Pts',(0.0299203627822675,3.93458314356511,
17.4067678903817));
#257789=CARTESIAN_POINT('Ctrl Pts',(-0.0855976786094879,3.9320684171841,
17.4126443767222));
#257790=CARTESIAN_POINT('Ctrl Pts',(-0.110896980453302,3.93151767358594,
17.4139313705105));
#257791=CARTESIAN_POINT('Ctrl Pts',(-0.136182211232252,3.93072294360493,
17.4152183642988));
#257792=CARTESIAN_POINT('Ctrl Pts',(-0.161448325108427,3.92968490318495,
17.4165053580872));
#257793=CARTESIAN_POINT('Ctrl Pts',(-0.276803700559333,3.9249456091658,
17.4223812776046));
#257794=CARTESIAN_POINT('Ctrl Pts',(-0.392140530454384,3.91511483242535,
17.428257197122));
#257795=CARTESIAN_POINT('Ctrl Pts',(-0.50697318805222,3.90018809630974,
17.4341331166395));
#257796=CARTESIAN_POINT('Ctrl Pts',(-0.62165848345037,3.88528051534314,
17.4400014957199));
#257797=CARTESIAN_POINT('Ctrl Pts',(-0.735840487596784,3.86529003304004,
17.4458698748003));
#257798=CARTESIAN_POINT('Ctrl Pts',(-0.849034869944904,3.84026415622905,
17.4517382538807));
#257799=CARTESIAN_POINT('Ctrl Pts',(-0.962114158566661,3.81526372521633,
17.4576006661136));
#257800=CARTESIAN_POINT('Ctrl Pts',(-1.07420742218651,3.7852381724168,17.4634630783465));
#257801=CARTESIAN_POINT('Ctrl Pts',(-1.18483740451374,3.75028656569937,
17.4693254905794));
#257802=CARTESIAN_POINT('Ctrl Pts',(-1.29892457249747,3.71424272167995,
17.4753711031262));
#257803=CARTESIAN_POINT('Ctrl Pts',(-1.41145505743273,3.67295994118316,
17.4814167156729));
#257804=CARTESIAN_POINT('Ctrl Pts',(-1.52191857161317,3.62660348830403,
17.4874623282197));
#257805=CARTESIAN_POINT('Ctrl Pts',(-1.62891311449737,3.58170280302043,
17.493318085713));
#257806=CARTESIAN_POINT('Ctrl Pts',(-1.73396815795937,3.53204251637407,
17.4991738432063));
#257807=CARTESIAN_POINT('Ctrl Pts',(-1.83663804450311,3.47782255060315,
17.5050296006995));
#257808=CARTESIAN_POINT('Ctrl Pts',(-1.93929286772474,3.42361053977244,
17.5108844990591));
#257809=CARTESIAN_POINT('Ctrl Pts',(-2.03956286497587,3.36484037276013,
17.5167393974187));
#257810=CARTESIAN_POINT('Ctrl Pts',(-2.13702608290057,3.30175839833908,
17.5225942957782));
#257811=CARTESIAN_POINT('Ctrl Pts',(-2.23449851836854,3.23867045796655,
17.5284497478624));
#257812=CARTESIAN_POINT('Ctrl Pts',(-2.32916330028911,3.17127012383021,
17.5343051999465));
#257813=CARTESIAN_POINT('Ctrl Pts',(-2.42062721873252,3.09984723299895,
17.5401606520306));
#257814=CARTESIAN_POINT('Ctrl Pts',(-2.51212185663276,3.0284003537748,17.5460180707516));
#257815=CARTESIAN_POINT('Ctrl Pts',(-2.6004131681809,2.95292848524702,17.5518754894725));
#257816=CARTESIAN_POINT('Ctrl Pts',(-2.68514135502035,2.8737614555769,17.5577329081934));
#257817=CARTESIAN_POINT('Ctrl Pts',(-2.76996504873149,2.79450518765412,
17.5635969294838));
#257818=CARTESIAN_POINT('Ctrl Pts',(-2.85121729967337,2.71154572716617,
17.5694609507742));
#257819=CARTESIAN_POINT('Ctrl Pts',(-2.92857543508125,2.62524949691238,
17.5753249720646));
#257820=CARTESIAN_POINT('Ctrl Pts',(-3.00598584335641,2.53889495409239,
17.5811929558239));
#257821=CARTESIAN_POINT('Ctrl Pts',(-3.0794966354121,2.44919947017301,17.5870609395832));
#257822=CARTESIAN_POINT('Ctrl Pts',(-3.14882673908066,2.35656087705169,
17.5929289233425));
#257823=CARTESIAN_POINT('Ctrl Pts',(-3.21825693856327,2.26378853632436,
17.5988053790437));
#257824=CARTESIAN_POINT('Ctrl Pts',(-3.2834941725723,2.16806494631924,17.6046818347449));
#257825=CARTESIAN_POINT('Ctrl Pts',(-3.34430177547875,2.06981512085734,
17.6105582904461));
#257826=CARTESIAN_POINT('Ctrl Pts',(-3.35762233069981,2.04829244666907,
17.6118455908647));
#257827=CARTESIAN_POINT('Ctrl Pts',(-3.37073049823953,2.02664862920047,
17.6131328912832));
#257828=CARTESIAN_POINT('Ctrl Pts',(-3.3836240952532,2.00488827170543,17.6144201917018));
#257829=CARTESIAN_POINT('Ctrl Pts',(-3.44454128761214,1.90207911131986,
17.6205021816334));
#257830=CARTESIAN_POINT('Ctrl Pts',(-3.50085414675206,1.79634782237633,
17.6265841715651));
#257831=CARTESIAN_POINT('Ctrl Pts',(-3.55228244957488,1.68812866762055,
17.6326661614968));
#257832=CARTESIAN_POINT('Ctrl Pts',(-3.60362884969778,1.58008185845017,
17.6387384654896));
#257833=CARTESIAN_POINT('Ctrl Pts',(-3.65010602275546,1.46955540601067,
17.6448107694824));
#257834=CARTESIAN_POINT('Ctrl Pts',(-3.69147830432186,1.35701029057301,
17.6508830734753));
#257835=CARTESIAN_POINT('Ctrl Pts',(-3.73277151972813,1.24468025899781,
17.6569437727477));
#257836=CARTESIAN_POINT('Ctrl Pts',(-3.76897915975207,1.13033960097184,
17.6630044720201));
#257837=CARTESIAN_POINT('Ctrl Pts',(-3.7999129418847,1.01447061766085,17.6690651712925));
#257838=CARTESIAN_POINT('Ctrl Pts',(-3.83081195534235,0.898731867730426,
17.6751190585146));
#257839=CARTESIAN_POINT('Ctrl Pts',(-3.85644881503235,0.781468569978592,
17.6811729457366));
#257840=CARTESIAN_POINT('Ctrl Pts',(-3.87668426530563,0.66318029760524,
17.6872268329586));
#257841=CARTESIAN_POINT('Ctrl Pts',(-3.89689414166229,0.545041520023117,
17.6932730691719));
#257842=CARTESIAN_POINT('Ctrl Pts',(-3.91171614982977,0.425880715184696,
17.6993193053852));
#257843=CARTESIAN_POINT('Ctrl Pts',(-3.92106171204903,0.306209161037272,
17.7053655415984));
#257844=CARTESIAN_POINT('Ctrl Pts',(-3.92903276452442,0.204138443883995,
17.7105225203873));
#257845=CARTESIAN_POINT('Ctrl Pts',(-3.93302062486231,0.101696518362754,
17.7156794991761));
#257846=CARTESIAN_POINT('Ctrl Pts',(-3.93299991974402,-0.000794539836274554,
17.720836477965));
#257847=CARTESIAN_POINT('',(-3.93299894594177,-0.00287944802932865,18.970836477928));
#257848=CARTESIAN_POINT('Ctrl Pts',(-3.93299991974386,-0.000794540591381787,
17.720836478003));
#257849=CARTESIAN_POINT('Ctrl Pts',(-3.93297488581434,-0.124713247691418,
17.7270716184659));
#257850=CARTESIAN_POINT('Ctrl Pts',(-3.92708906524364,-0.248483679099339,
17.7333067589288));
#257851=CARTESIAN_POINT('Ctrl Pts',(-3.91540977936332,-0.371557881986174,
17.7395418993916));
#257852=CARTESIAN_POINT('Ctrl Pts',(-3.90369131069854,-0.495044985971108,
17.7457979580996));
#257853=CARTESIAN_POINT('Ctrl Pts',(-3.88614052210331,-0.617830863470176,
17.7520540168076));
#257854=CARTESIAN_POINT('Ctrl Pts',(-3.8628763889649,-0.739374738260309,
17.7583100755156));
#257855=CARTESIAN_POINT('Ctrl Pts',(-3.83957308099714,-0.86112328263881,
17.7645766688965));
#257856=CARTESIAN_POINT('Ctrl Pts',(-3.8105372973786,-0.98162533375304,
17.7708432622774));
#257857=CARTESIAN_POINT('Ctrl Pts',(-3.77593807307681,-1.1003547920053,
17.7771098556582));
#257858=CARTESIAN_POINT('Ctrl Pts',(-3.74123648688048,-1.21943551166669,
17.7833949887718));
#257859=CARTESIAN_POINT('Ctrl Pts',(-3.70093863710898,-1.33673283863354,
17.7896801218854));
#257860=CARTESIAN_POINT('Ctrl Pts',(-3.65526274537066,-1.45173801434877,
17.795965254999));
#257861=CARTESIAN_POINT('Ctrl Pts',(-3.61560811683237,-1.5515825351541,
17.8014218451048));
#257862=CARTESIAN_POINT('Ctrl Pts',(-3.57190073260232,-1.64969963998605,
17.8068784352106));
#257863=CARTESIAN_POINT('Ctrl Pts',(-3.52431099124079,-1.74577233252775,
17.8123350253164));
#257864=CARTESIAN_POINT('Ctrl Pts',(-3.47306336887225,-1.84922944169551,
17.8182110242431));
#257865=CARTESIAN_POINT('Ctrl Pts',(-3.41717183874442,-1.95059870997914,
17.8240870231698));
#257866=CARTESIAN_POINT('Ctrl Pts',(-3.35682983759973,-2.04943466385249,
17.8299630220965));
#257867=CARTESIAN_POINT('Ctrl Pts',(-3.2965652673676,-2.14814379133698,
17.8358314809358));
#257868=CARTESIAN_POINT('Ctrl Pts',(-3.23186179656452,-2.24432572013498,
17.8416999397752));
#257869=CARTESIAN_POINT('Ctrl Pts',(-3.16295982397821,-2.33755730451678,
17.8475683986145));
#257870=CARTESIAN_POINT('Ctrl Pts',(-3.09412790559635,-2.43069409822382,
17.8534308908582));
#257871=CARTESIAN_POINT('Ctrl Pts',(-3.02110622035992,-2.52088618428527,
17.8592933831018));
#257872=CARTESIAN_POINT('Ctrl Pts',(-2.94417939310716,-2.60773785131926,
17.8651558753454));
#257873=CARTESIAN_POINT('Ctrl Pts',(-2.86485007840845,-2.69730196662597,
17.8712014579948));
#257874=CARTESIAN_POINT('Ctrl Pts',(-2.78136792497248,-2.7833132051691,
17.8772470406442));
#257875=CARTESIAN_POINT('Ctrl Pts',(-2.69409144613518,-2.86537262495845,
17.8832926232936));
#257876=CARTESIAN_POINT('Ctrl Pts',(-2.60955420333167,-2.94485654992269,
17.889148460916));
#257877=CARTESIAN_POINT('Ctrl Pts',(-2.52145757372515,-3.0206327066666,
17.8950042985383));
#257878=CARTESIAN_POINT('Ctrl Pts',(-2.43016546459566,-3.09237527067569,
17.9008601361607));
#257879=CARTESIAN_POINT('Ctrl Pts',(-2.33888675076927,-3.16410730788899,
17.9067151145552));
#257880=CARTESIAN_POINT('Ctrl Pts',(-2.24441381420525,-3.23180667427304,
17.9125700929497));
#257881=CARTESIAN_POINT('Ctrl Pts',(-2.14714333413732,-3.29518808304923,
17.9184250713442));
#257882=CARTESIAN_POINT('Ctrl Pts',(-2.04986365787679,-3.35857548406112,
17.9242806032829));
#257883=CARTESIAN_POINT('Ctrl Pts',(-1.94978625816811,-3.4176438905975,
17.9301361352217));
#257884=CARTESIAN_POINT('Ctrl Pts',(-1.84733585251232,-3.47215196211551,
17.9359916671604));
#257885=CARTESIAN_POINT('Ctrl Pts',(-1.74485104256939,-3.52667833821056,
17.9418491654691));
#257886=CARTESIAN_POINT('Ctrl Pts',(-1.63999200626029,-3.57664114030922,
17.9477066637778));
#257887=CARTESIAN_POINT('Ctrl Pts',(-1.53320640599483,-3.62184581624017,
17.9535641620865));
#257888=CARTESIAN_POINT('Ctrl Pts',(-1.42630045149718,-3.66710144074518,
17.9594282621721));
#257889=CARTESIAN_POINT('Ctrl Pts',(-1.31746397952908,-3.70758807470327,
17.9652923622577));
#257890=CARTESIAN_POINT('Ctrl Pts',(-1.20716298407007,-3.74315996584317,
17.9711564623433));
#257891=CARTESIAN_POINT('Ctrl Pts',(-1.0967874633723,-3.77875589125102,
17.9770245245279));
#257892=CARTESIAN_POINT('Ctrl Pts',(-0.984945845856242,-3.80943035263879,
17.9828925867125));
#257893=CARTESIAN_POINT('Ctrl Pts',(-0.872115900019499,-3.83508837667832,
17.988760648897));
#257894=CARTESIAN_POINT('Ctrl Pts',(-0.759123079087412,-3.86078343922817,
17.994637181893));
#257895=CARTESIAN_POINT('Ctrl Pts',(-0.645139487153175,-3.88144753966241,
18.0005137148889));
#257896=CARTESIAN_POINT('Ctrl Pts',(-0.530649664272131,-3.89703732774115,
18.0063902478849));
#257897=CARTESIAN_POINT('Ctrl Pts',(-0.505584648024338,-3.90045036727305,
18.0076767849003));
#257898=CARTESIAN_POINT('Ctrl Pts',(-0.480495372701463,-3.90362039622428,
18.0089633219157));
#257899=CARTESIAN_POINT('Ctrl Pts',(-0.45538692229026,-3.90654729281587,
18.0102498589311));
#257900=CARTESIAN_POINT('Ctrl Pts',(-0.340713484564884,-3.91991479612761,
18.0161256346122));
#257901=CARTESIAN_POINT('Ctrl Pts',(-0.225261720292381,-3.92825086847855,
18.0220014102934));
#257902=CARTESIAN_POINT('Ctrl Pts',(-0.109510553206871,-3.93147509705153,
18.0278771859746));
#257903=CARTESIAN_POINT('Ctrl Pts',(0.00609206620409948,-3.93469518785494,
18.0337454210595));
#257904=CARTESIAN_POINT('Ctrl Pts',(0.12199291537467,-3.93281646991857,
18.0396136561444));
#257905=CARTESIAN_POINT('Ctrl Pts',(0.237706215873664,-3.92581007626898,
18.0454818912294));
#257906=CARTESIAN_POINT('Ctrl Pts',(0.353301858790676,-3.91881080673849,
18.0513441594777));
#257907=CARTESIAN_POINT('Ctrl Pts',(0.468709922737927,-3.90669425729709,
18.0572064277261));
#257908=CARTESIAN_POINT('Ctrl Pts',(0.58344354785797,-3.88948359380303,
18.0630686959745));
#257909=CARTESIAN_POINT('Ctrl Pts',(0.70176655989913,-3.87173450288295,
18.0691143624983));
#257910=CARTESIAN_POINT('Ctrl Pts',(0.819371792889485,-3.84856730564004,
18.0751600290221));
#257911=CARTESIAN_POINT('Ctrl Pts',(0.935729352959446,-3.82006538923224,
18.0812056955459));
#257912=CARTESIAN_POINT('Ctrl Pts',(1.04842908682777,-3.79245946150426,
18.0870613099802));
#257913=CARTESIAN_POINT('Ctrl Pts',(1.15995798684355,-3.75984930431401,
18.0929169244146));
#257914=CARTESIAN_POINT('Ctrl Pts',(1.26984462171162,-3.72236264175189,
18.0987725388489));
#257915=CARTESIAN_POINT('Ctrl Pts',(1.37971514505317,-3.68488147546653,
18.1046272947358));
#257916=CARTESIAN_POINT('Ctrl Pts',(1.48794349146881,-3.642525358783,18.1104820506227));
#257917=CARTESIAN_POINT('Ctrl Pts',(1.59407437776438,-3.59547157938359,
18.1163368065096));
#257918=CARTESIAN_POINT('Ctrl Pts',(1.70021531495974,-3.5484133438561,18.1221921168587));
#257919=CARTESIAN_POINT('Ctrl Pts',(1.80425801978836,-3.49665672854094,
18.1280474272078));
#257920=CARTESIAN_POINT('Ctrl Pts',(1.90576879438018,-3.44042647100134,
18.1339027375569));
#257921=CARTESIAN_POINT('Ctrl Pts',(2.00731367905753,-3.38417731872961,
18.1397600154325));
#257922=CARTESIAN_POINT('Ctrl Pts',(2.1063245808304,-3.32345173494806,18.1456172933081));
#257923=CARTESIAN_POINT('Ctrl Pts',(2.20239454523198,-3.25851918317698,
18.1514745711837));
#257924=CARTESIAN_POINT('Ctrl Pts',(2.29857283674299,-3.19351341439491,
18.1573384536415));
#257925=CARTESIAN_POINT('Ctrl Pts',(2.39180323002588,-3.12429144095205,
18.1632023360993));
#257926=CARTESIAN_POINT('Ctrl Pts',(2.48170971374509,-3.0511646787257,18.1690662185571));
#257927=CARTESIAN_POINT('Ctrl Pts',(2.57167696652274,-2.97798848909095,
18.1749340644957));
#257928=CARTESIAN_POINT('Ctrl Pts',(2.6583155284195,-2.90090252884139,18.1808019104342));
#257929=CARTESIAN_POINT('Ctrl Pts',(2.74128556283274,-2.82025574425526,
18.1866697563728));
#257930=CARTESIAN_POINT('Ctrl Pts',(2.82437542406964,-2.73949248812487,
18.1925460767606));
#257931=CARTESIAN_POINT('Ctrl Pts',(2.90378590270158,-2.65515844412652,
18.1984223971483));
#257932=CARTESIAN_POINT('Ctrl Pts',(2.97921676953516,-2.56763635278061,
18.204298717536));
#257933=CARTESIAN_POINT('Ctrl Pts',(2.99575851827648,-2.54844303703158,
18.2055873758726));
#257934=CARTESIAN_POINT('Ctrl Pts',(3.0121090476354,-2.52909651654374,18.2068760342091));
#257935=CARTESIAN_POINT('Ctrl Pts',(3.02826547238151,-2.50960100987826,
18.2081646925457));
#257936=CARTESIAN_POINT('Ctrl Pts',(3.10193627915747,-2.42070450417717,
18.2140407759492));
#257937=CARTESIAN_POINT('Ctrl Pts',(3.17181087799,-2.32841464196013,18.2199168593528));
#257938=CARTESIAN_POINT('Ctrl Pts',(3.23756097330368,-2.23308932739846,
18.2257929427563));
#257939=CARTESIAN_POINT('Ctrl Pts',(3.30322668534541,-2.13788635276503,
18.2316614848303));
#257940=CARTESIAN_POINT('Ctrl Pts',(3.36477818866503,-2.03965600993005,
18.2375300269042));
#257941=CARTESIAN_POINT('Ctrl Pts',(3.42192668560722,-1.93879002430103,
18.2433985689781));
#257942=CARTESIAN_POINT('Ctrl Pts',(3.47901706632259,-1.83802661268206,
18.2492611431343));
#257943=CARTESIAN_POINT('Ctrl Pts',(3.53171314487032,-1.73463324670722,
18.2551237172906));
#257944=CARTESIAN_POINT('Ctrl Pts',(3.57976917376844,-1.62903089674114,
18.2609862914469));
#257945=CARTESIAN_POINT('Ctrl Pts',(3.62932508338567,-1.52013258303776,
18.2670318428933));
#257946=CARTESIAN_POINT('Ctrl Pts',(3.67394629137763,-1.40888549915709,
18.2730773943397));
#257947=CARTESIAN_POINT('Ctrl Pts',(3.71341416183815,-1.29577940354826,
18.2791229457861));
#257948=CARTESIAN_POINT('Ctrl Pts',(3.75164401190339,-1.18622119769277,
18.2849788615642));
#257949=CARTESIAN_POINT('Ctrl Pts',(3.78503884728929,-1.0749192827355,18.2908347773422));
#257950=CARTESIAN_POINT('Ctrl Pts',(3.81344901027675,-0.962338633755953,
18.2966906931203));
#257951=CARTESIAN_POINT('Ctrl Pts',(3.84185499733292,-0.849774532694668,
18.3025457481536));
#257952=CARTESIAN_POINT('Ctrl Pts',(3.86527766794579,-0.7359324714477,18.3084008031868));
#257953=CARTESIAN_POINT('Ctrl Pts',(3.88361772652158,-0.621290877325088,
18.31425585822));
#257954=CARTESIAN_POINT('Ctrl Pts',(3.90195951400109,-0.506638476024428,
18.3201114652049));
#257955=CARTESIAN_POINT('Ctrl Pts',(3.91521767176824,-0.39118679959254,
18.3259670721898));
#257956=CARTESIAN_POINT('Ctrl Pts',(3.92334445499873,-0.275422016967966,
18.3318226791747));
#257957=CARTESIAN_POINT('Ctrl Pts',(3.93147396496573,-0.159618392399321,
18.3376802508604));
#257958=CARTESIAN_POINT('Ctrl Pts',(3.93446864792641,-0.0435018642342749,
18.3435378225461));
#257959=CARTESIAN_POINT('Ctrl Pts',(3.93233283481887,0.0724394657999363,
18.3493953942318));
#257960=CARTESIAN_POINT('Ctrl Pts',(3.93019461556805,0.188511411874933,
18.3552595648829));
#257961=CARTESIAN_POINT('Ctrl Pts',(3.92291437187116,0.304407353006746,
18.361123735534));
#257962=CARTESIAN_POINT('Ctrl Pts',(3.91054847183753,0.419642287441569,
18.3669879061851));
#257963=CARTESIAN_POINT('Ctrl Pts',(3.89817422013104,0.534955049165209,
18.3728560373756));
#257964=CARTESIAN_POINT('Ctrl Pts',(3.88070753460741,0.649605508229467,
18.3787241685661));
#257965=CARTESIAN_POINT('Ctrl Pts',(3.85825596185029,0.763118557530013,
18.3845922997566));
#257966=CARTESIAN_POINT('Ctrl Pts',(3.83577199021616,0.876795412518599,
18.3904688989891));
#257967=CARTESIAN_POINT('Ctrl Pts',(3.80828887319298,0.989331182825753,
18.3963454982216));
#257968=CARTESIAN_POINT('Ctrl Pts',(3.77596407233751,1.10026556994951,18.4022220974541));
#257969=CARTESIAN_POINT('Ctrl Pts',(3.76889135279296,1.1245381961439,18.4035079070228));
#257970=CARTESIAN_POINT('Ctrl Pts',(3.76158702439922,1.14873423410985,18.4047937165915));
#257971=CARTESIAN_POINT('Ctrl Pts',(3.75405304017374,1.17284899776666,18.4060795261603));
#257972=CARTESIAN_POINT('Ctrl Pts',(3.71962208134895,1.28305555112387,18.4119557869796));
#257973=CARTESIAN_POINT('Ctrl Pts',(3.68027731276114,1.39192630389124,18.4178320477989));
#257974=CARTESIAN_POINT('Ctrl Pts',(3.63614013207501,1.49899097392663,18.4237083086182));
#257975=CARTESIAN_POINT('Ctrl Pts',(3.59205956952264,1.60591830392999,18.4295770315088));
#257976=CARTESIAN_POINT('Ctrl Pts',(3.54319897664802,1.71104378055194,18.4354457543994));
#257977=CARTESIAN_POINT('Ctrl Pts',(3.48972962711575,1.81391183072126,18.44131447729));
#257978=CARTESIAN_POINT('Ctrl Pts',(3.43631462206099,1.9166753292084,18.4471772354048));
#257979=CARTESIAN_POINT('Ctrl Pts',(3.37830036708313,2.01718560101243,18.4530399935197));
#257980=CARTESIAN_POINT('Ctrl Pts',(3.31590610828367,2.11500725319018,18.4589027516345));
#257981=CARTESIAN_POINT('Ctrl Pts',(3.25156719723852,2.21587772907773,18.464948235307));
#257982=CARTESIAN_POINT('Ctrl Pts',(3.18257095061507,2.31388883067095,18.4709937189796));
#257983=CARTESIAN_POINT('Ctrl Pts',(3.10920903409692,2.40859049701066,18.4770392026521));
#257984=CARTESIAN_POINT('Ctrl Pts',(3.03814521112503,2.50032559297483,18.4828953089518));
#257985=CARTESIAN_POINT('Ctrl Pts',(2.96298542301897,2.58895514989585,18.4887514152515));
#257986=CARTESIAN_POINT('Ctrl Pts',(2.88403815099348,2.67410039894057,18.4946075215513));
#257987=CARTESIAN_POINT('Ctrl Pts',(2.80510245468572,2.75923316348337,18.500462769194));
#257988=CARTESIAN_POINT('Ctrl Pts',(2.72238065927654,2.84088233348448,18.5063180168366));
#257989=CARTESIAN_POINT('Ctrl Pts',(2.63621995589132,2.91870405217116,18.5121732644793));
#257990=CARTESIAN_POINT('Ctrl Pts',(2.55005110297565,2.99653313164346,18.5180290659419));
#257991=CARTESIAN_POINT('Ctrl Pts',(2.4604430017628,3.07053376349345,18.5238848674046));
#257992=CARTESIAN_POINT('Ctrl Pts',(2.36777741151076,3.14040110965771,18.5297406688672));
#257993=CARTESIAN_POINT('Ctrl Pts',(2.27508070458647,3.21029191695038,18.5355984366807));
#257994=CARTESIAN_POINT('Ctrl Pts',(2.17932479641105,3.27604643033228,18.5414562044941));
#257995=CARTESIAN_POINT('Ctrl Pts',(2.08092142884035,3.33740243407849,18.5473139723075));
#257996=CARTESIAN_POINT('Ctrl Pts',(1.98240718282173,3.39882757223172,18.5531783405068));
#257997=CARTESIAN_POINT('Ctrl Pts',(1.88123987386353,3.45584409037383,18.5590427087062));
#257998=CARTESIAN_POINT('Ctrl Pts',(1.77785698489317,3.50823510347676,18.5649070769056));
#257999=CARTESIAN_POINT('Ctrl Pts',(1.67440425686416,3.56066150869411,18.5707754067078));
#258000=CARTESIAN_POINT('Ctrl Pts',(1.56873334356251,3.60845601710389,18.5766437365101));
#258001=CARTESIAN_POINT('Ctrl Pts',(1.46130130311543,3.65145005463763,18.5825120663124));
#258002=CARTESIAN_POINT('Ctrl Pts',(1.35371423721524,3.69450613297523,18.5883888641702));
#258003=CARTESIAN_POINT('Ctrl Pts',(1.24436136058433,3.73274778058609,18.594265662028));
#258004=CARTESIAN_POINT('Ctrl Pts',(1.13371449742192,3.76605635092405,18.6001424598859));
#258005=CARTESIAN_POINT('Ctrl Pts',(1.10954029857822,3.77333362910018,18.6014264265155));
#258006=CARTESIAN_POINT('Ctrl Pts',(1.08530436796868,3.78037562719454,18.6027103931452));
#258007=CARTESIAN_POINT('Ctrl Pts',(1.06101167767463,3.78718143476624,18.6039943597749));
#258008=CARTESIAN_POINT('Ctrl Pts',(0.949861003344788,3.81832125879547,
18.6098691210705));
#258009=CARTESIAN_POINT('Ctrl Pts',(0.837154478092364,3.84461515798849,
18.6157438823661));
#258010=CARTESIAN_POINT('Ctrl Pts',(0.723352382783124,3.86590873279776,
18.6216186436618));
#258011=CARTESIAN_POINT('Ctrl Pts',(0.609696392508168,3.88717496981093,
18.627485862634));
#258012=CARTESIAN_POINT('Ctrl Pts',(0.494948031629236,3.90345357400914,
18.6333530816063));
#258013=CARTESIAN_POINT('Ctrl Pts',(0.379582426893661,3.91463998104468,
18.6392203005786));
#258014=CARTESIAN_POINT('Ctrl Pts',(0.264334156778507,3.92581501074791,
18.6450815521924));
#258015=CARTESIAN_POINT('Ctrl Pts',(0.148470300141058,3.93190810551321,
18.6509428038063));
#258016=CARTESIAN_POINT('Ctrl Pts',(0.0324752019179193,3.93286592210571,
18.6568040554202));
#258017=CARTESIAN_POINT('Ctrl Pts',(-0.0871770345004511,3.93385393710916,
18.6628501028356));
#258018=CARTESIAN_POINT('Ctrl Pts',(-0.206968485783391,3.92937740804405,
18.668896150251));
#258019=CARTESIAN_POINT('Ctrl Pts',(-0.326362506474011,3.91943573928289,
18.6749421976664));
#258020=CARTESIAN_POINT('Ctrl Pts',(-0.441975985118381,3.90980886766604,
18.6807968005158));
#258021=CARTESIAN_POINT('Ctrl Pts',(-0.557216380231496,3.89505777357661,
18.6866514033652));
#258022=CARTESIAN_POINT('Ctrl Pts',(-0.671598214632129,3.8752348107054,
18.6925060062147));
#258023=CARTESIAN_POINT('Ctrl Pts',(-0.785963345652738,3.85541474261626,
18.6983597541062));
#258024=CARTESIAN_POINT('Ctrl Pts',(-0.89946975849245,3.83052434898566,
18.7042135019977));
#258025=CARTESIAN_POINT('Ctrl Pts',(-1.01164016905407,3.80066746353272,
18.7100672498892));
#258026=CARTESIAN_POINT('Ctrl Pts',(-1.12382129359438,3.77080772629353,
18.7159215569026));
#258027=CARTESIAN_POINT('Ctrl Pts',(-1.23466576311504,3.73598066043904,
18.721775863916));
#258028=CARTESIAN_POINT('Ctrl Pts',(-1.34371018966508,3.69634034231025,
18.7276301709294));
#258029=CARTESIAN_POINT('Ctrl Pts',(-1.45279137087877,3.65668666296157,
18.7334864512035));
#258030=CARTESIAN_POINT('Ctrl Pts',(-1.56007091479021,3.61221664632338,
18.7393427314777));
#258031=CARTESIAN_POINT('Ctrl Pts',(-1.66510485227562,3.56313272709959,
18.7451990117518));
#258032=CARTESIAN_POINT('Ctrl Pts',(-1.77025748546047,3.51399333961228,
18.7510619100324));
#258033=CARTESIAN_POINT('Ctrl Pts',(-1.87315907298071,3.4602298178422,18.7569248083131));
#258034=CARTESIAN_POINT('Ctrl Pts',(-1.97338964691929,3.40209087201265,
18.7627877065937));
#258035=CARTESIAN_POINT('Ctrl Pts',(-2.07368809359793,3.34391255646383,
18.7686545750299));
#258036=CARTESIAN_POINT('Ctrl Pts',(-2.17131157832395,3.28135313929512,
18.7745214434662));
#258037=CARTESIAN_POINT('Ctrl Pts',(-2.2658699964757,3.2147040546637,18.7803883119024));
#258038=CARTESIAN_POINT('Ctrl Pts',(-2.36056527542287,3.14795850430331,
18.7862636718542));
#258039=CARTESIAN_POINT('Ctrl Pts',(-2.45218630920164,3.07711172534182,
18.7921390318059));
#258040=CARTESIAN_POINT('Ctrl Pts',(-2.54037683090483,3.00249472222716,
18.7980143917577));
#258041=CARTESIAN_POINT('Ctrl Pts',(-2.55986412420316,2.98600674373859,
18.7993126589683));
#258042=CARTESIAN_POINT('Ctrl Pts',(-2.57918406329377,2.96933481511489,
18.800610926179));
#258043=CARTESIAN_POINT('Ctrl Pts',(-2.59833305960692,2.95248273684263,
18.8019091933896));
#258044=CARTESIAN_POINT('Ctrl Pts',(-2.68376370729919,2.87729947719728,
18.8077012363179));
#258045=CARTESIAN_POINT('Ctrl Pts',(-2.76608902957665,2.79826365860864,
18.8134932792462));
#258046=CARTESIAN_POINT('Ctrl Pts',(-2.84493415261627,2.71566541887574,
18.8192853221745));
#258047=CARTESIAN_POINT('Ctrl Pts',(-2.92367726215477,2.63317404860156,
18.8250698710873));
#258048=CARTESIAN_POINT('Ctrl Pts',(-2.99894883105194,2.54712972324905,
18.8308544200001));
#258049=CARTESIAN_POINT('Ctrl Pts',(-3.07040720799903,2.45786260337465,
18.8366389689128));
#258050=CARTESIAN_POINT('Ctrl Pts',(-3.14178558698597,2.36869541842465,
18.8424170419982));
#258051=CARTESIAN_POINT('Ctrl Pts',(-3.20935900137614,2.27631294623772,
18.8481951150836));
#258052=CARTESIAN_POINT('Ctrl Pts',(-3.27282351652875,2.18108120657082,
18.853973188169));
#258053=CARTESIAN_POINT('Ctrl Pts',(-3.33624872740734,2.08590844497033,
18.8597476828301));
#258054=CARTESIAN_POINT('Ctrl Pts',(-3.39556985957282,1.9878902747605,18.8655221774911));
#258055=CARTESIAN_POINT('Ctrl Pts',(-3.45052439071638,1.88742428432808,
18.8712966721521));
#258056=CARTESIAN_POINT('Ctrl Pts',(-3.50545905190921,1.78699461945858,
18.8770690789248));
#258057=CARTESIAN_POINT('Ctrl Pts',(-3.55603004609453,1.68411926648386,
18.8828414856975));
#258058=CARTESIAN_POINT('Ctrl Pts',(-3.60201964944105,1.57922241785019,
18.8886138924702));
#258059=CARTESIAN_POINT('Ctrl Pts',(-3.64800447626287,1.47433646390469,
18.8943856997151));
#258060=CARTESIAN_POINT('Ctrl Pts',(-3.68940868866779,1.36742982206938,
18.9001575069601));
#258061=CARTESIAN_POINT('Ctrl Pts',(-3.72606213610041,1.2589479567952,18.905929314205));
#258062=CARTESIAN_POINT('Ctrl Pts',(-3.76273881891724,1.15039732260583,
18.9117047803189));
#258063=CARTESIAN_POINT('Ctrl Pts',(-3.79465858306969,1.04026987371933,
18.9174802464327));
#258064=CARTESIAN_POINT('Ctrl Pts',(-3.82170081340551,0.929027390777956,
18.9232557125466));
#258065=CARTESIAN_POINT('Ctrl Pts',(-3.84875170762517,0.81774926758282,
18.9290330290243));
#258066=CARTESIAN_POINT('Ctrl Pts',(-3.87092187129608,0.705355816281533,
18.9348103455021));
#258067=CARTESIAN_POINT('Ctrl Pts',(-3.8881419432584,0.592318519949188,
18.9405876619799));
#258068=CARTESIAN_POINT('Ctrl Pts',(-3.90538360762339,0.479139485137241,
18.9463722226866));
#258069=CARTESIAN_POINT('Ctrl Pts',(-3.9176627359606,0.365315416113108,
18.9521567833933));
#258070=CARTESIAN_POINT('Ctrl Pts',(-3.92496191163897,0.251322486426023,
18.9579413441));
#258071=CARTESIAN_POINT('Ctrl Pts',(-3.930385766159,0.166616884837634,18.9622397220427));
#258072=CARTESIAN_POINT('Ctrl Pts',(-3.93306095518726,0.0818181379921459,
18.9665380999854));
#258073=CARTESIAN_POINT('Ctrl Pts',(-3.93299894594177,-0.00287944802935699,
18.970836477928));
#258074=CARTESIAN_POINT('Ctrl Pts',(-3.93299894594123,-0.00287944875768067,
18.970836477965));
#258075=CARTESIAN_POINT('Ctrl Pts',(-3.93285955254499,-0.193274946860016,
18.9804989943114));
#258076=CARTESIAN_POINT('Ctrl Pts',(-3.91889275474165,-0.383164830983256,
18.9901615106578));
#258077=CARTESIAN_POINT('Ctrl Pts',(-3.89132795850799,-0.571012888938626,
18.9998240270042));
#258078=CARTESIAN_POINT('Ctrl Pts',(-3.87179907361845,-0.704097968524874,
19.0066696487847));
#258079=CARTESIAN_POINT('Ctrl Pts',(-3.84542340013612,-0.836284199472048,
19.0135152705652));
#258080=CARTESIAN_POINT('Ctrl Pts',(-3.81229009242283,-0.966919464699496,
19.0203608923457));
#258081=CARTESIAN_POINT('Ctrl Pts',(-3.77930457041597,-1.09697205266679,
19.0271759803485));
#258082=CARTESIAN_POINT('Ctrl Pts',(-3.73962153078669,-1.22548733640384,
19.0339910683513));
#258083=CARTESIAN_POINT('Ctrl Pts',(-3.6933803811278,-1.35182482604081,
19.0408061563541));
#258084=CARTESIAN_POINT('Ctrl Pts',(-3.64750954796444,-1.47715055760599,
19.0475666665724));
#258085=CARTESIAN_POINT('Ctrl Pts',(-3.59518520759239,-1.60033308325736,
19.0543271767906));
#258086=CARTESIAN_POINT('Ctrl Pts',(-3.53659449190347,-1.72075227730143,
19.0610876870088));
#258087=CARTESIAN_POINT('Ctrl Pts',(-3.51951458529148,-1.75585593774284,
19.0630584580059));
#258088=CARTESIAN_POINT('Ctrl Pts',(-3.50190250031843,-1.79072481372021,
19.0650292290029));
#258089=CARTESIAN_POINT('Ctrl Pts',(-3.48376370290062,-1.82534365595966,
19.067));
#258090=CARTESIAN_POINT('',(-3.56066877200036,1.66757030866008,19.0681870665394));
#258091=CARTESIAN_POINT('Origin',(0.,0.,19.067));
#258092=CARTESIAN_POINT('',(-3.93115504418186,-0.00207051908275006,17.9041635502338));
#258093=CARTESIAN_POINT('Ctrl Pts',(-3.56174364677249,1.66807409747762,
19.0669999597496));
#258094=CARTESIAN_POINT('Ctrl Pts',(-3.5099739625514,1.77861495663293,19.0608645385329));
#258095=CARTESIAN_POINT('Ctrl Pts',(-3.45310794955396,1.88662946387192,
19.0547291173162));
#258096=CARTESIAN_POINT('Ctrl Pts',(-3.39142665006682,1.99166118534668,
19.0485936960995));
#258097=CARTESIAN_POINT('Ctrl Pts',(-3.32695834632604,2.10143865402443,
19.0421810523669));
#258098=CARTESIAN_POINT('Ctrl Pts',(-3.25722971012385,2.2079571269901,19.0357684086343));
#258099=CARTESIAN_POINT('Ctrl Pts',(-3.18260936614508,2.31073291890812,
19.0293557649017));
#258100=CARTESIAN_POINT('Ctrl Pts',(-3.11090557499978,2.40949169601291,
19.0231937607835));
#258101=CARTESIAN_POINT('Ctrl Pts',(-3.03468553378717,2.50479464386839,
19.0170317566654));
#258102=CARTESIAN_POINT('Ctrl Pts',(-2.95431481317474,2.59624979242297,
19.0108697525473));
#258103=CARTESIAN_POINT('Ctrl Pts',(-2.87382287672716,2.68784287444543,
19.0046984548398));
#258104=CARTESIAN_POINT('Ctrl Pts',(-2.78916801121425,2.77557632717908,
18.9985271571323));
#258105=CARTESIAN_POINT('Ctrl Pts',(-2.70075115349836,2.85909639691936,
18.9923558594248));
#258106=CARTESIAN_POINT('Ctrl Pts',(-2.61213074260116,2.94280874646168,
18.9861703541633));
#258107=CARTESIAN_POINT('Ctrl Pts',(-2.51973129512467,3.02228810083865,
18.9799848489018));
#258108=CARTESIAN_POINT('Ctrl Pts',(-2.42398602642619,3.09722145538393,
18.9737993436403));
#258109=CARTESIAN_POINT('Ctrl Pts',(-2.41285472375999,3.10593317409939,
18.9730802195296));
#258110=CARTESIAN_POINT('Ctrl Pts',(-2.40167822774746,3.11458349748398,
18.9723610954189));
#258111=CARTESIAN_POINT('Ctrl Pts',(-2.39045724201333,3.12317197318784,
18.9716419713081));
#258112=CARTESIAN_POINT('Ctrl Pts',(-2.29862762614441,3.19345781468798,
18.9657568474505));
#258113=CARTESIAN_POINT('Ctrl Pts',(-2.20354696592246,3.25980387280755,
18.9598717235929));
#258114=CARTESIAN_POINT('Ctrl Pts',(-2.10558719971127,3.32189577566968,
18.9539865997352));
#258115=CARTESIAN_POINT('Ctrl Pts',(-2.00775261843656,3.38390832992557,
18.9481089966066));
#258116=CARTESIAN_POINT('Ctrl Pts',(-1.90704659310603,3.44167732316943,
18.942231393478));
#258117=CARTESIAN_POINT('Ctrl Pts',(-1.80387324554285,3.49492922875624,
18.9363537903493));
#258118=CARTESIAN_POINT('Ctrl Pts',(-1.70080450276349,3.54812714361576,
18.9304821463702));
#258119=CARTESIAN_POINT('Ctrl Pts',(-1.59527377741334,3.59681689371709,
18.9246105023911));
#258120=CARTESIAN_POINT('Ctrl Pts',(-1.48771267368374,3.64076914958375,
18.918738858412));
#258121=CARTESIAN_POINT('Ctrl Pts',(-1.37713666330677,3.6859533744781,18.9127026339494));
#258122=CARTESIAN_POINT('Ctrl Pts',(-1.26441514053429,3.72613035403407,
18.9066664094867));
#258123=CARTESIAN_POINT('Ctrl Pts',(-1.15004282740772,3.76110229788131,
18.900630185024));
#258124=CARTESIAN_POINT('Ctrl Pts',(-1.03891586331661,3.79508190222671,
18.8947652402592));
#258125=CARTESIAN_POINT('Ctrl Pts',(-0.926230951465942,3.8241477588249,
18.8889002954944));
#258126=CARTESIAN_POINT('Ctrl Pts',(-0.812459787741505,3.8481681477429,
18.8830353507297));
#258127=CARTESIAN_POINT('Ctrl Pts',(-0.698705966307203,3.872184875201,18.8771712999662));
#258128=CARTESIAN_POINT('Ctrl Pts',(-0.583866624546522,3.89115757953955,
18.8713072492028));
#258129=CARTESIAN_POINT('Ctrl Pts',(-0.468424941049874,3.90500538726932,
18.8654431984393));
#258130=CARTESIAN_POINT('Ctrl Pts',(-0.352973253377511,3.91885439505004,
18.8595786394973));
#258131=CARTESIAN_POINT('Ctrl Pts',(-0.23691952853528,3.92757757438164,
18.8537140805552));
#258132=CARTESIAN_POINT('Ctrl Pts',(-0.120752695437392,3.93114586177422,
18.8478495216132));
#258133=CARTESIAN_POINT('Ctrl Pts',(0.00136544168213387,3.93489695490011,
18.8416845174211));
#258134=CARTESIAN_POINT('Ctrl Pts',(0.123608077433709,3.93295095848204,
18.835519513229));
#258135=CARTESIAN_POINT('Ctrl Pts',(0.245407968231507,3.92533615492081,
18.8293545090369));
#258136=CARTESIAN_POINT('Ctrl Pts',(0.361440802866056,3.91808190176338,
18.8234814092561));
#258137=CARTESIAN_POINT('Ctrl Pts',(0.477071446451001,3.90568346212199,
18.8176083094753));
#258138=CARTESIAN_POINT('Ctrl Pts',(0.591816564619008,3.88821837784898,
18.8117352096945));
#258139=CARTESIAN_POINT('Ctrl Pts',(0.706639073366195,3.87074151413813,
18.805858148764));
#258140=CARTESIAN_POINT('Ctrl Pts',(0.82057446491756,3.84819128021455,18.7999810878335));
#258141=CARTESIAN_POINT('Ctrl Pts',(0.933151490277918,3.82069591778672,
18.794104026903));
#258142=CARTESIAN_POINT('Ctrl Pts',(1.04588576594911,3.79316214917189,18.7882187567517));
#258143=CARTESIAN_POINT('Ctrl Pts',(1.15725749601787,3.76066958284886,18.7823334866004));
#258144=CARTESIAN_POINT('Ctrl Pts',(1.26681240886458,3.72339567072138,18.7764482164491));
#258145=CARTESIAN_POINT('Ctrl Pts',(1.28281361141082,3.71795157513366,18.7755886347354));
#258146=CARTESIAN_POINT('Ctrl Pts',(1.29877609546574,3.71240556355235,18.7747290530217));
#258147=CARTESIAN_POINT('Ctrl Pts',(1.31469848687477,3.70675827221161,18.773869471308));
#258148=CARTESIAN_POINT('Ctrl Pts',(1.42373525580808,3.66808553862523,18.7679830431773));
#258149=CARTESIAN_POINT('Ctrl Pts',(1.53123667264062,3.62453649152885,18.7620966150467));
#258150=CARTESIAN_POINT('Ctrl Pts',(1.63673641344779,3.57625263549628,18.7562101869161));
#258151=CARTESIAN_POINT('Ctrl Pts',(1.74210449190753,3.52802903710775,18.7503311049736));
#258152=CARTESIAN_POINT('Ctrl Pts',(1.8454754922307,3.47508255194167,18.7444520230311));
#258153=CARTESIAN_POINT('Ctrl Pts',(1.9463999146736,3.41760389339646,18.7385729410886));
#258154=CARTESIAN_POINT('Ctrl Pts',(2.04722499176466,3.36018181419465,18.7326996462435));
#258155=CARTESIAN_POINT('Ctrl Pts',(2.14560792669137,3.29823663887568,18.7268263513984));
#258156=CARTESIAN_POINT('Ctrl Pts',(2.24112140797721,3.2320061625415,18.7209530565534));
#258157=CARTESIAN_POINT('Ctrl Pts',(2.33927549178774,3.16394465292631,18.7149173863348));
#258158=CARTESIAN_POINT('Ctrl Pts',(2.43439874195802,3.09135761886026,18.7088817161163));
#258159=CARTESIAN_POINT('Ctrl Pts',(2.52605653718554,3.01455259880172,18.7028460458977));
#258160=CARTESIAN_POINT('Ctrl Pts',(2.6151531417599,2.93989373880519,18.6969790302067));
#258161=CARTESIAN_POINT('Ctrl Pts',(2.7009750644671,2.8612497813171,18.6911120145157));
#258162=CARTESIAN_POINT('Ctrl Pts',(2.7831551469449,2.77894520061733,18.6852449988246));
#258163=CARTESIAN_POINT('Ctrl Pts',(2.86532485412331,2.69665101093495,18.6793787238489));
#258164=CARTESIAN_POINT('Ctrl Pts',(2.94385334506628,2.61069740788989,18.6735124488732));
#258165=CARTESIAN_POINT('Ctrl Pts',(3.01840991512097,2.52144612956522,18.6676461738975));
#258166=CARTESIAN_POINT('Ctrl Pts',(3.09297487133345,2.43218481221512,18.6617792390804));
#258167=CARTESIAN_POINT('Ctrl Pts',(3.16356675484448,2.33962539751845,18.6559123042634));
#258168=CARTESIAN_POINT('Ctrl Pts',(3.22989523474795,2.2441625994015,18.6500453694463));
#258169=CARTESIAN_POINT('Ctrl Pts',(3.29956371003566,2.14389273642279,18.6438830029348));
#258170=CARTESIAN_POINT('Ctrl Pts',(3.36452792857829,2.04041987981295,18.6377206364233));
#258171=CARTESIAN_POINT('Ctrl Pts',(3.4245038148658,1.93423437617307,18.6315582699117));
#258172=CARTESIAN_POINT('Ctrl Pts',(3.48169104609249,1.83298610248407,18.6256824304634));
#258173=CARTESIAN_POINT('Ctrl Pts',(3.53434325267981,1.72927216476109,18.619806591015));
#258174=CARTESIAN_POINT('Ctrl Pts',(3.58226258738736,1.62354049995828,18.6139307515667));
#258175=CARTESIAN_POINT('Ctrl Pts',(3.6302152500197,1.51773529872195,18.6080508254686));
#258176=CARTESIAN_POINT('Ctrl Pts',(3.67342833320686,1.40990995629303,18.6021708993706));
#258177=CARTESIAN_POINT('Ctrl Pts',(3.71175311641914,1.30052981617216,18.5962909732725));
#258178=CARTESIAN_POINT('Ctrl Pts',(3.75013246205207,1.19099395318178,18.5904026760116));
#258179=CARTESIAN_POINT('Ctrl Pts',(3.78360950228262,1.07989926721846,18.5845143787507));
#258180=CARTESIAN_POINT('Ctrl Pts',(3.81208604666243,0.967723603536469,
18.5786260814898));
#258181=CARTESIAN_POINT('Ctrl Pts',(3.81616307805429,0.951663238341362,
18.5777830447626));
#258182=CARTESIAN_POINT('Ctrl Pts',(3.82013769526064,0.935580726698167,
18.5769400080353));
#258183=CARTESIAN_POINT('Ctrl Pts',(3.82400969690509,0.919477480950912,
18.5760969713081));
#258184=CARTESIAN_POINT('Ctrl Pts',(3.85096434828551,0.807375933723437,
18.5702282338512));
#258185=CARTESIAN_POINT('Ctrl Pts',(3.87303090986046,0.693898836985092,
18.5643594963943));
#258186=CARTESIAN_POINT('Ctrl Pts',(3.89007150739674,0.579510713740539,
18.5584907589374));
#258187=CARTESIAN_POINT('Ctrl Pts',(3.90708995623147,0.465271267700331,
18.5526296494357));
#258188=CARTESIAN_POINT('Ctrl Pts',(3.91909537116961,0.350123555482149,
18.546768539934));
#258189=CARTESIAN_POINT('Ctrl Pts',(3.92600019717784,0.234545201953788,
18.5409074304324));
#258190=CARTESIAN_POINT('Ctrl Pts',(3.93289790151264,0.119086056539917,
18.5350523661095));
#258191=CARTESIAN_POINT('Ctrl Pts',(3.93470545608126,0.00319756395961585,
18.5291973017866));
#258192=CARTESIAN_POINT('Ctrl Pts',(3.93138681688566,-0.112635234352483,
18.5233422374637));
#258193=CARTESIAN_POINT('Ctrl Pts',(3.9279619922646,-0.232174297264666,
18.5172998305405));
#258194=CARTESIAN_POINT('Ctrl Pts',(3.91907734655091,-0.351653598483055,
18.5112574236174));
#258195=CARTESIAN_POINT('Ctrl Pts',(3.90475145217433,-0.470537030150045,
18.5052150166942));
#258196=CARTESIAN_POINT('Ctrl Pts',(3.89088586043468,-0.585600640475025,
18.4993667572195));
#258197=CARTESIAN_POINT('Ctrl Pts',(3.87192338100028,-0.700105644022471,
18.4935184977448));
#258198=CARTESIAN_POINT('Ctrl Pts',(3.8479336621843,-0.813569622975753,
18.4876702382701));
#258199=CARTESIAN_POINT('Ctrl Pts',(3.82394764991499,-0.927016071105226,
18.4818228823845));
#258200=CARTESIAN_POINT('Ctrl Pts',(3.79493602828602,-1.03942140959071,
18.4759755264988));
#258201=CARTESIAN_POINT('Ctrl Pts',(3.76101959801277,-1.15031325445021,
18.4701281706132));
#258202=CARTESIAN_POINT('Ctrl Pts',(3.72710016811007,-1.26121490678183,
18.4642802975769));
#258203=CARTESIAN_POINT('Ctrl Pts',(3.68827518840264,-1.37060240357491,
18.4584324245407));
#258204=CARTESIAN_POINT('Ctrl Pts',(3.64471516728602,-1.47801906258182,
18.4525845515045));
#258205=CARTESIAN_POINT('Ctrl Pts',(3.6011407108324,-1.58547131834998,18.4467347405441));
#258206=CARTESIAN_POINT('Ctrl Pts',(3.55282824846559,-1.69095105434521,
18.4408849295837));
#258207=CARTESIAN_POINT('Ctrl Pts',(3.49999590859855,-1.79402275342131,
18.4350351186233));
#258208=CARTESIAN_POINT('Ctrl Pts',(3.44710407083485,-1.89721052816843,
18.4291787198144));
#258209=CARTESIAN_POINT('Ctrl Pts',(3.38968238537155,-1.99798448502726,
18.4233223210056));
#258210=CARTESIAN_POINT('Ctrl Pts',(3.32799434560108,-2.09593478802352,
18.4174659221967));
#258211=CARTESIAN_POINT('Ctrl Pts',(3.26626468939241,-2.19395117097219,
18.4116055725011));
#258212=CARTESIAN_POINT('Ctrl Pts',(3.20026318330507,-2.28913976787733,
18.4057452228055));
#258213=CARTESIAN_POINT('Ctrl Pts',(3.13029491473867,-2.38112216124273,
18.3998848731099));
#258214=CARTESIAN_POINT('Ctrl Pts',(3.06022529354294,-2.47323779582747,
18.3940160343969));
#258215=CARTESIAN_POINT('Ctrl Pts',(2.98617770693884,-2.56213764191437,
18.3881471956839));
#258216=CARTESIAN_POINT('Ctrl Pts',(2.90849553066704,-2.64747856423614,
18.3822783569709));
#258217=CARTESIAN_POINT('Ctrl Pts',(2.89105048699147,-2.66664352830727,
18.3809603950833));
#258218=CARTESIAN_POINT('Ctrl Pts',(2.87342228256386,-2.68562916758781,
18.3796424331956));
#258219=CARTESIAN_POINT('Ctrl Pts',(2.85561503733998,-2.70443187352128,
18.378324471308));
#258220=CARTESIAN_POINT('Ctrl Pts',(2.77619379146872,-2.78829292626762,
18.3724462922967));
#258221=CARTESIAN_POINT('Ctrl Pts',(2.69294508776773,-2.86878994417562,
18.3665681132853));
#258222=CARTESIAN_POINT('Ctrl Pts',(2.60618517272479,-2.94555391148583,
18.3606899342739));
#258223=CARTESIAN_POINT('Ctrl Pts',(2.5195362893618,-3.02221963950839,18.3548192779081));
#258224=CARTESIAN_POINT('Ctrl Pts',(2.42938543727218,-3.09516154721246,
18.3489486215423));
#258225=CARTESIAN_POINT('Ctrl Pts',(2.33608716590236,-3.16404578874994,
18.3430779651765));
#258226=CARTESIAN_POINT('Ctrl Pts',(2.24288348542366,-3.23286019167526,
18.3372132608033));
#258227=CARTESIAN_POINT('Ctrl Pts',(2.14653906301677,-3.29762486813221,
18.33134855643));
#258228=CARTESIAN_POINT('Ctrl Pts',(2.04744263576382,-3.35804521310486,
18.3254838520568));
#258229=CARTESIAN_POINT('Ctrl Pts',(1.94540402006663,-3.42025944758195,
18.3194450236922));
#258230=CARTESIAN_POINT('Ctrl Pts',(1.84044776017657,-3.47786705033665,
18.3134061953277));
#258231=CARTESIAN_POINT('Ctrl Pts',(1.73303209652776,-3.53059325785407,
18.3073673669632));
#258232=CARTESIAN_POINT('Ctrl Pts',(1.62883166012331,-3.581741234291,18.3015092962724));
#258233=CARTESIAN_POINT('Ctrl Pts',(1.52231735461547,-3.62829569046279,
18.2956512255816));
#258234=CARTESIAN_POINT('Ctrl Pts',(1.41393308472613,-3.67005207482358,
18.2897931548907));
#258235=CARTESIAN_POINT('Ctrl Pts',(1.30556466749011,-3.71180235175304,
18.2839359410213));
#258236=CARTESIAN_POINT('Ctrl Pts',(1.1953272144696,-3.74875580416738,18.2780787271519));
#258237=CARTESIAN_POINT('Ctrl Pts',(1.08368403454574,-3.78075626208179,
18.2722215132825));
#258238=CARTESIAN_POINT('Ctrl Pts',(0.97203030496013,-3.81275974386212,
18.2663637459389));
#258239=CARTESIAN_POINT('Ctrl Pts',(0.858970980853819,-3.83980918710216,
18.2605059785952));
#258240=CARTESIAN_POINT('Ctrl Pts',(0.744983253302858,-3.86179866801705,
18.2546482112516));
#258241=CARTESIAN_POINT('Ctrl Pts',(0.630957311268464,-3.88379552092428,
18.2487884800864));
#258242=CARTESIAN_POINT('Ctrl Pts',(0.516002751566652,-3.90072896020009,
18.2429287489213));
#258243=CARTESIAN_POINT('Ctrl Pts',(0.400604948507621,-3.91254452693272,
18.2370690177561));
#258244=CARTESIAN_POINT('Ctrl Pts',(0.285077628217789,-3.92437335491854,
18.2312027098959));
#258245=CARTESIAN_POINT('Ctrl Pts',(0.169106482113305,-3.9310728038183,
18.2253364020358));
#258246=CARTESIAN_POINT('Ctrl Pts',(0.05318006704996,-3.93264044637551,
18.2194700941756));
#258247=CARTESIAN_POINT('Ctrl Pts',(-0.0628245292563574,-3.93420914615719,
18.2135998300537));
#258248=CARTESIAN_POINT('Ctrl Pts',(-0.178783923287657,-3.93063916050815,
18.2077295659318));
#258249=CARTESIAN_POINT('Ctrl Pts',(-0.294213214673637,-3.9219800591425,
18.2018593018099));
#258250=CARTESIAN_POINT('Ctrl Pts',(-0.409808110012898,-3.91330853474799,
18.1959806157447));
#258251=CARTESIAN_POINT('Ctrl Pts',(-0.524870977130521,-3.89953337277573,
18.1901019296795));
#258252=CARTESIAN_POINT('Ctrl Pts',(-0.638925607187836,-3.88075547651223,
18.1842232436143));
#258253=CARTESIAN_POINT('Ctrl Pts',(-0.662668191845239,-3.87684650945407,
18.1829994861789));
#258254=CARTESIAN_POINT('Ctrl Pts',(-0.68636713462133,-3.87272092654932,
18.1817757287435));
#258255=CARTESIAN_POINT('Ctrl Pts',(-0.710018223193508,-3.8683799093074,
18.180551971308));
#258256=CARTESIAN_POINT('Ctrl Pts',(-0.823612685446079,-3.84753031848538,
18.1746743531434));
#258257=CARTESIAN_POINT('Ctrl Pts',(-0.93647409787697,-3.82163880661589,
18.1687967349788));
#258258=CARTESIAN_POINT('Ctrl Pts',(-1.04812076214779,-3.79076929764325,
18.1629191168142));
#258259=CARTESIAN_POINT('Ctrl Pts',(-1.15962482068919,-3.75993921814102,
18.1570490061021));
#258260=CARTESIAN_POINT('Ctrl Pts',(-1.26991682277623,-3.72414389573843,
18.15117889539));
#258261=CARTESIAN_POINT('Ctrl Pts',(-1.37852367281272,-3.68349853854931,
18.1453087846778));
#258262=CARTESIAN_POINT('Ctrl Pts',(-1.48702069364622,-3.64289428417447,
18.1394446101436));
#258263=CARTESIAN_POINT('Ctrl Pts',(-1.5938355681219,-3.59744989487158,
18.1335804356094));
#258264=CARTESIAN_POINT('Ctrl Pts',(-1.69850946074777,-3.54733063186255,
18.1277162610751));
#258265=CARTESIAN_POINT('Ctrl Pts',(-1.80630452693748,-3.49571690910983,
18.1216772281681));
#258266=CARTESIAN_POINT('Ctrl Pts',(-1.911828495614,-3.43914525844542,18.1156381952612));
#258267=CARTESIAN_POINT('Ctrl Pts',(-2.01460110954849,-3.37785011055938,
18.1095991623542));
#258268=CARTESIAN_POINT('Ctrl Pts',(-2.11428581510268,-3.31839663813125,
18.1037415783723));
#258269=CARTESIAN_POINT('Ctrl Pts',(-2.21138176076628,-3.25449968645423,
18.0978839943904));
#258270=CARTESIAN_POINT('Ctrl Pts',(-2.30547553699735,-3.18641986378236,
18.0920264104085));
#258271=CARTESIAN_POINT('Ctrl Pts',(-2.39955582200104,-3.11834980244013,
18.0861696662908));
#258272=CARTESIAN_POINT('Ctrl Pts',(-2.49063445943363,-3.04609830442356,
18.0803129221731));
#258273=CARTESIAN_POINT('Ctrl Pts',(-2.57832802573415,-2.96996861796784,
18.0744561780554));
#258274=CARTESIAN_POINT('Ctrl Pts',(-2.66603014227994,-2.89383150876131,
18.068598862897));
#258275=CARTESIAN_POINT('Ctrl Pts',(-2.75034622007518,-2.81381572982717,
18.0627415477386));
#258276=CARTESIAN_POINT('Ctrl Pts',(-2.8309273955115,-2.73026355528957,
18.0568842325802));
#258277=CARTESIAN_POINT('Ctrl Pts',(-2.91153583817867,-2.64668310818809,
18.0510249354109));
#258278=CARTESIAN_POINT('Ctrl Pts',(-2.9884065791666,-2.55956418264079,
18.0451656382416));
#258279=CARTESIAN_POINT('Ctrl Pts',(-3.06122944348281,-2.46928396389599,
18.0393063410724));
#258280=CARTESIAN_POINT('Ctrl Pts',(-3.13413441001506,-2.37890196110175,
18.0334404379932));
#258281=CARTESIAN_POINT('Ctrl Pts',(-3.20298213222088,-2.28535187275344,
18.027574534914));
#258282=CARTESIAN_POINT('Ctrl Pts',(-3.26750432365938,-2.18904191254239,
18.0217086318348));
#258283=CARTESIAN_POINT('Ctrl Pts',(-3.3320702153965,-2.09266672246349,
18.0158387558323));
#258284=CARTESIAN_POINT('Ctrl Pts',(-3.39230452897062,-1.99352828995328,
18.0099688798298));
#258285=CARTESIAN_POINT('Ctrl Pts',(-3.44798456722994,-1.89206010056345,
18.0040990038274));
#258286=CARTESIAN_POINT('Ctrl Pts',(-3.5037447516381,-1.79044585731188,
17.9982206786935));
#258287=CARTESIAN_POINT('Ctrl Pts',(-3.5549373969427,-1.68649553343672,
17.9923423535597));
#258288=CARTESIAN_POINT('Ctrl Pts',(-3.60138758242706,-1.580663304167,17.9864640284259));
#258289=CARTESIAN_POINT('Ctrl Pts',(-3.61109263489564,-1.55855128615849,
17.98523584272));
#258290=CARTESIAN_POINT('Ctrl Pts',(-3.62059083489173,-1.53635716961777,
17.984007657014));
#258291=CARTESIAN_POINT('Ctrl Pts',(-3.62988086315592,-1.51408517570659,
17.9827794713081));
#258292=CARTESIAN_POINT('Ctrl Pts',(-3.67943525765663,-1.39528304279522,
17.9762281458156));
#258293=CARTESIAN_POINT('Ctrl Pts',(-3.72320130331636,-1.27393123983944,
17.9696768203231));
#258294=CARTESIAN_POINT('Ctrl Pts',(-3.76093818682342,-1.15057939964759,
17.9631254948306));
#258295=CARTESIAN_POINT('Ctrl Pts',(-3.79845718965327,-1.02793975346797,
17.956611994593));
#258296=CARTESIAN_POINT('Ctrl Pts',(-3.8300163393861,-0.903323327055673,
17.9500984943553));
#258297=CARTESIAN_POINT('Ctrl Pts',(-3.85542529309697,-0.777293258267532,
17.9435849941176));
#258298=CARTESIAN_POINT('Ctrl Pts',(-3.88105557945092,-0.65016536512386,
17.9370147559977));
#258299=CARTESIAN_POINT('Ctrl Pts',(-3.90042783164738,-0.521599290631718,
17.9304445178778));
#258300=CARTESIAN_POINT('Ctrl Pts',(-3.91339665537872,-0.392193342205873,
17.9238742797579));
#258301=CARTESIAN_POINT('Ctrl Pts',(-3.92636547911007,-0.262787393780027,
17.917304041638));
#258302=CARTESIAN_POINT('Ctrl Pts',(-3.93293072645011,-0.132541816141693,
17.9107338035181));
#258303=CARTESIAN_POINT('Ctrl Pts',(-3.93299945431987,-0.00207179139282337,
17.9041635653982));
#258304=CARTESIAN_POINT('',(-3.93113584355659,0.00341903309056729,16.654163522035));
#258305=CARTESIAN_POINT('Ctrl Pts',(-3.92772530458877,-0.00206815318150977,
17.904163522035));
#258306=CARTESIAN_POINT('Ctrl Pts',(-3.92400119087583,0.785602615821928,
17.8644446717927));
#258307=CARTESIAN_POINT('Ctrl Pts',(-3.31313291637687,2.88598162922864,
17.7588016548837));
#258308=CARTESIAN_POINT('Ctrl Pts',(0.103372134188801,4.64201135434511,
17.587234471308));
#258309=CARTESIAN_POINT('Ctrl Pts',(3.94766405912961,2.44442860147959,17.3894619713081));
#258310=CARTESIAN_POINT('Ctrl Pts',(4.20154746985927,-1.97643607916758,
17.191689471308));
#258311=CARTESIAN_POINT('Ctrl Pts',(0.634085622619158,-4.59968875606274,
16.993916971308));
#258312=CARTESIAN_POINT('Ctrl Pts',(-3.12038746571605,-3.18621803741959,
16.8147416548837));
#258313=CARTESIAN_POINT('Ctrl Pts',(-3.92323046052567,-0.9330686808722,
16.701490505126));
#258314=CARTESIAN_POINT('Ctrl Pts',(-3.93113584355659,0.00341903309056729,
16.654163522035));
#258315=CARTESIAN_POINT('',(-3.93909859392385,-0.000902565702873282,15.404163522035));
#258316=CARTESIAN_POINT('Ctrl Pts',(-3.93113584355659,0.00341903309056729,
16.654163522035));
#258317=CARTESIAN_POINT('Ctrl Pts',(-3.93424227143049,0.371412782013792,
16.6355663384593));
#258318=CARTESIAN_POINT('Ctrl Pts',(-3.71846148902814,2.04031595755692,
16.5510449882172));
#258319=CARTESIAN_POINT('Ctrl Pts',(-1.35548843458597,4.44093334314415,
16.4005994713079));
#258320=CARTESIAN_POINT('Ctrl Pts',(2.98365116613823,3.55767782069685,16.2028269713081));
#258321=CARTESIAN_POINT('Ctrl Pts',(4.60914037559767,-0.561310729341494,
16.005054471308));
#258322=CARTESIAN_POINT('Ctrl Pts',(2.04258527805945,-4.16978279364218,
15.807281971308));
#258323=CARTESIAN_POINT('Ctrl Pts',(-2.38171473979766,-3.98580973400276,
15.609509471308));
#258324=CARTESIAN_POINT('Ctrl Pts',(-3.91594831015911,-1.3977922893583,
15.4751366548837));
#258325=CARTESIAN_POINT('Ctrl Pts',(-3.93925372265761,-0.0505946126246084,
15.406688005126));
#258326=CARTESIAN_POINT('Ctrl Pts',(-3.93909859392385,-0.000902565702873282,
15.404163522035));
#258327=CARTESIAN_POINT('',(-3.93161494696421,-0.00266436291445193,14.1541639891901));
#258328=CARTESIAN_POINT('Ctrl Pts',(-3.93909859392385,-0.000902565702873282,
15.404163522035));
#258329=CARTESIAN_POINT('Ctrl Pts',(-3.93520270225845,1.24705986361814,
15.3407638384593));
#258330=CARTESIAN_POINT('Ctrl Pts',(-2.62185579271932,3.79973940462817,
15.2114399882171));
#258331=CARTESIAN_POINT('Ctrl Pts',(1.71950142291712,4.31306839047415,15.016191971308));
#258332=CARTESIAN_POINT('Ctrl Pts',(4.55309266773441,0.910269848327174,
14.818419471308));
#258333=CARTESIAN_POINT('Ctrl Pts',(3.24561556297038,-3.32042521907114,
14.620646971308));
#258334=CARTESIAN_POINT('Ctrl Pts',(-1.01377068166446,-4.53117126656537,
14.422874471308));
#258335=CARTESIAN_POINT('Ctrl Pts',(-3.63768788039038,-2.24294951629792,
14.267380475811));
#258336=CARTESIAN_POINT('Ctrl Pts',(-3.93159311262421,-0.471316921337659,
14.1778106469806));
#258337=CARTESIAN_POINT('Ctrl Pts',(-3.92866495709156,-0.00268210302728455,
14.1541649848169));
#258338=CARTESIAN_POINT('',(-3.93299876508478,0.00311670364493707,12.9041635219956));
#258339=CARTESIAN_POINT('Ctrl Pts',(-3.93299910315985,-0.00265603912754121,
14.154163522035));
#258340=CARTESIAN_POINT('Ctrl Pts',(-3.9330778785801,0.113992715771548,
14.148284295995));
#258341=CARTESIAN_POINT('Ctrl Pts',(-3.92796280482098,0.230678078603042,
14.142405069955));
#258342=CARTESIAN_POINT('Ctrl Pts',(-3.91767077265389,0.346907360967524,
14.136525843915));
#258343=CARTESIAN_POINT('Ctrl Pts',(-3.90737884254069,0.463135490823962,
14.1306466761723));
#258344=CARTESIAN_POINT('Ctrl Pts',(-3.8919100916819,0.578907143014563,
14.1247675084296));
#258345=CARTESIAN_POINT('Ctrl Pts',(-3.87133335419905,0.693734142641077,
14.118888340687));
#258346=CARTESIAN_POINT('Ctrl Pts',(-3.85075201344031,0.808586830516746,
14.1130078577002));
#258347=CARTESIAN_POINT('Ctrl Pts',(-3.82506048462843,0.922494044084642,
14.1071273747135));
#258348=CARTESIAN_POINT('Ctrl Pts',(-3.79437872290933,1.03497782929536,
14.1012468917268));
#258349=CARTESIAN_POINT('Ctrl Pts',(-3.76223968652257,1.1528041946425,14.0950871066919));
#258350=CARTESIAN_POINT('Ctrl Pts',(-3.72462484474384,1.26906810645793,
14.088927321657));
#258351=CARTESIAN_POINT('Ctrl Pts',(-3.68173017534728,1.38323964515817,
14.0827675366221));
#258352=CARTESIAN_POINT('Ctrl Pts',(-3.64070817178212,1.49242676172739,
14.0768766712252));
#258353=CARTESIAN_POINT('Ctrl Pts',(-3.59485785034093,1.59969999551068,
14.0709858058282));
#258354=CARTESIAN_POINT('Ctrl Pts',(-3.54439896097547,1.70461872729242,
14.0650949404312));
#258355=CARTESIAN_POINT('Ctrl Pts',(-3.49390086133653,1.8096189886563,14.059199497398));
#258356=CARTESIAN_POINT('Ctrl Pts',(-3.43878725398647,1.91226074630146,
14.0533040543647));
#258357=CARTESIAN_POINT('Ctrl Pts',(-3.37932260894418,2.01213014108896,
14.0474086113315));
#258358=CARTESIAN_POINT('Ctrl Pts',(-3.31976746413456,2.11215152798851,
14.0415041959715));
#258359=CARTESIAN_POINT('Ctrl Pts',(-3.25584828985909,2.20939179302548,
14.0355997806116));
#258360=CARTESIAN_POINT('Ctrl Pts',(-3.18787143305446,2.30346797813977,
14.0296953652516));
#258361=CARTESIAN_POINT('Ctrl Pts',(-3.17879201118603,2.31603339249659,
14.0289067339371));
#258362=CARTESIAN_POINT('Ctrl Pts',(-3.16964025615249,2.3285424115323,14.0281181026225));
#258363=CARTESIAN_POINT('Ctrl Pts',(-3.16041694862804,2.34099417146319,
14.027329471308));
#258364=CARTESIAN_POINT('Ctrl Pts',(-3.09168960483071,2.43377828208552,
14.0214529963733));
#258365=CARTESIAN_POINT('Ctrl Pts',(-3.01875971553102,2.52368598879652,
14.0155765214385));
#258366=CARTESIAN_POINT('Ctrl Pts',(-2.94189651046244,2.61031299305828,
14.0097000465037));
#258367=CARTESIAN_POINT('Ctrl Pts',(-2.8651317994684,2.69682899171461,14.0038311018035));
#258368=CARTESIAN_POINT('Ctrl Pts',(-2.78444406782172,2.78007234256194,
13.9979621571032));
#258369=CARTESIAN_POINT('Ctrl Pts',(-2.70014481638619,2.85966903164384,
13.992093212403));
#258370=CARTESIAN_POINT('Ctrl Pts',(-2.61593113489753,2.93918492422589,
13.9862302251137));
#258371=CARTESIAN_POINT('Ctrl Pts',(-2.52811352405206,3.01506123645907,
13.9803672378245));
#258372=CARTESIAN_POINT('Ctrl Pts',(-2.43704216015887,3.08695878003063,
13.9745042505352));
#258373=CARTESIAN_POINT('Ctrl Pts',(-2.34322944318998,3.16102052257517,
13.9684647805674));
#258374=CARTESIAN_POINT('Ctrl Pts',(-2.24596427876282,3.23085983307217,
13.9624253105996));
#258375=CARTESIAN_POINT('Ctrl Pts',(-2.14566873027637,3.29614846448308,
13.9563858406318));
#258376=CARTESIAN_POINT('Ctrl Pts',(-2.0484141738828,3.35945752436892,13.9505294892639));
#258377=CARTESIAN_POINT('Ctrl Pts',(-1.94831071920802,3.4184876422181,13.9446731378961));
#258378=CARTESIAN_POINT('Ctrl Pts',(-1.84577418286868,3.47298238778366,
13.9388167865282));
#258379=CARTESIAN_POINT('Ctrl Pts',(-1.74325260953445,3.52746918101158,
13.932961289769));
#258380=CARTESIAN_POINT('Ctrl Pts',(-1.63829902486732,3.57742172440048,
13.9271057930098));
#258381=CARTESIAN_POINT('Ctrl Pts',(-1.53135433771683,3.6226292789017,13.9212502962506));
#258382=CARTESIAN_POINT('Ctrl Pts',(-1.42439946656333,3.6678411383748,13.9153942418911));
#258383=CARTESIAN_POINT('Ctrl Pts',(-1.315453496126,3.70830695004004,13.9095381875316));
#258384=CARTESIAN_POINT('Ctrl Pts',(-1.20497716694659,3.74386418385301,
13.903682133172));
#258385=CARTESIAN_POINT('Ctrl Pts',(-1.0944636756262,3.77943337844478,13.8978241089469));
#258386=CARTESIAN_POINT('Ctrl Pts',(-0.982419194522758,3.81009058551966,
13.8919660847218));
#258387=CARTESIAN_POINT('Ctrl Pts',(-0.869318781506862,3.83572338107422,
13.8861080604966));
#258388=CARTESIAN_POINT('Ctrl Pts',(-0.756091053279677,3.86138503103076,
13.8802434419933));
#258389=CARTESIAN_POINT('Ctrl Pts',(-0.64180542340723,3.88201088972378,
13.8743788234899));
#258390=CARTESIAN_POINT('Ctrl Pts',(-0.526946369473274,3.89753980399161,
13.8685142049866));
#258391=CARTESIAN_POINT('Ctrl Pts',(-0.412009668866924,3.91307921606938,
13.8626456219014));
#258392=CARTESIAN_POINT('Ctrl Pts',(-0.296499182246349,3.92351478552903,
13.8567770388163));
#258393=CARTESIAN_POINT('Ctrl Pts',(-0.180902007055634,3.92883741886111,
13.8509084557312));
#258394=CARTESIAN_POINT('Ctrl Pts',(-0.0651384508610817,3.93416771315096,
13.8450314258934));
#258395=CARTESIAN_POINT('Ctrl Pts',(0.050711631895831,3.93437038447231,
13.8391543960556));
#258396=CARTESIAN_POINT('Ctrl Pts',(0.166163602504942,3.92948834547229,
13.8332773662179));
#258397=CARTESIAN_POINT('Ctrl Pts',(0.190525507278744,3.92845817016569,
13.8320372345813));
#258398=CARTESIAN_POINT('Ctrl Pts',(0.214869714223744,3.9272017725209,13.8307971029446));
#258399=CARTESIAN_POINT('Ctrl Pts',(0.23919172235873,3.92571984735985,13.829556971308));
#258400=CARTESIAN_POINT('Ctrl Pts',(0.354443738328614,3.91869761213242,
13.8236804963725));
#258401=CARTESIAN_POINT('Ctrl Pts',(0.46957595871394,3.90658413568195,13.817804021437));
#258402=CARTESIAN_POINT('Ctrl Pts',(0.584102673278668,3.88938466432271,
13.8119275465015));
#258403=CARTESIAN_POINT('Ctrl Pts',(0.698482630981103,3.87220723271603,
13.8060586018005));
#258404=CARTESIAN_POINT('Ctrl Pts',(0.812258221494294,3.84995682811163,
13.8001896570996));
#258405=CARTESIAN_POINT('Ctrl Pts',(0.924946073218048,3.82269064425027,
13.7943207123986));
#258406=CARTESIAN_POINT('Ctrl Pts',(1.03751953847568,3.79545213757298,13.7884577251086));
#258407=CARTESIAN_POINT('Ctrl Pts',(1.14900706246548,3.76320807563182,13.7825947378186));
#258408=CARTESIAN_POINT('Ctrl Pts',(1.25893337942031,3.72606706141762,13.7767317505286));
#258409=CARTESIAN_POINT('Ctrl Pts',(1.37216860526202,3.68780805985148,13.7706922805611));
#258410=CARTESIAN_POINT('Ctrl Pts',(1.48374670444182,3.64435268868069,13.7646528105936));
#258411=CARTESIAN_POINT('Ctrl Pts',(1.59316238680228,3.59587577778744,13.7586133406261));
#258412=CARTESIAN_POINT('Ctrl Pts',(1.69926055180413,3.54886870183842,13.7527569892575));
#258413=CARTESIAN_POINT('Ctrl Pts',(1.80332513603157,3.49714038499151,13.7469006378889));
#258414=CARTESIAN_POINT('Ctrl Pts',(1.90491445763304,3.44089957846791,13.7410442865203));
#258415=CARTESIAN_POINT('Ctrl Pts',(2.00648895445501,3.38466697908205,13.7351887897603));
#258416=CARTESIAN_POINT('Ctrl Pts',(2.10558854597426,3.32392339926162,13.7293332930004));
#258417=CARTESIAN_POINT('Ctrl Pts',(2.20179617070332,3.25892353740866,13.7234777962405));
#258418=CARTESIAN_POINT('Ctrl Pts',(2.29801295697871,3.19391748582545,13.7176217418803));
#258419=CARTESIAN_POINT('Ctrl Pts',(2.39133688705236,3.12465457751915,13.71176568752));
#258420=CARTESIAN_POINT('Ctrl Pts',(2.48138049870848,3.05143242111459,13.7059096331598));
#258421=CARTESIAN_POINT('Ctrl Pts',(2.57145439932694,2.97818563416605,13.700051608934));
#258422=CARTESIAN_POINT('Ctrl Pts',(2.65824546736195,2.9009772110248,13.6941935847082));
#258423=CARTESIAN_POINT('Ctrl Pts',(2.74140043679727,2.82014408233475,13.6883355604823));
#258424=CARTESIAN_POINT('Ctrl Pts',(2.82464901236726,2.73921996116667,13.6824709419783));
#258425=CARTESIAN_POINT('Ctrl Pts',(2.90425302396592,2.65466327850392,13.6766063234742));
#258426=CARTESIAN_POINT('Ctrl Pts',(2.97989704860918,2.56684681656119,13.6707417049702));
#258427=CARTESIAN_POINT('Ctrl Pts',(3.05559220989862,2.47897098919779,13.6648731218844));
#258428=CARTESIAN_POINT('Ctrl Pts',(3.12732179899887,2.38783131792171,13.6590045387986));
#258429=CARTESIAN_POINT('Ctrl Pts',(3.19481260479563,2.29383116646343,13.6531359557127));
#258430=CARTESIAN_POINT('Ctrl Pts',(3.26240055127037,2.19969571896985,13.6472589258743));
#258431=CARTESIAN_POINT('Ctrl Pts',(3.32573731448605,2.10269191915057,13.6413818960359));
#258432=CARTESIAN_POINT('Ctrl Pts',(3.3845946194405,2.00324942582156,13.6355048661975));
#258433=CARTESIAN_POINT('Ctrl Pts',(3.39701429528465,1.98226573427747,13.6342647345677));
#258434=CARTESIAN_POINT('Ctrl Pts',(3.40923468476728,1.96117353142325,13.6330246029378));
#258435=CARTESIAN_POINT('Ctrl Pts',(3.42125391619583,1.9399769691712,13.631784471308));
#258436=CARTESIAN_POINT('Ctrl Pts',(3.47820812214531,1.83953515813686,13.6259079963713));
#258437=CARTESIAN_POINT('Ctrl Pts',(3.53082914630815,1.73641778663748,13.6200315214345));
#258438=CARTESIAN_POINT('Ctrl Pts',(3.57885655466612,1.63103487428178,13.6141550464978));
#258439=CARTESIAN_POINT('Ctrl Pts',(3.62682241972617,1.52578700173337,13.6082861017955));
#258440=CARTESIAN_POINT('Ctrl Pts',(3.67020620576742,1.41827973399494,13.6024171570933));
#258441=CARTESIAN_POINT('Ctrl Pts',(3.70879230016866,1.3089494544136,13.596548212391));
#258442=CARTESIAN_POINT('Ctrl Pts',(3.74733922684326,1.19973015311524,13.5906852250997));
#258443=CARTESIAN_POINT('Ctrl Pts',(3.78109801249512,1.08869190775323,13.5848222378084));
#258444=CARTESIAN_POINT('Ctrl Pts',(3.80990055930484,0.976292337473103,
13.5789592505172));
#258445=CARTESIAN_POINT('Ctrl Pts',(3.83957009597436,0.860509410564029,
13.5729197805501));
#258446=CARTESIAN_POINT('Ctrl Pts',(3.86398009968608,0.743282309532098,
13.5668803105831));
#258447=CARTESIAN_POINT('Ctrl Pts',(3.88300161831438,0.625129932228423,
13.560840840616));
#258448=CARTESIAN_POINT('Ctrl Pts',(3.90144639861543,0.510559971543423,
13.5549844892461));
#258449=CARTESIAN_POINT('Ctrl Pts',(3.91482467444911,0.395120471390472,
13.5491281378762));
#258450=CARTESIAN_POINT('Ctrl Pts',(3.9230706113381,0.279295503822177,13.5432717865062));
#258451=CARTESIAN_POINT('Ctrl Pts',(3.93131534490975,0.163487438419818,
13.537416289745));
#258452=CARTESIAN_POINT('Ctrl Pts',(3.93442919952694,0.0472944289759187,
13.5315607929837));
#258453=CARTESIAN_POINT('Ctrl Pts',(3.93239828128702,-0.0687950385629423,
13.5257052962225));
#258454=CARTESIAN_POINT('Ctrl Pts',(3.93036716964921,-0.184895560933151,
13.5198492418609));
#258455=CARTESIAN_POINT('Ctrl Pts',(3.92319031845648,-0.300892109174371,
13.5139931874993));
#258456=CARTESIAN_POINT('Ctrl Pts',(3.91090594330545,-0.416297613034404,
13.5081371331377));
#258457=CARTESIAN_POINT('Ctrl Pts',(3.89861743592375,-0.531741937115748,
13.5022791089105));
#258458=CARTESIAN_POINT('Ctrl Pts',(3.88121803186177,-0.646594411352283,
13.4964210846833));
#258459=CARTESIAN_POINT('Ctrl Pts',(3.85879755477098,-0.760375191134925,
13.4905630604562));
#258460=CARTESIAN_POINT('Ctrl Pts',(3.83635183933042,-0.874284052006421,
13.4846984419508));
#258461=CARTESIAN_POINT('Ctrl Pts',(3.80887384969728,-0.987118405537053,
13.4788338234453));
#258462=CARTESIAN_POINT('Ctrl Pts',(3.77650409680879,-1.09841058206228,
13.4729692049399));
#258463=CARTESIAN_POINT('Ctrl Pts',(3.74411246141731,-1.20977799398997,
13.4671006218528));
#258464=CARTESIAN_POINT('Ctrl Pts',(3.70682261015782,-1.31960076317401,
13.4612320387656));
#258465=CARTESIAN_POINT('Ctrl Pts',(3.66482370558852,-1.42742993066436,
13.4553634556784));
#258466=CARTESIAN_POINT('Ctrl Pts',(3.62276435127318,-1.53541429853093,
13.4494864258386));
#258467=CARTESIAN_POINT('Ctrl Pts',(3.57598258358747,-1.64139896238258,
13.4436093959988));
#258468=CARTESIAN_POINT('Ctrl Pts',(3.52471410888429,-1.74495829481166,
13.437732366159));
#258469=CARTESIAN_POINT('Ctrl Pts',(3.51389577748777,-1.76681069404737,
13.436492234542));
#258470=CARTESIAN_POINT('Ctrl Pts',(3.50287782348456,-1.78855520180486,
13.435252102925));
#258471=CARTESIAN_POINT('Ctrl Pts',(3.49166270678754,-1.81018798527365,
13.434011971308));
#258472=CARTESIAN_POINT('Ctrl Pts',(3.4385188700611,-1.91269687070594,13.4281354963722));
#258473=CARTESIAN_POINT('Ctrl Pts',(3.38076952327136,-2.01303219564053,
13.4222590214364));
#258474=CARTESIAN_POINT('Ctrl Pts',(3.31861637510571,-2.11075208276107,
13.4163825465005));
#258475=CARTESIAN_POINT('Ctrl Pts',(3.25654287124843,-2.20834674963047,
13.4105136017992));
#258476=CARTESIAN_POINT('Ctrl Pts',(3.19007700817169,-2.30333229878898,
13.4046446570979));
#258477=CARTESIAN_POINT('Ctrl Pts',(3.11946703335963,-2.39529005086701,
13.3987757123966));
#258478=CARTESIAN_POINT('Ctrl Pts',(3.04892873287071,-2.48715445905622,
13.3929127251062));
#258479=CARTESIAN_POINT('Ctrl Pts',(2.97425493800888,-2.57599685827205,
13.3870497378159));
#258480=CARTESIAN_POINT('Ctrl Pts',(2.89573760499766,-2.66142682089935,
13.3811867505256));
#258481=CARTESIAN_POINT('Ctrl Pts',(2.81485680973775,-2.74942832389657,
13.3751472805582));
#258482=CARTESIAN_POINT('Ctrl Pts',(2.72989765575555,-2.83380831947677,
13.3691078105908));
#258483=CARTESIAN_POINT('Ctrl Pts',(2.6412248117809,-2.91417578289865,13.3630683406234));
#258484=CARTESIAN_POINT('Ctrl Pts',(2.55524055587679,-2.99210647995857,
13.3572119892544));
#258485=CARTESIAN_POINT('Ctrl Pts',(2.46576489163852,-3.06626416307308,
13.3513556378854));
#258486=CARTESIAN_POINT('Ctrl Pts',(2.37316770886201,-3.13632970613975,
13.3454992865164));
#258487=CARTESIAN_POINT('Ctrl Pts',(2.28058403865545,-3.20638502464533,
13.3396437897562));
#258488=CARTESIAN_POINT('Ctrl Pts',(2.18488008469697,-3.27234914160957,
13.3337882929959));
#258489=CARTESIAN_POINT('Ctrl Pts',(2.08645775726643,-3.33394406478914,
13.3279327962356));
#258490=CARTESIAN_POINT('Ctrl Pts',(1.98802605738985,-3.39554485345786,
13.3220767418749));
#258491=CARTESIAN_POINT('Ctrl Pts',(1.88687581927528,-3.45277540231397,
13.3162206875143));
#258492=CARTESIAN_POINT('Ctrl Pts',(1.78343617899,-3.50540217314213,13.3103646331536));
#258493=CARTESIAN_POINT('Ctrl Pts',(1.67996174357306,-3.55804664661711,
13.3045066089274));
#258494=CARTESIAN_POINT('Ctrl Pts',(1.57419674222064,-3.60608407561705,
13.2986485847012));
#258495=CARTESIAN_POINT('Ctrl Pts',(1.46659239303793,-3.64932812346098,
13.292790560475));
#258496=CARTESIAN_POINT('Ctrl Pts',(1.35886691546933,-3.69262085039414,
13.2869259419706));
#258497=CARTESIAN_POINT('Ctrl Pts',(1.24929834064817,-3.73110927279107,
13.2810613234661));
#258498=CARTESIAN_POINT('Ctrl Pts',(1.1383553177923,-3.76465618223683,13.2751967049617));
#258499=CARTESIAN_POINT('Ctrl Pts',(1.0273372955672,-3.7982257699636,13.2693281218754));
#258500=CARTESIAN_POINT('Ctrl Pts',(0.914943374010366,-3.82684709123545,
13.2634595387892));
#258501=CARTESIAN_POINT('Ctrl Pts',(0.8016530447359,-3.85043392306187,13.257590955703));
#258502=CARTESIAN_POINT('Ctrl Pts',(0.688199654741695,-3.87405470382108,
13.2517139258641));
#258503=CARTESIAN_POINT('Ctrl Pts',(0.573847687929116,-3.89262646845106,
13.2458368960253));
#258504=CARTESIAN_POINT('Ctrl Pts',(0.459082455495839,-3.90611473193708,
13.2399598661865));
#258505=CARTESIAN_POINT('Ctrl Pts',(0.434865461839885,-3.90896093530674,
13.2387197345603));
#258506=CARTESIAN_POINT('Ctrl Pts',(0.410630067428487,-3.91158097243245,
13.2374796029342));
#258507=CARTESIAN_POINT('Ctrl Pts',(0.386380826472741,-3.9139748155723,
13.236239471308));
#258508=CARTESIAN_POINT('Ctrl Pts',(0.271473623326335,-3.92531825599066,
13.230362996372));
#258509=CARTESIAN_POINT('Ctrl Pts',(0.155877324156971,-3.93161588281209,
13.224486521436));
#258510=CARTESIAN_POINT('Ctrl Pts',(0.0400723249525348,-3.93279585139795,
13.2186100465));
#258511=CARTESIAN_POINT('Ctrl Pts',(-0.0755842793700643,-3.93397430794806,
13.2127411017985));
#258512=CARTESIAN_POINT('Ctrl Pts',(-0.191448642919037,-3.93004814395898,
13.206872157097));
#258513=CARTESIAN_POINT('Ctrl Pts',(-0.307034440858103,-3.92099717573565,
13.2010032123955));
#258514=CARTESIAN_POINT('Ctrl Pts',(-0.422502910702303,-3.91195539491144,
13.195140225105));
#258515=CARTESIAN_POINT('Ctrl Pts',(-0.537692968378007,-3.89779918952418,
13.1892772378144));
#258516=CARTESIAN_POINT('Ctrl Pts',(-0.652118139763882,-3.87856042002582,
13.1834142505239));
#258517=CARTESIAN_POINT('Ctrl Pts',(-0.769987640727734,-3.85874254138545,
13.1773747805566));
#258518=CARTESIAN_POINT('Ctrl Pts',(-0.887045031542341,-3.83353125909403,
13.1713353105893));
#258519=CARTESIAN_POINT('Ctrl Pts',(-1.00276369128009,-3.80301906114738,
13.1652958406219));
#258520=CARTESIAN_POINT('Ctrl Pts',(-1.1149737254482,-3.77343200248375,
13.1594394892528));
#258521=CARTESIAN_POINT('Ctrl Pts',(-1.22592461250148,-3.73886095797199,
13.1535831378836));
#258522=CARTESIAN_POINT('Ctrl Pts',(-1.33514715562305,-3.69944199479214,
13.1477267865145));
#258523=CARTESIAN_POINT('Ctrl Pts',(-1.44435376006093,-3.66002878396312,
13.141871289754));
#258524=CARTESIAN_POINT('Ctrl Pts',(-1.55183213403117,-3.61576920127481,
13.1360157929935));
#258525=CARTESIAN_POINT('Ctrl Pts',(-1.65713010316883,-3.56684858399844,
13.130160296233));
#258526=CARTESIAN_POINT('Ctrl Pts',(-1.76243809949759,-3.51792330816709,
13.1243042418722));
#258527=CARTESIAN_POINT('Ctrl Pts',(-1.86556490397208,-3.46433628928523,
13.1184481875114));
#258528=CARTESIAN_POINT('Ctrl Pts',(-1.96608076218818,-3.40631992574883,
13.1125921331505));
#258529=CARTESIAN_POINT('Ctrl Pts',(-2.06663043203135,-3.3482840466088,
13.1067341089241));
#258530=CARTESIAN_POINT('Ctrl Pts',(-2.16456705197183,-3.28581606623922,
13.1008760846977));
#258531=CARTESIAN_POINT('Ctrl Pts',(-2.25948839534632,-3.21919263034931,
13.0950180604714));
#258532=CARTESIAN_POINT('Ctrl Pts',(-2.35451659006255,-3.1524941975908,
13.0891534419667));
#258533=CARTESIAN_POINT('Ctrl Pts',(-2.44652239576883,-3.08163121032613,
13.0832888234621));
#258534=CARTESIAN_POINT('Ctrl Pts',(-2.53513526457622,-3.00692171336436,
13.0774242049575));
#258535=CARTESIAN_POINT('Ctrl Pts',(-2.62380803718929,-2.93216171151263,
13.0715556218711));
#258536=CARTESIAN_POINT('Ctrl Pts',(-2.70908300292042,-2.85355030105153,
13.0656870387847));
#258537=CARTESIAN_POINT('Ctrl Pts',(-2.7906264419413,-2.77144241533863,
13.0598184556982));
#258538=CARTESIAN_POINT('Ctrl Pts',(-2.87228724783648,-2.68921635033361,
13.0539414258592));
#258539=CARTESIAN_POINT('Ctrl Pts',(-2.95020553235073,-2.60348407114684,
13.0480643960202));
#258540=CARTESIAN_POINT('Ctrl Pts',(-3.02408777323364,-2.51463359950884,
13.0421873661812));
#258541=CARTESIAN_POINT('Ctrl Pts',(-3.03967791075394,-2.49588496580436,
13.0409472345568));
#258542=CARTESIAN_POINT('Ctrl Pts',(-3.05508849156538,-2.47699759080929,
13.0397071029324));
#258543=CARTESIAN_POINT('Ctrl Pts',(-3.07031700924428,-2.45797527708178,
13.038466971308));
#258544=CARTESIAN_POINT('Ctrl Pts',(-3.14227544215279,-2.36809023935273,
13.0326070491426));
#258545=CARTESIAN_POINT('Ctrl Pts',(-3.21040812691704,-2.27488676098109,
13.0267471269773));
#258546=CARTESIAN_POINT('Ctrl Pts',(-3.27439259146059,-2.17872489245154,
13.0208872048119));
#258547=CARTESIAN_POINT('Ctrl Pts',(-3.33829802090321,-2.08268180530181,
13.0150345209588));
#258548=CARTESIAN_POINT('Ctrl Pts',(-3.39806518766487,-1.98368793322563,
13.0091818371058));
#258549=CARTESIAN_POINT('Ctrl Pts',(-3.45341137449383,-1.88213678528332,
13.0033291532528));
#258550=CARTESIAN_POINT('Ctrl Pts',(-3.50870271804399,-1.78068626573544,
12.9974822689027));
#258551=CARTESIAN_POINT('Ctrl Pts',(-3.55958159431877,-1.67668387017918,
12.9916353845526));
#258552=CARTESIAN_POINT('Ctrl Pts',(-3.60580860118161,-1.57055191943619,
12.9857885002025));
#258553=CARTESIAN_POINT('Ctrl Pts',(-3.65200109233267,-1.46449921284228,
12.9799459814687));
#258554=CARTESIAN_POINT('Ctrl Pts',(-3.6935484568733,-1.35632049214502,
12.9741034627349));
#258555=CARTESIAN_POINT('Ctrl Pts',(-3.73025760894366,-1.24646186099611,
12.9682609440011));
#258556=CARTESIAN_POINT('Ctrl Pts',(-3.7669519298529,-1.13664761472043,
12.9624207857505));
#258557=CARTESIAN_POINT('Ctrl Pts',(-3.79881179126718,-1.02515519938419,
12.9565806274999));
#258558=CARTESIAN_POINT('Ctrl Pts',(-3.82569278444555,-0.912449296696138,
12.9507404692493));
#258559=CARTESIAN_POINT('Ctrl Pts',(-3.85256701909957,-0.79977173096654,
12.9449017793541));
#258560=CARTESIAN_POINT('Ctrl Pts',(-3.87446478275368,-0.685881688865453,
12.9390630894589));
#258561=CARTESIAN_POINT('Ctrl Pts',(-3.8912921706179,-0.57125672240054,
12.9332243995637));
#258562=CARTESIAN_POINT('Ctrl Pts',(-3.90812426445964,-0.456599699711643,
12.92738407681));
#258563=CARTESIAN_POINT('Ctrl Pts',(-3.91988308810419,-0.341207752495339,
12.9215437540563));
#258564=CARTESIAN_POINT('Ctrl Pts',(-3.92652632663352,-0.225565968740512,
12.9157034313026));
#258565=CARTESIAN_POINT('Ctrl Pts',(-3.93090179086183,-0.149400332675666,
12.9118567948801));
#258566=CARTESIAN_POINT('Ctrl Pts',(-3.933059183935,-0.0731264525454888,
12.9080101584575));
#258567=CARTESIAN_POINT('Ctrl Pts',(-3.9329987650854,0.00311670286490963,
12.904163522035));
#258568=CARTESIAN_POINT('',(-3.93299999997998,1.25478604955714E-5,11.6541635220815));
#258569=CARTESIAN_POINT('Ctrl Pts',(-3.93299876508478,0.00311670364493542,
12.9041635219957));
#258570=CARTESIAN_POINT('Ctrl Pts',(-3.93289051723057,0.13971572794475,
12.8972717980195));
#258571=CARTESIAN_POINT('Ctrl Pts',(-3.92566195699015,0.276017078558251,
12.8903800740433));
#258572=CARTESIAN_POINT('Ctrl Pts',(-3.91142917386115,0.411352425382229,
12.8834883500672));
#258573=CARTESIAN_POINT('Ctrl Pts',(-3.89669952620131,0.551412310829302,
12.8763560369407));
#258574=CARTESIAN_POINT('Ctrl Pts',(-3.874467964418,0.690437391631793,12.8692237238141));
#258575=CARTESIAN_POINT('Ctrl Pts',(-3.84491697545102,0.827709158997629,
12.8620914106876));
#258576=CARTESIAN_POINT('Ctrl Pts',(-3.81536598648405,0.964980926363465,
12.8549590975611));
#258577=CARTESIAN_POINT('Ctrl Pts',(-3.77849571199835,1.10049933560846,
12.8478267844346));
#258578=CARTESIAN_POINT('Ctrl Pts',(-3.73454091440123,1.23356927598867,
12.8406944713081));
#258579=CARTESIAN_POINT('Ctrl Pts',(-3.69832555736119,1.34320862517502,
12.8348179963721));
#258580=CARTESIAN_POINT('Ctrl Pts',(-3.65721828267301,1.45143226609062,
12.828941521436));
#258581=CARTESIAN_POINT('Ctrl Pts',(-3.61134817310259,1.55777192574156,
12.8230650465));
#258582=CARTESIAN_POINT('Ctrl Pts',(-3.56553684242359,1.66397531958963,
12.8171961017985));
#258583=CARTESIAN_POINT('Ctrl Pts',(-3.51497497647907,1.76829915778894,
12.8113271570969));
#258584=CARTESIAN_POINT('Ctrl Pts',(-3.45984128668686,1.87029069156027,
12.8054582123954));
#258585=CARTESIAN_POINT('Ctrl Pts',(-3.40476356164893,1.97217869641585,
12.7995952251049));
#258586=CARTESIAN_POINT('Ctrl Pts',(-3.34512343896653,2.07173874515476,
12.7937322378143));
#258587=CARTESIAN_POINT('Ctrl Pts',(-3.28114726590327,2.16853905186315,
12.7878692505237));
#258588=CARTESIAN_POINT('Ctrl Pts',(-3.215245336274,2.26825315940252,12.7818297805564));
#258589=CARTESIAN_POINT('Ctrl Pts',(-3.14474235240354,2.36503833783608,
12.7757903105891));
#258590=CARTESIAN_POINT('Ctrl Pts',(-3.0699363592589,2.45845068083544,12.7697508406218));
#258591=CARTESIAN_POINT('Ctrl Pts',(-2.9973985069728,2.5490307326915,12.7638944892526));
#258592=CARTESIAN_POINT('Ctrl Pts',(-2.92081509741286,2.63643918672693,
12.7580381378834));
#258593=CARTESIAN_POINT('Ctrl Pts',(-2.84050073232488,2.72030229747759,
12.7521817865142));
#258594=CARTESIAN_POINT('Ctrl Pts',(-2.76019808739336,2.80415317020857,
12.7463262897537));
#258595=CARTESIAN_POINT('Ctrl Pts',(-2.67616585492461,2.88445943047131,
12.7404707929932));
#258596=CARTESIAN_POINT('Ctrl Pts',(-2.5887567750199,2.96088286829935,12.7346152962327));
#258597=CARTESIAN_POINT('Ctrl Pts',(-2.50133937142617,3.03731358368861,
12.7287592418719));
#258598=CARTESIAN_POINT('Ctrl Pts',(-2.41054479183504,3.10986046998059,
12.722903187511));
#258599=CARTESIAN_POINT('Ctrl Pts',(-2.31675970719597,3.17822489121101,
12.7170471331502));
#258600=CARTESIAN_POINT('Ctrl Pts',(-2.22294307503436,3.24661230893526,
12.7111891089238));
#258601=CARTESIAN_POINT('Ctrl Pts',(-2.12613427078891,3.31081422103607,
12.7053310846974));
#258602=CARTESIAN_POINT('Ctrl Pts',(-2.02674925330031,3.37057509399311,
12.699473060471));
#258603=CARTESIAN_POINT('Ctrl Pts',(-1.92725235978758,3.43040323874858,
12.6936084419663));
#258604=CARTESIAN_POINT('Ctrl Pts',(-1.82517381881096,3.48578015379365,
12.6877438234617));
#258605=CARTESIAN_POINT('Ctrl Pts',(-1.7209545905739,3.53649604795235,12.681879204957));
#258606=CARTESIAN_POINT('Ctrl Pts',(-1.61666490836746,3.58724622691737,
12.6760106218706));
#258607=CARTESIAN_POINT('Ctrl Pts',(-1.51023203498892,3.63332894710027,
12.6701420387842));
#258608=CARTESIAN_POINT('Ctrl Pts',(-1.40211572117287,3.67458303817452,
12.6642734556977));
#258609=CARTESIAN_POINT('Ctrl Pts',(-1.29384379368602,3.7158965069719,12.6583964258587));
#258610=CARTESIAN_POINT('Ctrl Pts',(-1.18388398044833,3.75236734777742,
12.6525193960197));
#258611=CARTESIAN_POINT('Ctrl Pts',(-1.07270998281249,3.78388455066674,
12.6466423661806));
#258612=CARTESIAN_POINT('Ctrl Pts',(-1.04925078760107,3.79053510053291,
12.6454022345564));
#258613=CARTESIAN_POINT('Ctrl Pts',(-1.02573755873963,3.79696526409723,
12.6441621029322));
#258614=CARTESIAN_POINT('Ctrl Pts',(-1.00217478841056,3.80317429175606,
12.642921971308));
#258615=CARTESIAN_POINT('Ctrl Pts',(-0.890520487721301,3.83259632624208,
12.637045496372));
#258616=CARTESIAN_POINT('Ctrl Pts',(-0.777385639151944,3.85714567500466,
12.6311690214359));
#258617=CARTESIAN_POINT('Ctrl Pts',(-0.663233166504726,3.87667522070757,
12.6252925464998));
#258618=CARTESIAN_POINT('Ctrl Pts',(-0.549226971157995,3.89617974085336,
12.6194236017983));
#258619=CARTESIAN_POINT('Ctrl Pts',(-0.43420614817201,3.91067718146114,
12.6135546570967));
#258620=CARTESIAN_POINT('Ctrl Pts',(-0.318647667633408,3.92007049221207,
12.6076857123952));
#258621=CARTESIAN_POINT('Ctrl Pts',(-0.203206487460461,3.92945426806101,
12.6018227251046));
#258622=CARTESIAN_POINT('Ctrl Pts',(-0.0872291442570081,3.93374418671206,
12.595959737814));
#258623=CARTESIAN_POINT('Ctrl Pts',(0.0287989912652807,3.93289455974885,
12.5900967505234));
#258624=CARTESIAN_POINT('Ctrl Pts',(0.148319707432526,3.93201935803453,
12.5840572805561));
#258625=CARTESIAN_POINT('Ctrl Pts',(0.267893882975228,3.92569021573269,
12.5780178105888));
#258626=CARTESIAN_POINT('Ctrl Pts',(0.386986894000942,3.91391493825192,
12.5719783406215));
#258627=CARTESIAN_POINT('Ctrl Pts',(0.502468968083502,3.90249669082778,
12.5661219892523));
#258628=CARTESIAN_POINT('Ctrl Pts',(0.617498195405212,3.88595784810588,
12.5602656378831));
#258629=CARTESIAN_POINT('Ctrl Pts',(0.73158973869103,3.86435834961537,12.5544092865139));
#258630=CARTESIAN_POINT('Ctrl Pts',(0.845664632766857,3.84276200310769,
12.5485537897533));
#258631=CARTESIAN_POINT('Ctrl Pts',(0.9588017095401,3.81610654606005,12.5426982929928));
#258632=CARTESIAN_POINT('Ctrl Pts',(1.07052512546853,3.7845032640679,12.5368427962323));
#258633=CARTESIAN_POINT('Ctrl Pts',(1.18225918046291,3.75289697259561,12.5309867418714));
#258634=CARTESIAN_POINT('Ctrl Pts',(1.29257890989874,3.71634203187436,12.5251306875105));
#258635=CARTESIAN_POINT('Ctrl Pts',(1.40102314347583,3.67499974849592,12.5192746331496));
#258636=CARTESIAN_POINT('Ctrl Pts',(1.50950385563515,3.63364355835791,12.5134166089232));
#258637=CARTESIAN_POINT('Ctrl Pts',(1.6161074320524,3.58749697027091,12.5075585846968));
#258638=CARTESIAN_POINT('Ctrl Pts',(1.72039286503307,3.53676934361619,12.5017005604703));
#258639=CARTESIAN_POINT('Ctrl Pts',(1.82479569035204,3.48598461373488,12.4958359419656));
#258640=CARTESIAN_POINT('Ctrl Pts',(1.92687479272097,3.4306087335386,12.489971323461));
#258641=CARTESIAN_POINT('Ctrl Pts',(2.02621387723058,3.37089696130247,12.4841067049563));
#258642=CARTESIAN_POINT('Ctrl Pts',(2.12562011664947,3.31114482289358,12.4782381218698));
#258643=CARTESIAN_POINT('Ctrl Pts',(2.22228230672707,3.24705118323557,12.4723695387834));
#258644=CARTESIAN_POINT('Ctrl Pts',(2.31581466475513,3.1789135626036,12.4665009556969));
#258645=CARTESIAN_POINT('Ctrl Pts',(2.40948164551545,3.11067787032185,12.4606239258579));
#258646=CARTESIAN_POINT('Ctrl Pts',(2.50000948309522,3.03838683782404,12.4547468960188));
#258647=CARTESIAN_POINT('Ctrl Pts',(2.5870468365032,2.96237702964001,12.4488698661797));
#258648=CARTESIAN_POINT('Ctrl Pts',(2.60541287808837,2.94633794706996,12.4476297345558));
#258649=CARTESIAN_POINT('Ctrl Pts',(2.62362363686524,2.9301334045145,12.4463896029319));
#258650=CARTESIAN_POINT('Ctrl Pts',(2.64167603511197,2.91376675894195,12.445149471308));
#258651=CARTESIAN_POINT('Ctrl Pts',(2.72721894345236,2.83621194085533,12.439272996372));
#258652=CARTESIAN_POINT('Ctrl Pts',(2.80948446166904,2.75475919996778,12.4333965214359));
#258653=CARTESIAN_POINT('Ctrl Pts',(2.88809685722913,2.66971637880566,12.4275200464998));
#258654=CARTESIAN_POINT('Ctrl Pts',(2.96660851726647,2.58478253324447,12.4216511017982));
#258655=CARTESIAN_POINT('Ctrl Pts',(3.04147608666776,2.49626805670776,12.4157821570967));
#258656=CARTESIAN_POINT('Ctrl Pts',(3.11235814417319,2.40451986525352,12.4099132123951));
#258657=CARTESIAN_POINT('Ctrl Pts',(3.18316825117169,2.31286480496842,12.4040502251045));
#258658=CARTESIAN_POINT('Ctrl Pts',(3.25000064271123,2.21798288372013,12.3981872378139));
#258659=CARTESIAN_POINT('Ctrl Pts',(3.31255237255257,2.12025606451115,12.3923242505233));
#258660=CARTESIAN_POINT('Ctrl Pts',(3.37698698157607,2.01958755537781,12.386284780556));
#258661=CARTESIAN_POINT('Ctrl Pts',(3.43687883344845,1.9159004897512,12.3802453105887));
#258662=CARTESIAN_POINT('Ctrl Pts',(3.49194296937092,1.80964728570542,12.3742058406214));
#258663=CARTESIAN_POINT('Ctrl Pts',(3.54533754365489,1.70661571168199,12.3683494892522));
#258664=CARTESIAN_POINT('Ctrl Pts',(3.59419273431216,1.60117176068095,12.3624931378829));
#258665=CARTESIAN_POINT('Ctrl Pts',(3.63829443129475,1.49375454182059,12.3566367865137));
#258666=CARTESIAN_POINT('Ctrl Pts',(3.68238969258198,1.38635299819595,12.3507812897532));
#258667=CARTESIAN_POINT('Ctrl Pts',(3.72173268285892,1.27697914095696,12.3449257929926));
#258668=CARTESIAN_POINT('Ctrl Pts',(3.75615723803829,1.16609253626485,12.3390702962321));
#258669=CARTESIAN_POINT('Ctrl Pts',(3.7905850713587,1.05519537219359,12.3332142418712));
#258670=CARTESIAN_POINT('Ctrl Pts',(3.82009341615424,0.942785568433326,
12.3273581875103));
#258671=CARTESIAN_POINT('Ctrl Pts',(3.84456604025781,0.829337664703831,
12.3215021331494));
#258672=CARTESIAN_POINT('Ctrl Pts',(3.8690468964877,0.715851599252443,12.3156441089229));
#258673=CARTESIAN_POINT('Ctrl Pts',(3.88848857670796,0.601327142618534,
12.3097860846965));
#258674=CARTESIAN_POINT('Ctrl Pts',(3.90282612382881,0.486248133322302,
12.30392806047));
#258675=CARTESIAN_POINT('Ctrl Pts',(3.9171798104826,0.371039581542509,12.2980634419653));
#258676=CARTESIAN_POINT('Ctrl Pts',(3.92641784539432,0.255275640874513,
12.2921988234606));
#258677=CARTESIAN_POINT('Ctrl Pts',(3.93052722196335,0.13944445992978,12.2863342049559));
#258678=CARTESIAN_POINT('Ctrl Pts',(3.93463937654077,0.0235349751381991,
12.2804656218695));
#258679=CARTESIAN_POINT('Ctrl Pts',(3.93361597255984,-0.092441428839417,
12.274597038783));
#258680=CARTESIAN_POINT('Ctrl Pts',(3.9274960673015,-0.207999137813684,
12.2687284556965));
#258681=CARTESIAN_POINT('Ctrl Pts',(3.92136735355823,-0.323723170986733,
12.2628514258574));
#258682=CARTESIAN_POINT('Ctrl Pts',(3.91012753949836,-0.439026897450485,
12.2569743960184));
#258683=CARTESIAN_POINT('Ctrl Pts',(3.89386719148217,-0.553432285920135,
12.2510973661793));
#258684=CARTESIAN_POINT('Ctrl Pts',(3.89043604133658,-0.577573347655859,
12.2498572345555));
#258685=CARTESIAN_POINT('Ctrl Pts',(3.88678152268101,-0.601674456093228,
12.2486171029318));
#258686=CARTESIAN_POINT('Ctrl Pts',(3.88290477146283,-0.625731200877199,
12.247376971308));
#258687=CARTESIAN_POINT('Ctrl Pts',(3.86453443807978,-0.739726243870756,
12.241500496372));
#258688=CARTESIAN_POINT('Ctrl Pts',(3.84110958488746,-0.853099259789004,
12.2356240214359));
#258689=CARTESIAN_POINT('Ctrl Pts',(3.81268340188325,-0.965367431087237,
12.2297475464998));
#258690=CARTESIAN_POINT('Ctrl Pts',(3.78429364476817,-1.07749173966707,
12.2238786017983));
#258691=CARTESIAN_POINT('Ctrl Pts',(3.75091540363758,-1.18851362275136,
12.2180096570967));
#258692=CARTESIAN_POINT('Ctrl Pts',(3.71265333098622,-1.29795772038883,
12.2121407123952));
#258693=CARTESIAN_POINT('Ctrl Pts',(3.67443009715556,-1.40729072420958,
12.2062777251046));
#258694=CARTESIAN_POINT('Ctrl Pts',(3.63133302828834,-1.51504874105127,
12.200414737814));
#258695=CARTESIAN_POINT('Ctrl Pts',(3.58351713425597,-1.62076955440737,
12.1945517505234));
#258696=CARTESIAN_POINT('Ctrl Pts',(3.53426192668763,-1.72967268612805,
12.1885122805561));
#258697=CARTESIAN_POINT('Ctrl Pts',(3.4799994135655,-1.83641359285394,12.1824728105888));
#258698=CARTESIAN_POINT('Ctrl Pts',(3.42095347312482,-1.94050672112087,
12.1764333406215));
#258699=CARTESIAN_POINT('Ctrl Pts',(3.36369782386785,-2.04144371353101,
12.1705769892523));
#258700=CARTESIAN_POINT('Ctrl Pts',(3.30194485399917,-2.13989079154352,
12.1647206378831));
#258701=CARTESIAN_POINT('Ctrl Pts',(3.23594591522378,-2.23542904914169,
12.1588642865139));
#258702=CARTESIAN_POINT('Ctrl Pts',(3.1699566075758,-2.3309533649834,12.1530087897533));
#258703=CARTESIAN_POINT('Ctrl Pts',(3.09972279759509,-2.42356936504171,
12.1471532929928));
#258704=CARTESIAN_POINT('Ctrl Pts',(3.02553912800216,-2.51288718109826,
12.1412977962323));
#258705=CARTESIAN_POINT('Ctrl Pts',(2.95134839413403,-2.60221350260669,
12.1354417418714));
#258706=CARTESIAN_POINT('Ctrl Pts',(2.87320731661203,-2.68824069829287,
12.1295856875105));
#258707=CARTESIAN_POINT('Ctrl Pts',(2.79145031533835,-2.77061259236968,
12.1237296331496));
#258708=CARTESIAN_POINT('Ctrl Pts',(2.70966581256091,-2.85301219478851,
12.1178716089232));
#258709=CARTESIAN_POINT('Ctrl Pts',(2.62426325791441,-2.93175375787231,
12.1120135846968));
#258710=CARTESIAN_POINT('Ctrl Pts',(2.53561282382302,-3.00651901834402,
12.1061555604703));
#258711=CARTESIAN_POINT('Ctrl Pts',(2.44686259744573,-3.08136844079782,
12.1002909419656));
#258712=CARTESIAN_POINT('Ctrl Pts',(2.35485751013449,-3.15223236079099,
12.094426323461));
#258713=CARTESIAN_POINT('Ctrl Pts',(2.25999967318794,-3.21883371381474,
12.0885617049563));
#258714=CARTESIAN_POINT('Ctrl Pts',(2.16507771073154,-3.285480090485,12.0826931218698));
#258715=CARTESIAN_POINT('Ctrl Pts',(2.06729950548291,-3.3478579408293,12.0768245387834));
#258716=CARTESIAN_POINT('Ctrl Pts',(1.96709343185303,-3.40573522610914,
12.0709559556969));
#258717=CARTESIAN_POINT('Ctrl Pts',(1.86674312989721,-3.46369581516153,
12.0650789258578));
#258718=CARTESIAN_POINT('Ctrl Pts',(1.76395835053689,-3.51714272235285,
12.0592018960188));
#258719=CARTESIAN_POINT('Ctrl Pts',(1.65918919677122,-3.56589122230582,
12.0533248661797));
#258720=CARTESIAN_POINT('Ctrl Pts',(1.63708150898486,-3.57617780550591,
12.0520847345558));
#258721=CARTESIAN_POINT('Ctrl Pts',(1.61488552214605,-3.58625535991692,
12.0508446029319));
#258722=CARTESIAN_POINT('Ctrl Pts',(1.5926055527196,-3.59612243304461,12.049604471308));
#258723=CARTESIAN_POINT('Ctrl Pts',(1.48702991914283,-3.64287844410842,
12.043727996372));
#258724=CARTESIAN_POINT('Ctrl Pts',(1.37921975576809,-3.68505821602127,
12.0378515214359));
#258725=CARTESIAN_POINT('Ctrl Pts',(1.26960879846334,-3.72244308201811,
12.0319750464998));
#258726=CARTESIAN_POINT('Ctrl Pts',(1.16013829886895,-3.75978004228718,
12.0261061017983));
#258727=CARTESIAN_POINT('Ctrl Pts',(1.04887198157874,-3.7923341839783,12.0202371570967));
#258728=CARTESIAN_POINT('Ctrl Pts',(0.93626539069549,-3.8199340463136,12.0143682123951));
#258729=CARTESIAN_POINT('Ctrl Pts',(0.823773103792509,-3.84750589275663,
12.0085052251046));
#258730=CARTESIAN_POINT('Ctrl Pts',(0.709943647958522,-3.8701333655085,
12.002642237814));
#258731=CARTESIAN_POINT('Ctrl Pts',(0.595249006656992,-3.88769438357413,
11.9967792505234));
#258732=CARTESIAN_POINT('Ctrl Pts',(0.47710192442408,-3.90578400852915,
11.9907397805561));
#258733=CARTESIAN_POINT('Ctrl Pts',(0.358037166249289,-3.9184971851488,
11.9847003105888));
#258734=CARTESIAN_POINT('Ctrl Pts',(0.238583828644082,-3.92575683871397,
11.9786608406215));
#258735=CARTESIAN_POINT('Ctrl Pts',(0.122752353195335,-3.93279637733683,
11.9728044892523));
#258736=CARTESIAN_POINT('Ctrl Pts',(0.00655596343611999,-3.93470830404591,
11.966948137883));
#258737=CARTESIAN_POINT('Ctrl Pts',(-0.109517133238559,-3.93147491376038,
11.9610917865138));
#258738=CARTESIAN_POINT('Ctrl Pts',(-0.225573291538121,-3.92824199531871,
11.9552362897533));
#258739=CARTESIAN_POINT('Ctrl Pts',(-0.341505780128436,-3.91986526442406,
11.9493807929928));
#258740=CARTESIAN_POINT('Ctrl Pts',(-0.456827129013423,-3.90637913856263,
11.9435252962322));
#258741=CARTESIAN_POINT('Ctrl Pts',(-0.57215945958413,-3.89289172846029,
11.9376692418713));
#258742=CARTESIAN_POINT('Ctrl Pts',(-0.686880124866386,-3.87429400410638,
11.9318131875105));
#258743=CARTESIAN_POINT('Ctrl Pts',(-0.800508210034658,-3.85067209791578,
11.9259571331496));
#258744=CARTESIAN_POINT('Ctrl Pts',(-0.914174517534386,-3.82704224576423,
11.9200991089231));
#258745=CARTESIAN_POINT('Ctrl Pts',(-1.02674711030018,-3.79838493509126,
11.9142410846967));
#258746=CARTESIAN_POINT('Ctrl Pts',(-1.13775736069864,-3.76483694044989,
11.9083830604702));
#258747=CARTESIAN_POINT('Ctrl Pts',(-1.24889257344802,-3.7312511814015,
11.9025184419656));
#258748=CARTESIAN_POINT('Ctrl Pts',(-1.35846153845435,-3.69276386978575,
11.8966538234609));
#258749=CARTESIAN_POINT('Ctrl Pts',(-1.46601274944517,-3.64956101722717,
11.8907892049562));
#258750=CARTESIAN_POINT('Ctrl Pts',(-1.57363666688249,-3.60632895880601,
11.8849206218697));
#258751=CARTESIAN_POINT('Ctrl Pts',(-1.67923973935278,-3.55837518189441,
11.8790520387833));
#258752=CARTESIAN_POINT('Ctrl Pts',(-1.78239388471749,-3.50593226399508,
11.8731834556968));
#258753=CARTESIAN_POINT('Ctrl Pts',(-1.88569650161834,-3.45341386410176,
11.8673064258577));
#258754=CARTESIAN_POINT('Ctrl Pts',(-1.98654279946989,-3.39639363114801,
11.8614293960187));
#258755=CARTESIAN_POINT('Ctrl Pts',(-2.08453251033331,-3.33514815463474,
11.8555523661796));
#258756=CARTESIAN_POINT('Ctrl Pts',(-2.10520964531166,-3.32222454282366,
11.8543122345558));
#258757=CARTESIAN_POINT('Ctrl Pts',(-2.12575970130394,-3.30911293981966,
11.8530721029319));
#258758=CARTESIAN_POINT('Ctrl Pts',(-2.14617910718161,-3.29581617204254,
11.851831971308));
#258759=CARTESIAN_POINT('Ctrl Pts',(-2.24292913726319,-3.23281420763031,
11.8459560524575));
#258760=CARTESIAN_POINT('Ctrl Pts',(-2.33706204953458,-3.16544462936648,
11.840080133607));
#258761=CARTESIAN_POINT('Ctrl Pts',(-2.42815809443204,-3.09395172367705,
11.8342042147565));
#258762=CARTESIAN_POINT('Ctrl Pts',(-2.51913739990764,-3.02255043602093,
11.8283358258856));
#258763=CARTESIAN_POINT('Ctrl Pts',(-2.60708725581871,-2.94703658198866,
11.8224674370148));
#258764=CARTESIAN_POINT('Ctrl Pts',(-2.6916155892492,-2.86769847084918,
11.816599048144));
#258765=CARTESIAN_POINT('Ctrl Pts',(-2.77605812574587,-2.78844088852641,
11.8107366157348));
#258766=CARTESIAN_POINT('Ctrl Pts',(-2.85708574857717,-2.70536705107285,
11.8048741833256));
#258767=CARTESIAN_POINT('Ctrl Pts',(-2.93433881231637,-2.61880597496908,
11.7990117509163));
#258768=CARTESIAN_POINT('Ctrl Pts',(-3.01387042901268,-2.52969180923521,
11.7929764080482));
#258769=CARTESIAN_POINT('Ctrl Pts',(-3.08940101458313,-2.43688177027347,
11.7869410651801));
#258770=CARTESIAN_POINT('Ctrl Pts',(-3.1605781230071,-2.34077656523832,
11.780905722312));
#258771=CARTESIAN_POINT('Ctrl Pts',(-3.22963783539814,-2.24753032405252,
11.7750499204695));
#258772=CARTESIAN_POINT('Ctrl Pts',(-3.2945991648606,-2.15118255228048,
11.769194118627));
#258773=CARTESIAN_POINT('Ctrl Pts',(-3.35518108726665,-2.05213276170139,
11.7633383167844));
#258774=CARTESIAN_POINT('Ctrl Pts',(-3.41575418820649,-1.95309739397891,
11.7574833676181));
#258775=CARTESIAN_POINT('Ctrl Pts',(-3.47194893482579,-1.8513611418387,
11.7516284184517));
#258776=CARTESIAN_POINT('Ctrl Pts',(-3.5235283962209,-1.74735132157932,
11.7457734692853));
#258777=CARTESIAN_POINT('Ctrl Pts',(-3.57511279231883,-1.64333155050736,
11.739917959965));
#258778=CARTESIAN_POINT('Ctrl Pts',(-3.62208084204468,-1.53703814871761,
11.7340624506448));
#258779=CARTESIAN_POINT('Ctrl Pts',(-3.66424253896638,-1.42892113695236,
11.7282069413245));
#258780=CARTESIAN_POINT('Ctrl Pts',(-3.70641844247636,-1.32076769463558,
11.722349458962));
#258781=CARTESIAN_POINT('Ctrl Pts',(-3.74378462291302,-1.21078980480763,
11.7164919765995));
#258782=CARTESIAN_POINT('Ctrl Pts',(-3.7762002249795,-1.09945480164708,
11.710634494237));
#258783=CARTESIAN_POINT('Ctrl Pts',(-3.80865232096792,-0.987994456038543,
11.7047704174418));
#258784=CARTESIAN_POINT('Ctrl Pts',(-3.83614259932708,-0.875174344191746,
11.6989063406467));
#258785=CARTESIAN_POINT('Ctrl Pts',(-3.85858081435279,-0.761474293137025,
11.6930422638515));
#258786=CARTESIAN_POINT('Ctrl Pts',(-3.88103421481454,-0.647697293677529,
11.6871742184446));
#258787=CARTESIAN_POINT('Ctrl Pts',(-3.89842868196084,-0.533039576235783,
11.6813061730378));
#258788=CARTESIAN_POINT('Ctrl Pts',(-3.91072577682643,-0.417986720441329,
11.6754381276309));
#258789=CARTESIAN_POINT('Ctrl Pts',(-3.92304055730816,-0.302768396244369,
11.6695616428325));
#258790=CARTESIAN_POINT('Ctrl Pts',(-3.93024331012025,-0.187154209903649,
11.6636851580341));
#258791=CARTESIAN_POINT('Ctrl Pts',(-3.93234765545738,-0.071630416854992,
11.6578086732356));
#258792=CARTESIAN_POINT('Ctrl Pts',(-3.93278276006484,-0.047744159338664,
11.6565936228509));
#258793=CARTESIAN_POINT('Ctrl Pts',(-3.93300007614865,-0.0238617492305318,
11.6553785724662));
#258794=CARTESIAN_POINT('Ctrl Pts',(-3.93299999997998,1.25478604846101E-5,
11.6541635220815));
#258795=CARTESIAN_POINT('',(-3.93299875665656,-0.00312732120702944,10.4041635220741));
#258796=CARTESIAN_POINT('Ctrl Pts',(-3.93299999997998,1.254881375347E-5,
11.654163522033));
#258797=CARTESIAN_POINT('Ctrl Pts',(-3.93299963153457,0.115489264304682,
11.648286489212));
#258798=CARTESIAN_POINT('Ctrl Pts',(-3.92790919375625,0.231155856959505,
11.642409456391));
#258799=CARTESIAN_POINT('Ctrl Pts',(-3.91770442456459,0.346527115457176,
11.63653242357));
#258800=CARTESIAN_POINT('Ctrl Pts',(-3.90751273112395,0.461750544462173,
11.6306629212101));
#258801=CARTESIAN_POINT('Ctrl Pts',(-3.89221977489077,0.576678984593512,
11.6247934188503));
#258802=CARTESIAN_POINT('Ctrl Pts',(-3.87185328733267,0.690826404656908,
11.6189239164904));
#258803=CARTESIAN_POINT('Ctrl Pts',(-3.85150747450685,0.804857949690607,
11.6130603724672));
#258804=CARTESIAN_POINT('Ctrl Pts',(-3.82609844717892,0.918109647932914,
11.607196828444));
#258805=CARTESIAN_POINT('Ctrl Pts',(-3.7957057434686,1.03010043636505,11.6013332844209));
#258806=CARTESIAN_POINT('Ctrl Pts',(-3.76437976836089,1.14553013568222,
11.5952896880412));
#258807=CARTESIAN_POINT('Ctrl Pts',(-3.72775913984388,1.25961979118295,
11.5892460916615));
#258808=CARTESIAN_POINT('Ctrl Pts',(-3.6859879483633,1.37185343405209,11.5832024952818));
#258809=CARTESIAN_POINT('Ctrl Pts',(-3.64550711673329,1.48062005140654,
11.5773455925023));
#258810=CARTESIAN_POINT('Ctrl Pts',(-3.60018941256176,1.58764322468082,
11.5714886897227));
#258811=CARTESIAN_POINT('Ctrl Pts',(-3.55021640761558,1.69246933771254,
11.5656317869432));
#258812=CARTESIAN_POINT('Ctrl Pts',(-3.50025071090823,1.79728012058209,
11.559775740699));
#258813=CARTESIAN_POINT('Ctrl Pts',(-3.4456312447062,1.89989410979751,11.5539196944549));
#258814=CARTESIAN_POINT('Ctrl Pts',(-3.38658693868387,1.99987947305227,
11.5480636482107));
#258815=CARTESIAN_POINT('Ctrl Pts',(-3.32753703631444,2.09987431313613,
11.5422070469178));
#258816=CARTESIAN_POINT('Ctrl Pts',(-3.26406167019856,2.19723967670041,
11.5363504456248));
#258817=CARTESIAN_POINT('Ctrl Pts',(-3.196434399675,2.29157066846613,11.5304938443319));
#258818=CARTESIAN_POINT('Ctrl Pts',(-3.12878441945234,2.38593333722283,
11.5246352763523));
#258819=CARTESIAN_POINT('Ctrl Pts',(-3.05698000263036,2.47725927284569,
11.5187767083727));
#258820=CARTESIAN_POINT('Ctrl Pts',(-2.98133603676951,2.56517532263575,
11.5129181403931));
#258821=CARTESIAN_POINT('Ctrl Pts',(-2.90560692994552,2.65319032621639,
11.5070529783102));
#258822=CARTESIAN_POINT('Ctrl Pts',(-2.82602991785966,2.73778747083878,
11.5011878162274));
#258823=CARTESIAN_POINT('Ctrl Pts',(-2.7429579755543,2.81862919596442,11.4953226541445));
#258824=CARTESIAN_POINT('Ctrl Pts',(-2.65982993761201,2.89952551073773,
11.4894535315186));
#258825=CARTESIAN_POINT('Ctrl Pts',(-2.57320257736082,2.97666108262849,
11.4835844088927));
#258826=CARTESIAN_POINT('Ctrl Pts',(-2.48346196311381,3.04973862449996,
11.4777152862668));
#258827=CARTESIAN_POINT('Ctrl Pts',(-2.39359208342735,3.12292142975348,
11.4718377095566));
#258828=CARTESIAN_POINT('Ctrl Pts',(-2.30060033017896,3.19203429461456,
11.4659601328465));
#258829=CARTESIAN_POINT('Ctrl Pts',(-2.20490175587179,3.25682318324982,
11.4600825561363));
#258830=CARTESIAN_POINT('Ctrl Pts',(-2.18430187973036,3.27076950471688,
11.4588173611936));
#258831=CARTESIAN_POINT('Ctrl Pts',(-2.16357666935699,3.28451564075698,
11.4575521662508));
#258832=CARTESIAN_POINT('Ctrl Pts',(-2.1427304044802,3.29805934053894,11.4562869713081));
#258833=CARTESIAN_POINT('Ctrl Pts',(-2.04590536280434,3.36096601967711,
11.450410496372));
#258834=CARTESIAN_POINT('Ctrl Pts',(-1.94614836124524,3.41970872241911,
11.4445340214359));
#258835=CARTESIAN_POINT('Ctrl Pts',(-1.84385297068083,3.47400276662404,
11.4386575464999));
#258836=CARTESIAN_POINT('Ctrl Pts',(-1.74168866351076,3.52822723733629,
11.4327886017983));
#258837=CARTESIAN_POINT('Ctrl Pts',(-1.6369927974258,3.57801419475766,11.4269196570968));
#258838=CARTESIAN_POINT('Ctrl Pts',(-1.53018796156289,3.62312210700771,
11.4210507123952));
#258839=CARTESIAN_POINT('Ctrl Pts',(-1.42349154047165,3.66818423140586,
11.4151877251046));
#258840=CARTESIAN_POINT('Ctrl Pts',(-1.31469078583114,3.70857659860889,
11.409324737814));
#258841=CARTESIAN_POINT('Ctrl Pts',(-1.20423234882466,3.74410382468812,
11.4034617505234));
#258842=CARTESIAN_POINT('Ctrl Pts',(-1.09044898551991,3.78070046123066,
11.3974222805561));
#258843=CARTESIAN_POINT('Ctrl Pts',(-0.974906954394349,3.81213420969258,
11.3913828105888));
#258844=CARTESIAN_POINT('Ctrl Pts',(-0.858116434120484,3.83824506584615,
11.3853433406215));
#258845=CARTESIAN_POINT('Ctrl Pts',(-0.744867038557684,3.86356423276215,
11.3794869892523));
#258846=CARTESIAN_POINT('Ctrl Pts',(-0.630444202922027,3.88387854155951,
11.3736306378831));
#258847=CARTESIAN_POINT('Ctrl Pts',(-0.515327149098713,3.89909309063041,
11.3677742865139));
#258848=CARTESIAN_POINT('Ctrl Pts',(-0.400226894136644,3.91430541946469,
11.3619187897533));
#258849=CARTESIAN_POINT('Ctrl Pts',(-0.284433031437971,3.9244194143499,
11.3560632929928));
#258850=CARTESIAN_POINT('Ctrl Pts',(-0.168432320485068,3.92939175361989,
11.3502077962323));
#258851=CARTESIAN_POINT('Ctrl Pts',(-0.0524205631529066,3.93436456638996,
11.3443517418714));
#258852=CARTESIAN_POINT('Ctrl Pts',(0.0637976692825216,3.93419473254505,
11.3384956875105));
#258853=CARTESIAN_POINT('Ctrl Pts',(0.179733888538592,3.9288910304704,11.3326396331496));
#258854=CARTESIAN_POINT('Ctrl Pts',(0.295709106538668,3.92358554433103,
11.3267816089231));
#258855=CARTESIAN_POINT('Ctrl Pts',(0.411401710717966,3.9131427748111,11.3209235846967));
#258856=CARTESIAN_POINT('Ctrl Pts',(0.526327313606261,3.89762345012342,
11.3150655604703));
#258857=CARTESIAN_POINT('Ctrl Pts',(0.641382286291133,3.88208665559589,
11.3092009419656));
#258858=CARTESIAN_POINT('Ctrl Pts',(0.755668125284889,3.86146195551416,
11.3033363234609));
#258859=CARTESIAN_POINT('Ctrl Pts',(0.868709539743867,3.83586140724062,
11.2974717049562));
#258860=CARTESIAN_POINT('Ctrl Pts',(0.981827372120121,3.81024355256138,
11.2916031218697));
#258861=CARTESIAN_POINT('Ctrl Pts',(1.09369870776683,3.77964326014677,11.2857345387833));
#258862=CARTESIAN_POINT('Ctrl Pts',(1.20386399908539,3.7442222786189,11.2798659556968));
#258863=CARTESIAN_POINT('Ctrl Pts',(1.31418785320323,3.70875031506288,11.2739889258577));
#258864=CARTESIAN_POINT('Ctrl Pts',(1.42280037731297,3.66844395870327,11.2681118960187));
#258865=CARTESIAN_POINT('Ctrl Pts',(1.52926250657235,3.62351282404134,11.2622348661796));
#258866=CARTESIAN_POINT('Ctrl Pts',(1.55172743475087,3.61403175579499,11.2609947345557));
#258867=CARTESIAN_POINT('Ctrl Pts',(1.57409670390057,3.60434492285895,11.2597546029319));
#258868=CARTESIAN_POINT('Ctrl Pts',(1.59636633986488,3.59445454957305,11.258514471308));
#258869=CARTESIAN_POINT('Ctrl Pts',(1.7018930074074,3.54758812861831,11.252637996372));
#258870=CARTESIAN_POINT('Ctrl Pts',(1.80552775613501,3.49599352287628,11.2467615214359));
#258871=CARTESIAN_POINT('Ctrl Pts',(1.90681735073534,3.43984543125628,11.2408850464998));
#258872=CARTESIAN_POINT('Ctrl Pts',(2.00797715078876,3.383769288943,11.2350161017982));
#258873=CARTESIAN_POINT('Ctrl Pts',(2.10679741541973,3.32315146315843,11.2291471570967));
#258874=CARTESIAN_POINT('Ctrl Pts',(2.20284525902097,3.25821450564704,11.2232782123951));
#258875=CARTESIAN_POINT('Ctrl Pts',(2.29879560698957,3.19334346392843,11.2174152251045));
#258876=CARTESIAN_POINT('Ctrl Pts',(2.3919787919248,3.12416224115855,11.211552237814));
#258877=CARTESIAN_POINT('Ctrl Pts',(2.48198749317454,3.05093872172569,11.2056892505234));
#258878=CARTESIAN_POINT('Ctrl Pts',(2.57470556010034,2.97551108994061,11.1996497805561));
#258879=CARTESIAN_POINT('Ctrl Pts',(2.66405461129145,2.89579416231397,11.1936103105888));
#258880=CARTESIAN_POINT('Ctrl Pts',(2.749622345888,2.8121283674458,11.1875708406214));
#258881=CARTESIAN_POINT('Ctrl Pts',(2.83259564029596,2.73099934536517,11.1817144892522));
#258882=CARTESIAN_POINT('Ctrl Pts',(2.91201329817608,2.64615777493143,11.175858137883));
#258883=CARTESIAN_POINT('Ctrl Pts',(2.98753447169513,2.55795363140799,11.1700017865138));
#258884=CARTESIAN_POINT('Ctrl Pts',(3.06304462452115,2.4697623593846,11.1641462897533));
#258885=CARTESIAN_POINT('Ctrl Pts',(3.1346591553342,2.37820980339812,11.1582907929927));
#258886=CARTESIAN_POINT('Ctrl Pts',(3.20207634466161,2.28368038108632,11.1524352962322));
#258887=CARTESIAN_POINT('Ctrl Pts',(3.2694999539138,2.18914195703792,11.1465792418713));
#258888=CARTESIAN_POINT('Ctrl Pts',(3.33272518749005,2.09162643912829,11.1407231875104));
#258889=CARTESIAN_POINT('Ctrl Pts',(3.39149305750062,1.99154810158457,11.1348671331495));
#258890=CARTESIAN_POINT('Ctrl Pts',(3.45028069590743,1.89143609958726,11.1290091089231));
#258891=CARTESIAN_POINT('Ctrl Pts',(3.50460778041299,1.78875991935942,11.1231510846966));
#258892=CARTESIAN_POINT('Ctrl Pts',(3.55426110735821,1.68395872298605,11.1172930604702));
#258893=CARTESIAN_POINT('Ctrl Pts',(3.60397032820906,1.57903955368837,11.1114284419655));
#258894=CARTESIAN_POINT('Ctrl Pts',(3.64899511406278,1.47199096702418,11.1055638234608));
#258895=CARTESIAN_POINT('Ctrl Pts',(3.68917024914258,1.36327248664427,11.0996992049561));
#258896=CARTESIAN_POINT('Ctrl Pts',(3.72937254329648,1.25448051072396,11.0938306218697));
#258897=CARTESIAN_POINT('Ctrl Pts',(3.76471853296518,1.14401678523187,11.0879620387832));
#258898=CARTESIAN_POINT('Ctrl Pts',(3.79509324129745,1.03235473063208,11.0820934556968));
#258899=CARTESIAN_POINT('Ctrl Pts',(3.82551166847004,0.920531958915893,
11.0762164258577));
#258900=CARTESIAN_POINT('Ctrl Pts',(3.85094444483676,0.807507817057756,
11.0703393960186));
#258901=CARTESIAN_POINT('Ctrl Pts',(3.87132788650239,0.693764654035434,
11.0644623661795));
#258902=CARTESIAN_POINT('Ctrl Pts',(3.87562906435998,0.669763330693276,
11.0632222345557));
#258903=CARTESIAN_POINT('Ctrl Pts',(3.87970559692021,0.645730003481113,
11.0619821029319));
#258904=CARTESIAN_POINT('Ctrl Pts',(3.88355718189753,0.621669216651523,
11.060741971308));
#258905=CARTESIAN_POINT('Ctrl Pts',(3.90180826278956,0.507655020070562,
11.054865496372));
#258906=CARTESIAN_POINT('Ctrl Pts',(3.91506425903091,0.392648746114955,
11.0489890214359));
#258907=CARTESIAN_POINT('Ctrl Pts',(3.92322449143385,0.277125584913448,
11.0431125464998));
#258908=CARTESIAN_POINT('Ctrl Pts',(3.931374267149,0.161750457440614,11.0372436017983));
#258909=CARTESIAN_POINT('Ctrl Pts',(3.93444123627607,0.0458601679209655,
11.0313746570967));
#258910=CARTESIAN_POINT('Ctrl Pts',(3.93237592910319,-0.0700610605816664,
11.0255057123952));
#258911=CARTESIAN_POINT('Ctrl Pts',(3.93031271836915,-0.185864620502874,
11.0196427251046));
#258912=CARTESIAN_POINT('Ctrl Pts',(3.92312760137356,-0.301698646731676,
11.013779737814));
#258913=CARTESIAN_POINT('Ctrl Pts',(3.91082304886289,-0.417075629212228,
11.0079167505234));
#258914=CARTESIAN_POINT('Ctrl Pts',(3.89814811513608,-0.535925591880217,
11.0018772805561));
#258915=CARTESIAN_POINT('Ctrl Pts',(3.88004062454556,-0.654290114789306,
10.9958378105888));
#258916=CARTESIAN_POINT('Ctrl Pts',(3.85656114444387,-0.771637958608704,
10.9897983406215));
#258917=CARTESIAN_POINT('Ctrl Pts',(3.83379356944368,-0.885427779494729,
10.9839419892522));
#258918=CARTESIAN_POINT('Ctrl Pts',(3.80597515660557,-0.998261251319322,
10.978085637883));
#258919=CARTESIAN_POINT('Ctrl Pts',(3.77321343554066,-1.10966182679925,
10.9722292865138));
#258920=CARTESIAN_POINT('Ctrl Pts',(3.74045649534521,-1.2210461457581,10.9663737897533));
#258921=CARTESIAN_POINT('Ctrl Pts',(3.70275779775884,-1.33099758836577,
10.9605182929928));
#258922=CARTESIAN_POINT('Ctrl Pts',(3.66027507920438,-1.43905362810264,
10.9546627962322));
#258923=CARTESIAN_POINT('Ctrl Pts',(3.61778831515557,-1.54711995767296,
10.9488067418713));
#258924=CARTESIAN_POINT('Ctrl Pts',(3.57051677551205,-1.65329014149911,
10.9429506875105));
#258925=CARTESIAN_POINT('Ctrl Pts',(3.51866652400122,-1.75712119470262,
10.9370946331496));
#258926=CARTESIAN_POINT('Ctrl Pts',(3.46679883104976,-1.860987174702,10.9312366089231));
#258927=CARTESIAN_POINT('Ctrl Pts',(3.41034954783291,-1.9625120904682,10.9253785846967));
#258928=CARTESIAN_POINT('Ctrl Pts',(3.34957056466185,-2.0612777669084,10.9195205604702));
#258929=CARTESIAN_POINT('Ctrl Pts',(3.28872316362313,-2.16015462219082,
10.9136559419656));
#258930=CARTESIAN_POINT('Ctrl Pts',(3.22353655135716,-2.25626568726273,
10.9077913234609));
#258931=CARTESIAN_POINT('Ctrl Pts',(3.15430585201212,-2.34922191203004,
10.9019267049562));
#258932=CARTESIAN_POINT('Ctrl Pts',(3.08502835153775,-2.44224097678508,
10.8960581218697));
#258933=CARTESIAN_POINT('Ctrl Pts',(3.01170158035158,-2.53210063549052,
10.8901895387833));
#258934=CARTESIAN_POINT('Ctrl Pts',(2.93465970456777,-2.61844637493041,
10.8843209556968));
#258935=CARTESIAN_POINT('Ctrl Pts',(2.85750694108657,-2.70491639327873,
10.8784439258577));
#258936=CARTESIAN_POINT('Ctrl Pts',(2.77662868887771,-2.78786210489861,
10.8725668960186));
#258937=CARTESIAN_POINT('Ctrl Pts',(2.69239456592323,-2.86696712596902,
10.8666898661796));
#258938=CARTESIAN_POINT('Ctrl Pts',(2.67462004332537,-2.88365933970976,
10.8654497345557));
#258939=CARTESIAN_POINT('Ctrl Pts',(2.65669620556759,-2.90018068876621,
10.8642096029319));
#258940=CARTESIAN_POINT('Ctrl Pts',(2.63862669716608,-2.91652844200128,
10.862969471308));
#258941=CARTESIAN_POINT('Ctrl Pts',(2.55300271081917,-2.99399373705519,
10.857092996372));
#258942=CARTESIAN_POINT('Ctrl Pts',(2.46382353700696,-3.06781270103919,
10.8512165214359));
#258943=CARTESIAN_POINT('Ctrl Pts',(2.37143262106348,-3.13764184121706,
10.8453400464998));
#258944=CARTESIAN_POINT('Ctrl Pts',(2.27916009671913,-3.20738150091423,
10.8394711017983));
#258945=CARTESIAN_POINT('Ctrl Pts',(2.18368434133317,-3.27314125789395,
10.8336021570967));
#258946=CARTESIAN_POINT('Ctrl Pts',(2.08538429412416,-3.33461562190011,
10.8277332123952));
#258947=CARTESIAN_POINT('Ctrl Pts',(1.98718402870016,-3.39602758490092,
10.8218702251046));
#258948=CARTESIAN_POINT('Ctrl Pts',(1.88616552191402,-3.45316259015437,
10.816007237814));
#258949=CARTESIAN_POINT('Ctrl Pts',(1.78273878875029,-3.50575689560545,
10.8101442505234));
#258950=CARTESIAN_POINT('Ctrl Pts',(1.67619879168062,-3.55993435028507,
10.8041047805561));
#258951=CARTESIAN_POINT('Ctrl Pts',(1.56710364355383,-3.60929314032474,
10.7980653105888));
#258952=CARTESIAN_POINT('Ctrl Pts',(1.45593169352115,-3.65359438140041,
10.7920258406215));
#258953=CARTESIAN_POINT('Ctrl Pts',(1.3481305114114,-3.69655239513933,10.7861694892523));
#258954=CARTESIAN_POINT('Ctrl Pts',(1.23837706107286,-3.73475496829349,
10.780313137883));
#258955=CARTESIAN_POINT('Ctrl Pts',(1.12712945065788,-3.76803240451295,
10.7744567865138));
#258956=CARTESIAN_POINT('Ctrl Pts',(1.01589807444195,-3.80130498460542,
10.7686012897533));
#258957=CARTESIAN_POINT('Ctrl Pts',(0.903173366977586,-3.82965373869254,
10.7627457929928));
#258958=CARTESIAN_POINT('Ctrl Pts',(0.789429058247675,-3.85295870234735,
10.7568902962322));
#258959=CARTESIAN_POINT('Ctrl Pts',(0.675673918008615,-3.87626588525981,
10.7510342418714));
#258960=CARTESIAN_POINT('Ctrl Pts',(0.560899387779055,-3.89452824010562,
10.7451781875105));
#258961=CARTESIAN_POINT('Ctrl Pts',(0.445589166560199,-3.90767696907564,
10.7393221331496));
#258962=CARTESIAN_POINT('Ctrl Pts',(0.330240157171288,-3.92083012102855,
10.7334641089232));
#258963=CARTESIAN_POINT('Ctrl Pts',(0.214355508254845,-3.92886617991995,
10.7276060846967));
#258964=CARTESIAN_POINT('Ctrl Pts',(0.0984231081634105,-3.93176829070324,
10.7217480604703));
#258965=CARTESIAN_POINT('Ctrl Pts',(-0.0176397950592482,-3.93467366834328,
10.7158834419656));
#258966=CARTESIAN_POINT('Ctrl Pts',(-0.133750143999501,-3.93243355295864,
10.7100188234609));
#258967=CARTESIAN_POINT('Ctrl Pts',(-0.249420891978136,-3.92508321168416,
10.7041542049562));
#258968=CARTESIAN_POINT('Ctrl Pts',(-0.365169835348115,-3.91772790145407,
10.6982856218698));
#258969=CARTESIAN_POINT('Ctrl Pts',(-0.480478176761877,-3.90525553056381,
10.6924170387833));
#258970=CARTESIAN_POINT('Ctrl Pts',(-0.594866533463926,-3.8877529251953,
10.6865484556969));
#258971=CARTESIAN_POINT('Ctrl Pts',(-0.709419531295986,-3.87022512802572,
10.6806714258578));
#258972=CARTESIAN_POINT('Ctrl Pts',(-0.823049498770957,-3.84765272788506,
10.6747943960187));
#258973=CARTESIAN_POINT('Ctrl Pts',(-0.935289686065408,-3.82017305931808,
10.6689173661797));
#258974=CARTESIAN_POINT('Ctrl Pts',(-0.958973861498471,-3.81437448300713,
10.6676772345558));
#258975=CARTESIAN_POINT('Ctrl Pts',(-0.982596218813739,-3.80835757603493,
10.6664371029319));
#258976=CARTESIAN_POINT('Ctrl Pts',(-1.00615248140522,-3.80212390436742,
10.665196971308));
#258977=CARTESIAN_POINT('Ctrl Pts',(-1.11777594462562,-3.77258509202802,
10.659320496372));
#258978=CARTESIAN_POINT('Ctrl Pts',(-1.22828123126072,-3.73807790275959,
10.6534440214359));
#258979=CARTESIAN_POINT('Ctrl Pts',(-1.33719313729155,-3.69870295016785,
10.6475675464998));
#258980=CARTESIAN_POINT('Ctrl Pts',(-1.44596548139053,-3.65937845344133,
10.6416986017983));
#258981=CARTESIAN_POINT('Ctrl Pts',(-1.55314812084941,-3.61519873747118,
10.6358296570967));
#258982=CARTESIAN_POINT('Ctrl Pts',(-1.65827835528228,-3.56631489024768,
10.6299607123951));
#258983=CARTESIAN_POINT('Ctrl Pts',(-1.76330187478718,-3.51748066372809,
10.6240977251046));
#258984=CARTESIAN_POINT('Ctrl Pts',(-1.86627676131745,-3.46395197718809,
10.618234737814));
#258985=CARTESIAN_POINT('Ctrl Pts',(-1.96675836703128,-3.40592873174299,
10.6123717505234));
#258986=CARTESIAN_POINT('Ctrl Pts',(-2.0702645849194,-3.3461589197167,10.6063322805561));
#258987=CARTESIAN_POINT('Ctrl Pts',(-2.17112462101919,-3.28161982600654,
10.6002928105888));
#258988=CARTESIAN_POINT('Ctrl Pts',(-2.26887740614487,-3.21258218819151,
10.5942533406215));
#258989=CARTESIAN_POINT('Ctrl Pts',(-2.36366629657974,-3.14563779291604,
10.5883969892522));
#258990=CARTESIAN_POINT('Ctrl Pts',(-2.45553328457484,-3.074463970667,10.582540637883));
#258991=CARTESIAN_POINT('Ctrl Pts',(-2.5440863358764,-2.99935221599714,
10.5766842865138));
#258992=CARTESIAN_POINT('Ctrl Pts',(-2.63262646476228,-2.92425142227446,
10.5708287897533));
#258993=CARTESIAN_POINT('Ctrl Pts',(-2.71785330395911,-2.84521410569714,
10.5649732929927));
#258994=CARTESIAN_POINT('Ctrl Pts',(-2.79940799052347,-2.76257197238251,
10.5591177962322));
#258995=CARTESIAN_POINT('Ctrl Pts',(-2.88097044328147,-2.67992196932013,
10.5532617418713));
#258996=CARTESIAN_POINT('Ctrl Pts',(-2.95885975838638,-2.59366676086053,
10.5474056875104));
#258997=CARTESIAN_POINT('Ctrl Pts',(-3.03275452905179,-2.50417430833315,
10.5415496331496));
#258998=CARTESIAN_POINT('Ctrl Pts',(-3.10667415651591,-2.41465175224286,
10.5356916089231));
#258999=CARTESIAN_POINT('Ctrl Pts',(-3.17659630502371,-2.32189010475253,
10.5298335846967));
#259000=CARTESIAN_POINT('Ctrl Pts',(-3.24224082591309,-2.22628916063984,
10.5239755604702));
#259001=CARTESIAN_POINT('Ctrl Pts',(-3.3079592417231,-2.13058060017039,
10.5181109419655));
#259002=CARTESIAN_POINT('Ctrl Pts',(-3.36939018554241,-2.03202670430909,
10.5122463234609));
#259003=CARTESIAN_POINT('Ctrl Pts',(-3.42629766038499,-1.93105498172381,
10.5063817049562));
#259004=CARTESIAN_POINT('Ctrl Pts',(-3.48324360564761,-1.83001500053821,
10.5005131218697));
#259005=CARTESIAN_POINT('Ctrl Pts',(-3.53565980672289,-1.72655430510248,
10.4946445387833));
#259006=CARTESIAN_POINT('Ctrl Pts',(-3.58335766604816,-1.62112209200107,
10.4887759556968));
#259007=CARTESIAN_POINT('Ctrl Pts',(-3.63112417772309,-1.51553812850115,
10.4828989258577));
#259008=CARTESIAN_POINT('Ctrl Pts',(-3.67415864226214,-1.40797736605348,
10.4770218960187));
#259009=CARTESIAN_POINT('Ctrl Pts',(-3.71232169009813,-1.29890595087826,
10.4711448661796));
#259010=CARTESIAN_POINT('Ctrl Pts',(-3.72037460182053,-1.27589042859561,
10.4699047345557));
#259011=CARTESIAN_POINT('Ctrl Pts',(-3.72821078614053,-1.2528076828768,
10.4686646029319));
#259012=CARTESIAN_POINT('Ctrl Pts',(-3.73582922396418,-1.22966215253425,
10.467424471308));
#259013=CARTESIAN_POINT('Ctrl Pts',(-3.77875150432028,-1.0992602295483,
10.4604375694694));
#259014=CARTESIAN_POINT('Ctrl Pts',(-3.81487274743111,-0.966516379801271,
10.4534506676308));
#259015=CARTESIAN_POINT('Ctrl Pts',(-3.84397267993236,-0.832083551053413,
10.4464637657922));
#259016=CARTESIAN_POINT('Ctrl Pts',(-3.87333558081508,-0.696435888443252,
10.4394137251725));
#259017=CARTESIAN_POINT('Ctrl Pts',(-3.8955494943805,-0.559068587730943,
10.4323636845529));
#259018=CARTESIAN_POINT('Ctrl Pts',(-3.91043755570927,-0.420674604532453,
10.4253136439332));
#259019=CARTESIAN_POINT('Ctrl Pts',(-3.92532561703803,-0.282280621333972,
10.4182636033135));
#259020=CARTESIAN_POINT('Ctrl Pts',(-3.93288764831246,-0.142860003044011,
10.4112135626938));
#259021=CARTESIAN_POINT('Ctrl Pts',(-3.93299875665656,-0.00312732120702682,
10.4041635220741));
#259022=CARTESIAN_POINT('',(-3.93299911320432,0.00264112363370479,9.15416352198993));
#259023=CARTESIAN_POINT('Ctrl Pts',(-3.93299875665718,-0.00312732043226372,
10.404163522035));
#259024=CARTESIAN_POINT('Ctrl Pts',(-3.93309078967956,0.112615779917745,
10.398323846247));
#259025=CARTESIAN_POINT('Ctrl Pts',(-3.92806927566635,0.228430631313712,
10.3924841704591));
#259026=CARTESIAN_POINT('Ctrl Pts',(-3.91794197275038,0.343830915074334,
10.3866444946711));
#259027=CARTESIAN_POINT('Ctrl Pts',(-3.90781704942902,0.459204083432567,
10.3808061910215));
#259028=CARTESIAN_POINT('Ctrl Pts',(-3.8925887583352,0.574162464627012,
10.3749678873719));
#259029=CARTESIAN_POINT('Ctrl Pts',(-3.87231687339564,0.688223097560241,
10.3691295837223));
#259030=CARTESIAN_POINT('Ctrl Pts',(-3.85204479682467,0.802284808715876,
10.3632912248829));
#259031=CARTESIAN_POINT('Ctrl Pts',(-3.82672910434552,0.915448346124159,
10.3574528660435));
#259032=CARTESIAN_POINT('Ctrl Pts',(-3.79648088756923,1.02723992831351,
10.351614507204));
#259033=CARTESIAN_POINT('Ctrl Pts',(-3.7662249914741,1.13905989178595,10.345774666141));
#259034=CARTESIAN_POINT('Ctrl Pts',(-3.73103418970762,1.24950680701535,
10.3399348250781));
#259035=CARTESIAN_POINT('Ctrl Pts',(-3.69106952592704,1.35812177464789,
10.3340949840151));
#259036=CARTESIAN_POINT('Ctrl Pts',(-3.65105991031265,1.46685891125452,
10.3282485743603));
#259037=CARTESIAN_POINT('Ctrl Pts',(-3.60626585456031,1.57375959587137,
10.3224021647054));
#259038=CARTESIAN_POINT('Ctrl Pts',(-3.55689674711794,1.67838450014942,
10.3165557550506));
#259039=CARTESIAN_POINT('Ctrl Pts',(-3.50749770353745,1.78307284623849,
10.3107058002856));
#259040=CARTESIAN_POINT('Ctrl Pts',(-3.45351827707842,1.88548229723389,
10.3048558455205));
#259041=CARTESIAN_POINT('Ctrl Pts',(-3.39521316212138,1.98519938136141,
10.2990058907555));
#259042=CARTESIAN_POINT('Ctrl Pts',(-3.33681352420546,2.08507812461354,
10.2931464521736));
#259043=CARTESIAN_POINT('Ctrl Pts',(-3.27407441730308,2.18225543563252,
10.2872870135916));
#259044=CARTESIAN_POINT('Ctrl Pts',(-3.20729327165033,2.27634770402646,
10.2814275750097));
#259045=CARTESIAN_POINT('Ctrl Pts',(-3.16255700013714,2.3393795257333,10.2775023737758));
#259046=CARTESIAN_POINT('Ctrl Pts',(-3.11600768858825,2.40102757864677,
10.273577172542));
#259047=CARTESIAN_POINT('Ctrl Pts',(-3.06774420917845,2.46118558159519,
10.2696519713081));
#259048=CARTESIAN_POINT('Ctrl Pts',(-2.99548826351334,2.55124898865822,
10.263775496372));
#259049=CARTESIAN_POINT('Ctrl Pts',(-2.91914387804605,2.63827599189948,
10.2578990214359));
#259050=CARTESIAN_POINT('Ctrl Pts',(-2.838995680598,2.72187298115579,10.2520225464998));
#259051=CARTESIAN_POINT('Ctrl Pts',(-2.75895018668055,2.80536284752952,
10.2461536017983));
#259052=CARTESIAN_POINT('Ctrl Pts',(-2.67511085747126,2.88543114576499,
10.2402846570967));
#259053=CARTESIAN_POINT('Ctrl Pts',(-2.58780339201678,2.96171615862602,
10.2344157123952));
#259054=CARTESIAN_POINT('Ctrl Pts',(-2.50058455006753,3.03792373658269,
10.2285527251046));
#259055=CARTESIAN_POINT('Ctrl Pts',(-2.40990488344022,3.11035539816109,
10.222689737814));
#259056=CARTESIAN_POINT('Ctrl Pts',(-2.31612739419673,3.17868571800539,
10.2168267505234));
#259057=CARTESIAN_POINT('Ctrl Pts',(-2.21952709441381,3.24907285925295,
10.2107872805561));
#259058=CARTESIAN_POINT('Ctrl Pts',(-2.11963982650347,3.31510751082604,
10.2047478105888));
#259059=CARTESIAN_POINT('Ctrl Pts',(-2.01690000395989,3.37647795402644,
10.1987083406214));
#259060=CARTESIAN_POINT('Ctrl Pts',(-1.91727528462475,3.43598762640026,
10.1928519892522));
#259061=CARTESIAN_POINT('Ctrl Pts',(-1.8149688772172,3.49111162716366,10.186995637883));
#259062=CARTESIAN_POINT('Ctrl Pts',(-1.71040618228331,3.54160975992655,
10.1811392865138));
#259063=CARTESIAN_POINT('Ctrl Pts',(-1.60585874602865,3.59210052357171,
10.1752837897533));
#259064=CARTESIAN_POINT('Ctrl Pts',(-1.49905604847651,3.63796658212048,
10.1694282929927));
#259065=CARTESIAN_POINT('Ctrl Pts',(-1.39044680087717,3.67901436446373,
10.1635727962322));
#259066=CARTESIAN_POINT('Ctrl Pts',(-1.28182721076438,3.72006605565682,
10.1577167418713));
#259067=CARTESIAN_POINT('Ctrl Pts',(-1.17140111465654,3.7562984126361,10.1518606875105));
#259068=CARTESIAN_POINT('Ctrl Pts',(-1.05963518074281,3.78756680254384,
10.1460046331496));
#259069=CARTESIAN_POINT('Ctrl Pts',(-0.947831650889574,3.81884571054465,
10.1401466089231));
#259070=CARTESIAN_POINT('Ctrl Pts',(-0.834687784210151,3.84515722000133,
10.1342885846967));
#259071=CARTESIAN_POINT('Ctrl Pts',(-0.720682622384007,3.86640731917806,
10.1284305604702));
#259072=CARTESIAN_POINT('Ctrl Pts',(-0.606549126886282,3.88768133923,10.1225659419655));
#259073=CARTESIAN_POINT('Ctrl Pts',(-0.491552807025955,3.90388250173589,
10.1167013234609));
#259074=CARTESIAN_POINT('Ctrl Pts',(-0.376180139063614,3.91496839105683,
10.1108367049562));
#259075=CARTESIAN_POINT('Ctrl Pts',(-0.260729477216973,3.92606177462735,
10.1049681218697));
#259076=CARTESIAN_POINT('Ctrl Pts',(-0.144902371729417,3.93203297799127,
10.0990995387833));
#259077=CARTESIAN_POINT('Ctrl Pts',(-0.0291859082189477,3.93289170747955,
10.0932309556968));
#259078=CARTESIAN_POINT('Ctrl Pts',(0.0866971079884395,3.93375167295196,
10.0873539258577));
#259079=CARTESIAN_POINT('Ctrl Pts',(0.202468753687625,3.92948449489353,
10.0814768960187));
#259080=CARTESIAN_POINT('Ctrl Pts',(0.317646406652164,3.92015175220819,
10.0755998661796));
#259081=CARTESIAN_POINT('Ctrl Pts',(0.341950426491008,3.91818241911677,
10.0743597345557));
#259082=CARTESIAN_POINT('Ctrl Pts',(0.366228033625769,3.9159877149394,10.0731196029319));
#259083=CARTESIAN_POINT('Ctrl Pts',(0.390474757234038,3.91356850763635,
10.071879471308));
#259084=CARTESIAN_POINT('Ctrl Pts',(0.505370031917421,3.90210487683449,
10.066002996372));
#259085=CARTESIAN_POINT('Ctrl Pts',(0.619949171234503,3.88555841742889,
10.0601265214359));
#259086=CARTESIAN_POINT('Ctrl Pts',(0.73372702899801,3.86395311137671,10.0542500464998));
#259087=CARTESIAN_POINT('Ctrl Pts',(0.847359089500328,3.84237549080316,
10.0483811017982));
#259088=CARTESIAN_POINT('Ctrl Pts',(0.960191508640707,3.81575199186813,
10.0425121570967));
#259089=CARTESIAN_POINT('Ctrl Pts',(1.0717434813489,3.784158415049,10.0366432123951));
#259090=CARTESIAN_POINT('Ctrl Pts',(1.18318222059205,3.75259690803634,10.0307802251045));
#259091=CARTESIAN_POINT('Ctrl Pts',(1.29334270404577,3.71607547016882,10.0249172378139));
#259092=CARTESIAN_POINT('Ctrl Pts',(1.40175420989629,3.67472096015984,10.0190542505233));
#259093=CARTESIAN_POINT('Ctrl Pts',(1.51342902705711,3.63212163172327,10.013014780556));
#259094=CARTESIAN_POINT('Ctrl Pts',(1.62324746636208,3.58439373749369,10.0069753105887));
#259095=CARTESIAN_POINT('Ctrl Pts',(1.73071135911118,3.53173147215973,10.0009358406214));
#259096=CARTESIAN_POINT('Ctrl Pts',(1.83491691338163,3.48066594300497,9.9950794892522));
#259097=CARTESIAN_POINT('Ctrl Pts',(1.93690824726824,3.42496114726119,9.98922313788299));
#259098=CARTESIAN_POINT('Ctrl Pts',(2.03625206176144,3.36484272158036,9.98336678651377));
#259099=CARTESIAN_POINT('Ctrl Pts',(2.13558137915908,3.30473306889225,9.97751128975323));
#259100=CARTESIAN_POINT('Ctrl Pts',(2.23226359244968,3.24021128059932,9.97165579299268));
#259101=CARTESIAN_POINT('Ctrl Pts',(2.32589177737904,3.17154795642768,9.96580029623214));
#259102=CARTESIAN_POINT('Ctrl Pts',(2.41952887822285,3.10287809366592,9.95994424187125));
#259103=CARTESIAN_POINT('Ctrl Pts',(2.51011103978352,3.03006615507781,9.95408818751037));
#259104=CARTESIAN_POINT('Ctrl Pts',(2.59726257059164,2.95342447667174,9.94823213314948));
#259105=CARTESIAN_POINT('Ctrl Pts',(2.68444341752092,2.87675701745942,9.94237410892303));
#259106=CARTESIAN_POINT('Ctrl Pts',(2.76819102926681,2.79625752911366,9.93651608469658));
#259107=CARTESIAN_POINT('Ctrl Pts',(2.84816540221072,2.7122763210355,9.93065806047013));
#259108=CARTESIAN_POINT('Ctrl Pts',(2.92822980094584,2.62820057673997,9.92479344196546));
#259109=CARTESIAN_POINT('Ctrl Pts',(3.00451219871417,2.54063558922418,9.91892882346079));
#259110=CARTESIAN_POINT('Ctrl Pts',(3.07671178996934,2.4499660327163,9.91306420495611));
#259111=CARTESIAN_POINT('Ctrl Pts',(3.14896018937547,2.35923518204699,9.90719562186964));
#259112=CARTESIAN_POINT('Ctrl Pts',(3.2171200443725,2.26539591626727,9.90132703878317));
#259113=CARTESIAN_POINT('Ctrl Pts',(3.28093390974316,2.16886183974393,9.8954584556967));
#259114=CARTESIAN_POINT('Ctrl Pts',(3.34483962350809,2.0721888200635,9.88958142585763));
#259115=CARTESIAN_POINT('Ctrl Pts',(3.40438665320248,1.97281360176912,9.88370439601856));
#259116=CARTESIAN_POINT('Ctrl Pts',(3.45936347077419,1.87117433102134,9.87782736617949));
#259117=CARTESIAN_POINT('Ctrl Pts',(3.47096431200072,1.84972709026777,9.87658723455569));
#259118=CARTESIAN_POINT('Ctrl Pts',(3.48236182869111,1.82817910781322,9.87534710293188));
#259119=CARTESIAN_POINT('Ctrl Pts',(3.49355431073443,1.80653460469178,9.87410697130808));
#259120=CARTESIAN_POINT('Ctrl Pts',(3.54659089083413,1.70397018519341,9.86823049637202));
#259121=CARTESIAN_POINT('Ctrl Pts',(3.5951942876369,1.5988993790448,9.86235402143594));
#259122=CARTESIAN_POINT('Ctrl Pts',(3.63912008030365,1.49174194857245,9.85647754649988));
#259123=CARTESIAN_POINT('Ctrl Pts',(3.68298958556625,1.38472183181104,9.85060860179832));
#259124=CARTESIAN_POINT('Ctrl Pts',(3.72219325199971,1.27562078670707,9.84473965709676));
#259125=CARTESIAN_POINT('Ctrl Pts',(3.75653246394915,1.16488319040843,9.8388707123952));
#259126=CARTESIAN_POINT('Ctrl Pts',(3.79083681907021,1.05425800092319,9.83300772510461));
#259127=CARTESIAN_POINT('Ctrl Pts',(3.82028642015564,0.941999956514412,
9.82714473781403));
#259128=CARTESIAN_POINT('Ctrl Pts',(3.84473095028929,0.828572821113264,
9.82128175052345));
#259129=CARTESIAN_POINT('Ctrl Pts',(3.8699112889614,0.711731398169494,9.81524228055614));
#259130=CARTESIAN_POINT('Ctrl Pts',(3.88978029191589,0.593649798330309,
9.80920281058883));
#259131=CARTESIAN_POINT('Ctrl Pts',(3.90422912302375,0.474851508298298,
9.80316334062152));
#259132=CARTESIAN_POINT('Ctrl Pts',(3.91823986110178,0.359655219177676,
9.79730698925231));
#259133=CARTESIAN_POINT('Ctrl Pts',(3.9271543186426,0.24378551259495,9.79145063788309));
#259134=CARTESIAN_POINT('Ctrl Pts',(3.93092538653102,0.12772864019454,9.78559428651388));
#259135=CARTESIAN_POINT('Ctrl Pts',(3.9346959041131,0.0116887038014935,
9.77973878975334));
#259136=CARTESIAN_POINT('Ctrl Pts',(3.93332451113864,-0.104537931754083,
9.7738832929928));
#259137=CARTESIAN_POINT('Ctrl Pts',(3.92681617069035,-0.220462608178249,
9.76802779623226));
#259138=CARTESIAN_POINT('Ctrl Pts',(3.92030721047351,-0.336398323740624,
9.76217174187139));
#259139=CARTESIAN_POINT('Ctrl Pts',(3.90866035348079,-0.452031610972567,
9.75631568751052));
#259140=CARTESIAN_POINT('Ctrl Pts',(3.89193257887595,-0.566877236695884,
9.75045963314965));
#259141=CARTESIAN_POINT('Ctrl Pts',(3.87519917736507,-0.681761494309081,
9.74460160892318));
#259142=CARTESIAN_POINT('Ctrl Pts',(3.85338151910736,-0.795857155424221,
9.7387435846967));
#259143=CARTESIAN_POINT('Ctrl Pts',(3.82658787411862,-0.908688198255243,
9.73288556047023));
#259144=CARTESIAN_POINT('Ctrl Pts',(3.79976406797954,-1.0216462530716,9.72702094196555));
#259145=CARTESIAN_POINT('Ctrl Pts',(3.76795319081166,-1.13333644665078,
9.72115632346087));
#259146=CARTESIAN_POINT('Ctrl Pts',(3.73131369244653,-1.2432968786903,9.7152917049562));
#259147=CARTESIAN_POINT('Ctrl Pts',(3.69464942515776,-1.35333164585084,
9.70942312186973));
#259148=CARTESIAN_POINT('Ctrl Pts',(3.65315018399584,-1.46163393861627,
9.70355453878326));
#259149=CARTESIAN_POINT('Ctrl Pts',(3.60702231229754,-1.56776243053204,
9.69768595569679));
#259150=CARTESIAN_POINT('Ctrl Pts',(3.56082804795985,-1.67404367501221,
9.69180892585772));
#259151=CARTESIAN_POINT('Ctrl Pts',(3.50999203841075,-1.77814450541052,
9.68593189601864));
#259152=CARTESIAN_POINT('Ctrl Pts',(3.45476623595575,-1.87964870518407,
9.68005486617957));
#259153=CARTESIAN_POINT('Ctrl Pts',(3.44311285560011,-1.90106744416246,
9.67881473455573));
#259154=CARTESIAN_POINT('Ctrl Pts',(3.43126416390677,-1.92237067020355,
9.6775746029319));
#259155=CARTESIAN_POINT('Ctrl Pts',(3.41922276683365,-1.9435546482583,9.67633447130806));
#259156=CARTESIAN_POINT('Ctrl Pts',(3.3621635267212,-2.0439368284175,9.67045799637199));
#259157=CARTESIAN_POINT('Ctrl Pts',(3.30058606534913,-2.14196937778998,
9.66458152143592));
#259158=CARTESIAN_POINT('Ctrl Pts',(3.23470898962048,-2.2372185303337,9.65870504649985));
#259159=CARTESIAN_POINT('Ctrl Pts',(3.16891633011683,-2.33234562867565,
9.6528361017983));
#259160=CARTESIAN_POINT('Ctrl Pts',(3.09883524605315,-2.42469608704472,
9.64696715709676));
#259161=CARTESIAN_POINT('Ctrl Pts',(3.02472995346133,-2.51386111562151,
9.64109821239522));
#259162=CARTESIAN_POINT('Ctrl Pts',(2.95069988319724,-2.60293563512983,
9.63523522510463));
#259163=CARTESIAN_POINT('Ctrl Pts',(2.87265399203605,-2.68883084111629,
9.62937223781404));
#259164=CARTESIAN_POINT('Ctrl Pts',(2.79089908220354,-2.77116786084052,
9.62350925052345));
#259165=CARTESIAN_POINT('Ctrl Pts',(2.70668325533213,-2.8559833197825,9.61746978055614));
#259166=CARTESIAN_POINT('Ctrl Pts',(2.61853183037083,-2.93702261751076,
9.61143031058884));
#259167=CARTESIAN_POINT('Ctrl Pts',(2.52682429095157,-3.01390908997884,
9.60539084062153));
#259168=CARTESIAN_POINT('Ctrl Pts',(2.43789735250282,-3.08846434081218,
9.59953448925231));
#259169=CARTESIAN_POINT('Ctrl Pts',(2.34562717472276,-3.15911468227834,
9.59367813788309));
#259170=CARTESIAN_POINT('Ctrl Pts',(2.25039568444709,-3.22555549687521,
9.58782178651387));
#259171=CARTESIAN_POINT('Ctrl Pts',(2.15517809116175,-3.29198661586242,
9.58196628975332));
#259172=CARTESIAN_POINT('Ctrl Pts',(2.05700038303853,-3.35420919342828,
9.57611079299279));
#259173=CARTESIAN_POINT('Ctrl Pts',(1.95627489654002,-3.41196095070963,
9.57025529623225));
#259174=CARTESIAN_POINT('Ctrl Pts',(1.85553981827368,-3.4697182075072,9.56439924187137));
#259175=CARTESIAN_POINT('Ctrl Pts',(1.75225683734641,-3.52300359241427,
9.55854318751049));
#259176=CARTESIAN_POINT('Ctrl Pts',(1.6468637806232,-3.57160029791569,9.55268713314961));
#259177=CARTESIAN_POINT('Ctrl Pts',(1.54143527167537,-3.62021335042681,
9.54682910892315));
#259178=CARTESIAN_POINT('Ctrl Pts',(1.43389565005852,-3.66413441461709,
9.54097108469669));
#259179=CARTESIAN_POINT('Ctrl Pts',(1.32470298711665,-3.70319470132536,
9.53511306047024));
#259180=CARTESIAN_POINT('Ctrl Pts',(1.21538740785142,-3.74229895753398,
9.52924844196555));
#259181=CARTESIAN_POINT('Ctrl Pts',(1.10441546207365,-3.77653137635416,
9.52338382346086));
#259182=CARTESIAN_POINT('Ctrl Pts',(0.992260743807369,-3.80577293283491,
9.51751920495618));
#259183=CARTESIAN_POINT('Ctrl Pts',(0.880030207045497,-3.8350342571048,
9.51165062186972));
#259184=CARTESIAN_POINT('Ctrl Pts',(0.766615708140619,-3.8592979145663,
9.50578203878325));
#259185=CARTESIAN_POINT('Ctrl Pts',(0.65249970833359,-3.87849624605008,
9.49991345569679));
#259186=CARTESIAN_POINT('Ctrl Pts',(0.538219459404579,-3.89772221002269,
9.49403642585771));
#259187=CARTESIAN_POINT('Ctrl Pts',(0.423236102552506,-3.91186824846193,
9.48815939601864));
#259188=CARTESIAN_POINT('Ctrl Pts',(0.308035918127367,-3.92091862618232,
9.48228236617957));
#259189=CARTESIAN_POINT('Ctrl Pts',(0.2837271438504,-3.9228283765028,9.48104223455574));
#259190=CARTESIAN_POINT('Ctrl Pts',(0.259408708406923,-3.92451141903962,
9.4798021029319));
#259191=CARTESIAN_POINT('Ctrl Pts',(0.235085163687484,-3.92596790178091,
9.47856197130807));
#259192=CARTESIAN_POINT('Ctrl Pts',(0.119825865276744,-3.9328695758932,
9.472685496372));
#259193=CARTESIAN_POINT('Ctrl Pts',(0.00407266020957847,-3.93470260675513,
9.46680902143594));
#259194=CARTESIAN_POINT('Ctrl Pts',(-0.111691641314658,-3.93141373773614,
9.46093254649988));
#259195=CARTESIAN_POINT('Ctrl Pts',(-0.227307600108367,-3.9281290831408,
9.45506360179832));
#259196=CARTESIAN_POINT('Ctrl Pts',(-0.34293421826802,-3.91973559295167,
9.44919465709676));
#259197=CARTESIAN_POINT('Ctrl Pts',(-0.458084754329627,-3.90623186176279,
9.4433257123952));
#259198=CARTESIAN_POINT('Ctrl Pts',(-0.573118404118721,-3.89274183785532,
9.43746272510464));
#259199=CARTESIAN_POINT('Ctrl Pts',(-0.687676525602775,-3.8741519389711,
9.43159973781408));
#259200=CARTESIAN_POINT('Ctrl Pts',(-0.80127423609795,-3.85051277086126,
9.42573675052352));
#259201=CARTESIAN_POINT('Ctrl Pts',(-0.918291368643197,-3.82616203653826,
9.41969728055621));
#259202=CARTESIAN_POINT('Ctrl Pts',(-1.03428890876868,-3.79645324686516,
9.4136578105889));
#259203=CARTESIAN_POINT('Ctrl Pts',(-1.14874419599218,-3.76149913893042,
9.40761834062159));
#259204=CARTESIAN_POINT('Ctrl Pts',(-1.2597291634933,-3.72760485036346,
9.40176198925237));
#259205=CARTESIAN_POINT('Ctrl Pts',(-1.36926363050524,-3.68877886688265,
9.39590563788315));
#259206=CARTESIAN_POINT('Ctrl Pts',(-1.47688399926232,-3.64517525679122,
9.39004928651393));
#259207=CARTESIAN_POINT('Ctrl Pts',(-1.58448866313818,-3.60157800971012,
9.3841937897534));
#259208=CARTESIAN_POINT('Ctrl Pts',(-1.69017940181734,-3.55320467729791,
9.37833829299287));
#259209=CARTESIAN_POINT('Ctrl Pts',(-1.79351152823802,-3.50025790450894,
9.37248279623235));
#259210=CARTESIAN_POINT('Ctrl Pts',(-1.89685349464887,-3.44730608976698,
9.36662674187146));
#259211=CARTESIAN_POINT('Ctrl Pts',(-1.99783603503181,-3.38978015707795,
9.36077068751058));
#259212=CARTESIAN_POINT('Ctrl Pts',(-2.09603868129343,-3.32792891248021,
9.35491463314969));
#259213=CARTESIAN_POINT('Ctrl Pts',(-2.19427436106121,-3.26605686229781,
9.34905660892328));
#259214=CARTESIAN_POINT('Ctrl Pts',(-2.28972793827619,-3.19985682684637,
9.34319858469686));
#259215=CARTESIAN_POINT('Ctrl Pts',(-2.38200815922846,-3.12962076446477,
9.33734056047045));
#259216=CARTESIAN_POINT('Ctrl Pts',(-2.47439225845652,-3.05930563854188,
9.33147594196576));
#259217=CARTESIAN_POINT('Ctrl Pts',(-2.5635955432187,-2.98494566788812,
9.32561132346107));
#259218=CARTESIAN_POINT('Ctrl Pts',(-2.64926001224255,-2.90687295689588,
9.31974670495638));
#259219=CARTESIAN_POINT('Ctrl Pts',(-2.73498239190311,-2.82874746742437,
9.31387812186992));
#259220=CARTESIAN_POINT('Ctrl Pts',(-2.81716090045971,-2.74690453024212,
9.30800953878347));
#259221=CARTESIAN_POINT('Ctrl Pts',(-2.89547576050465,-2.66171168993375,
9.30214095569702));
#259222=CARTESIAN_POINT('Ctrl Pts',(-2.97390334047536,-2.57639623010427,
9.29626392585794));
#259223=CARTESIAN_POINT('Ctrl Pts',(-3.04845590970486,-2.48772155966338,
9.29038689601886));
#259224=CARTESIAN_POINT('Ctrl Pts',(-3.11885513504136,-2.39608673603986,
9.28450986617978));
#259225=CARTESIAN_POINT('Ctrl Pts',(-3.13371030985389,-2.37675056696504,
9.28326973455588));
#259226=CARTESIAN_POINT('Ctrl Pts',(-3.14838070876592,-2.35728268751127,
9.28202960293198));
#259227=CARTESIAN_POINT('Ctrl Pts',(-3.16286397392929,-2.33768699410769,
9.28078947130807));
#259228=CARTESIAN_POINT('Ctrl Pts',(-3.23181323616237,-2.24439942477283,
9.27488568099729));
#259229=CARTESIAN_POINT('Ctrl Pts',(-3.29674593639203,-2.14790444279783,
9.26898189068651));
#259230=CARTESIAN_POINT('Ctrl Pts',(-3.357351231072,-2.04858041365707,9.26307810037573));
#259231=CARTESIAN_POINT('Ctrl Pts',(-3.41787820237606,-1.94938474612748,
9.25718193984038));
#259232=CARTESIAN_POINT('Ctrl Pts',(-3.47408867880547,-1.8473676458361,
9.25128577930502));
#259233=CARTESIAN_POINT('Ctrl Pts',(-3.5257129685583,-1.74293920242212,
9.24538961876966));
#259234=CARTESIAN_POINT('Ctrl Pts',(-3.57728259270084,-1.63862133960143,
9.23949970175292));
#259235=CARTESIAN_POINT('Ctrl Pts',(-3.62427550994493,-1.53189757501787,
9.23360978473617));
#259236=CARTESIAN_POINT('Ctrl Pts',(-3.66646648705797,-1.4232050095755,
9.22771986771942));
#259237=CARTESIAN_POINT('Ctrl Pts',(-3.71037505838516,-1.31008757098965,
9.22159017224572));
#259238=CARTESIAN_POINT('Ctrl Pts',(-3.74908218615332,-1.1948380113328,
9.21546047677202));
#259239=CARTESIAN_POINT('Ctrl Pts',(-3.78238784457942,-1.07797550676157,
9.20933078129831));
#259240=CARTESIAN_POINT('Ctrl Pts',(-3.81434471613369,-0.965845609783869,
9.20344932150509));
#259241=CARTESIAN_POINT('Ctrl Pts',(-3.84132894942371,-0.852231291647644,
9.19756786171186));
#259242=CARTESIAN_POINT('Ctrl Pts',(-3.86321398196001,-0.737608791696994,
9.19168640191864));
#259243=CARTESIAN_POINT('Ctrl Pts',(-3.88509192118417,-0.623023442852632,
9.1858068484068));
#259244=CARTESIAN_POINT('Ctrl Pts',(-3.90187387451445,-0.507430962637488,
9.17992729489496));
#259245=CARTESIAN_POINT('Ctrl Pts',(-3.91348423597454,-0.391318456987147,
9.17404774138312));
#259246=CARTESIAN_POINT('Ctrl Pts',(-3.9250946136188,-0.275205789482569,
9.16816817967552));
#259247=CARTESIAN_POINT('Ctrl Pts',(-3.93153334311241,-0.158573500149906,
9.16228861796792));
#259248=CARTESIAN_POINT('Ctrl Pts',(-3.9327766547239,-0.0419140079057827,
9.15640905626031));
#259249=CARTESIAN_POINT('Ctrl Pts',(-3.9329349374279,-0.0270623973281688,
9.15566054485186));
#259250=CARTESIAN_POINT('Ctrl Pts',(-3.93300908639746,-0.0122103481301702,
9.15491203344342));
#259251=CARTESIAN_POINT('Ctrl Pts',(-3.93299911320492,0.00264112274000227,
9.15416352203497));
#259252=CARTESIAN_POINT('',(-3.93424124989278,0.000925550842382836,7.90416352203497));
#259253=CARTESIAN_POINT('Ctrl Pts',(-3.93299911320432,0.00264112363370051,
9.15416352198993));
#259254=CARTESIAN_POINT('Ctrl Pts',(-3.93291035429015,0.134815447560986,
9.14750196030159));
#259255=CARTESIAN_POINT('Ctrl Pts',(-3.92615470656503,0.26673201376134,
9.14084039861325));
#259256=CARTESIAN_POINT('Ctrl Pts',(-3.91283401044963,0.397767528424178,
9.13417883692491));
#259257=CARTESIAN_POINT('Ctrl Pts',(-3.89945202944097,0.529405901785881,
9.12748662720636));
#259258=CARTESIAN_POINT('Ctrl Pts',(-3.87944456837661,0.660154926868483,
9.12079441748782));
#259259=CARTESIAN_POINT('Ctrl Pts',(-3.85296449477469,0.789400786676568,
9.11410220776927));
#259260=CARTESIAN_POINT('Ctrl Pts',(-3.82633163095001,0.919392396062604,
9.10737138395058));
#259261=CARTESIAN_POINT('Ctrl Pts',(-3.79315134365712,1.04786327566221,
9.10064056013189));
#259262=CARTESIAN_POINT('Ctrl Pts',(-3.75362763403148,1.17420977045638,
9.0939097363132));
#259263=CARTESIAN_POINT('Ctrl Pts',(-3.73230669359977,1.24236698835868,
9.09027881464482));
#259264=CARTESIAN_POINT('Ctrl Pts',(-3.70914062135989,1.30990637709726,
9.08664789297644));
#259265=CARTESIAN_POINT('Ctrl Pts',(-3.68416709535157,1.37673592730371,
9.08301697130806));
#259266=CARTESIAN_POINT('Ctrl Pts',(-3.64374862504109,1.48489639250922,
9.07714049637199));
#259267=CARTESIAN_POINT('Ctrl Pts',(-3.59849649986989,1.59145346478966,
9.07126402143592));
#259268=CARTESIAN_POINT('Ctrl Pts',(-3.54855777328464,1.6959442000435,9.06538754649985));
#259269=CARTESIAN_POINT('Ctrl Pts',(-3.49868303919946,1.80030103874369,
9.0595186017983));
#259270=CARTESIAN_POINT('Ctrl Pts',(-3.44413382341125,1.90259643727877,
9.05364965709675));
#259271=CARTESIAN_POINT('Ctrl Pts',(-3.38510617211613,2.0023848789634,9.04778071239519));
#259272=CARTESIAN_POINT('Ctrl Pts',(-3.32613843823298,2.10207202803281,
9.04191772510462));
#259273=CARTESIAN_POINT('Ctrl Pts',(-3.26270152026241,2.19925692900491,
9.03605473781404));
#259274=CARTESIAN_POINT('Ctrl Pts',(-3.19503825599498,2.29351685032583,
9.03019175052346));
#259275=CARTESIAN_POINT('Ctrl Pts',(-3.12533824946592,2.39061410394828,
9.02415228055615));
#259276=CARTESIAN_POINT('Ctrl Pts',(-3.05115361762181,2.4846070925014,9.01811281058884));
#259277=CARTESIAN_POINT('Ctrl Pts',(-2.97279931020066,2.57506373926365,
9.01207334062154));
#259278=CARTESIAN_POINT('Ctrl Pts',(-2.89682072962432,2.66277771250764,
9.00621698925232));
#259279=CARTESIAN_POINT('Ctrl Pts',(-2.81692196968616,2.74716636468995,
9.00036063788311));
#259280=CARTESIAN_POINT('Ctrl Pts',(-2.73343181764692,2.82786836650426,
8.9945042865139));
#259281=CARTESIAN_POINT('Ctrl Pts',(-2.6499538492019,2.90855859159498,8.98864878975337));
#259282=CARTESIAN_POINT('Ctrl Pts',(-2.56288582743188,2.98556294936955,
8.98279329299284));
#259283=CARTESIAN_POINT('Ctrl Pts',(-2.4725932785355,3.05855709100567,8.97693779623231));
#259284=CARTESIAN_POINT('Ctrl Pts',(-2.3822921313666,3.13155818364195,8.97108174187143));
#259285=CARTESIAN_POINT('Ctrl Pts',(-2.28876616759336,3.20054804155024,
8.96522568751055));
#259286=CARTESIAN_POINT('Ctrl Pts',(-2.19241329216521,3.2652431695568,8.95936963314967));
#259287=CARTESIAN_POINT('Ctrl Pts',(-2.0960280054582,3.32996005977673,8.95351160892323));
#259288=CARTESIAN_POINT('Ctrl Pts',(-1.99681425861177,3.39037911747974,
8.94765358469679));
#259289=CARTESIAN_POINT('Ctrl Pts',(-1.89519755969265,3.44626104782197,
8.94179556047035));
#259290=CARTESIAN_POINT('Ctrl Pts',(-1.79346647258389,3.50220588350274,
8.93593094196567));
#259291=CARTESIAN_POINT('Ctrl Pts',(-1.68932739639763,3.5536031991818,8.93006632346099));
#259292=CARTESIAN_POINT('Ctrl Pts',(-1.58322905712907,3.60026037289835,
8.92420170495631));
#259293=CARTESIAN_POINT('Ctrl Pts',(-1.47705899358003,3.64694908765727,
8.91833312186986));
#259294=CARTESIAN_POINT('Ctrl Pts',(-1.36892741328657,3.68889113074596,
8.9124645387834));
#259295=CARTESIAN_POINT('Ctrl Pts',(-1.25929994290721,3.72594318982374,
8.90659595569695));
#259296=CARTESIAN_POINT('Ctrl Pts',(-1.14951468382348,3.76304857856766,
8.90071892585788));
#259297=CARTESIAN_POINT('Ctrl Pts',(-1.03822963275164,3.79524982333243,
8.89484189601882));
#259298=CARTESIAN_POINT('Ctrl Pts',(-0.925922421305458,3.82245427307167,
8.88896486617975));
#259299=CARTESIAN_POINT('Ctrl Pts',(-0.902224102882769,3.82819477454199,
8.88772473455586));
#259300=CARTESIAN_POINT('Ctrl Pts',(-0.8784802939293,3.83371296908723,8.88648460293196));
#259301=CARTESIAN_POINT('Ctrl Pts',(-0.854695512203774,3.83900828097814,
8.88524447130806));
#259302=CARTESIAN_POINT('Ctrl Pts',(-0.741989190570715,3.86410059134748,
8.87936799637199));
#259303=CARTESIAN_POINT('Ctrl Pts',(-0.62799142012608,3.88426672184273,
8.87349152143592));
#259304=CARTESIAN_POINT('Ctrl Pts',(-0.513170456044613,3.89937752507281,
8.86761504649985));
#259305=CARTESIAN_POINT('Ctrl Pts',(-0.398496625882081,3.91446896501226,
8.86174610179829));
#259306=CARTESIAN_POINT('Ctrl Pts',(-0.283002105394635,3.9245179073427,
8.85587715709674));
#259307=CARTESIAN_POINT('Ctrl Pts',(-0.167167253910271,3.92944577634303,
8.85000821239518));
#259308=CARTESIAN_POINT('Ctrl Pts',(-0.0514499833282893,3.93436864319353,
8.84414522510459));
#259309=CARTESIAN_POINT('Ctrl Pts',(0.0646065211783655,3.93418075938562,
8.838282237814));
#259310=CARTESIAN_POINT('Ctrl Pts',(0.180515487543246,3.92885519696985,
8.8324192505234));
#259311=CARTESIAN_POINT('Ctrl Pts',(0.299913447423724,3.92336932898568,
8.8263797805561));
#259312=CARTESIAN_POINT('Ctrl Pts',(0.419154404326305,3.91243151860435,
8.82034031058879));
#259313=CARTESIAN_POINT('Ctrl Pts',(0.537704433560517,3.8960701921461,8.81430084062148));
#259314=CARTESIAN_POINT('Ctrl Pts',(0.652659989227609,3.88020494616845,
8.80844448925227));
#259315=CARTESIAN_POINT('Ctrl Pts',(0.766965473795392,3.85924038906495,
8.80258813788305));
#259316=CARTESIAN_POINT('Ctrl Pts',(0.880138723547427,3.83325512160518,
8.79673178651384));
#259317=CARTESIAN_POINT('Ctrl Pts',(0.993295458094677,3.80727364613701,
8.79087628975331));
#259318=CARTESIAN_POINT('Ctrl Pts',(1.10531988427633,3.77627300953238,8.78502079299278));
#259319=CARTESIAN_POINT('Ctrl Pts',(1.21574080643334,3.74038277340339,8.77916529623225));
#259320=CARTESIAN_POINT('Ctrl Pts',(1.32617224362404,3.7044891195612,8.77330924187136));
#259321=CARTESIAN_POINT('Ctrl Pts',(1.43499948076815,3.66370506814976,8.76745318751047));
#259322=CARTESIAN_POINT('Ctrl Pts',(1.54176791442105,3.6182095984149,8.76159713314958));
#259323=CARTESIAN_POINT('Ctrl Pts',(1.64857226294889,3.5726988248674,8.75573910892314));
#259324=CARTESIAN_POINT('Ctrl Pts',(1.75331605144466,3.52247364324909,8.7498810846967));
#259325=CARTESIAN_POINT('Ctrl Pts',(1.85556667801781,3.46776027190894,8.74402306047025));
#259326=CARTESIAN_POINT('Ctrl Pts',(1.95793240638224,3.41298531065722,8.73815844196557));
#259327=CARTESIAN_POINT('Ctrl Pts',(2.05779900733597,3.35371227073252,8.73229382346089));
#259328=CARTESIAN_POINT('Ctrl Pts',(2.15476034423315,3.29021228174114,8.7264292049562));
#259329=CARTESIAN_POINT('Ctrl Pts',(2.25178722864191,3.22666936567803,8.72056062186974));
#259330=CARTESIAN_POINT('Ctrl Pts',(2.34590460410072,3.15889405105692,8.71469203878328));
#259331=CARTESIAN_POINT('Ctrl Pts',(2.43673845398853,3.08719852080387,8.70882345569682));
#259332=CARTESIAN_POINT('Ctrl Pts',(2.52770304259934,3.01539979794056,8.70294642585775));
#259333=CARTESIAN_POINT('Ctrl Pts',(2.61537436318139,2.93966986790048,8.69706939601868));
#259334=CARTESIAN_POINT('Ctrl Pts',(2.69941432158252,2.86035859997224,8.69119236617961));
#259335=CARTESIAN_POINT('Ctrl Pts',(2.71714787287179,2.84362286539573,8.68995223455576));
#259336=CARTESIAN_POINT('Ctrl Pts',(2.7347198732339,2.82672778510936,8.68871210293192));
#259337=CARTESIAN_POINT('Ctrl Pts',(2.75212737675622,2.8096768323259,8.68747197130808));
#259338=CARTESIAN_POINT('Ctrl Pts',(2.83461439360333,2.72887936313655,8.681595496372));
#259339=CARTESIAN_POINT('Ctrl Pts',(2.9136760718494,2.64431332078843,8.67571902143593));
#259340=CARTESIAN_POINT('Ctrl Pts',(2.98894883581638,2.55630081501999,8.66984254649985));
#259341=CARTESIAN_POINT('Ctrl Pts',(3.06412514373247,2.46840109026675,8.6639736017983));
#259342=CARTESIAN_POINT('Ctrl Pts',(3.13552192723564,2.37706399588563,8.65810465709674));
#259343=CARTESIAN_POINT('Ctrl Pts',(3.20281140389944,2.28264936226563,8.65223571239519));
#259344=CARTESIAN_POINT('Ctrl Pts',(3.27003257679035,2.18833056644988,8.64637272510459));
#259345=CARTESIAN_POINT('Ctrl Pts',(3.33315449791145,2.0909407794463,8.640509737814));
#259346=CARTESIAN_POINT('Ctrl Pts',(3.39188918338247,1.99087336806062,8.63464675052341));
#259347=CARTESIAN_POINT('Ctrl Pts',(3.45239185059966,1.88779381222744,8.6286072805561));
#259348=CARTESIAN_POINT('Ctrl Pts',(3.50823868180835,1.78187321487768,8.6225678105888));
#259349=CARTESIAN_POINT('Ctrl Pts',(3.55916238545576,1.67357465144429,8.61652834062149));
#259350=CARTESIAN_POINT('Ctrl Pts',(3.60854206665222,1.56855973396298,8.61067198925227));
#259351=CARTESIAN_POINT('Ctrl Pts',(3.65329267031689,1.46130937299166,8.60481563788305));
#259352=CARTESIAN_POINT('Ctrl Pts',(3.69321718741445,1.35227061144822,8.59895928651384));
#259353=CARTESIAN_POINT('Ctrl Pts',(3.73313587838633,1.2432477617698,8.5931037897533));
#259354=CARTESIAN_POINT('Ctrl Pts',(3.76822974136158,1.13243741788122,8.58724829299277));
#259355=CARTESIAN_POINT('Ctrl Pts',(3.79835046683571,1.02030521467303,8.58139279623224));
#259356=CARTESIAN_POINT('Ctrl Pts',(3.82847406061084,0.908162333471344,
8.57553674187135));
#259357=CARTESIAN_POINT('Ctrl Pts',(3.85362346839962,0.794697741277012,
8.56968068751046));
#259358=CARTESIAN_POINT('Ctrl Pts',(3.87370085314682,0.680390108929896,
8.56382463314957));
#259359=CARTESIAN_POINT('Ctrl Pts',(3.89378499154524,0.566044025664439,
8.55796660892313));
#259360=CARTESIAN_POINT('Ctrl Pts',(3.90879364292156,0.450854744561919,
8.55210858469668));
#259361=CARTESIAN_POINT('Ctrl Pts',(3.91868056588485,0.335308250057171,
8.54625056047023));
#259362=CARTESIAN_POINT('Ctrl Pts',(3.92857861838916,0.219631686828761,
8.54038594196555));
#259363=CARTESIAN_POINT('Ctrl Pts',(3.93334340015094,0.103597519004202,
8.53452132346087));
#259364=CARTESIAN_POINT('Ctrl Pts',(3.9329807478794,-0.0123059664400662,
8.52865670495618));
#259365=CARTESIAN_POINT('Ctrl Pts',(3.93261785044875,-0.128287804610262,
8.52278812186971));
#259366=CARTESIAN_POINT('Ctrl Pts',(3.92712063629491,-0.244138373326166,
8.51691953878325));
#259367=CARTESIAN_POINT('Ctrl Pts',(3.91654686946191,-0.35937392686186,
8.51105095569678));
#259368=CARTESIAN_POINT('Ctrl Pts',(3.90595788362437,-0.474775340912462,
8.50517392585771));
#259369=CARTESIAN_POINT('Ctrl Pts',(3.89027781912066,-0.589559566020484,
8.49929689601864));
#259370=CARTESIAN_POINT('Ctrl Pts',(3.86961561816118,-0.703252421028928,
8.49341986617956));
#259371=CARTESIAN_POINT('Ctrl Pts',(3.86525561837737,-0.727243128709607,
8.49217973455573));
#259372=CARTESIAN_POINT('Ctrl Pts',(3.86067395786117,-0.751185294892164,
8.4909396029319));
#259373=CARTESIAN_POINT('Ctrl Pts',(3.8558719418734,-0.775074556332128,
8.48969947130807));
#259374=CARTESIAN_POINT('Ctrl Pts',(3.83311715838715,-0.888275964469223,
8.48382299637199));
#259375=CARTESIAN_POINT('Ctrl Pts',(3.80533561733877,-1.00066079646393,
8.47794652143592));
#259376=CARTESIAN_POINT('Ctrl Pts',(3.77259909706671,-1.11174864641762,
8.47207004649985));
#259377=CARTESIAN_POINT('Ctrl Pts',(3.73990452603765,-1.22269414614068,
8.4662011017983));
#259378=CARTESIAN_POINT('Ctrl Pts',(3.70226771868287,-1.33234557675928,
8.46033215709674));
#259379=CARTESIAN_POINT('Ctrl Pts',(3.65981158979467,-1.44023196992867,
8.45446321239519));
#259380=CARTESIAN_POINT('Ctrl Pts',(3.61739855700303,-1.54800885046608,
8.4486002251046));
#259381=CARTESIAN_POINT('Ctrl Pts',(3.57017608374951,-1.65402387562024,
8.44273723781401));
#259382=CARTESIAN_POINT('Ctrl Pts',(3.51831689761231,-1.75782115358067,
8.43687425052341));
#259383=CARTESIAN_POINT('Ctrl Pts',(3.46489669018543,-1.86474284927257,
8.43083478055611));
#259384=CARTESIAN_POINT('Ctrl Pts',(3.40655632782321,-1.96931073926958,
8.4247953105888));
#259385=CARTESIAN_POINT('Ctrl Pts',(3.34353825557212,-2.0710482692409,8.4187558406215));
#259386=CARTESIAN_POINT('Ctrl Pts',(3.28243091077021,-2.1697010858247,8.41289948925228));
#259387=CARTESIAN_POINT('Ctrl Pts',(3.21692565909362,-2.26569232740226,
8.40704313788307));
#259388=CARTESIAN_POINT('Ctrl Pts',(3.14728982722824,-2.35861309744214,
8.40118678651385));
#259389=CARTESIAN_POINT('Ctrl Pts',(3.07766415721673,-2.45152030769161,
8.39533128975332));
#259390=CARTESIAN_POINT('Ctrl Pts',(3.00390935302893,-2.54135760724159,
8.38947579299279));
#259391=CARTESIAN_POINT('Ctrl Pts',(2.92633487980487,-2.62774678598175,
8.38362029623227));
#259392=CARTESIAN_POINT('Ctrl Pts',(2.84875301941015,-2.71414419128897,
8.37776424187138));
#259393=CARTESIAN_POINT('Ctrl Pts',(2.76735104263499,-2.79709251599194,
8.3719081875105));
#259394=CARTESIAN_POINT('Ctrl Pts',(2.68247686227203,-2.87624875199889,
8.36605213314961));
#259395=CARTESIAN_POINT('Ctrl Pts',(2.59757413184547,-2.95543161466148,
8.36019410892317));
#259396=CARTESIAN_POINT('Ctrl Pts',(2.50919717692449,-3.03081957083429,
8.35433608469673));
#259397=CARTESIAN_POINT('Ctrl Pts',(2.41772817347323,-3.10210887610248,
8.3484780604703));
#259398=CARTESIAN_POINT('Ctrl Pts',(2.32615620492044,-3.17347843052916,
8.34261344196561));
#259399=CARTESIAN_POINT('Ctrl Pts',(2.23148556649261,-3.24073987169441,
8.33674882346093));
#259400=CARTESIAN_POINT('Ctrl Pts',(2.13412875972782,-3.30363185553454,
8.33088420495625));
#259401=CARTESIAN_POINT('Ctrl Pts',(2.03670613810714,-3.36656635542455,
8.32501562186979));
#259402=CARTESIAN_POINT('Ctrl Pts',(1.9365940875158,-3.42512530829786,8.31914703878333));
#259403=CARTESIAN_POINT('Ctrl Pts',(1.83422961587707,-3.47909337561374,
8.31327845569688));
#259404=CARTESIAN_POINT('Ctrl Pts',(1.73171780929298,-3.53313912009752,
8.3074014258578));
#259405=CARTESIAN_POINT('Ctrl Pts',(1.62694748362794,-3.58258061700573,
8.30152439601873));
#259406=CARTESIAN_POINT('Ctrl Pts',(1.52037553378327,-3.62725064425844,
8.29564736617966));
#259407=CARTESIAN_POINT('Ctrl Pts',(1.49788743199745,-3.63667661536151,
8.2944072345558));
#259408=CARTESIAN_POINT('Ctrl Pts',(1.47531916159813,-3.64589030657686,
8.29316710293194));
#259409=CARTESIAN_POINT('Ctrl Pts',(1.45267509187603,-3.65489043302846,
8.29192697130807));
#259410=CARTESIAN_POINT('Ctrl Pts',(1.34537413638719,-3.69753833950591,
8.286050496372));
#259411=CARTESIAN_POINT('Ctrl Pts',(1.23601687412186,-3.73552720202288,
8.28017402143592));
#259412=CARTESIAN_POINT('Ctrl Pts',(1.12504515455434,-3.7686552509103,8.27429754649985));
#259413=CARTESIAN_POINT('Ctrl Pts',(1.01421563640559,-3.80174084884201,
8.26842860179829));
#259414=CARTESIAN_POINT('Ctrl Pts',(0.901776167133158,-3.82997790347437,
8.26255965709674));
#259415=CARTESIAN_POINT('Ctrl Pts',(0.788188566919396,-3.85321265737794,
8.25669071239519));
#259416=CARTESIAN_POINT('Ctrl Pts',(0.674716266482581,-3.87642382629567,
8.2508277251046));
#259417=CARTESIAN_POINT('Ctrl Pts',(0.560098555277048,-3.89464271255726,
8.24496473781401));
#259418=CARTESIAN_POINT('Ctrl Pts',(0.444811775447612,-3.90776553600944,
8.23910175052342));
#259419=CARTESIAN_POINT('Ctrl Pts',(0.326054730634482,-3.92128337157646,
8.23306228055611));
#259420=CARTESIAN_POINT('Ctrl Pts',(0.206588125901247,-3.92939335631743,
8.22702281058881));
#259421=CARTESIAN_POINT('Ctrl Pts',(0.0869436374963476,-3.93203888636658,
8.2209833406215));
#259422=CARTESIAN_POINT('Ctrl Pts',(-0.0290731930007671,-3.93460420312608,
8.21512698925228));
#259423=CARTESIAN_POINT('Ctrl Pts',(-0.145256833890354,-3.93203164671809,
8.20927063788307));
#259424=CARTESIAN_POINT('Ctrl Pts',(-0.261118758180631,-3.92432236113781,
8.20341428651385));
#259425=CARTESIAN_POINT('Ctrl Pts',(-0.376963774911809,-3.91661420056216,
8.19755878975332));
#259426=CARTESIAN_POINT('Ctrl Pts',(-0.492486756747227,-3.90377082876646,
8.19170329299278));
#259427=CARTESIAN_POINT('Ctrl Pts',(-0.607201924524633,-3.88584544505486,
8.18584779623225));
#259428=CARTESIAN_POINT('Ctrl Pts',(-0.721928016263048,-3.8679183543659,
8.17999174187137));
#259429=CARTESIAN_POINT('Ctrl Pts',(-0.835845733284041,-3.8449083534386,
8.17413568751048));
#259430=CARTESIAN_POINT('Ctrl Pts',(-0.948477841967473,-3.81692006509132,
8.16827963314959));
#259431=CARTESIAN_POINT('Ctrl Pts',(-1.06114783795495,-3.78892236201495,
8.16242160892314));
#259432=CARTESIAN_POINT('Ctrl Pts',(-1.17253096540947,-3.75594314104913,
8.15656358469669));
#259433=CARTESIAN_POINT('Ctrl Pts',(-1.28216422261669,-3.71813715538329,
8.15070556047024));
#259434=CARTESIAN_POINT('Ctrl Pts',(-1.39192089211684,-3.68028861216242,
8.14484094196556));
#259435=CARTESIAN_POINT('Ctrl Pts',(-1.4999233695722,-3.63760259441104,
8.13897632346088));
#259436=CARTESIAN_POINT('Ctrl Pts',(-1.6057276615338,-3.59028239515852,
8.13311170495619));
#259437=CARTESIAN_POINT('Ctrl Pts',(-1.71160347899483,-3.54293020664713,
8.12724312186974));
#259438=CARTESIAN_POINT('Ctrl Pts',(-1.81527778397138,-3.4909377829408,
8.12137453878328));
#259439=CARTESIAN_POINT('Ctrl Pts',(-1.91633178630073,-3.43455404453234,
8.11550595569682));
#259440=CARTESIAN_POINT('Ctrl Pts',(-2.01753123739441,-3.37808915203902,
8.10962892585775));
#259441=CARTESIAN_POINT('Ctrl Pts',(-2.11610250971854,-3.31722054741486,
8.10375189601868));
#259442=CARTESIAN_POINT('Ctrl Pts',(-2.21165630466072,-3.25224005726122,
8.09787486617961));
#259443=CARTESIAN_POINT('Ctrl Pts',(-2.23181942891412,-3.23852830779269,
8.09663473455576));
#259444=CARTESIAN_POINT('Ctrl Pts',(-2.25184831577001,-3.22463361002975,
8.09539460293191));
#259445=CARTESIAN_POINT('Ctrl Pts',(-2.27173950580696,-3.21055892606816,
8.09415447130807));
#259446=CARTESIAN_POINT('Ctrl Pts',(-2.36541204959047,-3.144277750976,8.08831438413299));
#259447=CARTESIAN_POINT('Ctrl Pts',(-2.45634508284629,-3.07377766099405,
8.08247429695792));
#259448=CARTESIAN_POINT('Ctrl Pts',(-2.54413139898459,-2.99931399234903,
8.07663420978283));
#259449=CARTESIAN_POINT('Ctrl Pts',(-2.63180489291161,-2.92494602376442,
8.07080162823709));
#259450=CARTESIAN_POINT('Ctrl Pts',(-2.71633939417977,-2.84662487243111,
8.06496904669133));
#259451=CARTESIAN_POINT('Ctrl Pts',(-2.79735680083598,-2.76464897027031,
8.05913646514558));
#259452=CARTESIAN_POINT('Ctrl Pts',(-2.87829237462163,-2.68275586912311,
8.05330977488802));
#259453=CARTESIAN_POINT('Ctrl Pts',(-2.95571762607744,-2.59721565412246,
8.04748308463046));
#259454=CARTESIAN_POINT('Ctrl Pts',(-3.02928825524465,-2.50836633421771,
8.0416563943729));
#259455=CARTESIAN_POINT('Ctrl Pts',(-3.10280642452256,-2.41958036874584,
8.03583385886471));
#259456=CARTESIAN_POINT('Ctrl Pts',(-3.17247517203039,-2.32749031240236,
8.03001132335653));
#259457=CARTESIAN_POINT('Ctrl Pts',(-3.23798824238765,-2.23246974048011,
8.02418878784835));
#259458=CARTESIAN_POINT('Ctrl Pts',(-3.30347679317533,-2.13748473189679,
8.01836843153988));
#259459=CARTESIAN_POINT('Ctrl Pts',(-3.36481252099727,-2.03957173170653,
8.01254807523142));
#259460=CARTESIAN_POINT('Ctrl Pts',(-3.4217309428114,-1.93913546587313,
8.00672771892296));
#259461=CARTESIAN_POINT('Ctrl Pts',(-3.47864223314819,-1.8387117839964,
8.00090809186414));
#259462=CARTESIAN_POINT('Ctrl Pts',(-3.53113711173155,-1.73576582906683,
7.99508846480533));
#259463=CARTESIAN_POINT('Ctrl Pts',(-3.57899614054457,-1.63072855680126,
7.98926883774651));
#259464=CARTESIAN_POINT('Ctrl Pts',(-3.62686108896054,-1.52567829265173,
7.98344849086779));
#259465=CARTESIAN_POINT('Ctrl Pts',(-3.67008887487706,-1.41853657797749,
7.97762814398907));
#259466=CARTESIAN_POINT('Ctrl Pts',(-3.70850778308308,-1.30975532936966,
7.97180779711035));
#259467=CARTESIAN_POINT('Ctrl Pts',(-3.74696460218192,-1.20086673793379,
7.96598170684753));
#259468=CARTESIAN_POINT('Ctrl Pts',(-3.78060292647502,-1.09033577653945,
7.9601556165847));
#259469=CARTESIAN_POINT('Ctrl Pts',(-3.80930060036575,-0.978630643324191,
7.95432952632187));
#259470=CARTESIAN_POINT('Ctrl Pts',(-3.83801263407408,-0.866869614800349,
7.94850052078467));
#259471=CARTESIAN_POINT('Ctrl Pts',(-3.86177900736688,-0.753933653675194,
7.94267151524746));
#259472=CARTESIAN_POINT('Ctrl Pts',(-3.88052886830953,-0.640300478069776,
7.93684250971026));
#259473=CARTESIAN_POINT('Ctrl Pts',(-3.89930857883885,-0.5264863996121,
7.93100422445591));
#259474=CARTESIAN_POINT('Ctrl Pts',(-3.91305577257815,-0.411973304872136,
7.92516593920156));
#259475=CARTESIAN_POINT('Ctrl Pts',(-3.92175154018954,-0.297243767001051,
7.91932765394721));
#259476=CARTESIAN_POINT('Ctrl Pts',(-3.92928022149421,-0.197912441065812,
7.9142729433098));
#259477=CARTESIAN_POINT('Ctrl Pts',(-3.93302326243764,-0.0984190716634967,
7.90921823267238));
#259478=CARTESIAN_POINT('Ctrl Pts',(-3.93299989116401,0.000925258806245537,
7.90416352203497));
#259479=CARTESIAN_POINT('',(-3.93117425036855,-0.0034247740854032,6.65416352203497));
#259480=CARTESIAN_POINT('Ctrl Pts',(-3.93908469165526,0.000926690287404459,
7.90416352203497));
#259481=CARTESIAN_POINT('Ctrl Pts',(-3.93924795559323,0.0519846458656478,
7.90156967179267));
#259482=CARTESIAN_POINT('Ctrl Pts',(-3.91527744507353,1.40055255217221,
7.83305165488378));
#259483=CARTESIAN_POINT('Ctrl Pts',(-2.37754416811895,3.98829885572659,
7.69860947130798));
#259484=CARTESIAN_POINT('Ctrl Pts',(2.04694591492513,4.16764399334989,7.50083697130812));
#259485=CARTESIAN_POINT('Ctrl Pts',(4.60972494745586,0.556488942156041,
7.30306447130803));
#259486=CARTESIAN_POINT('Ctrl Pts',(2.97992819577477,-3.56079653756905,
7.1052919713081));
#259487=CARTESIAN_POINT('Ctrl Pts',(-1.36013325384479,-4.43951366319872,
6.90751947130804));
#259488=CARTESIAN_POINT('Ctrl Pts',(-3.71950508566899,-2.0375324526334,
6.75714332155038));
#259489=CARTESIAN_POINT('Ctrl Pts',(-3.93427653238721,-0.370036660280284,
6.67269133845934));
#259490=CARTESIAN_POINT('Ctrl Pts',(-3.93117425036855,-0.0034247740854032,
6.65416352203497));
#259491=CARTESIAN_POINT('',(-3.92771320559034,0.00202021301316996,5.40416352203497));
#259492=CARTESIAN_POINT('Ctrl Pts',(-3.93117425036855,-0.0034247740854032,
6.65416352203497));
#259493=CARTESIAN_POINT('Ctrl Pts',(-3.92323824529709,0.934411879900014,
6.60676717179267));
#259494=CARTESIAN_POINT('Ctrl Pts',(-3.11850751936548,3.1889329285567,6.49344665488371));
#259495=CARTESIAN_POINT('Ctrl Pts',(0.638898125826581,4.5990274209643,6.31420197130807));
#259496=CARTESIAN_POINT('Ctrl Pts',(4.2036098479625,1.97203151090957,6.11642947130806));
#259497=CARTESIAN_POINT('Ctrl Pts',(3.94511019507904,-2.44854029629629,
5.91865697130807));
#259498=CARTESIAN_POINT('Ctrl Pts',(0.0985063367380218,-4.64214826731606,
5.72088447130805));
#259499=CARTESIAN_POINT('Ctrl Pts',(-3.31475397322523,-2.88317796999455,
5.54938665488371));
#259500=CARTESIAN_POINT('Ctrl Pts',(-3.92402635340491,-0.784273446107112,
5.443813005126));
#259501=CARTESIAN_POINT('Ctrl Pts',(-3.92771320559034,0.00202021301316996,
5.40416352203497));
#259502=CARTESIAN_POINT('',(-3.93835609680327,0.00176884156033657,4.15416352203497));
#259503=CARTESIAN_POINT('Ctrl Pts',(-3.92771320559034,0.00202021301316996,
5.40416352203497));
#259504=CARTESIAN_POINT('Ctrl Pts',(-3.93015638686309,0.523076617291602,
5.37788883845933));
#259505=CARTESIAN_POINT('Ctrl Pts',(-3.59181156520463,2.34843854388582,
5.28568998821704));
#259506=CARTESIAN_POINT('Ctrl Pts',(-0.833417785374429,4.56778489316098,
5.12756697130806));
#259507=CARTESIAN_POINT('Ctrl Pts',(3.37464468803266,3.18920323300653,4.92979447130806));
#259508=CARTESIAN_POINT('Ctrl Pts',(4.51344516429205,-1.0899801753418,4.73202197130807));
#259509=CARTESIAN_POINT('Ctrl Pts',(1.54723696509406,-4.37781929912556,
4.53424947130806));
#259510=CARTESIAN_POINT('Ctrl Pts',(-2.71224270174677,-3.70207996991296,
4.34162998821703));
#259511=CARTESIAN_POINT('Ctrl Pts',(-3.93161373910733,-1.19505393419467,
4.21493467179267));
#259512=CARTESIAN_POINT('Ctrl Pts',(-3.93835609680327,0.00176884156033657,
4.15416352203497));
#259513=CARTESIAN_POINT('',(-3.93264116285329,-0.00353165188606064,2.90416352203497));
#259514=CARTESIAN_POINT('Ctrl Pts',(-3.93835609680327,0.00176884156033657,
4.15416352203497));
#259515=CARTESIAN_POINT('Ctrl Pts',(-3.93892780695442,0.103251996397657,
4.149010505126));
#259516=CARTESIAN_POINT('Ctrl Pts',(-3.88947668791503,1.50247512506948,
4.07793332155035));
#259517=CARTESIAN_POINT('Ctrl Pts',(-2.22189842665676,4.07705916880626,
3.94093197130807));
#259518=CARTESIAN_POINT('Ctrl Pts',(2.20621683484524,4.08556620217308,3.74315947130806));
#259519=CARTESIAN_POINT('Ctrl Pts',(4.62776308396295,0.378223395423315,
3.54538697130807));
#259520=CARTESIAN_POINT('Ctrl Pts',(2.84032772545949,-3.6731162177948,3.34761447130806));
#259521=CARTESIAN_POINT('Ctrl Pts',(-1.53040473322048,-4.38373180256663,
3.14984197130807));
#259522=CARTESIAN_POINT('Ctrl Pts',(-3.75680152222125,-1.93490720171295,
3.00202498821703));
#259523=CARTESIAN_POINT('Ctrl Pts',(-3.93548612495526,-0.319204885198335,
2.92013217179267));
#259524=CARTESIAN_POINT('Ctrl Pts',(-3.93264116285329,-0.00353165188606064,
2.90416352203497));
#259525=CARTESIAN_POINT('',(-3.92706270663355,0.00129905399659486,1.65416352203497));
#259526=CARTESIAN_POINT('Ctrl Pts',(-3.93264116285329,-0.00353165188606064,
2.90416352203497));
#259527=CARTESIAN_POINT('Ctrl Pts',(-3.92374112718673,0.984004538319144,
2.854208005126));
#259528=CARTESIAN_POINT('Ctrl Pts',(-3.04753415908209,3.28882845637856,
2.73832832155037));
#259529=CARTESIAN_POINT('Ctrl Pts',(0.815860814369345,4.57095274380756,
2.55652447130806));
#259530=CARTESIAN_POINT('Ctrl Pts',(4.27656469796981,1.8083818743231,2.35875197130806));
#259531=CARTESIAN_POINT('Ctrl Pts',(3.84770343210594,-2.59892886654929,
2.16097947130807));
#259532=CARTESIAN_POINT('Ctrl Pts',(-0.0806683086839,-4.64248789480798,
1.96320697130806));
#259533=CARTESIAN_POINT('Ctrl Pts',(-3.37364175399093,-2.78134286902773,
1.79426832155037));
#259534=CARTESIAN_POINT('Ctrl Pts',(-3.92487363956869,-0.734550070664457,
1.69125383845933));
#259535=CARTESIAN_POINT('Ctrl Pts',(-3.92706270663355,0.00129905399659486,
1.65416352203497));
#259536=CARTESIAN_POINT('Ctrl Pts',(-3.92706270663355,0.00129905399659486,
1.65416352203497));
#259537=CARTESIAN_POINT('Ctrl Pts',(-3.92876447782353,0.573344954566663,
1.62532967179267));
#259538=CARTESIAN_POINT('Ctrl Pts',(-3.54452519170164,2.45110582699664,
1.5305716548837));
#259539=CARTESIAN_POINT('Ctrl Pts',(-0.656570351814675,4.59650634559706,
1.36988947130806));
#259540=CARTESIAN_POINT('Ctrl Pts',(3.49518900507133,3.0566909045963,1.17211697130807));
#259541=CARTESIAN_POINT('Ctrl Pts',(4.46800855191978,-1.26342377815173,
0.974344471308062));
#259542=CARTESIAN_POINT('Ctrl Pts',(1.37722468627986,-4.43402775821398,
0.776571971308065));
#259543=CARTESIAN_POINT('Ctrl Pts',(-2.79693116634906,-3.60624455861583,
0.586511654883699));
#259544=CARTESIAN_POINT('Ctrl Pts',(-3.92873859619418,-1.14444899111955,
0.462375505126));
#259545=CARTESIAN_POINT('Ctrl Pts',(-3.93722999530371,0.00274405186980325,
0.404163522034968));
#259546=CARTESIAN_POINT('Origin',(0.,0.,-2.31077344927308));
#259547=CARTESIAN_POINT('Ctrl Pts',(-3.22274894448584,-0.00260831658724833,
19.5642265507269));
#259548=CARTESIAN_POINT('Ctrl Pts',(-3.22268270099715,-0.0844565608860859,
19.5693102004846));
#259549=CARTESIAN_POINT('Ctrl Pts',(-3.21949864137641,-0.166205662479208,
19.5743938502423));
#259550=CARTESIAN_POINT('Ctrl Pts',(-3.21321799883013,-0.24768458671075,
19.5794774999999));
#259551=CARTESIAN_POINT('Ctrl Pts',(-3.20537591739532,-0.349420094556691,
19.5858250026785));
#259552=CARTESIAN_POINT('Ctrl Pts',(-3.19268680426057,-0.450926465041492,
19.5921725053571));
#259553=CARTESIAN_POINT('Ctrl Pts',(-3.17517278854975,-0.551720332553758,
19.5985200080356));
#259554=CARTESIAN_POINT('Ctrl Pts',(-3.15768470707801,-0.65236494747302,
19.604858111519));
#259555=CARTESIAN_POINT('Ctrl Pts',(-3.13538601009322,-0.752298763341892,
19.6111962150024));
#259556=CARTESIAN_POINT('Ctrl Pts',(-3.10835063807583,-0.851042815182392,
19.6175343184858));
#259557=CARTESIAN_POINT('Ctrl Pts',(-3.07996430191294,-0.954721131420382,
19.6241891385489));
#259558=CARTESIAN_POINT('Ctrl Pts',(-3.04635564880892,-1.05708724839055,
19.630843958612));
#259559=CARTESIAN_POINT('Ctrl Pts',(-3.00767141738148,-1.15759673788694,
19.637498778675));
#259560=CARTESIAN_POINT('Ctrl Pts',(-2.97091947693275,-1.25308574299826,
19.6438211881331));
#259561=CARTESIAN_POINT('Ctrl Pts',(-2.92958690288105,-1.34689867276782,
19.6501435975912));
#259562=CARTESIAN_POINT('Ctrl Pts',(-2.88385076064012,-1.43858345355958,
19.6564660070493));
#259563=CARTESIAN_POINT('Ctrl Pts',(-2.83814591721452,-1.53020549130214,
19.6627840898651));
#259564=CARTESIAN_POINT('Ctrl Pts',(-2.78804368302485,-1.61970191747214,
19.669102172681));
#259565=CARTESIAN_POINT('Ctrl Pts',(-2.73376870195253,-1.70664180387238,
19.6754202554968));
#259566=CARTESIAN_POINT('Ctrl Pts',(-2.67951945686945,-1.79354046531157,
19.6817353424182));
#259567=CARTESIAN_POINT('Ctrl Pts',(-2.62110161771166,-1.87788465763653,
19.6880504293396));
#259568=CARTESIAN_POINT('Ctrl Pts',(-2.55878480582845,-1.95926973129314,
19.6943655162611));
#259569=CARTESIAN_POINT('Ctrl Pts',(-2.49648445582225,-2.04063330591869,
19.700678934962));
#259570=CARTESIAN_POINT('Ctrl Pts',(-2.43028743041509,-2.11903899800435,
19.7069923536629));
#259571=CARTESIAN_POINT('Ctrl Pts',(-2.3605051650532,-2.19411324417342,
19.7133057723638));
#259572=CARTESIAN_POINT('Ctrl Pts',(-2.29070847910578,-2.26920300452192,
19.7196204957399));
#259573=CARTESIAN_POINT('Ctrl Pts',(-2.21732534519101,-2.34095964406943,
19.7259352191161));
#259574=CARTESIAN_POINT('Ctrl Pts',(-2.14070560633903,-2.40904484588574,
19.7322499424923));
#259575=CARTESIAN_POINT('Ctrl Pts',(-2.06407817695149,-2.47713688160247,
19.7385652996947));
#259576=CARTESIAN_POINT('Ctrl Pts',(-1.98421380250134,-2.54155648191869,
19.7448806568971));
#259577=CARTESIAN_POINT('Ctrl Pts',(-1.9014962663222,-2.60200490231336,
19.7511960140996));
#259578=CARTESIAN_POINT('Ctrl Pts',(-1.81872555031785,-2.66249218552453,
19.7575154315002));
#259579=CARTESIAN_POINT('Ctrl Pts',(-1.73309834020476,-2.71900295700267,
19.7638348489009));
#259580=CARTESIAN_POINT('Ctrl Pts',(-1.6450281803835,-2.77128126473011,
19.7701542663016));
#259581=CARTESIAN_POINT('Ctrl Pts',(-1.61206509949341,-2.79084809746795,
19.7725195108677));
#259582=CARTESIAN_POINT('Ctrl Pts',(-1.57876005794138,-2.80982246879779,
19.7748847554338));
#259583=CARTESIAN_POINT('Ctrl Pts',(-1.54513563095214,-2.82819261091994,
19.77725));
#259584=CARTESIAN_POINT('Origin',(0.,0.,19.5));
#259585=CARTESIAN_POINT('Ctrl Pts',(-3.55851891020094,1.66656297071707,
19.0705612398686));
#259586=CARTESIAN_POINT('Ctrl Pts',(-3.59687330580814,1.55040695638482,
19.0850916788804));
#259587=CARTESIAN_POINT('Ctrl Pts',(-3.6298262220845,1.43277962313427,19.099504081714));
#259588=CARTESIAN_POINT('Ctrl Pts',(-3.65724210796529,1.31411610773058,
19.1138295224127));
#259589=CARTESIAN_POINT('Ctrl Pts',(-3.68417457330094,1.19754496977377,
19.1279023645857));
#259590=CARTESIAN_POINT('Ctrl Pts',(-3.70576340599889,1.07997411133984,
19.1418913836265));
#259591=CARTESIAN_POINT('Ctrl Pts',(-3.72187102178874,0.961821544164156,
19.15585840718));
#259592=CARTESIAN_POINT('Ctrl Pts',(-3.73769233592671,0.845769056577946,
19.1695771766176));
#259593=CARTESIAN_POINT('Ctrl Pts',(-3.74822573132689,0.729155654508635,
19.1832748790167));
#259594=CARTESIAN_POINT('Ctrl Pts',(-3.75333170678875,0.61237871638476,
19.1970397591525));
#259595=CARTESIAN_POINT('Ctrl Pts',(-3.75558091286343,0.560937928904781,
19.203103253239));
#259596=CARTESIAN_POINT('Ctrl Pts',(-3.75677682158521,0.509465397590146,
19.2091801600778));
#259597=CARTESIAN_POINT('Ctrl Pts',(-3.7569066961667,0.457994939495345,
19.2152797608931));
#259598=CARTESIAN_POINT('Ctrl Pts',(-3.75697600074545,0.430528915151644,
19.2185346723643));
#259599=CARTESIAN_POINT('Ctrl Pts',(-3.75674173389767,0.40306347870438,
19.221796063762));
#259600=CARTESIAN_POINT('Ctrl Pts',(-3.75620188182415,0.375603748088969,
19.2250654637997));
#259601=CARTESIAN_POINT('Ctrl Pts',(-3.75585189969696,0.357801806771246,
19.2271849917889));
#259602=CARTESIAN_POINT('Ctrl Pts',(-3.75537348402805,0.340002263203687,
19.2293078873353));
#259603=CARTESIAN_POINT('Ctrl Pts',(-3.75476607182455,0.32220650793041,
19.2314345849014));
#259604=CARTESIAN_POINT('Ctrl Pts',(-3.75432939366825,0.309412860456961,
19.2329635011247));
#259605=CARTESIAN_POINT('Ctrl Pts',(-3.75382607099664,0.296622655712598,
19.2344942061387));
#259606=CARTESIAN_POINT('Ctrl Pts',(-3.75325632212278,0.283843398119468,
19.236026023707));
#259607=CARTESIAN_POINT('Ctrl Pts',(-3.7489693790417,0.187688842255025,
19.2475518292456));
#259608=CARTESIAN_POINT('Ctrl Pts',(-3.74091892861043,0.0920269731287933,
19.2591552753384));
#259609=CARTESIAN_POINT('Ctrl Pts',(-3.72908658133375,-0.00295912595350346,
19.2709122445952));
#259610=CARTESIAN_POINT('Ctrl Pts',(2.28383702403548,-3.20593235360934,
-0.412058650086213));
#259611=CARTESIAN_POINT('Ctrl Pts',(3.3469402646796,-2.44868256130438,-0.34609107865597));
#259612=CARTESIAN_POINT('Ctrl Pts',(4.64210938897443,0.19229506283688,-0.214199340559059));
#259613=CARTESIAN_POINT('Ctrl Pts',(2.36472936830208,4.00381224408868,-0.0163834357954821));
#259614=CARTESIAN_POINT('Ctrl Pts',(-2.06494558101047,4.16156058203527,
0.181389064204519));
#259615=CARTESIAN_POINT('Ctrl Pts',(-4.61545750661852,0.540050558253595,
0.379161564204519));
#259616=CARTESIAN_POINT('Ctrl Pts',(-2.96874505650394,-3.57559009225921,
0.57693406420452));
#259617=CARTESIAN_POINT('Ctrl Pts',(1.37835608349618,-4.43767033499375,
0.774706564204519));
#259618=CARTESIAN_POINT('Ctrl Pts',(4.47167904409764,-1.26446168733233,
0.97247906420452));
#259619=CARTESIAN_POINT('Ctrl Pts',(3.49806032095048,3.05920199201367,1.17025156420451));
#259620=CARTESIAN_POINT('Ctrl Pts',(-0.657109727760937,4.60028239937832,
1.36802406420452));
#259621=CARTESIAN_POINT('Ctrl Pts',(-4.21461215365385,1.95748915205319,
1.56579656420451));
#259622=CARTESIAN_POINT('Ctrl Pts',(-3.93890797286949,-2.46571316296779,
1.76356906420452));
#259623=CARTESIAN_POINT('Ctrl Pts',(-0.0807345781174718,-4.64630172267007,
1.96134156420452));
#259624=CARTESIAN_POINT('Ctrl Pts',(3.85086434041363,-2.60106390008049,
2.15911406420451));
#259625=CARTESIAN_POINT('Ctrl Pts',(4.2800779180295,1.80986746940371,2.35688656420452));
#259626=CARTESIAN_POINT('Ctrl Pts',(0.816531048256037,4.57470780517246,
2.55465906420451));
#259627=CARTESIAN_POINT('Ctrl Pts',(-3.38965584783304,3.17882299039181,
2.75243156420452));
#259628=CARTESIAN_POINT('Ctrl Pts',(-4.51292822741089,-1.10822387779583,
2.95020406420452));
#259629=CARTESIAN_POINT('Ctrl Pts',(-1.53166196863923,-4.38733306095833,
3.14797656420451));
#259630=CARTESIAN_POINT('Ctrl Pts',(2.84266106940413,-3.67613370180096,
3.34574906420452));
#259631=CARTESIAN_POINT('Ctrl Pts',(4.63156481531668,0.378534107902338,
3.54352156420453));
#259632=CARTESIAN_POINT('Ctrl Pts',(2.20802925340745,4.08892251597919,3.74129406420452));
#259633=CARTESIAN_POINT('Ctrl Pts',(-2.22372372772789,4.08040849403945,
3.93906656420452));
#259634=CARTESIAN_POINT('Ctrl Pts',(-4.63298505560038,0.360735531134475,
4.13683906420452));
#259635=CARTESIAN_POINT('Ctrl Pts',(-2.8285153723176,-3.68702880618816,
4.33461156420452));
#259636=CARTESIAN_POINT('Ctrl Pts',(1.54850802827834,-4.38141570036494,
4.53238406420451));
#259637=CARTESIAN_POINT('Ctrl Pts',(4.51715298288247,-1.09087559970398,
4.73015656420452));
#259638=CARTESIAN_POINT('Ctrl Pts',(3.37741697613064,3.1918231799883,4.92792906420452));
#259639=CARTESIAN_POINT('Ctrl Pts',(-0.834102442403632,4.57153735212035,
5.12570156420453));
#259640=CARTESIAN_POINT('Ctrl Pts',(-4.28700009044229,1.79340761385376,
5.32347406420452));
#259641=CARTESIAN_POINT('Ctrl Pts',(-3.84084237808476,-2.61583838787399,
5.52124656420452));
#259642=CARTESIAN_POINT('Ctrl Pts',(0.0985872602042438,-4.64596181617238,
5.71901906420452));
#259643=CARTESIAN_POINT('Ctrl Pts',(3.94835112354715,-2.45055178483769,
5.91679156420453));
#259644=CARTESIAN_POINT('Ctrl Pts',(4.20706313523509,1.97365154501452,6.11456406420452));
#259645=CARTESIAN_POINT('Ctrl Pts',(0.639422983947544,4.60280554582189,
6.31233656420453));
#259646=CARTESIAN_POINT('Ctrl Pts',(-3.50977666360783,3.04567700464268,
6.51010906420451));
#259647=CARTESIAN_POINT('Ctrl Pts',(-4.46681087492398,-1.28151521749841,
6.70788156420452));
#259648=CARTESIAN_POINT('Ctrl Pts',(-1.36125061036072,-4.44316074667783,
6.90565406420451));
#259649=CARTESIAN_POINT('Ctrl Pts',(2.98237622222907,-3.5637217503761,7.10342656420454));
#259650=CARTESIAN_POINT('Ctrl Pts',(4.61351186038695,0.556946100705404,
7.30119906420452));
#259651=CARTESIAN_POINT('Ctrl Pts',(2.04862749160126,4.17106773448699,7.49897156420452));
#259652=CARTESIAN_POINT('Ctrl Pts',(-2.37949733297311,3.99157526390221,
7.69674406420453));
#259653=CARTESIAN_POINT('Ctrl Pts',(-4.64345335994372,0.181718295858487,
7.89451656420453));
#259654=CARTESIAN_POINT('Ctrl Pts',(-2.6841573851303,-3.79341268212052,
8.09228906420453));
#259655=CARTESIAN_POINT('Ctrl Pts',(1.71639774986823,-4.31840936101126,
8.29006156420452));
#259656=CARTESIAN_POINT('Ctrl Pts',(4.55587760940055,-0.915783737126305,
8.48783406420454));
#259657=CARTESIAN_POINT('Ctrl Pts',(3.25175620015281,3.31975334321544,8.68560656420453));
#259658=CARTESIAN_POINT('Ctrl Pts',(-1.0098593017621,4.53595247281834,8.88337906420453));
#259659=CARTESIAN_POINT('Ctrl Pts',(-4.35300098966657,1.62667237911762,
9.08115156420452));
#259660=CARTESIAN_POINT('Ctrl Pts',(-3.73705905632412,-2.76207716303657,
9.27892406420453));
#259661=CARTESIAN_POINT('Ctrl Pts',(0.277763175149986,-4.63869898393428,
9.47669656420453));
#259662=CARTESIAN_POINT('Ctrl Pts',(4.03995793423611,-2.29639293994407,
9.67446906420453));
#259663=CARTESIAN_POINT('Ctrl Pts',(4.12778383240777,2.13449789832069,9.87224156420453));
#259664=CARTESIAN_POINT('Ctrl Pts',(0.461362625713666,4.6240485694483,10.0700140642046));
#259665=CARTESIAN_POINT('Ctrl Pts',(-3.62467098613596,2.9079960260094,10.2677865642046));
#259666=CARTESIAN_POINT('Ctrl Pts',(-4.41404200413699,-1.45289842409465,
10.4655590642046));
#259667=CARTESIAN_POINT('Ctrl Pts',(-1.18881218846961,-4.49237200436122,
10.6633315642046));
#259668=CARTESIAN_POINT('Ctrl Pts',(3.11765029295676,-3.44600308993607,
10.8611040642046));
#259669=CARTESIAN_POINT('Ctrl Pts',(4.58858890454678,0.734528767368906,
11.0588765642046));
#259670=CARTESIAN_POINT('Ctrl Pts',(1.88617510483447,4.24700177995311,11.2566490642046));
#259671=CARTESIAN_POINT('Ctrl Pts',(-2.5317276143798,3.89679816408415,11.4544215642046));
#259672=CARTESIAN_POINT('Ctrl Pts',(-4.64700707314824,0.00243045926715866,
11.6521940642046));
#259673=CARTESIAN_POINT('Ctrl Pts',(-2.53580240411764,-3.8941477645683,
11.8499665642046));
#259674=CARTESIAN_POINT('Ctrl Pts',(1.88173157397906,-4.24897245560811,
12.0477390642046));
#259675=CARTESIAN_POINT('Ctrl Pts',(4.58781805371527,-0.739328175456174,
12.2455115642046));
#259676=CARTESIAN_POINT('Ctrl Pts',(3.12125321615583,3.44274004328707,12.4432840642046));
#259677=CARTESIAN_POINT('Ctrl Pts',(-1.18411237407708,4.4936130819872,12.6410565642046));
#259678=CARTESIAN_POINT('Ctrl Pts',(-4.41251981128717,1.45751485755395,
12.8388290642046));
#259679=CARTESIAN_POINT('Ctrl Pts',(-3.62771085945,-2.90420291391904,13.0366015642046));
#259680=CARTESIAN_POINT('Ctrl Pts',(0.456525471432565,-4.62452863967124,
13.2343740642046));
#259681=CARTESIAN_POINT('Ctrl Pts',(4.12554882142769,-2.13881452369848,
13.4321465642046));
#259682=CARTESIAN_POINT('Ctrl Pts',(4.04235782408847,2.29216575903919,13.6299190642046));
#259683=CARTESIAN_POINT('Ctrl Pts',(0.282615249824077,4.63840589716145,
13.8276915642046));
#259684=CARTESIAN_POINT('Ctrl Pts',(-3.73416779116287,2.76598473430493,
14.0254640642046));
#259685=CARTESIAN_POINT('Ctrl Pts',(-4.35470015938386,-1.62211811119156,
14.2232365642046));
#259686=CARTESIAN_POINT('Ctrl Pts',(-1.01460349953272,-4.53489364724057,
14.4210090642046));
#259687=CARTESIAN_POINT('Ctrl Pts',(3.24828185297365,-3.32315296559463,
14.6187815642046));
#259688=CARTESIAN_POINT('Ctrl Pts',(4.55683305695415,0.911017639724529,
14.8165540642046));
#259689=CARTESIAN_POINT('Ctrl Pts',(1.72091400224631,4.31661159850661,15.0143265642046));
#259690=CARTESIAN_POINT('Ctrl Pts',(-2.68018788222611,3.79621830794186,
15.2120990642046));
#259691=CARTESIAN_POINT('Ctrl Pts',(-4.64364091052774,-0.17686097194712,
15.4098715642046));
#259692=CARTESIAN_POINT('Ctrl Pts',(-2.38367133079787,-3.98908409735304,
15.6076440642046));
#259693=CARTESIAN_POINT('Ctrl Pts',(2.04426327244963,-4.17320829181426,
15.8054165642046));
#259694=CARTESIAN_POINT('Ctrl Pts',(4.61292680830011,-0.561771849014371,
16.0031890642046));
#259695=CARTESIAN_POINT('Ctrl Pts',(2.98610225103185,3.56060047146191,16.2009615642046));
#259696=CARTESIAN_POINT('Ctrl Pts',(-1.35660197535887,4.44458159289761,
16.3987340642046));
#259697=CARTESIAN_POINT('Ctrl Pts',(-4.46546831401767,1.28618815797446,
16.5965065642045));
#259698=CARTESIAN_POINT('Ctrl Pts',(-3.51295987415327,-3.04200632858649,
16.7942790642046));
#259699=CARTESIAN_POINT('Ctrl Pts',(0.634606527243763,-4.60346742421083,
16.9920515642045));
#259700=CARTESIAN_POINT('Ctrl Pts',(4.20499906287745,-1.97805973164798,
17.1898240642046));
#259701=CARTESIAN_POINT('Ctrl Pts',(3.95090708561034,2.44643671224224,17.3875965642045));
#259702=CARTESIAN_POINT('Ctrl Pts',(0.103457054932767,4.6458247907269,17.5853690642046));
#259703=CARTESIAN_POINT('Ctrl Pts',(-3.83812323138877,2.61991467372935,
17.7831415642046));
#259704=CARTESIAN_POINT('Ctrl Pts',(-4.28883691552302,-1.78903737920712,
17.9809140642046));
#259705=CARTESIAN_POINT('Ctrl Pts',(-0.838954441256415,-4.57044187584642,
18.1786865642046));
#259706=CARTESIAN_POINT('Ctrl Pts',(3.37421140880478,-3.19577675801525,
18.3764590642046));
#259707=CARTESIAN_POINT('Ctrl Pts',(4.51803287068356,1.08695978779998,18.5742315642046));
#259708=CARTESIAN_POINT('Ctrl Pts',(1.55358642717095,4.3782366249204,18.7720040642046));
#259709=CARTESIAN_POINT('Ctrl Pts',(-2.82561198434755,3.6930169760152,18.9697765642046));
#259710=CARTESIAN_POINT('Ctrl Pts',(-4.63188723191833,-0.363030295585548,
19.1675926032154));
#259711=CARTESIAN_POINT('Ctrl Pts',(-3.03081717849875,-2.83058498061266,
19.2994844755598));
#259712=CARTESIAN_POINT('Ctrl Pts',(-1.88494306520931,-3.45556123458669,
19.3654521812374));
#259713=CARTESIAN_POINT('Ctrl Pts',(2.14474796587059,-3.01068632383087,
-0.273654916792053));
#259714=CARTESIAN_POINT('Ctrl Pts',(3.14310664422014,-2.29955416570856,
-0.207687345361809));
#259715=CARTESIAN_POINT('Ctrl Pts',(4.35939805011098,0.180584008633708,
-0.075795607264898));
#259716=CARTESIAN_POINT('Ctrl Pts',(2.22071384653295,3.75997414695711,0.122020297498679));
#259717=CARTESIAN_POINT('Ctrl Pts',(-1.93918733600355,3.9081153774257,0.319792797498679));
#259718=CARTESIAN_POINT('Ctrl Pts',(-4.3343693068741,0.507160679195471,
0.51756529749868));
#259719=CARTESIAN_POINT('Ctrl Pts',(-2.78794408450143,-3.35783135856578,
0.715337797498679));
#259720=CARTESIAN_POINT('Ctrl Pts',(1.29441215603915,-4.16740963738492,
0.913110297498681));
#259721=CARTESIAN_POINT('Ctrl Pts',(4.19934716572204,-1.18745409733102,
1.11088279749868));
#259722=CARTESIAN_POINT('Ctrl Pts',(3.28502326518657,2.8728920586308,1.30865529749868));
#259723=CARTESIAN_POINT('Ctrl Pts',(-0.617090771862006,4.32011838614606,
1.50642779749868));
#259724=CARTESIAN_POINT('Ctrl Pts',(-3.95793602973923,1.83827516276157,
1.70420029749868));
#259725=CARTESIAN_POINT('Ctrl Pts',(-3.69902264200789,-2.31554757850064,
1.90197279749868));
#259726=CARTESIAN_POINT('Ctrl Pts',(-0.0758177227054686,-4.3633350644738,
2.09974529749868));
#259727=CARTESIAN_POINT('Ctrl Pts',(3.61634099720126,-2.44265525520715,
2.29751779749868));
#259728=CARTESIAN_POINT('Ctrl Pts',(4.01941483207982,1.69964385928032,2.49529029749868));
#259729=CARTESIAN_POINT('Ctrl Pts',(0.766803097763436,4.29610132261495,
2.69306279749868));
#259730=CARTESIAN_POINT('Ctrl Pts',(-3.18322078507834,2.98522796099457,
2.89083529749868));
#259731=CARTESIAN_POINT('Ctrl Pts',(-4.23808421266269,-1.04073140185459,
3.08860779749868));
#259732=CARTESIAN_POINT('Ctrl Pts',(-1.43838148566121,-4.12013797791067,
3.28638029749868));
#259733=CARTESIAN_POINT('Ctrl Pts',(2.66953879900375,-3.45225171333561,
3.48415279749868));
#259734=CARTESIAN_POINT('Ctrl Pts',(4.3494956566103,0.355480819949967,3.68192529749868));
#259735=CARTESIAN_POINT('Ctrl Pts',(2.07355700077952,3.83990107720247,3.87969779749868));
#259736=CARTESIAN_POINT('Ctrl Pts',(-2.08829565836325,3.83190557181197,
4.07747029749868));
#259737=CARTESIAN_POINT('Ctrl Pts',(-4.35082940215671,0.338766202875003,
4.27524279749868));
#259738=CARTESIAN_POINT('Ctrl Pts',(-2.65625459582596,-3.46248328972505,
4.47301529749868));
#259739=CARTESIAN_POINT('Ctrl Pts',(1.45420159531167,-4.1145809933437,4.67078779749869));
#259740=CARTESIAN_POINT('Ctrl Pts',(4.24205167426729,-1.02443965959917,
4.86856029749868));
#259741=CARTESIAN_POINT('Ctrl Pts',(3.17172727879392,2.99743641978549,5.06633279749868));
#259742=CARTESIAN_POINT('Ctrl Pts',(-0.783304367976271,4.29312395485058,
5.26410529749868));
#259743=CARTESIAN_POINT('Ctrl Pts',(-4.0259154339378,1.68418643331785,5.46187779749868));
#259744=CARTESIAN_POINT('Ctrl Pts',(-3.60692938722528,-2.45652995480633,
5.65965029749867));
#259745=CARTESIAN_POINT('Ctrl Pts',(0.0925831500052695,-4.36301585878538,
5.85742279749869));
#259746=CARTESIAN_POINT('Ctrl Pts',(3.70789069081969,-2.30130955075952,
6.05519529749868));
#259747=CARTESIAN_POINT('Ctrl Pts',(3.95084675772568,1.85345324204774,6.25296779749868));
#259748=CARTESIAN_POINT('Ctrl Pts',(0.600481176948914,4.32248786923329,
6.45074029749868));
#259749=CARTESIAN_POINT('Ctrl Pts',(-3.29602606521889,2.86019076302732,
6.64851279749868));
#259750=CARTESIAN_POINT('Ctrl Pts',(-4.194775475263,-1.20346904224601,6.84628529749869));
#259751=CARTESIAN_POINT('Ctrl Pts',(-1.27834843155858,-4.17256567486365,
7.04405779749867));
#259752=CARTESIAN_POINT('Ctrl Pts',(2.80074509203999,-3.34668581628575,
7.24183029749869));
#259753=CARTESIAN_POINT('Ctrl Pts',(4.33254215338042,0.523027258082037,
7.43960279749867));
#259754=CARTESIAN_POINT('Ctrl Pts',(1.92386304241383,3.91704353020872,7.6373752974987));
#259755=CARTESIAN_POINT('Ctrl Pts',(-2.23458242027749,3.7484824169925,7.83514779749867));
#259756=CARTESIAN_POINT('Ctrl Pts',(-4.36066017125721,0.170651382433251,
8.0329202974987));
#259757=CARTESIAN_POINT('Ctrl Pts',(-2.5206882239182,-3.56238823001025,
8.23069279749867));
#259758=CARTESIAN_POINT('Ctrl Pts',(1.61186658413571,-4.05541183339768,
8.42846529749869));
#259759=CARTESIAN_POINT('Ctrl Pts',(4.27841791366164,-0.860011150843142,
8.62623779749867));
#259760=CARTESIAN_POINT('Ctrl Pts',(3.05371943023388,3.11757544654935,8.82401029749869));
#259761=CARTESIAN_POINT('Ctrl Pts',(-0.948357374223968,4.25970624741547,
9.02178279749868));
#259762=CARTESIAN_POINT('Ctrl Pts',(-4.08789678062198,1.52760562138784,
9.21955529749868));
#259763=CARTESIAN_POINT('Ctrl Pts',(-3.50946662351017,-2.59386257191539,
9.41732779749867));
#259764=CARTESIAN_POINT('Ctrl Pts',(0.260846986289807,-4.35619534379014,
9.61510029749869));
#259765=CARTESIAN_POINT('Ctrl Pts',(3.79391851102637,-2.15653920789927,
9.81287279749867));
#259766=CARTESIAN_POINT('Ctrl Pts',(3.87639568188924,2.00450381415097,10.0106452974987));
#259767=CARTESIAN_POINT('Ctrl Pts',(0.433264958319839,4.34243716125028,
10.2084177974987));
#259768=CARTESIAN_POINT('Ctrl Pts',(-3.40392315329433,2.73089475996095,
10.4061902974987));
#259769=CARTESIAN_POINT('Ctrl Pts',(-4.14522030688164,-1.36441475766407,
10.6039627974987));
#259770=CARTESIAN_POINT('Ctrl Pts',(-1.11641176502036,-4.21877989404988,
10.8017352974987));
#259771=CARTESIAN_POINT('Ctrl Pts',(2.92778077145794,-3.23613639666138,
10.9995077974987));
#259772=CARTESIAN_POINT('Ctrl Pts',(4.30913704247314,0.689794877265052,
11.1972802974987));
#259773=CARTESIAN_POINT('Ctrl Pts',(1.771304246667,3.9883530798131,11.3950527974987));
#259774=CARTESIAN_POINT('Ctrl Pts',(-2.37754165202425,3.65947738296135,
11.5928252974987));
#259775=CARTESIAN_POINT('Ctrl Pts',(-4.3639974580629,0.0022824406971417,
11.7905977974987));
#259776=CARTESIAN_POINT('Ctrl Pts',(-2.38136828103039,-3.65698839670247,
11.9883702974987));
#259777=CARTESIAN_POINT('Ctrl Pts',(1.76713133342362,-3.99020373840124,
12.1861427974987));
#259778=CARTESIAN_POINT('Ctrl Pts',(4.30841313759926,-0.694301994289642,
12.3839152974987));
#259779=CARTESIAN_POINT('Ctrl Pts',(2.93116427129658,3.23307207438738,12.5816877974987));
#259780=CARTESIAN_POINT('Ctrl Pts',(-1.11199817628692,4.21994538820984,
12.7794602974987));
#259781=CARTESIAN_POINT('Ctrl Pts',(-4.14379081783146,1.36875004348661,
12.9772327974987));
#259782=CARTESIAN_POINT('Ctrl Pts',(-3.40677789382007,-2.72733265401625,
13.1750052974987));
#259783=CARTESIAN_POINT('Ctrl Pts',(0.428722393900526,-4.34288799448544,
13.3727777974987));
#259784=CARTESIAN_POINT('Ctrl Pts',(3.87429678638894,-2.00855755064833,
13.5705502974987));
#259785=CARTESIAN_POINT('Ctrl Pts',(3.79617224403135,2.15256946857392,13.7683227974987));
#259786=CARTESIAN_POINT('Ctrl Pts',(0.265403562428066,4.35592010643597,
13.9660952974987));
#259787=CARTESIAN_POINT('Ctrl Pts',(-3.50675144068053,2.59753216630456,
14.1638677974987));
#259788=CARTESIAN_POINT('Ctrl Pts',(-4.08949246838623,-1.52332871512547,
14.3616402974987));
#259789=CARTESIAN_POINT('Ctrl Pts',(-0.952812643321995,-4.25871190588399,
14.5594127974987));
#259790=CARTESIAN_POINT('Ctrl Pts',(3.05045667594506,-3.12076802688922,
14.7571852974987));
#259791=CARTESIAN_POINT('Ctrl Pts',(4.27931517304376,0.855535315833938,
14.9549577974987));
#259792=CARTESIAN_POINT('Ctrl Pts',(1.6161077900533,4.0537235572929,15.1527302974987));
#259793=CARTESIAN_POINT('Ctrl Pts',(-2.51696046962155,3.56502298906262,
15.3505027974987));
#259794=CARTESIAN_POINT('Ctrl Pts',(-4.36083629973281,-0.166089876744038,
15.5482752974987));
#259795=CARTESIAN_POINT('Ctrl Pts',(-2.23850221545109,-3.74614296617676,
15.7460477974987));
#259796=CARTESIAN_POINT('Ctrl Pts',(1.91976461067398,-3.91905372442359,
15.9438202974987));
#259797=CARTESIAN_POINT('Ctrl Pts',(4.3319927318324,-0.52755911116981,16.1415927974987));
#259798=CARTESIAN_POINT('Ctrl Pts',(2.80424420016869,3.34375462788149,16.3393652974987));
#259799=CARTESIAN_POINT('Ctrl Pts',(-1.27398290531514,4.17389998944372,
16.5371377974987));
#259800=CARTESIAN_POINT('Ctrl Pts',(-4.19351467830484,1.20785739372427,
16.7349102974987));
#259801=CARTESIAN_POINT('Ctrl Pts',(-3.2990154135263,-2.85674363658093,
16.9326827974987));
#259802=CARTESIAN_POINT('Ctrl Pts',(0.595958049593802,-4.3231094382478,
17.1304552974987));
#259803=CARTESIAN_POINT('Ctrl Pts',(3.94890839043248,-1.85759296358465,
17.3282277974988));
#259804=CARTESIAN_POINT('Ctrl Pts',(3.71029099100666,2.29744509218147,17.5260002974987));
#259805=CARTESIAN_POINT('Ctrl Pts',(0.0971563670203983,4.36288717839253,
17.7237727974988));
#259806=CARTESIAN_POINT('Ctrl Pts',(-3.60437584059141,2.46035798881423,
17.9215452974987));
#259807=CARTESIAN_POINT('Ctrl Pts',(-4.02764039364993,-1.68008235243554,
18.1193177974987));
#259808=CARTESIAN_POINT('Ctrl Pts',(-0.787860872910852,-4.29209519470465,
18.3170902974987));
#259809=CARTESIAN_POINT('Ctrl Pts',(3.16871693526713,-3.00114921905351,
18.5148627974987));
#259810=CARTESIAN_POINT('Ctrl Pts',(4.24287797559777,1.02076232644127,18.7126352974987));
#259811=CARTESIAN_POINT('Ctrl Pts',(1.45897071218826,4.11159552830341,18.9104077974987));
#259812=CARTESIAN_POINT('Ctrl Pts',(-2.65352802848456,3.46810677113839,
19.1081802974987));
#259813=CARTESIAN_POINT('Ctrl Pts',(-4.34979843756326,-0.340921212771463,
19.3059963365096));
#259814=CARTESIAN_POINT('Ctrl Pts',(-2.84623592230972,-2.65819816190986,
19.4378882088539));
#259815=CARTESIAN_POINT('Ctrl Pts',(-1.77014724008023,-3.24511243614284,
19.5038559145315));
#259816=CARTESIAN_POINT('Ctrl Pts',(2.00565890770568,-2.81544029405241,
-0.135251183497891));
#259817=CARTESIAN_POINT('Ctrl Pts',(2.93927302376069,-2.15042577011275,
-0.0692836120676477));
#259818=CARTESIAN_POINT('Ctrl Pts',(4.07668671124753,0.168872954430536,
0.0626081260292637));
#259819=CARTESIAN_POINT('Ctrl Pts',(2.07669832476383,3.51613604982555,0.26042403079284));
#259820=CARTESIAN_POINT('Ctrl Pts',(-1.81342909099665,3.65467017281614,
0.45819653079284));
#259821=CARTESIAN_POINT('Ctrl Pts',(-4.05328110712969,0.474270800137351,
0.655969030792841));
#259822=CARTESIAN_POINT('Ctrl Pts',(-2.60714311249892,-3.14007262487236,
0.853741530792841));
#259823=CARTESIAN_POINT('Ctrl Pts',(1.21046822858213,-3.89714893977609,
1.05151403079284));
#259824=CARTESIAN_POINT('Ctrl Pts',(3.92701528734643,-1.1104465073297,1.24928653079284));
#259825=CARTESIAN_POINT('Ctrl Pts',(3.07198620942266,2.68658212524793,1.44705903079284));
#259826=CARTESIAN_POINT('Ctrl Pts',(-0.577071815963079,4.03995437291379,
1.64483153079285));
#259827=CARTESIAN_POINT('Ctrl Pts',(-3.70125990582461,1.71906117346994,
1.84260403079284));
#259828=CARTESIAN_POINT('Ctrl Pts',(-3.45913731114628,-2.1653819940335,
2.04037653079284));
#259829=CARTESIAN_POINT('Ctrl Pts',(-0.0709008672934647,-4.08036840627753,
2.23814903079284));
#259830=CARTESIAN_POINT('Ctrl Pts',(3.38181765398889,-2.28424661033382,
2.43592153079284));
#259831=CARTESIAN_POINT('Ctrl Pts',(3.75875174613015,1.58942024915694,2.63369403079284));
#259832=CARTESIAN_POINT('Ctrl Pts',(0.717075147270833,4.01749484005744,
2.83146653079284));
#259833=CARTESIAN_POINT('Ctrl Pts',(-2.97678572232363,2.79163293159735,
3.02923903079284));
#259834=CARTESIAN_POINT('Ctrl Pts',(-3.96324019791451,-0.973238925913344,
3.22701153079285));
#259835=CARTESIAN_POINT('Ctrl Pts',(-1.34510100268319,-3.85294289486299,
3.42478403079284));
#259836=CARTESIAN_POINT('Ctrl Pts',(2.49641652860337,-3.22836972487026,
3.62255653079285));
#259837=CARTESIAN_POINT('Ctrl Pts',(4.06742649790391,0.332427531997598,
3.82032903079284));
#259838=CARTESIAN_POINT('Ctrl Pts',(1.93908474815161,3.59087963842575,4.01810153079285));
#259839=CARTESIAN_POINT('Ctrl Pts',(-1.95286758899861,3.5834026495845,4.21587403079284));
#259840=CARTESIAN_POINT('Ctrl Pts',(-4.06867374871303,0.316796874615529,
4.41364653079285));
#259841=CARTESIAN_POINT('Ctrl Pts',(-2.48399381933433,-3.23793777326195,
4.61141903079284));
#259842=CARTESIAN_POINT('Ctrl Pts',(1.359895162345,-3.84774628632246,4.80919153079285));
#259843=CARTESIAN_POINT('Ctrl Pts',(3.9669503656521,-0.958003719494359,
5.00696403079284));
#259844=CARTESIAN_POINT('Ctrl Pts',(2.96603758145719,2.80304965958268,5.20473653079285));
#259845=CARTESIAN_POINT('Ctrl Pts',(-0.732506293548905,4.01471055758082,
5.40250903079284));
#259846=CARTESIAN_POINT('Ctrl Pts',(-3.76483077743333,1.57496525278195,
5.60028153079285));
#259847=CARTESIAN_POINT('Ctrl Pts',(-3.3730163963658,-2.29722152173868,
5.79805403079284));
#259848=CARTESIAN_POINT('Ctrl Pts',(0.0865790398062952,-4.08006990139837,
5.99582653079285));
#259849=CARTESIAN_POINT('Ctrl Pts',(3.46743025809225,-2.15206731668136,
6.19359903079284));
#259850=CARTESIAN_POINT('Ctrl Pts',(3.69463038021628,1.73325493908096,6.39137153079286));
#259851=CARTESIAN_POINT('Ctrl Pts',(0.561539369950281,4.0421701926447,6.58914403079284));
#259852=CARTESIAN_POINT('Ctrl Pts',(-3.08227546682996,2.67470452141197,
6.78691653079286));
#259853=CARTESIAN_POINT('Ctrl Pts',(-3.92274007560203,-1.1254228669936,
6.98468903079284));
#259854=CARTESIAN_POINT('Ctrl Pts',(-1.19544625275643,-3.90197060304948,
7.18246153079285));
#259855=CARTESIAN_POINT('Ctrl Pts',(2.6191139618509,-3.12964988219538,7.38023403079285));
#259856=CARTESIAN_POINT('Ctrl Pts',(4.05157244637388,0.489108415458669,
7.57800653079284));
#259857=CARTESIAN_POINT('Ctrl Pts',(1.79909859322641,3.66301932593045,7.77577903079285));
#259858=CARTESIAN_POINT('Ctrl Pts',(-2.08966750758188,3.50538957008279,
7.97355153079285));
#259859=CARTESIAN_POINT('Ctrl Pts',(-4.0778669825707,0.159584469008015,
8.17132403079285));
#259860=CARTESIAN_POINT('Ctrl Pts',(-2.35721906270609,-3.33136377789996,
8.36909653079284));
#259861=CARTESIAN_POINT('Ctrl Pts',(1.50733541840319,-3.79241430578413,
8.56686903079285));
#259862=CARTESIAN_POINT('Ctrl Pts',(4.00095821792272,-0.804238564559976,
8.76464153079284));
#259863=CARTESIAN_POINT('Ctrl Pts',(2.85568266031496,2.91539754988326,8.96241403079285));
#259864=CARTESIAN_POINT('Ctrl Pts',(-0.886855446685837,3.98346002201258,
9.16018653079284));
#259865=CARTESIAN_POINT('Ctrl Pts',(-3.82279257157741,1.42853886365807,
9.35795903079284));
#259866=CARTESIAN_POINT('Ctrl Pts',(-3.28187419069619,-2.42564798079422,
9.55573153079285));
#259867=CARTESIAN_POINT('Ctrl Pts',(0.243930797429626,-4.07369170364599,
9.75350403079284));
#259868=CARTESIAN_POINT('Ctrl Pts',(3.54787908781661,-2.01668547585448,
9.95127653079285));
#259869=CARTESIAN_POINT('Ctrl Pts',(3.62500753137072,1.87450972998126,10.1490490307928));
#259870=CARTESIAN_POINT('Ctrl Pts',(0.405167290926007,4.06082575305226,
10.3468215307929));
#259871=CARTESIAN_POINT('Ctrl Pts',(-3.18317532045269,2.55379349391248,
10.5445940307928));
#259872=CARTESIAN_POINT('Ctrl Pts',(-3.87639860962629,-1.27593109123349,
10.7423665307929));
#259873=CARTESIAN_POINT('Ctrl Pts',(-1.04401134157109,-3.94518778373853,
10.9401390307929));
#259874=CARTESIAN_POINT('Ctrl Pts',(2.73791124995913,-3.02626970338668,
11.1379115307928));
#259875=CARTESIAN_POINT('Ctrl Pts',(4.0296851803995,0.645060987161196,11.3356840307929));
#259876=CARTESIAN_POINT('Ctrl Pts',(1.65643338849953,3.7297043796731,11.5334565307928));
#259877=CARTESIAN_POINT('Ctrl Pts',(-2.2233556896687,3.42215660183855,11.7312290307929));
#259878=CARTESIAN_POINT('Ctrl Pts',(-4.08098784297757,0.00213442212713404,
11.9290015307929));
#259879=CARTESIAN_POINT('Ctrl Pts',(-2.22693415794315,-3.41982902883666,
12.1267740307928));
#259880=CARTESIAN_POINT('Ctrl Pts',(1.65253109286818,-3.73143502119435,
12.3245465307929));
#259881=CARTESIAN_POINT('Ctrl Pts',(4.02900822148325,-0.649275813123116,
12.5223190307928));
#259882=CARTESIAN_POINT('Ctrl Pts',(2.74107532643733,3.0234041054877,12.7200915307929));
#259883=CARTESIAN_POINT('Ctrl Pts',(-1.03988397849677,3.94627769443245,
12.9178640307928));
#259884=CARTESIAN_POINT('Ctrl Pts',(-3.87506182437573,1.27998522941927,
13.1156365307929));
#259885=CARTESIAN_POINT('Ctrl Pts',(-3.18584492819014,-2.55046239411347,
13.3134090307928));
#259886=CARTESIAN_POINT('Ctrl Pts',(0.400919316368492,-4.06124734929963,
13.5111815307929));
#259887=CARTESIAN_POINT('Ctrl Pts',(3.6230447513502,-1.87830057759819,13.7089540307929));
#259888=CARTESIAN_POINT('Ctrl Pts',(3.54998666397424,2.01297317810865,13.9067265307929));
#259889=CARTESIAN_POINT('Ctrl Pts',(0.248191875032054,4.07343431571049,
14.1044990307928));
#259890=CARTESIAN_POINT('Ctrl Pts',(-3.27933509019819,2.42907959830422,
14.3022715307929));
#259891=CARTESIAN_POINT('Ctrl Pts',(-3.8242847773886,-1.42453931905938,
14.5000440307929));
#259892=CARTESIAN_POINT('Ctrl Pts',(-0.891021787111275,-3.9825301645274,
14.6978165307929));
#259893=CARTESIAN_POINT('Ctrl Pts',(2.85263149891647,-2.91838308818382,
14.8955890307928));
#259894=CARTESIAN_POINT('Ctrl Pts',(4.00179728913336,0.800052991943351,
15.0933615307929));
#259895=CARTESIAN_POINT('Ctrl Pts',(1.51130157786028,3.79083551607919,15.2911340307928));
#259896=CARTESIAN_POINT('Ctrl Pts',(-2.35373305701698,3.33382767018338,
15.4889065307929));
#259897=CARTESIAN_POINT('Ctrl Pts',(-4.07803168893789,-0.155318781540962,
15.6866790307929));
#259898=CARTESIAN_POINT('Ctrl Pts',(-2.09333310010432,-3.50320183500046,
15.8844515307929));
#259899=CARTESIAN_POINT('Ctrl Pts',(1.79526594889833,-3.66489915703294,
16.0822240307929));
#259900=CARTESIAN_POINT('Ctrl Pts',(4.0510586553647,-0.493346373325246,
16.2799965307929));
#259901=CARTESIAN_POINT('Ctrl Pts',(2.62238614930553,3.12690878430107,16.4777690307929));
#259902=CARTESIAN_POINT('Ctrl Pts',(-1.19136383527139,3.90321838598983,
16.6755415307929));
#259903=CARTESIAN_POINT('Ctrl Pts',(-3.92156104259203,1.12952662947407,
16.8733140307929));
#259904=CARTESIAN_POINT('Ctrl Pts',(-3.08507095289933,-2.67148094457537,
17.0710865307928));
#259905=CARTESIAN_POINT('Ctrl Pts',(0.557309571943842,-4.04275145228477,
17.2688590307928));
#259906=CARTESIAN_POINT('Ctrl Pts',(3.6928177179875,-1.73712619552131,17.4666315307929));
#259907=CARTESIAN_POINT('Ctrl Pts',(3.46967489640299,2.14845347212071,17.6644040307928));
#259908=CARTESIAN_POINT('Ctrl Pts',(0.0908556791080224,4.07994956605816,
17.8621765307929));
#259909=CARTESIAN_POINT('Ctrl Pts',(-3.37062844979403,2.3008013038991,18.0599490307929));
#259910=CARTESIAN_POINT('Ctrl Pts',(-3.76644387177684,-1.57112732566396,
18.2577215307929));
#259911=CARTESIAN_POINT('Ctrl Pts',(-0.736767304565286,-4.01374851356288,
18.4554940307928));
#259912=CARTESIAN_POINT('Ctrl Pts',(2.9632224617295,-2.80652168009177,18.6532665307929));
#259913=CARTESIAN_POINT('Ctrl Pts',(3.96772308051197,0.954564865082551,
18.8510390307928));
#259914=CARTESIAN_POINT('Ctrl Pts',(1.36435499720556,3.84495443168642,19.0488115307929));
#259915=CARTESIAN_POINT('Ctrl Pts',(-2.48144407262158,3.24319656626158,
19.2465840307929));
#259916=CARTESIAN_POINT('Ctrl Pts',(-4.06770964320818,-0.31881212995738,
19.4444000698038));
#259917=CARTESIAN_POINT('Ctrl Pts',(-2.66165466612069,-2.48581134320706,
19.5762919421481));
#259918=CARTESIAN_POINT('Ctrl Pts',(-1.65535141495114,-3.03466363769899,
19.6422596478257));
#259919=CARTESIAN_POINT('Ctrl Pts',(1.86656984954077,-2.62019426427394,
0.00315254979626938));
#259920=CARTESIAN_POINT('Ctrl Pts',(2.73543940330123,-2.00129737451693,
0.0691201212265132));
#259921=CARTESIAN_POINT('Ctrl Pts',(3.79397537238408,0.157161900227365,
0.201011859323424));
#259922=CARTESIAN_POINT('Ctrl Pts',(1.9326828029947,3.27229795269397,0.398827764087002));
#259923=CARTESIAN_POINT('Ctrl Pts',(-1.68767084598974,3.40122496820657,
0.596600264087));
#259924=CARTESIAN_POINT('Ctrl Pts',(-3.77219290738527,0.441380921079229,
0.794372764087002));
#259925=CARTESIAN_POINT('Ctrl Pts',(-2.4263421404964,-2.92231389117894,
0.992145264087002));
#259926=CARTESIAN_POINT('Ctrl Pts',(1.12652430112509,-3.62688824216726,
1.18991776408701));
#259927=CARTESIAN_POINT('Ctrl Pts',(3.65468340897082,-1.0334389173284,1.38769026408701));
#259928=CARTESIAN_POINT('Ctrl Pts',(2.85894915365876,2.50027219186506,1.58546276408701));
#259929=CARTESIAN_POINT('Ctrl Pts',(-0.537052860064148,3.75979035968154,
1.78323526408701));
#259930=CARTESIAN_POINT('Ctrl Pts',(-3.44458378191,1.59984718417832,1.98100776408701));
#259931=CARTESIAN_POINT('Ctrl Pts',(-3.21925198028467,-2.01521640956636,
2.17878026408701));
#259932=CARTESIAN_POINT('Ctrl Pts',(-0.0659840118814633,-3.79740174808127,
2.37655276408701));
#259933=CARTESIAN_POINT('Ctrl Pts',(3.14729431077653,-2.12583796546047,
2.57432526408699));
#259934=CARTESIAN_POINT('Ctrl Pts',(3.49808866018047,1.47919663903355,2.77209776408701));
#259935=CARTESIAN_POINT('Ctrl Pts',(0.667347196778231,3.73888835749994,
2.969870264087));
#259936=CARTESIAN_POINT('Ctrl Pts',(-2.77035065956893,2.59803790220012,
3.167642764087));
#259937=CARTESIAN_POINT('Ctrl Pts',(-3.68839618316631,-0.905746449972094,
3.36541526408701));
#259938=CARTESIAN_POINT('Ctrl Pts',(-1.25182051970517,-3.58574781181533,
3.56318776408701));
#259939=CARTESIAN_POINT('Ctrl Pts',(2.32329425820301,-3.00448773640491,
3.76096026408701));
#259940=CARTESIAN_POINT('Ctrl Pts',(3.78535733919753,0.309374244045226,
3.95873276408701));
#259941=CARTESIAN_POINT('Ctrl Pts',(1.8046124955237,3.34185819964903,4.156505264087));
#259942=CARTESIAN_POINT('Ctrl Pts',(-1.81743951963397,3.33489972735703,
4.354277764087));
#259943=CARTESIAN_POINT('Ctrl Pts',(-3.78651809526935,0.294827546356054,
4.55205026408701));
#259944=CARTESIAN_POINT('Ctrl Pts',(-2.31173304284269,-3.01339225679884,
4.74982276408699));
#259945=CARTESIAN_POINT('Ctrl Pts',(1.26558872937833,-3.58091157930122,
4.94759526408702));
#259946=CARTESIAN_POINT('Ctrl Pts',(3.69184905703692,-0.891567779389545,
5.145367764087));
#259947=CARTESIAN_POINT('Ctrl Pts',(2.76034788412047,2.60866289937987,5.34314026408701));
#259948=CARTESIAN_POINT('Ctrl Pts',(-0.681708219121542,3.73629716031106,
5.54091276408699));
#259949=CARTESIAN_POINT('Ctrl Pts',(-3.50374612092884,1.46574407224603,
5.73868526408701));
#259950=CARTESIAN_POINT('Ctrl Pts',(-3.13910340550632,-2.13791308867103,
5.93645776408699));
#259951=CARTESIAN_POINT('Ctrl Pts',(0.080574929607317,-3.79712394401137,
6.134230264087));
#259952=CARTESIAN_POINT('Ctrl Pts',(3.2269698253648,-2.00282508260319,6.332002764087));
#259953=CARTESIAN_POINT('Ctrl Pts',(3.43841400270688,1.61305663611419,6.52977526408701));
#259954=CARTESIAN_POINT('Ctrl Pts',(0.522597562951646,3.76185251605611,
6.727547764087));
#259955=CARTESIAN_POINT('Ctrl Pts',(-2.86852486844103,2.4892182797966,6.925320264087));
#259956=CARTESIAN_POINT('Ctrl Pts',(-3.65070467594106,-1.04737669174119,
7.12309276408701));
#259957=CARTESIAN_POINT('Ctrl Pts',(-1.11254407395429,-3.63137553123531,
7.320865264087));
#259958=CARTESIAN_POINT('Ctrl Pts',(2.43748283166181,-2.91261394810503,
7.51863776408702));
#259959=CARTESIAN_POINT('Ctrl Pts',(3.77060273936735,0.4551895728353,7.71641026408699));
#259960=CARTESIAN_POINT('Ctrl Pts',(1.67433414403899,3.40899512165219,7.91418276408701));
#259961=CARTESIAN_POINT('Ctrl Pts',(-1.94475259488627,3.26229672317309,
8.11195526408701));
#259962=CARTESIAN_POINT('Ctrl Pts',(-3.79507379388419,0.14851755558278,
8.309727764087));
#259963=CARTESIAN_POINT('Ctrl Pts',(-2.19374990149398,-3.10033932578968,
8.507500264087));
#259964=CARTESIAN_POINT('Ctrl Pts',(1.40280425267068,-3.52941677817056,
8.70527276408699));
#259965=CARTESIAN_POINT('Ctrl Pts',(3.7234985221838,-0.748465978276811,
8.90304526408702));
#259966=CARTESIAN_POINT('Ctrl Pts',(2.65764589039604,2.71321965321718,9.10081776408701));
#259967=CARTESIAN_POINT('Ctrl Pts',(-0.825353519147718,3.7072137966097,
9.29859026408701));
#259968=CARTESIAN_POINT('Ctrl Pts',(-3.55768836253281,1.32947210592829,
9.49636276408701));
#259969=CARTESIAN_POINT('Ctrl Pts',(-3.05428175788224,-2.25743338967303,
9.69413526408699));
#259970=CARTESIAN_POINT('Ctrl Pts',(0.227014608569453,-3.79118806350185,
9.89190776408703));
#259971=CARTESIAN_POINT('Ctrl Pts',(3.30183966460686,-1.87683174380968,
10.089680264087));
#259972=CARTESIAN_POINT('Ctrl Pts',(3.3736193808522,1.74451564581155,10.287452764087));
#259973=CARTESIAN_POINT('Ctrl Pts',(0.377069623532174,3.77921434485424,
10.485225264087));
#259974=CARTESIAN_POINT('Ctrl Pts',(-2.96242748761104,2.37669222786403,
10.682997764087));
#259975=CARTESIAN_POINT('Ctrl Pts',(-3.60757691237093,-1.18744742480291,
10.880770264087));
#259976=CARTESIAN_POINT('Ctrl Pts',(-0.97161091812183,-3.67159567342719,
11.078542764087));
#259977=CARTESIAN_POINT('Ctrl Pts',(2.54804172846031,-2.81640301011199,
11.276315264087));
#259978=CARTESIAN_POINT('Ctrl Pts',(3.75023331832587,0.60032709705734,11.474087764087));
#259979=CARTESIAN_POINT('Ctrl Pts',(1.54156253033206,3.47105567953309,11.671860264087));
#259980=CARTESIAN_POINT('Ctrl Pts',(-2.06916972731314,3.18483582071574,
11.869632764087));
#259981=CARTESIAN_POINT('Ctrl Pts',(-3.79797822789224,0.00198640355712319,
12.067405264087));
#259982=CARTESIAN_POINT('Ctrl Pts',(-2.07250003485589,-3.18266966097084,
12.265177764087));
#259983=CARTESIAN_POINT('Ctrl Pts',(1.53793085231274,-3.47266630398747,
12.462950264087));
#259984=CARTESIAN_POINT('Ctrl Pts',(3.74960330536725,-0.60424963195659,
12.660722764087));
#259985=CARTESIAN_POINT('Ctrl Pts',(2.55098638157809,2.81373613658802,12.858495264087));
#259986=CARTESIAN_POINT('Ctrl Pts',(-0.967769780706639,3.67261000065507,
13.056267764087));
#259987=CARTESIAN_POINT('Ctrl Pts',(-3.60633283092,1.19122041535194,13.254040264087));
#259988=CARTESIAN_POINT('Ctrl Pts',(-2.96491196256021,-2.37359213421067,
13.451812764087));
#259989=CARTESIAN_POINT('Ctrl Pts',(0.373116238836454,-3.77960670411384,
13.649585264087));
#259990=CARTESIAN_POINT('Ctrl Pts',(3.37179271631145,-1.74804360454804,
13.847357764087));
#259991=CARTESIAN_POINT('Ctrl Pts',(3.30380108391712,1.87337688764339,14.045130264087));
#259992=CARTESIAN_POINT('Ctrl Pts',(0.230980187636045,3.790948524985,14.242902764087));
#259993=CARTESIAN_POINT('Ctrl Pts',(-3.05191873971586,2.26062703030387,
14.440675264087));
#259994=CARTESIAN_POINT('Ctrl Pts',(-3.55907708639098,-1.32574992299329,
14.638447764087));
#259995=CARTESIAN_POINT('Ctrl Pts',(-0.829230930900554,-3.70634842317082,
14.836220264087));
#259996=CARTESIAN_POINT('Ctrl Pts',(2.65480632188787,-2.71599814947841,
15.033992764087));
#259997=CARTESIAN_POINT('Ctrl Pts',(3.72427940522297,0.74457066805276,15.231765264087));
#259998=CARTESIAN_POINT('Ctrl Pts',(1.40649536566728,3.52794747486548,15.429537764087));
#259999=CARTESIAN_POINT('Ctrl Pts',(-2.19050564441242,3.10263235130414,
15.627310264087));
#260000=CARTESIAN_POINT('Ctrl Pts',(-3.79522707814296,-0.144547686337884,
15.825082764087));
#260001=CARTESIAN_POINT('Ctrl Pts',(-1.94816398475754,-3.26026070382418,
16.022855264087));
#260002=CARTESIAN_POINT('Ctrl Pts',(1.67076728712268,-3.41074458964229,
16.220627764087));
#260003=CARTESIAN_POINT('Ctrl Pts',(3.77012457889698,-0.459133635480682,
16.418400264087));
#260004=CARTESIAN_POINT('Ctrl Pts',(2.44052809844237,2.91006294072064,16.616172764087));
#260005=CARTESIAN_POINT('Ctrl Pts',(-1.10874476522764,3.63253678253595,
16.813945264087));
#260006=CARTESIAN_POINT('Ctrl Pts',(-3.6496074068792,1.05119586522387,17.011717764087));
#260007=CARTESIAN_POINT('Ctrl Pts',(-2.87112649227236,-2.48621825256981,
17.209490264087));
#260008=CARTESIAN_POINT('Ctrl Pts',(0.51866109429388,-3.76239346632174,
17.407262764087));
#260009=CARTESIAN_POINT('Ctrl Pts',(3.43672704554254,-1.61665942745799,
17.605035264087));
#260010=CARTESIAN_POINT('Ctrl Pts',(3.22905880179933,1.99946185205994,17.802807764087));
#260011=CARTESIAN_POINT('Ctrl Pts',(0.0845549911956499,3.79701195372378,
18.000580264087));
#260012=CARTESIAN_POINT('Ctrl Pts',(-3.13688105899666,2.14124461898399,
18.198352764087));
#260013=CARTESIAN_POINT('Ctrl Pts',(-3.50524734990374,-1.4621722988924,
18.396125264087));
#260014=CARTESIAN_POINT('Ctrl Pts',(-0.685673736219726,-3.73540183242111,
18.593897764087));
#260015=CARTESIAN_POINT('Ctrl Pts',(2.75772798819186,-2.61189414113004,
18.791670264087));
#260016=CARTESIAN_POINT('Ctrl Pts',(3.69256818542617,0.88836740372384,18.989442764087));
#260017=CARTESIAN_POINT('Ctrl Pts',(1.26973928222288,3.57831333506942,19.187215264087));
#260018=CARTESIAN_POINT('Ctrl Pts',(-2.3093601167586,3.01828636138478,19.384987764087));
#260019=CARTESIAN_POINT('Ctrl Pts',(-3.78562084885311,-0.296703047143297,
19.582803803098));
#260020=CARTESIAN_POINT('Ctrl Pts',(-2.47707340993165,-2.31342452450426,
19.7146956754422));
#260021=CARTESIAN_POINT('Ctrl Pts',(-1.54055558982206,-2.82421483925514,
19.7806633811199));
#260022=CARTESIAN_POINT('Ctrl Pts',(1.75279930320746,3.52789804876769,2.86229373536173E-16));
#260023=CARTESIAN_POINT('Ctrl Pts',(1.83447079285969,3.47853779768125,-2.03614959547088E-15));
#260024=CARTESIAN_POINT('Ctrl Pts',(1.9140947383689,3.42607984753856,-1.70822902311683E-16));
#260025=CARTESIAN_POINT('Ctrl Pts',(1.99146917849576,3.3705151092053,8.74300631892311E-16));
#260026=CARTESIAN_POINT('Ctrl Pts',(2.09010694656004,3.29968058344612,2.05149679631144E-15));
#260027=CARTESIAN_POINT('Ctrl Pts',(2.18509043883734,3.22379765720304,-9.10996029650036E-16));
#260028=CARTESIAN_POINT('Ctrl Pts',(2.27623490042508,3.1432744471131,8.11850586757146E-16));
#260029=CARTESIAN_POINT('Ctrl Pts',(2.35348132939542,3.07502970332593,2.2719914056588E-15));
#260030=CARTESIAN_POINT('Ctrl Pts',(2.4279697040414,3.00345097986864,1.81605216791664E-15));
#260031=CARTESIAN_POINT('Ctrl Pts',(2.49956303211591,2.92877198870791,2.2065682614425E-15));
#260032=CARTESIAN_POINT('Ctrl Pts',(2.5242255442793,2.90304652549249,2.34109347720781E-15));
#260033=CARTESIAN_POINT('Ctrl Pts',(2.54854878077249,2.87694774894346,2.37550202059879E-15));
#260034=CARTESIAN_POINT('Ctrl Pts',(2.57249452004371,2.85052138616924,2.06779038336435E-15));
#260035=CARTESIAN_POINT('Ctrl Pts',(2.65366236625338,2.7609450767789,1.02475343365563E-15));
#260036=CARTESIAN_POINT('Ctrl Pts',(2.73057055546618,2.66753281357049,2.79320129631381E-15));
#260037=CARTESIAN_POINT('Ctrl Pts',(2.8030366800126,2.57068789639114,3.66373598126302E-15));
#260038=CARTESIAN_POINT('Ctrl Pts',(2.87558533260316,2.47373268738027,4.53526207461651E-15));
#260039=CARTESIAN_POINT('Ctrl Pts',(2.94368213761813,2.37333611107257,6.88960740750642E-16));
#260040=CARTESIAN_POINT('Ctrl Pts',(3.007096443202,2.26988275097777,4.34374758384592E-15));
#260041=CARTESIAN_POINT('Ctrl Pts',(3.02439282495162,2.24166563509191,5.34059818198255E-15));
#260042=CARTESIAN_POINT('Ctrl Pts',(3.04134056895315,2.21322104129718,6.55777160202515E-15));
#260043=CARTESIAN_POINT('Ctrl Pts',(3.05793432949856,2.18455664797758,5.21804821573824E-15));
#260044=CARTESIAN_POINT('Ctrl Pts',(3.0719333338598,2.16037448830406,3.74557415333203E-15));
#260045=CARTESIAN_POINT('Ctrl Pts',(3.08568039890931,2.13603589347975,7.06947186048359E-15));
#260046=CARTESIAN_POINT('Ctrl Pts',(3.09917214976624,2.11154546334535,6.63358257213531E-15));
#260047=CARTESIAN_POINT('Ctrl Pts',(3.10952920728848,2.09274517594482,6.49618977517167E-15));
#260048=CARTESIAN_POINT('Ctrl Pts',(3.11973673264636,2.07385347610629,4.30040482780213E-15));
#260049=CARTESIAN_POINT('Ctrl Pts',(3.12978288789371,2.05489234507567,4.13558076672871E-15));
#260050=CARTESIAN_POINT('Ctrl Pts',(3.18543717352967,1.94985034877193,4.71724120995002E-15));
#260051=CARTESIAN_POINT('Ctrl Pts',(3.23621623074516,1.84254873547601,4.73048287775305E-15));
#260052=CARTESIAN_POINT('Ctrl Pts',(3.28194760804037,1.7333657774407,4.74620343027254E-15));
#260053=CARTESIAN_POINT('Ctrl Pts',(3.32735401483942,1.62495868145335,4.71586595529493E-15));
#260054=CARTESIAN_POINT('Ctrl Pts',(3.36778445351152,1.51469601660824,5.7165044333348E-15));
#260055=CARTESIAN_POINT('Ctrl Pts',(3.40302049110049,1.40293613231933,6.38378239159465E-15));
#260056=CARTESIAN_POINT('Ctrl Pts',(3.43721763530565,1.29447135759175,7.65246346190412E-15));
#260057=CARTESIAN_POINT('Ctrl Pts',(3.46652217571582,1.18459561281048,5.23326451904315E-15));
#260058=CARTESIAN_POINT('Ctrl Pts',(3.4906860815092,1.07363693774357,5.10702591327572E-15));
#260059=CARTESIAN_POINT('Ctrl Pts',(3.50717437800193,0.997924031535933,
5.33424237539366E-15));
#260060=CARTESIAN_POINT('Ctrl Pts',(3.52126818188651,0.921706923658275,
5.80367298533689E-15));
#260061=CARTESIAN_POINT('Ctrl Pts',(3.53287506570147,0.845092524005051,
7.07767178198537E-15));
#260062=CARTESIAN_POINT('Ctrl Pts',(3.53714290814536,0.816921466909462,
7.04204661411027E-15));
#260063=CARTESIAN_POINT('Ctrl Pts',(3.54107426600386,0.788697812530836,
5.43860166991208E-15));
#260064=CARTESIAN_POINT('Ctrl Pts',(3.54466460187288,0.76042337864298,4.44089209850063E-15));
#260065=CARTESIAN_POINT('Ctrl Pts',(3.54781671197229,0.735600038469682,
3.56496000438575E-15));
#260066=CARTESIAN_POINT('Ctrl Pts',(3.55070529414814,0.710740908665674,
3.35794494782224E-15));
#260067=CARTESIAN_POINT('Ctrl Pts',(3.55332435291955,0.685880474621733,
3.91353616180368E-15));
#260068=CARTESIAN_POINT('Ctrl Pts',(3.56503933400909,0.57468040615398,6.39868106818853E-15));
#260069=CARTESIAN_POINT('Ctrl Pts',(3.57138461782529,0.463318188425493,
1.67998447934304E-15));
#260070=CARTESIAN_POINT('Ctrl Pts',(3.57216496053255,0.352111263492755,
1.99840144432528E-15));
#260071=CARTESIAN_POINT('Ctrl Pts',(3.57263270387297,0.285452988786406,
2.18926298946545E-15));
#260072=CARTESIAN_POINT('Ctrl Pts',(3.57110006250948,0.218850497592311,
5.55435765969798E-15));
#260073=CARTESIAN_POINT('Ctrl Pts',(3.56751601518668,0.152373241746208,
5.10702591327572E-15));
#260074=CARTESIAN_POINT('Ctrl Pts',(3.56141928221821,0.0392904499003424,
4.04931262847179E-15));
#260075=CARTESIAN_POINT('Ctrl Pts',(3.54938889023284,-0.0734312531627452,
3.16088255514917E-15));
#260076=CARTESIAN_POINT('Ctrl Pts',(3.53163824840077,-0.185433964967349,
1.60982338570648E-15));
#260077=CARTESIAN_POINT('Ctrl Pts',(3.51910644172461,-0.264506955387629,
5.14788409583811E-16));
#260078=CARTESIAN_POINT('Ctrl Pts',(3.50372242082101,-0.343221283764593,
9.58919127278865E-16));
#260079=CARTESIAN_POINT('Ctrl Pts',(3.4855479178701,-0.421443262011223,
6.66133814775094E-16));
#260080=CARTESIAN_POINT('Ctrl Pts',(3.47646066639465,-0.460554251134538,
5.19741158523209E-16));
#260081=CARTESIAN_POINT('Ctrl Pts',(3.46667563378722,-0.499542035897557,
2.2271828927908E-15));
#260082=CARTESIAN_POINT('Ctrl Pts',(3.45619963468214,-0.538389119328871,
1.49880108324396E-15));
#260083=CARTESIAN_POINT('Ctrl Pts',(3.44942611035294,-0.563506691610151,
1.02784725264275E-15));
#260084=CARTESIAN_POINT('Ctrl Pts',(3.44236353288121,-0.588566040585249,
-1.81790838627316E-15));
#260085=CARTESIAN_POINT('Ctrl Pts',(3.43501403463685,-0.613560869415645,
-1.88737914186277E-15));
#260086=CARTESIAN_POINT('Ctrl Pts',(3.43099672687466,-0.627223287792596,
-1.92535253765069E-15));
#260087=CARTESIAN_POINT('Ctrl Pts',(3.42689421896722,-0.640864516596422,
-1.22266932942972E-15));
#260088=CARTESIAN_POINT('Ctrl Pts',(3.42270950093411,-0.654475540993858,
-1.22124532708767E-15));
#260089=CARTESIAN_POINT('Ctrl Pts',(3.38999385410531,-0.760884972559132,
-1.58862401117716E-15));
#260090=CARTESIAN_POINT('Ctrl Pts',(3.35221828589833,-0.865585500186228,
3.4290659176697E-16));
#260091=CARTESIAN_POINT('Ctrl Pts',(3.30961957687026,-0.968251586859118,
-9.99200722162641E-16));
#260092=CARTESIAN_POINT('Ctrl Pts',(3.266944521034,-1.07110167507115,-2.34371340498723E-15));
#260093=CARTESIAN_POINT('Ctrl Pts',(3.21942843768939,-1.17191077813822,
-6.00747044203194E-15));
#260094=CARTESIAN_POINT('Ctrl Pts',(3.16726458926213,-1.27032445089415,
-4.38538094726937E-15));
#260095=CARTESIAN_POINT('Ctrl Pts',(3.11601107760244,-1.36702065863472,
-2.79159932763245E-15));
#260096=CARTESIAN_POINT('Ctrl Pts',(3.06026996439313,-1.46140489503514,
-2.78742529000394E-15));
#260097=CARTESIAN_POINT('Ctrl Pts',(3.00019063179608,-1.55310502918845,
-1.72084568816899E-15));
#260098=CARTESIAN_POINT('Ctrl Pts',(2.94705920041998,-1.63420046041805,
-7.77611160214002E-16));
#260099=CARTESIAN_POINT('Ctrl Pts',(2.89053421382684,-1.71319648990997,
-5.06270758738262E-15));
#260100=CARTESIAN_POINT('Ctrl Pts',(2.830702015742,-1.78980623133405,-2.38697950294409E-15));
#260101=CARTESIAN_POINT('Ctrl Pts',(2.82029713655003,-1.80312874212189,
-1.13314336364148E-15));
#260102=CARTESIAN_POINT('Ctrl Pts',(2.80979659776632,-1.81637333173455,
-3.50715845124803E-15));
#260103=CARTESIAN_POINT('Ctrl Pts',(2.79920599239979,-1.82953264244366,
-3.27515792264421E-15));
#260104=CARTESIAN_POINT('Ctrl Pts',(2.73180388711991,-1.9132828356696,-2.89142751403143E-15));
#260105=CARTESIAN_POINT('Ctrl Pts',(2.66069563561445,-1.9936599364221,-1.01197196229115E-15));
#260106=CARTESIAN_POINT('Ctrl Pts',(2.58605721113782,-2.07034386466854,
-1.83186799063151E-15));
#260107=CARTESIAN_POINT('Ctrl Pts',(2.51246520689647,-2.14595269500396,
-2.15041636385202E-15));
#260108=CARTESIAN_POINT('Ctrl Pts',(2.43544073059348,-2.21797169194816,
-2.64088159904353E-15));
#260109=CARTESIAN_POINT('Ctrl Pts',(2.3551241205076,-2.28605318007106,-3.77475828372553E-15));
#260110=CARTESIAN_POINT('Ctrl Pts',(2.27727340703588,-2.3520444167395,-4.19887348472418E-15));
#260111=CARTESIAN_POINT('Ctrl Pts',(2.19632906523751,-2.41433649943972,
-1.81897112986788E-15));
#260112=CARTESIAN_POINT('Ctrl Pts',(2.11240041152739,-2.47256856817298,
-3.60822483003176E-15));
#260113=CARTESIAN_POINT('Ctrl Pts',(2.03466386030107,-2.52650438143806,
-3.18302953207866E-15));
#260114=CARTESIAN_POINT('Ctrl Pts',(1.95436666507115,-2.57695701945168,
-1.65126864917111E-15));
#260115=CARTESIAN_POINT('Ctrl Pts',(1.87158653173908,-2.62360084935054,
-8.32667268468867E-16));
#260116=CARTESIAN_POINT('Ctrl Pts',(-1.43037430634624,2.88158472091696,
-0.413345808225853));
#260117=CARTESIAN_POINT('Ctrl Pts',(-2.38593513615963,2.4072590315855,-0.347374197020977));
#260118=CARTESIAN_POINT('Ctrl Pts',(-3.77197008027487,0.441785045807912,
-0.215430974611227));
#260119=CARTESIAN_POINT('Ctrl Pts',(-2.42248806046208,-2.92946651123822,
-0.0175161409965988));
#260120=CARTESIAN_POINT('Ctrl Pts',(1.13632421357434,-3.62384868015713,
0.180398692618027));
#260121=CARTESIAN_POINT('Ctrl Pts',(3.65866024061303,-1.02244510071097,
0.378313526232654));
#260122=CARTESIAN_POINT('Ctrl Pts',(2.84987228722314,2.5124186827546,0.576228359847282));
#260123=CARTESIAN_POINT('Ctrl Pts',(-0.554751695607484,3.75800204913211,
0.774143193461907));
#260124=CARTESIAN_POINT('Ctrl Pts',(-3.4539307032892,1.58177692684051,0.972058027076536));
#260125=CARTESIAN_POINT('Ctrl Pts',(-3.20771217175408,-2.03531056509857,
1.16997286069116));
#260126=CARTESIAN_POINT('Ctrl Pts',(-0.0401470203663782,-3.79865643127254,
1.36788769430579));
#260127=CARTESIAN_POINT('Ctrl Pts',(3.163947729481,-2.10263059238148,1.56580252792041));
#260128=CARTESIAN_POINT('Ctrl Pts',(3.48663178432909,1.50832114879186,1.76371736153505));
#260129=CARTESIAN_POINT('Ctrl Pts',(0.634008830268578,3.74561072927655,
1.96163219514967));
#260130=CARTESIAN_POINT('Ctrl Pts',(-2.79600544339863,2.57176105983533,
2.1595470287643));
#260131=CARTESIAN_POINT('Ctrl Pts',(-3.67968187030208,-0.944214684454183,
2.35746186237892));
#260132=CARTESIAN_POINT('Ctrl Pts',(-1.21224693115205,-3.60028454405826,
2.55537669599355));
#260133=CARTESIAN_POINT('Ctrl Pts',(2.35918847985848,-2.97755376163462,
2.75329152960818));
#260134=CARTESIAN_POINT('Ctrl Pts',(3.78209600952429,0.356855453303921,
2.9512063632228));
#260135=CARTESIAN_POINT('Ctrl Pts',(1.76062403462141,3.36627360473104,3.14912119683744));
#260136=CARTESIAN_POINT('Ctrl Pts',(-1.86425955536149,3.31000484381239,
3.34703603045206));
#260137=CARTESIAN_POINT('Ctrl Pts',(-3.7913499457688,0.239293105077073,
3.54495086406669));
#260138=CARTESIAN_POINT('Ctrl Pts',(-2.26563336564454,-3.04934434403637,
3.74286569768131));
#260139=CARTESIAN_POINT('Ctrl Pts',(1.32341017753202,-3.560924190624,3.94078053129594));
#260140=CARTESIAN_POINT('Ctrl Pts',(3.70721550972523,-0.829547300363254,
4.13869536491057));
#260141=CARTESIAN_POINT('Ctrl Pts',(2.71483566892025,2.65730367782625,4.33661019852519));
#260142=CARTESIAN_POINT('Ctrl Pts',(-0.749962592571982,3.7241309954383,
4.53452503213983));
#260143=CARTESIAN_POINT('Ctrl Pts',(-3.53176506589602,1.39936809859862,
4.73243986575444));
#260144=CARTESIAN_POINT('Ctrl Pts',(-3.09716622458576,-2.19980838530159,
4.93035469936908));
#260145=CARTESIAN_POINT('Ctrl Pts',(0.158041951713996,-3.79560512941772,
5.1282695329837));
#260146=CARTESIAN_POINT('Ctrl Pts',(3.26932029938714,-1.93471970478396,
5.32618436659833));
#260147=CARTESIAN_POINT('Ctrl Pts',(3.40320748108887,1.68812748234117,5.52409920021295));
#260148=CARTESIAN_POINT('Ctrl Pts',(0.43777157361897,3.77358604057225,5.72201403382758));
#260149=CARTESIAN_POINT('Ctrl Pts',(-2.92634574058982,2.42241535717116,
5.9199288674422));
#260150=CARTESIAN_POINT('Ctrl Pts',(-3.62542104038862,-1.13486467741114,
6.11784370105684));
#260151=CARTESIAN_POINT('Ctrl Pts',(-1.02280192366893,-3.65861610190322,
6.31575853467146));
#260152=CARTESIAN_POINT('Ctrl Pts',(2.51128952770567,-2.85044215240023,
6.5136733682861));
#260153=CARTESIAN_POINT('Ctrl Pts',(3.75833334529226,0.553647922249075,
6.71158820190071));
#260154=CARTESIAN_POINT('Ctrl Pts',(1.58263864965663,3.45352724917065,6.90950303551535));
#260155=CARTESIAN_POINT('Ctrl Pts',(-2.03437531199935,3.20825694826264,
7.10741786912997));
#260156=CARTESIAN_POINT('Ctrl Pts',(-3.79867050418984,0.0412062707186327,
7.30533270274459));
#260157=CARTESIAN_POINT('Ctrl Pts',(-2.10349187136144,-3.16337122438474,
7.50324753635922));
#260158=CARTESIAN_POINT('Ctrl Pts',(1.50735042908147,-3.48704606222752,
7.70116236997385));
#260159=CARTESIAN_POINT('Ctrl Pts',(3.74543893348258,-0.635045472152602,
7.89907720358848));
#260160=CARTESIAN_POINT('Ctrl Pts',(2.57253194898869,2.79529514140836,8.0969920372031));
#260161=CARTESIAN_POINT('Ctrl Pts',(-0.943196538906329,3.67994236981285,
8.29490687081774));
#260162=CARTESIAN_POINT('Ctrl Pts',(-3.59994983150709,1.21324225395456,
8.49282170443235));
#260163=CARTESIAN_POINT('Ctrl Pts',(-2.97820550244154,-2.35836543847123,
8.69073653804698));
#260164=CARTESIAN_POINT('Ctrl Pts',(0.355809861940216,-3.78219445537836,
8.8886513716616));
#260165=CARTESIAN_POINT('Ctrl Pts',(3.36578688114091,-1.7615544916035,9.08656620527623));
#260166=CARTESIAN_POINT('Ctrl Pts',(3.31051999380733,1.86334455395415,9.28448103889086));
#260167=CARTESIAN_POINT('Ctrl Pts',(0.240341112094004,3.79128364884325,
9.48239587250549));
#260168=CARTESIAN_POINT('Ctrl Pts',(-3.04871797664126,2.26647617570826,
9.68031070612012));
#260169=CARTESIAN_POINT('Ctrl Pts',(-3.56128986322979,-1.32242582635301,
9.87822553973474));
#260170=CARTESIAN_POINT('Ctrl Pts',(-0.83057201159013,-3.70698606548661,
10.0761403733494));
#260171=CARTESIAN_POINT('Ctrl Pts',(2.65655314905942,-2.71557009159609,
10.274055206964));
#260172=CARTESIAN_POINT('Ctrl Pts',(3.72433815535594,0.748933148357456,
10.4719700405786));
#260173=CARTESIAN_POINT('Ctrl Pts',(1.40034428802749,3.53137812066868,10.6698848741933));
#260174=CARTESIAN_POINT('Ctrl Pts',(-2.19895218980709,3.0977741723843,10.8677997078079));
#260175=CARTESIAN_POINT('Ctrl Pts',(-3.79564866990161,-0.156992773154816,
11.0657145414225));
#260176=CARTESIAN_POINT('Ctrl Pts',(-1.93562332903015,-3.26878538363457,
11.2636293750371));
#260177=CARTESIAN_POINT('Ctrl Pts',(1.68718671098545,-3.40367397945556,
11.4615442086518));
#260178=CARTESIAN_POINT('Ctrl Pts',(3.7734648885675,-0.43881464298359,11.6594590422664));
#260179=CARTESIAN_POINT('Ctrl Pts',(2.42322415848731,2.92567603023173,11.857373875881));
#260180=CARTESIAN_POINT('Ctrl Pts',(-1.13386250339844,3.62573459860695,
12.0552887094957));
#260181=CARTESIAN_POINT('Ctrl Pts',(-3.65833324154142,1.02381319095868,
12.2532035431103));
#260182=CARTESIAN_POINT('Ctrl Pts',(-2.85113620846061,-2.51050151901093,
12.4511183767249));
#260183=CARTESIAN_POINT('Ctrl Pts',(0.552609031119811,-3.758486239814,12.6490332103395));
#260184=CARTESIAN_POINT('Ctrl Pts',(3.45308964784694,-1.58359320536449,
12.8469480439542));
#260185=CARTESIAN_POINT('Ctrl Pts',(3.20881916310805,2.03348841517158,13.0448628775688));
#260186=CARTESIAN_POINT('Ctrl Pts',(0.0422562890258594,3.79865896892123,
13.2427777111834));
#260187=CARTESIAN_POINT('Ctrl Pts',(-3.1627896610741,2.10436620290518,13.440692544798));
#260188=CARTESIAN_POINT('Ctrl Pts',(-3.48746258741064,-1.5063864901418,
13.6386073784127));
#260189=CARTESIAN_POINT('Ctrl Pts',(-0.636080753601478,-3.74526325254614,
13.8365222120273));
#260190=CARTESIAN_POINT('Ctrl Pts',(2.79458394112346,-2.57330451988858,
14.0344370456419));
#260191=CARTESIAN_POINT('Ctrl Pts',(3.68020294556761,0.94217930161899,14.2323518792566));
#260192=CARTESIAN_POINT('Ctrl Pts',(1.21423729739401,3.59961433217161,14.4302667128712));
#260193=CARTESIAN_POINT('Ctrl Pts',(-2.35754211922225,2.97885728294461,
14.6281815464858));
#260194=CARTESIAN_POINT('Ctrl Pts',(-3.78229266369463,-0.354764383222645,
14.8260963801005));
#260195=CARTESIAN_POINT('Ctrl Pts',(-1.76248478622916,-3.36529982672292,
15.024011213715));
#260196=CARTESIAN_POINT('Ctrl Pts',(1.86242939393929,-3.31103493060374,
15.2219260473297));
#260197=CARTESIAN_POINT('Ctrl Pts',(3.79121707405805,-0.241389077501906,
15.4198408809443));
#260198=CARTESIAN_POINT('Ctrl Pts',(2.26731880001602,3.04809135937923,15.6177557145589));
#260199=CARTESIAN_POINT('Ctrl Pts',(-1.32144135527743,3.56165528174486,
15.8156705481736));
#260200=CARTESIAN_POINT('Ctrl Pts',(-3.70675637139401,0.831596632357296,
16.0135853817882));
#260201=CARTESIAN_POINT('Ctrl Pts',(-2.71630424424639,-2.65580236950805,
16.2115002154028));
#260202=CARTESIAN_POINT('Ctrl Pts',(0.747903527837983,-3.72454512026097,
16.4094150490174));
#260203=CARTESIAN_POINT('Ctrl Pts',(3.53099113340195,-1.40132019993944,
16.6073298826321));
#260204=CARTESIAN_POINT('Ctrl Pts',(3.09838144724328,2.19809550012073,16.8052447162467));
#260205=CARTESIAN_POINT('Ctrl Pts',(-0.155942746811587,3.79569254506809,
17.0031595498613));
#260206=CARTESIAN_POINT('Ctrl Pts',(-3.26825181952199,1.93652560855552,
17.201074383476));
#260207=CARTESIAN_POINT('Ctrl Pts',(-3.40413714935415,-1.68624351756118,
17.3989892170906));
#260208=CARTESIAN_POINT('Ctrl Pts',(-0.439863558166481,-3.77334784211365,
17.5969040507052));
#260209=CARTESIAN_POINT('Ctrl Pts',(2.92501736172631,-2.42402435559258,
17.7948188843198));
#260210=CARTESIAN_POINT('Ctrl Pts',(3.62602629419879,1.1328441110195,17.9927337179345));
#260211=CARTESIAN_POINT('Ctrl Pts',(1.02486574019099,3.65808101165132,18.1906485515491));
#260212=CARTESIAN_POINT('Ctrl Pts',(-2.50979256920917,2.85177081985058,
18.3885633851637));
#260213=CARTESIAN_POINT('Ctrl Pts',(-3.75848698963855,-0.551456610966241,
18.5864782187783));
#260214=CARTESIAN_POINT('Ctrl Pts',(-1.58483866315692,-3.45286925653142,
18.784393052393));
#260215=CARTESIAN_POINT('Ctrl Pts',(2.03315943800767,-3.20896423162532,
18.9823078860076));
#260216=CARTESIAN_POINT('Ctrl Pts',(3.79757377187795,-0.0441069402319698,
19.1802227196223));
#260217=CARTESIAN_POINT('Ctrl Pts',(2.10733370637857,3.16375838102537,19.3781375532368));
#260218=CARTESIAN_POINT('Ctrl Pts',(-1.51055995362578,3.48482947278868,
19.5760959260673));
#260219=CARTESIAN_POINT('Ctrl Pts',(-2.99356127193463,1.58998577181604,
19.7080826876928));
#260220=CARTESIAN_POINT('Ctrl Pts',(-3.17185176654334,0.537454353407991,
19.7740978381135));
#260221=CARTESIAN_POINT('Ctrl Pts',(-1.53694980720768,3.09628819646456,
-0.274955153680968));
#260222=CARTESIAN_POINT('Ctrl Pts',(-2.56370834631237,2.5866210600114,-0.208983542476093));
#260223=CARTESIAN_POINT('Ctrl Pts',(-4.05301511775646,0.474701927998286,
-0.0770403200663413));
#260224=CARTESIAN_POINT('Ctrl Pts',(-2.60298478585014,-3.14773760245323,
0.120874513548287));
#260225=CARTESIAN_POINT('Ctrl Pts',(1.2209903891798,-3.89385736698855,0.318789347162913));
#260226=CARTESIAN_POINT('Ctrl Pts',(3.93126269571537,-1.09862627806308,
0.51670418077754));
#260227=CARTESIAN_POINT('Ctrl Pts',(3.06221290677602,2.69961603263725,0.714619014392168));
#260228=CARTESIAN_POINT('Ctrl Pts',(-0.59608558950558,4.03800634510397,
0.912533848006791));
#260229=CARTESIAN_POINT('Ctrl Pts',(-3.71127900226987,1.69963325820862,
1.11044868162142));
#260230=CARTESIAN_POINT('Ctrl Pts',(-3.44671501863647,-2.18695915241001,
1.30836351523604));
#260231=CARTESIAN_POINT('Ctrl Pts',(-0.0431383274562087,-4.08168983726099,
1.50627834885068));
#260232=CARTESIAN_POINT('Ctrl Pts',(3.39968973943801,-2.25929511544758,
1.7041931824653));
#260233=CARTESIAN_POINT('Ctrl Pts',(3.74641660225106,1.62070437685965,1.90210801607993));
#260234=CARTESIAN_POINT('Ctrl Pts',(0.681248079699113,4.02469176263519,
2.10002284969455));
#260235=CARTESIAN_POINT('Ctrl Pts',(-3.00433250801347,2.76337994017454,
2.29793768330918));
#260236=CARTESIAN_POINT('Ctrl Pts',(-3.95385062221435,-1.01456700585002,
2.49585251692381));
#260237=CARTESIAN_POINT('Ctrl Pts',(-1.3025700188097,-3.86853749492883,
2.69376735053843));
#260238=CARTESIAN_POINT('Ctrl Pts',(2.53496882822741,-3.19940777710475,
2.89168218415307));
#260239=CARTESIAN_POINT('Ctrl Pts',(4.06389551803955,0.383444331824902,
3.08959701776769));
#260240=CARTESIAN_POINT('Ctrl Pts',(1.89180605284284,3.61709067678639,3.28751185138232));
#260241=CARTESIAN_POINT('Ctrl Pts',(-2.00316333388078,3.55662939692278,
3.48542668499694));
#260242=CARTESIAN_POINT('Ctrl Pts',(-4.07383895414842,0.257122551826211,
3.68334151861157));
#260243=CARTESIAN_POINT('Ctrl Pts',(-2.43444303290489,-3.27654739104502,
3.88125635222619));
#260244=CARTESIAN_POINT('Ctrl Pts',(1.42201590743771,-3.82624444802916,
4.07917118584083));
#260245=CARTESIAN_POINT('Ctrl Pts',(3.98343576060461,-0.89135589034721,
4.27708601945545));
#260246=CARTESIAN_POINT('Ctrl Pts',(2.91711486946803,2.85529623764002,4.47500085307008));
#260247=CARTESIAN_POINT('Ctrl Pts',(-0.805841419936308,4.00161159918771,
4.6729156866847));
#260248=CARTESIAN_POINT('Ctrl Pts',(-3.79491271134303,1.50363336352689,
4.87083052029933));
#260249=CARTESIAN_POINT('Ctrl Pts',(-3.32793242345554,-2.36371351098971,
5.06874535391395));
#260250=CARTESIAN_POINT('Ctrl Pts',(0.169817470951354,-4.07841118650735,
5.26666018752859));
#260251=CARTESIAN_POINT('Ctrl Pts',(3.51291349512468,-2.07887338585129,
5.4645750211432));
#260252=CARTESIAN_POINT('Ctrl Pts',(3.65677645266742,1.8139078680418,5.66248985475784));
#260253=CARTESIAN_POINT('Ctrl Pts',(0.470389416734859,4.0547514813478,5.86040468837246));
#260254=CARTESIAN_POINT('Ctrl Pts',(-3.1443843068682,2.60290666552285,6.05831952198709));
#260255=CARTESIAN_POINT('Ctrl Pts',(-3.89554688192456,-1.21942210470022,
6.25623435560171));
#260256=CARTESIAN_POINT('Ctrl Pts',(-1.09900968747838,-3.93121526828241,
6.45414918921635));
#260257=CARTESIAN_POINT('Ctrl Pts',(2.69840274557872,-3.06282523193468,
6.65206402283097));
#260258=CARTESIAN_POINT('Ctrl Pts',(4.03836232574987,0.594899575297352,
6.84997885644559));
#260259=CARTESIAN_POINT('Ctrl Pts',(1.70055918697444,3.71084548726127,7.04789369006024));
#260260=CARTESIAN_POINT('Ctrl Pts',(-2.18595421470653,3.44730038579951,
7.24580852367484));
#260261=CARTESIAN_POINT('Ctrl Pts',(-4.08170495873475,0.0442765013016559,
7.44372335728949));
#260262=CARTESIAN_POINT('Ctrl Pts',(-2.26022056730752,-3.39907027962765,
7.6416381909041));
#260263=CARTESIAN_POINT('Ctrl Pts',(1.61966132996968,-3.74686174750661,
7.83955302451875));
#260264=CARTESIAN_POINT('Ctrl Pts',(4.02450716653944,-0.682361960546052,
8.03746785813335));
#260265=CARTESIAN_POINT('Ctrl Pts',(2.76420826736859,3.00356928226049,8.23538269174799));
#260266=CARTESIAN_POINT('Ctrl Pts',(-1.01347299947942,3.95413053123613,
8.4332975253626));
#260267=CARTESIAN_POINT('Ctrl Pts',(-3.86817784334064,1.30363950193914,
8.63121235897725));
#260268=CARTESIAN_POINT('Ctrl Pts',(-3.20010807834974,-2.53408446299809,
8.82912719259186));
#260269=CARTESIAN_POINT('Ctrl Pts',(0.382320834683111,-4.064001298978,9.0270420262065));
#260270=CARTESIAN_POINT('Ctrl Pts',(3.61656768799618,-1.89280583707616,
9.22495685982112));
#260271=CARTESIAN_POINT('Ctrl Pts',(3.55718293013567,2.00218015679883,9.42287169343575));
#260272=CARTESIAN_POINT('Ctrl Pts',(0.258248644608689,4.0737677175172,9.62078652705038));
#260273=CARTESIAN_POINT('Ctrl Pts',(-3.27587435375479,2.43534863975144,
9.81870136066499));
#260274=CARTESIAN_POINT('Ctrl Pts',(-3.82663736646909,-1.42095821341447,
10.0166161942796));
#260275=CARTESIAN_POINT('Ctrl Pts',(-0.892456951597825,-3.98318922074665,
10.2145310278942));
#260276=CARTESIAN_POINT('Ctrl Pts',(2.85448978786086,-2.91790401311039,
10.4124458615089));
#260277=CARTESIAN_POINT('Ctrl Pts',(4.00183419434623,0.804735273048721,
10.6103606951235));
#260278=CARTESIAN_POINT('Ctrl Pts',(1.5046822876776,3.79449693528363,10.8082755287381));
#260279=CARTESIAN_POINT('Ctrl Pts',(-2.36279352137976,3.3285856687268,11.0061903623527));
#260280=CARTESIAN_POINT('Ctrl Pts',(-4.07845797114128,-0.168690119336393,
11.2041051959674));
#260281=CARTESIAN_POINT('Ctrl Pts',(-2.07984433807326,-3.5123387234309,
11.402020029582));
#260282=CARTESIAN_POINT('Ctrl Pts',(1.81289700092304,-3.65727770927665,
11.5999348631966));
#260283=CARTESIAN_POINT('Ctrl Pts',(4.0546213024502,-0.471510203966385,
11.7978496968113));
#260284=CARTESIAN_POINT('Ctrl Pts',(2.60377572967019,3.143664697182,11.9957645304259));
#260285=CARTESIAN_POINT('Ctrl Pts',(-1.21834525988501,3.89588380299556,
12.1936793640405));
#260286=CARTESIAN_POINT('Ctrl Pts',(-3.93091133232899,1.10009630309998,
12.3915941976551));
#260287=CARTESIAN_POINT('Ctrl Pts',(-3.06357100129271,-2.69755602328645,
12.5895090312698));
#260288=CARTESIAN_POINT('Ctrl Pts',(0.593783277616569,-4.03852661226194,
12.7874238648844));
#260289=CARTESIAN_POINT('Ctrl Pts',(3.71037528077956,-1.70158486550113,
12.985338698499));
#260290=CARTESIAN_POINT('Ctrl Pts',(3.4479044906093,2.1850012362432,13.1832535321136));
#260291=CARTESIAN_POINT('Ctrl Pts',(0.0454047552332988,4.08169256398689,
13.3811683657283));
#260292=CARTESIAN_POINT('Ctrl Pts',(-3.39844538472134,2.26116004426235,
13.5790831993429));
#260293=CARTESIAN_POINT('Ctrl Pts',(-3.74730930748937,-1.61862556907763,
13.7769980329575));
#260294=CARTESIAN_POINT('Ctrl Pts',(-0.683474379593425,-4.02431839582384,
13.9749128665721));
#260295=CARTESIAN_POINT('Ctrl Pts',(3.00280509128201,-2.76503840161413,
14.1728277001868));
#260296=CARTESIAN_POINT('Ctrl Pts',(3.95441052218274,1.01237996904276,14.3707425338014));
#260297=CARTESIAN_POINT('Ctrl Pts',(1.30470868489051,3.86781734634577,14.568657367416));
#260298=CARTESIAN_POINT('Ctrl Pts',(-2.53319979920386,3.2008084222486,14.7665722010306));
#260299=CARTESIAN_POINT('Ctrl Pts',(-4.06410682467997,-0.381197458580596,
14.9644870346453));
#260300=CARTESIAN_POINT('Ctrl Pts',(-1.89380544685607,-3.61604434372852,
15.1624018682599));
#260301=CARTESIAN_POINT('Ctrl Pts',(2.00119680929171,-3.55773623426484,
15.3603167018745));
#260302=CARTESIAN_POINT('Ctrl Pts',(4.07369618232338,-0.259374692681903,
15.5582315354892));
#260303=CARTESIAN_POINT('Ctrl Pts',(2.43625404700157,3.27520104798036,15.7561463691038));
#260304=CARTESIAN_POINT('Ctrl Pts',(-1.41990039056132,3.8270300118863,15.9540612027184));
#260305=CARTESIAN_POINT('Ctrl Pts',(-3.98294241241839,0.893557915648685,
16.1519760363331));
#260306=CARTESIAN_POINT('Ctrl Pts',(-2.91869286660792,-2.85368306861148,
16.3498908699477));
#260307=CARTESIAN_POINT('Ctrl Pts',(0.803628936719916,-4.00205657996199,
16.5478057035623));
#260308=CARTESIAN_POINT('Ctrl Pts',(3.79408111405252,-1.50573091363394,
16.7457205371769));
#260309=CARTESIAN_POINT('Ctrl Pts',(3.32923819091856,2.36187300075628,16.9436353707915));
#260310=CARTESIAN_POINT('Ctrl Pts',(-0.167561856769994,4.07850511539461,
17.1415502044062));
#260311=CARTESIAN_POINT('Ctrl Pts',(-3.51176540408623,2.08081384538083,
17.3394650380208));
#260312=CARTESIAN_POINT('Ctrl Pts',(-3.65777538941758,-1.81188353127027,
17.5373798716354));
#260313=CARTESIAN_POINT('Ctrl Pts',(-0.472637272581203,-4.05449553500327,
17.7352947052501));
#260314=CARTESIAN_POINT('Ctrl Pts',(3.14295695206386,-2.60463554851707,
17.9332095388647));
#260315=CARTESIAN_POINT('Ctrl Pts',(3.89619723248157,1.21725098829224,18.1311243724793));
#260316=CARTESIAN_POINT('Ctrl Pts',(1.10122727653295,3.93064030908756,18.3290392060939));
#260317=CARTESIAN_POINT('Ctrl Pts',(-2.69679425047197,3.06425289682812,
18.5269540397085));
#260318=CARTESIAN_POINT('Ctrl Pts',(-4.03852741795501,-0.592544991997906,
18.7248688733232));
#260319=CARTESIAN_POINT('Ctrl Pts',(-1.70292312088329,-3.71013846836731,
18.9227837069378));
#260320=CARTESIAN_POINT('Ctrl Pts',(2.1846477473792,-3.44806036801054,19.1206985405524));
#260321=CARTESIAN_POINT('Ctrl Pts',(4.08052651019308,-0.0473932962758928,
19.3186133741671));
#260322=CARTESIAN_POINT('Ctrl Pts',(2.26434865291609,3.3994862828525,19.5165282077817));
#260323=CARTESIAN_POINT('Ctrl Pts',(-1.6231099923986,3.74448000260561,19.7144865806121));
#260324=CARTESIAN_POINT('Ctrl Pts',(-3.21660798809866,1.7084537345319,19.8464733422378));
#260325=CARTESIAN_POINT('Ctrl Pts',(-3.40818269697037,0.577499442760154,
19.9124884926585));
#260326=CARTESIAN_POINT('Ctrl Pts',(-1.64352530806914,3.31099167201216,
-0.136564499136082));
#260327=CARTESIAN_POINT('Ctrl Pts',(-2.74148155646512,2.76598308843731,
-0.0705928879312071));
#260328=CARTESIAN_POINT('Ctrl Pts',(-4.33406015523805,0.507618810188653,
0.0613503344785438));
#260329=CARTESIAN_POINT('Ctrl Pts',(-2.78348151123821,-3.36600869366824,
0.259265168093171));
#260330=CARTESIAN_POINT('Ctrl Pts',(1.30565656478528,-4.16386605381997,
0.457180001707797));
#260331=CARTESIAN_POINT('Ctrl Pts',(4.20386515081771,-1.1748074554152,0.655094835322425));
#260332=CARTESIAN_POINT('Ctrl Pts',(3.27455352632889,2.88681338251992,0.853009668937051));
#260333=CARTESIAN_POINT('Ctrl Pts',(-0.637419483403673,4.31801064107583,
1.05092450255168));
#260334=CARTESIAN_POINT('Ctrl Pts',(-3.96862730125054,1.81748958957675,
1.24883933616631));
#260335=CARTESIAN_POINT('Ctrl Pts',(-3.68571786551885,-2.33860773972145,
1.44675416978093));
#260336=CARTESIAN_POINT('Ctrl Pts',(-0.0461296345460419,-4.36472324324944,
1.64466900339556));
#260337=CARTESIAN_POINT('Ctrl Pts',(3.63543174939503,-2.41595963851369,
1.84258383701018));
#260338=CARTESIAN_POINT('Ctrl Pts',(4.00620142017303,1.73308760492743,2.04049867062481));
#260339=CARTESIAN_POINT('Ctrl Pts',(0.728487329129644,4.30377279599383,
2.23841350423944));
#260340=CARTESIAN_POINT('Ctrl Pts',(-3.21265957262829,2.95499882051374,
2.43632833785407));
#260341=CARTESIAN_POINT('Ctrl Pts',(-4.22801937412663,-1.08491932724587,
2.63424317146869));
#260342=CARTESIAN_POINT('Ctrl Pts',(-1.39289310646734,-4.13679044579939,
2.83215800508332));
#260343=CARTESIAN_POINT('Ctrl Pts',(2.71074917659634,-3.42126179257488,
3.03007283869794));
#260344=CARTESIAN_POINT('Ctrl Pts',(4.34569502655482,0.410033210345885,
3.22798767231258));
#260345=CARTESIAN_POINT('Ctrl Pts',(2.02298807106426,3.86790774884172,3.4259025059272));
#260346=CARTESIAN_POINT('Ctrl Pts',(-2.14206711240008,3.80325395003319,
3.62381733954183));
#260347=CARTESIAN_POINT('Ctrl Pts',(-4.35632796252803,0.274951998575345,
3.82173217315645));
#260348=CARTESIAN_POINT('Ctrl Pts',(-2.60325270016525,-3.50375043805368,
4.01964700677108));
#260349=CARTESIAN_POINT('Ctrl Pts',(1.52062163734339,-4.09156470543431,
4.2175618403857));
#260350=CARTESIAN_POINT('Ctrl Pts',(4.259656011484,-0.953164480331169,4.41547667400034));
#260351=CARTESIAN_POINT('Ctrl Pts',(3.11939407001581,3.0532887974538,4.61339150761496));
#260352=CARTESIAN_POINT('Ctrl Pts',(-0.861720247300632,4.27909220293711,
4.81130634122959));
#260353=CARTESIAN_POINT('Ctrl Pts',(-4.05806035679004,1.60789862845514,
5.00922117484421));
#260354=CARTESIAN_POINT('Ctrl Pts',(-3.5586986223253,-2.52761863667785,
5.20713600845884));
#260355=CARTESIAN_POINT('Ctrl Pts',(0.181592990188709,-4.36121724359697,
5.40505084207346));
#260356=CARTESIAN_POINT('Ctrl Pts',(3.75650669086223,-2.22302706691864,
5.6029656756881));
#260357=CARTESIAN_POINT('Ctrl Pts',(3.91034542424596,1.93968825374242,5.80088050930272));
#260358=CARTESIAN_POINT('Ctrl Pts',(0.503007259850752,4.33591692212334,
5.99879534291735));
#260359=CARTESIAN_POINT('Ctrl Pts',(-3.3624228731466,2.78339797387454,6.19671017653197));
#260360=CARTESIAN_POINT('Ctrl Pts',(-4.1656727234605,-1.30397953198931,
6.39462501014661));
#260361=CARTESIAN_POINT('Ctrl Pts',(-1.17521745128784,-4.20381443466159,
6.59253984376122));
#260362=CARTESIAN_POINT('Ctrl Pts',(2.88551596345178,-3.2752083114691,6.79045467737586));
#260363=CARTESIAN_POINT('Ctrl Pts',(4.3183913062075,0.636151228345629,6.98836951099048));
#260364=CARTESIAN_POINT('Ctrl Pts',(1.81847972429224,3.96816372535188,7.18628434460512));
#260365=CARTESIAN_POINT('Ctrl Pts',(-2.33753311741372,3.68634382333638,
7.38419917821973));
#260366=CARTESIAN_POINT('Ctrl Pts',(-4.36473941327965,0.0473467318846832,
7.58211401183438));
#260367=CARTESIAN_POINT('Ctrl Pts',(-2.4169492632536,-3.63476933487058,
7.78002884544898));
#260368=CARTESIAN_POINT('Ctrl Pts',(1.73197223085787,-4.0066774327857,7.97794367906362));
#260369=CARTESIAN_POINT('Ctrl Pts',(4.3035753995963,-0.729678448939505,
8.17585851267824));
#260370=CARTESIAN_POINT('Ctrl Pts',(2.95588458574849,3.21184342311262,8.37377334629287));
#260371=CARTESIAN_POINT('Ctrl Pts',(-1.08374946005252,4.22831869265942,
8.5716881799075));
#260372=CARTESIAN_POINT('Ctrl Pts',(-4.13640585517419,1.39403674992373,
8.76960301352212));
#260373=CARTESIAN_POINT('Ctrl Pts',(-3.42201065425794,-2.70980348752494,
8.96751784713675));
#260374=CARTESIAN_POINT('Ctrl Pts',(0.40883180742601,-4.34580814257763,
9.16543268075137));
#260375=CARTESIAN_POINT('Ctrl Pts',(3.86734849485145,-2.02405718254882,
9.36334751436601));
#260376=CARTESIAN_POINT('Ctrl Pts',(3.803845866464,2.14101575964352,9.56126234798063));
#260377=CARTESIAN_POINT('Ctrl Pts',(0.276156177123374,4.35625178619118,
9.75917718159526));
#260378=CARTESIAN_POINT('Ctrl Pts',(-3.50303073086834,2.60422110379462,
9.95709201520989));
#260379=CARTESIAN_POINT('Ctrl Pts',(-4.0919848697084,-1.51949060047594,
10.1550068488245));
#260380=CARTESIAN_POINT('Ctrl Pts',(-0.954341891605521,-4.2593923760067,
10.3529216824392));
#260381=CARTESIAN_POINT('Ctrl Pts',(3.05242642666228,-3.12023793462469,
10.5508365160538));
#260382=CARTESIAN_POINT('Ctrl Pts',(4.27933023333652,0.860537397739989,
10.7487513496684));
#260383=CARTESIAN_POINT('Ctrl Pts',(1.60902028732771,4.05761574989858,10.9466661832831));
#260384=CARTESIAN_POINT('Ctrl Pts',(-2.52663485295242,3.55939716506929,
11.1445810168977));
#260385=CARTESIAN_POINT('Ctrl Pts',(-4.36126727238094,-0.18038746551797,
11.3424958505123));
#260386=CARTESIAN_POINT('Ctrl Pts',(-2.22406534711636,-3.75589206322724,
11.5404106841269));
#260387=CARTESIAN_POINT('Ctrl Pts',(1.93860729086062,-3.91088143909774,
11.7383255177416));
#260388=CARTESIAN_POINT('Ctrl Pts',(4.33577771633291,-0.504205764949182,
11.9362403513562));
#260389=CARTESIAN_POINT('Ctrl Pts',(2.78432730085307,3.36165336413227,12.1341551849708));
#260390=CARTESIAN_POINT('Ctrl Pts',(-1.30282801637157,4.16603300738415,
12.3320700185855));
#260391=CARTESIAN_POINT('Ctrl Pts',(-4.20348942311656,1.17637941524129,
12.5299848522001));
#260392=CARTESIAN_POINT('Ctrl Pts',(-3.27600579412479,-2.88461052756198,
12.7278996858147));
#260393=CARTESIAN_POINT('Ctrl Pts',(0.634957524113322,-4.31856698470986,
12.9258145194293));
#260394=CARTESIAN_POINT('Ctrl Pts',(3.96766091371217,-1.81957652563777,
13.123729353044));
#260395=CARTESIAN_POINT('Ctrl Pts',(3.68698981811055,2.33651405731482,13.3216441866586));
#260396=CARTESIAN_POINT('Ctrl Pts',(0.0485532214407396,4.36472615905254,
13.5195590202732));
#260397=CARTESIAN_POINT('Ctrl Pts',(-3.63410110836858,2.41795388561951,
13.7174738538878));
#260398=CARTESIAN_POINT('Ctrl Pts',(-4.0071560275681,-1.73086464801346,
13.9153886875025));
#260399=CARTESIAN_POINT('Ctrl Pts',(-0.730868005585374,-4.30337353910152,
14.1133035211171));
#260400=CARTESIAN_POINT('Ctrl Pts',(3.21102624144054,-2.95677228333969,
14.3112183547317));
#260401=CARTESIAN_POINT('Ctrl Pts',(4.22861809879787,1.08258063646653,14.5091331883463));
#260402=CARTESIAN_POINT('Ctrl Pts',(1.39518007238701,4.13602036051992,14.707048021961));
#260403=CARTESIAN_POINT('Ctrl Pts',(-2.70885747918549,3.42275956155259,
14.9049628555756));
#260404=CARTESIAN_POINT('Ctrl Pts',(-4.3459209856653,-0.407630533938537,
15.1028776891902));
#260405=CARTESIAN_POINT('Ctrl Pts',(-2.02512610748298,-3.86678886073412,
15.3007925228048));
#260406=CARTESIAN_POINT('Ctrl Pts',(2.13996422464412,-3.80443753792594,
15.4987073564195));
#260407=CARTESIAN_POINT('Ctrl Pts',(4.35617529058869,-0.277360307861903,
15.6966221900341));
#260408=CARTESIAN_POINT('Ctrl Pts',(2.60518929398711,3.50231073658149,15.8945370236487));
#260409=CARTESIAN_POINT('Ctrl Pts',(-1.51835942584521,4.09240474202774,
16.0924518572633));
#260410=CARTESIAN_POINT('Ctrl Pts',(-4.25912845344279,0.955519198940071,
16.290366690878));
#260411=CARTESIAN_POINT('Ctrl Pts',(-3.12108148896944,-3.05156376771492,
16.4882815244926));
#260412=CARTESIAN_POINT('Ctrl Pts',(0.859354345601846,-4.279568039663,16.6861963581073));
#260413=CARTESIAN_POINT('Ctrl Pts',(4.05717109470311,-1.61014162732844,
16.8841111917219));
#260414=CARTESIAN_POINT('Ctrl Pts',(3.56009493459384,2.52565050139181,17.0820260253365));
#260415=CARTESIAN_POINT('Ctrl Pts',(-0.1791809667284,4.36131768572114,17.2799408589511));
#260416=CARTESIAN_POINT('Ctrl Pts',(-3.75527898865047,2.22510208220613,
17.4778556925657));
#260417=CARTESIAN_POINT('Ctrl Pts',(-3.91141362948099,-1.93752354497935,
17.6757705261804));
#260418=CARTESIAN_POINT('Ctrl Pts',(-0.505410986995922,-4.33564322789287,
17.873685359795));
#260419=CARTESIAN_POINT('Ctrl Pts',(3.36089654240142,-2.78524674144156,
18.0716001934096));
#260420=CARTESIAN_POINT('Ctrl Pts',(4.16636817076433,1.30165786556497,18.2695150270243));
#260421=CARTESIAN_POINT('Ctrl Pts',(1.17758881287491,4.20319960652379,18.4674298606389));
#260422=CARTESIAN_POINT('Ctrl Pts',(-2.88379593173475,3.27673497380564,
18.6653446942535));
#260423=CARTESIAN_POINT('Ctrl Pts',(-4.31856784627148,-0.633633373029566,
18.8632595278681));
#260424=CARTESIAN_POINT('Ctrl Pts',(-1.82100757860965,-3.9674076802032,
19.0611743614828));
#260425=CARTESIAN_POINT('Ctrl Pts',(2.33613605675073,-3.68715650439574,
19.2590891950974));
#260426=CARTESIAN_POINT('Ctrl Pts',(4.36347924850822,-0.050679652319815,
19.457004028712));
#260427=CARTESIAN_POINT('Ctrl Pts',(2.42136359945361,3.63521418467965,19.6549188623266));
#260428=CARTESIAN_POINT('Ctrl Pts',(-1.73566003117141,4.00413053242251,
19.8528772351571));
#260429=CARTESIAN_POINT('Ctrl Pts',(-3.4396547042627,1.82692169724777,19.9848639967826));
#260430=CARTESIAN_POINT('Ctrl Pts',(-3.64451362739738,0.617544532112318,
20.0508791472033));
#260431=CARTESIAN_POINT('Ctrl Pts',(-1.75010080893059,3.52569514755975,
0.00182615540880226));
#260432=CARTESIAN_POINT('Ctrl Pts',(-2.91925476661787,2.94534511686322,
0.0677977666136779));
#260433=CARTESIAN_POINT('Ctrl Pts',(-4.61510519271965,0.540535692379026,
0.199740989023429));
#260434=CARTESIAN_POINT('Ctrl Pts',(-2.96397823662627,-3.58427978488325,
0.397655822638056));
#260435=CARTESIAN_POINT('Ctrl Pts',(1.39032274039075,-4.43387474065139,
0.595570656252683));
#260436=CARTESIAN_POINT('Ctrl Pts',(4.47646760592004,-1.25098863276732,
0.79348548986731));
#260437=CARTESIAN_POINT('Ctrl Pts',(3.48689414588177,3.07401073240257,0.991400323481937));
#260438=CARTESIAN_POINT('Ctrl Pts',(-0.678753377301771,4.59801493704769,
1.18931515709656));
#260439=CARTESIAN_POINT('Ctrl Pts',(-4.2259756002312,1.93534592094488,1.38722999071119));
#260440=CARTESIAN_POINT('Ctrl Pts',(-3.92472071240123,-2.4902563270329,
1.58514482432581));
#260441=CARTESIAN_POINT('Ctrl Pts',(-0.0491209416358709,-4.64775664923788,
1.78305965794044));
#260442=CARTESIAN_POINT('Ctrl Pts',(3.87117375935205,-2.57262416157981,
1.98097449155507));
#260443=CARTESIAN_POINT('Ctrl Pts',(4.26598623809502,1.84547083299521,2.17888932516969));
#260444=CARTESIAN_POINT('Ctrl Pts',(0.775726578560172,4.58285382935247,
2.37680415878432));
#260445=CARTESIAN_POINT('Ctrl Pts',(-3.42098663724313,3.14661770085293,
2.57471899239895));
#260446=CARTESIAN_POINT('Ctrl Pts',(-4.50218812603891,-1.1552716486417,
2.77263382601358));
#260447=CARTESIAN_POINT('Ctrl Pts',(-1.48321619412499,-4.40504339666996,
2.9705486596282));
#260448=CARTESIAN_POINT('Ctrl Pts',(2.88652952496526,-3.643115808045,3.16846349324284));
#260449=CARTESIAN_POINT('Ctrl Pts',(4.6274945350701,0.436622088866865,3.36637832685745));
#260450=CARTESIAN_POINT('Ctrl Pts',(2.15417008928569,4.11872482089706,3.56429316047209));
#260451=CARTESIAN_POINT('Ctrl Pts',(-2.28097089091936,4.04987850314359,
3.76220799408671));
#260452=CARTESIAN_POINT('Ctrl Pts',(-4.63881697090765,0.292781445324475,
3.96012282770134));
#260453=CARTESIAN_POINT('Ctrl Pts',(-2.77206236742561,-3.73095348506232,
4.15803766131596));
#260454=CARTESIAN_POINT('Ctrl Pts',(1.61922736724908,-4.35688496283948,
4.35595249493059));
#260455=CARTESIAN_POINT('Ctrl Pts',(4.53587626236338,-1.01497307031512,
4.55386732854522));
#260456=CARTESIAN_POINT('Ctrl Pts',(3.32167327056359,3.25128135726756,4.75178216215984));
#260457=CARTESIAN_POINT('Ctrl Pts',(-0.917599074664954,4.55657280668652,
4.94969699577447));
#260458=CARTESIAN_POINT('Ctrl Pts',(-4.32120800223705,1.71216389338339,
5.1476118293891));
#260459=CARTESIAN_POINT('Ctrl Pts',(-3.78946482119506,-2.69152376236598,
5.34552666300372));
#260460=CARTESIAN_POINT('Ctrl Pts',(0.193368509426066,-4.64402330068658,
5.54344149661836));
#260461=CARTESIAN_POINT('Ctrl Pts',(4.00009988659977,-2.36718074798598,
5.74135633023296));
#260462=CARTESIAN_POINT('Ctrl Pts',(4.16391439582449,2.06546863944303,5.93927116384762));
#260463=CARTESIAN_POINT('Ctrl Pts',(0.535625102966643,4.61708236289889,
6.13718599746222));
#260464=CARTESIAN_POINT('Ctrl Pts',(-3.58046143942498,2.96388928222623,
6.33510083107687));
#260465=CARTESIAN_POINT('Ctrl Pts',(-4.43579856499644,-1.3885369592784,
6.53301566469148));
#260466=CARTESIAN_POINT('Ctrl Pts',(-1.25142521509729,-4.47641360104077,
6.73093049830612));
#260467=CARTESIAN_POINT('Ctrl Pts',(3.07262918132483,-3.48759139100354,
6.92884533192075));
#260468=CARTESIAN_POINT('Ctrl Pts',(4.59842028666512,0.677402881393908,
7.12676016553538));
#260469=CARTESIAN_POINT('Ctrl Pts',(1.93640026161004,4.22548196344249,7.32467499914999));
#260470=CARTESIAN_POINT('Ctrl Pts',(-2.4891120201209,3.92538726087325,7.52258983276462));
#260471=CARTESIAN_POINT('Ctrl Pts',(-4.64777386782454,0.0504169624677064,
7.72050466637926));
#260472=CARTESIAN_POINT('Ctrl Pts',(-2.57367795919968,-3.8704683901135,
7.91841949999387));
#260473=CARTESIAN_POINT('Ctrl Pts',(1.84428313174606,-4.26649311806479,
8.11633433360852));
#260474=CARTESIAN_POINT('Ctrl Pts',(4.58264363265316,-0.776994937332951,
8.31424916722312));
#260475=CARTESIAN_POINT('Ctrl Pts',(3.14756090412839,3.42011756396473,8.51216400083777));
#260476=CARTESIAN_POINT('Ctrl Pts',(-1.15402592062561,4.5025068540827,8.71007883445239));
#260477=CARTESIAN_POINT('Ctrl Pts',(-4.40463386700773,1.48443399790831,
8.90799366806701));
#260478=CARTESIAN_POINT('Ctrl Pts',(-3.64391323016614,-2.88552251205178,
9.10590850168166));
#260479=CARTESIAN_POINT('Ctrl Pts',(0.43534278016891,-4.62761498617725,
9.30382333529625));
#260480=CARTESIAN_POINT('Ctrl Pts',(4.11812930170671,-2.15530852802148,
9.5017381689109));
#260481=CARTESIAN_POINT('Ctrl Pts',(4.05050880279234,2.2798513624882,9.69965300252552));
#260482=CARTESIAN_POINT('Ctrl Pts',(0.294063709638058,4.63873585486514,
9.89756783614015));
#260483=CARTESIAN_POINT('Ctrl Pts',(-3.73018710798186,2.7730935678378,10.0954826697548));
#260484=CARTESIAN_POINT('Ctrl Pts',(-4.3573323729477,-1.61802298753741,
10.2933975033694));
#260485=CARTESIAN_POINT('Ctrl Pts',(-1.01622683161321,-4.53559553126675,
10.491312336984));
#260486=CARTESIAN_POINT('Ctrl Pts',(3.25036306546372,-3.32257185613898,
10.6892271705987));
#260487=CARTESIAN_POINT('Ctrl Pts',(4.55682627232683,0.916339522431252,
10.8871420042133));
#260488=CARTESIAN_POINT('Ctrl Pts',(1.71335828697782,4.32073456451352,11.0850568378279));
#260489=CARTESIAN_POINT('Ctrl Pts',(-2.69047618452508,3.79020866141177,
11.2829716714425));
#260490=CARTESIAN_POINT('Ctrl Pts',(-4.64407657362062,-0.192084811699544,
11.4808865050572));
#260491=CARTESIAN_POINT('Ctrl Pts',(-2.36828635615946,-3.99944540302358,
11.6788013386718));
#260492=CARTESIAN_POINT('Ctrl Pts',(2.06431758079821,-4.16448516891884,
11.8767161722864));
#260493=CARTESIAN_POINT('Ctrl Pts',(4.61693413021561,-0.536901325931978,
12.074631005901));
#260494=CARTESIAN_POINT('Ctrl Pts',(2.96487887203597,3.57964203108254,12.2725458395157));
#260495=CARTESIAN_POINT('Ctrl Pts',(-1.38731077285814,4.43618221177274,
12.4704606731303));
#260496=CARTESIAN_POINT('Ctrl Pts',(-4.47606751390413,1.25266252738259,
12.6683755067449));
#260497=CARTESIAN_POINT('Ctrl Pts',(-3.48844058695688,-3.07166503183752,
12.8662903403595));
#260498=CARTESIAN_POINT('Ctrl Pts',(0.676131770610078,-4.59860735715779,
13.0642051739742));
#260499=CARTESIAN_POINT('Ctrl Pts',(4.22494654664478,-1.93756818577441,
13.2621200075888));
#260500=CARTESIAN_POINT('Ctrl Pts',(3.9260751456118,2.48802687838644,13.4600348412034));
#260501=CARTESIAN_POINT('Ctrl Pts',(0.0517016876481762,4.64775975411819,
13.657949674818));
#260502=CARTESIAN_POINT('Ctrl Pts',(-3.86975683201582,2.57474772697667,
13.8558645084327));
#260503=CARTESIAN_POINT('Ctrl Pts',(-4.26700274764684,-1.84310372694929,
14.0537793420473));
#260504=CARTESIAN_POINT('Ctrl Pts',(-0.778261631577316,-4.58242868237922,
14.2516941756619));
#260505=CARTESIAN_POINT('Ctrl Pts',(3.41924739159908,-3.14850616506524,
14.4496090092766));
#260506=CARTESIAN_POINT('Ctrl Pts',(4.50282567541301,1.15278130389029,14.6475238428912));
#260507=CARTESIAN_POINT('Ctrl Pts',(1.48565145988351,4.40422337469407,14.8454386765058));
#260508=CARTESIAN_POINT('Ctrl Pts',(-2.8845151591671,3.64471070085658,15.0433535101204));
#260509=CARTESIAN_POINT('Ctrl Pts',(-4.62773514665064,-0.434063609296485,
15.2412683437351));
#260510=CARTESIAN_POINT('Ctrl Pts',(-2.15644676810989,-4.11753337773972,
15.4391831773497));
#260511=CARTESIAN_POINT('Ctrl Pts',(2.27873163999654,-4.05113884158703,
15.6370980109643));
#260512=CARTESIAN_POINT('Ctrl Pts',(4.63865439885401,-0.2953459230419,15.8350128445789));
#260513=CARTESIAN_POINT('Ctrl Pts',(2.77412454097265,3.72942042518262,16.0329276781936));
#260514=CARTESIAN_POINT('Ctrl Pts',(-1.61681846112911,4.35777947216919,
16.2308425118082));
#260515=CARTESIAN_POINT('Ctrl Pts',(-4.53531449446717,1.01748048223146,
16.4287573454228));
#260516=CARTESIAN_POINT('Ctrl Pts',(-3.32347011133097,-3.24944446681835,
16.6266721790375));
#260517=CARTESIAN_POINT('Ctrl Pts',(0.91507975448378,-4.55707949936403,
16.8245870126521));
#260518=CARTESIAN_POINT('Ctrl Pts',(4.32026107535369,-1.71455234102294,
17.0225018462667));
#260519=CARTESIAN_POINT('Ctrl Pts',(3.79095167826912,2.68942800202735,17.2204166798813));
#260520=CARTESIAN_POINT('Ctrl Pts',(-0.190800076686807,4.64413025604767,
17.4183315134959));
#260521=CARTESIAN_POINT('Ctrl Pts',(-3.99879257321471,2.36939031903143,
17.6162463471106));
#260522=CARTESIAN_POINT('Ctrl Pts',(-4.16505186954441,-2.06316355868843,
17.8141611807252));
#260523=CARTESIAN_POINT('Ctrl Pts',(-0.538184701410647,-4.61679092078249,
18.0120760143399));
#260524=CARTESIAN_POINT('Ctrl Pts',(3.57883613273897,-2.96585793436604,
18.2099908479544));
#260525=CARTESIAN_POINT('Ctrl Pts',(4.43653910904709,1.3860647428377,18.4079056815691));
#260526=CARTESIAN_POINT('Ctrl Pts',(1.25395034921688,4.47575890396004,18.6058205151837));
#260527=CARTESIAN_POINT('Ctrl Pts',(-3.07079761299755,3.48921705078318,
18.8037353487984));
#260528=CARTESIAN_POINT('Ctrl Pts',(-4.59860827458794,-0.674721754061232,
19.001650182413));
#260529=CARTESIAN_POINT('Ctrl Pts',(-1.93909203633601,-4.22467689203909,
19.1995650160276));
#260530=CARTESIAN_POINT('Ctrl Pts',(2.48762436612226,-3.92625264078095,
19.3974798496422));
#260531=CARTESIAN_POINT('Ctrl Pts',(4.64643198682337,-0.0539660083637359,
19.5953946832569));
#260532=CARTESIAN_POINT('Ctrl Pts',(2.57837854599114,3.87094208650678,19.7933095168715));
#260533=CARTESIAN_POINT('Ctrl Pts',(-1.84821006994423,4.26378106223944,
19.9912678897019));
#260534=CARTESIAN_POINT('Ctrl Pts',(-3.66270142042672,1.94538965996362,
20.1232546513276));
#260535=CARTESIAN_POINT('Ctrl Pts',(-3.88084455782439,0.657589621464481,
20.1892698017482));
#260536=CARTESIAN_POINT('Ctrl Pts',(-1.87556942017163,-2.62718932281027,
2.51101223147643E-16));
#260537=CARTESIAN_POINT('Ctrl Pts',(-1.94321685966309,-2.58955705721538,
-2.98696319824802E-15));
#260538=CARTESIAN_POINT('Ctrl Pts',(-2.00929342641587,-2.54939743639506,
-3.18303088817132E-15));
#260539=CARTESIAN_POINT('Ctrl Pts',(-2.07363931685561,-2.5067408274455,
-3.47291639890557E-15));
#260540=CARTESIAN_POINT('Ctrl Pts',(-2.15991597834028,-2.44954572477035,
-4.04153294977544E-15));
#260541=CARTESIAN_POINT('Ctrl Pts',(-2.24308257138536,-2.38786373783807,
-3.13550384268977E-15));
#260542=CARTESIAN_POINT('Ctrl Pts',(-2.32304487609101,-2.32209391940347,
-2.33840724561674E-15));
#260543=CARTESIAN_POINT('Ctrl Pts',(-2.39668046934978,-2.26152788623596,
-1.60437786732316E-15));
#260544=CARTESIAN_POINT('Ctrl Pts',(-2.46759885376822,-2.19749435520736,
-1.58516999870415E-15));
#260545=CARTESIAN_POINT('Ctrl Pts',(-2.53570984456099,-2.13026962439171,
-1.08940634291343E-15));
#260546=CARTESIAN_POINT('Ctrl Pts',(-2.54906783404081,-2.11708544902489,
-1.04875430384881E-15));
#260547=CARTESIAN_POINT('Ctrl Pts',(-2.56231717356686,-2.10377893194792,
4.2212099467669E-16));
#260548=CARTESIAN_POINT('Ctrl Pts',(-2.57544805121062,-2.09036165114785,
5.759281940243E-16));
#260549=CARTESIAN_POINT('Ctrl Pts',(-2.6498106779512,-2.01437706953205,
-5.81331574431158E-17));
#260550=CARTESIAN_POINT('Ctrl Pts',(-2.72045456846015,-1.93476701230077,
-1.89288485759184E-15));
#260551=CARTESIAN_POINT('Ctrl Pts',(-2.78728141151529,-1.85194311734714,
-1.5404344466674E-15));
#260552=CARTESIAN_POINT('Ctrl Pts',(-2.85581727251888,-1.76700109864913,
-1.17897053082972E-15));
#260553=CARTESIAN_POINT('Ctrl Pts',(-2.9203389474257,-1.67867826627061,
1.37094499452068E-15));
#260554=CARTESIAN_POINT('Ctrl Pts',(-2.98071257569894,-1.58737132139589,
2.22044604925031E-15));
#260555=CARTESIAN_POINT('Ctrl Pts',(-3.01428701700591,-1.53659452117212,
2.69286296567517E-15));
#260556=CARTESIAN_POINT('Ctrl Pts',(-3.04657809338566,-1.48489406210769,
5.92055426793446E-15));
#260557=CARTESIAN_POINT('Ctrl Pts',(-3.07755815354105,-1.43233300373666,
3.56659146660832E-15));
#260558=CARTESIAN_POINT('Ctrl Pts',(-3.08697793780036,-1.41635131009848,
2.90579300526694E-15));
#260559=CARTESIAN_POINT('Ctrl Pts',(-3.0962717941836,-1.40029795380699,
4.94759990803286E-15));
#260560=CARTESIAN_POINT('Ctrl Pts',(-3.10543719647879,-1.38417861149924,
4.6074255521944E-15));
#260561=CARTESIAN_POINT('Ctrl Pts',(-3.16080948827413,-1.28679445998392,
2.67287859025293E-15));
#260562=CARTESIAN_POINT('Ctrl Pts',(-3.21152045425685,-1.18696368226749,
5.82879830159953E-15));
#260563=CARTESIAN_POINT('Ctrl Pts',(-3.25746102236525,-1.08512302646891,
4.46864767411626E-15));
#260564=CARTESIAN_POINT('Ctrl Pts',(-3.30388770314436,-0.982204760287715,
3.09410483336006E-15));
#260565=CARTESIAN_POINT('Ctrl Pts',(-3.34544306335798,-0.877233138262983,
2.6696688988621E-15));
#260566=CARTESIAN_POINT('Ctrl Pts',(-3.38197996308487,-0.770617372601717,
3.30291349825984E-15));
#260567=CARTESIAN_POINT('Ctrl Pts',(-3.41753428813729,-0.666868789214298,
3.91912846157006E-15));
#260568=CARTESIAN_POINT('Ctrl Pts',(-3.44833674489485,-0.561562436895271,
3.88870334882072E-15));
#260569=CARTESIAN_POINT('Ctrl Pts',(-3.47421314506653,-0.455048337768718,
3.66373598126302E-15));
#260570=CARTESIAN_POINT('Ctrl Pts',(-3.48715134515238,-0.401791288205442,
3.55125229748417E-15));
#260571=CARTESIAN_POINT('Ctrl Pts',(-3.49885739233011,-0.348231952880776,
3.07635813663633E-15));
#260572=CARTESIAN_POINT('Ctrl Pts',(-3.50930537873547,-0.294412451083064,
3.33066907387547E-15));
#260573=CARTESIAN_POINT('Ctrl Pts',(-3.51491240797328,-0.265529611037486,
3.4671478943173E-15));
#260574=CARTESIAN_POINT('Ctrl Pts',(-3.52015705948641,-0.236571826863691,
4.32442325837932E-15));
#260575=CARTESIAN_POINT('Ctrl Pts',(-3.52503497038303,-0.207545526731505,
4.30211422042248E-15));
#260576=CARTESIAN_POINT('Ctrl Pts',(-3.52881969857847,-0.185024275554966,
4.28480483393351E-15));
#260577=CARTESIAN_POINT('Ctrl Pts',(-3.53238441234349,-0.162456043358417,
2.9467404425913E-15));
#260578=CARTESIAN_POINT('Ctrl Pts',(-3.53572297498661,-0.139872357824409,
3.13638004456607E-15));
#260579=CARTESIAN_POINT('Ctrl Pts',(-3.53609939778504,-0.137326048224713,
3.15776190175956E-15));
#260580=CARTESIAN_POINT('Ctrl Pts',(-3.53647294545778,-0.134779558926291,
3.14642742435836E-15));
#260581=CARTESIAN_POINT('Ctrl Pts',(-3.53684361068852,-0.132232937888745,
3.1641356201817E-15));
#260582=CARTESIAN_POINT('Ctrl Pts',(-3.55353020233728,-0.0175892599457696,
5.186219913102E-15));
#260583=CARTESIAN_POINT('Ctrl Pts',(-3.56440026289145,0.0974665540390713,
5.07191696097025E-15));
#260584=CARTESIAN_POINT('Ctrl Pts',(-3.56931023113663,0.212509296148271,
3.83026943495679E-15));
#260585=CARTESIAN_POINT('Ctrl Pts',(-3.57218292020646,0.279817680096528,
1.70301208742856E-15));
#260586=CARTESIAN_POINT('Ctrl Pts',(-3.57301463943239,0.347122208748641,
5.48449796780725E-15));
#260587=CARTESIAN_POINT('Ctrl Pts',(-3.57176938301271,0.41434171205851,
4.19109191795997E-15));
#260588=CARTESIAN_POINT('Ctrl Pts',(-3.5697177817538,0.525088073558945,
2.14805900299604E-15));
#260589=CARTESIAN_POINT('Ctrl Pts',(-3.56203156872923,0.635603442404429,
5.535809693293E-15));
#260590=CARTESIAN_POINT('Ctrl Pts',(-3.54897252034833,0.745605368646729,
5.13478148889135E-15));
#260591=CARTESIAN_POINT('Ctrl Pts',(-3.53562561329751,0.858032051062244,
4.72491347915652E-15));
#260592=CARTESIAN_POINT('Ctrl Pts',(-3.5166663209495,0.969923083623129,
3.47522615189797E-15));
#260593=CARTESIAN_POINT('Ctrl Pts',(-3.49231997030835,1.0809798264328,2.1094237467878E-15));
#260594=CARTESIAN_POINT('Ctrl Pts',(-3.48394443529913,1.1191851267311,1.63956581907238E-15));
#260595=CARTESIAN_POINT('Ctrl Pts',(-3.47493090089764,1.1572916683045,1.00344127597866E-16));
#260596=CARTESIAN_POINT('Ctrl Pts',(-3.46528713442918,1.19528713766673,
4.44089209850063E-16));
#260597=CARTESIAN_POINT('Ctrl Pts',(-3.46131507764283,1.21093664166752,
3.61845925886729E-16));
#260598=CARTESIAN_POINT('Ctrl Pts',(-3.45723619243246,1.22656668453369,
-1.56589949516286E-16));
#260599=CARTESIAN_POINT('Ctrl Pts',(-3.45305468210887,1.2421634091862,5.55111512312578E-17));
#260600=CARTESIAN_POINT('Ctrl Pts',(-3.42263513893302,1.35562605838552,
3.11615268497786E-15));
#260601=CARTESIAN_POINT('Ctrl Pts',(-3.38674446557073,1.46750384585196,
-5.69849959668556E-16));
#260602=CARTESIAN_POINT('Ctrl Pts',(-3.34571175820367,1.57747597390746,
-7.7715611723761E-16));
#260603=CARTESIAN_POINT('Ctrl Pts',(-3.30470986567157,1.68736551484662,
-9.84306591561689E-16));
#260604=CARTESIAN_POINT('Ctrl Pts',(-3.25857332074224,1.79535300088055,
6.45103697825085E-16));
#260605=CARTESIAN_POINT('Ctrl Pts',(-3.20757486876686,1.90112149564073,
3.33066907387547E-16));
#260606=CARTESIAN_POINT('Ctrl Pts',(-3.15595880640236,2.00817088655903,
1.72512343350343E-17));
#260607=CARTESIAN_POINT('Ctrl Pts',(-3.09936212517733,2.11294801982453,
2.74834656774289E-15));
#260608=CARTESIAN_POINT('Ctrl Pts',(-3.03801481501982,2.21511582858276,
-7.21644966006352E-16));
#260609=CARTESIAN_POINT('Ctrl Pts',(-2.97799894244694,2.3150662612218,-4.11632631688848E-15));
#260610=CARTESIAN_POINT('Ctrl Pts',(-2.91343592049529,2.41252009783622,
1.82683910698455E-15));
#260611=CARTESIAN_POINT('Ctrl Pts',(-2.84449674836446,2.50714265484644,
-2.38697950294409E-15));
#260612=CARTESIAN_POINT('Ctrl Pts',(-2.83448523320077,2.52088397396958,
-2.89070916018422E-15));
#260613=CARTESIAN_POINT('Ctrl Pts',(-2.82438675889958,2.53455810077557,
-1.50365065139371E-15));
#260614=CARTESIAN_POINT('Ctrl Pts',(-2.81420395125994,2.54816172130323,
-1.22124532708767E-15));
#260615=CARTESIAN_POINT('Ctrl Pts',(-2.74076732429818,2.64626865225709,
1.88643940676309E-16));
#260616=CARTESIAN_POINT('Ctrl Pts',(-2.66291885988769,2.74075040032154,
-7.7831521150718E-16));
#260617=CARTESIAN_POINT('Ctrl Pts',(-2.58094817198274,2.83127269698007,
-4.9960036108132E-16));
#260618=CARTESIAN_POINT('Ctrl Pts',(-2.49883747965016,2.92194960405673,
-3.19828665886133E-16));
#260619=CARTESIAN_POINT('Ctrl Pts',(-2.41259008723588,3.00865435231219,
-9.23807423859023E-16));
#260620=CARTESIAN_POINT('Ctrl Pts',(-2.32244725468202,3.09103471217502,
-3.88578058618805E-16));
#260621=CARTESIAN_POINT('Ctrl Pts',(-2.23400471151706,3.17186119972475,
-1.22638691089234E-15));
#260622=CARTESIAN_POINT('Ctrl Pts',(-2.14181179126767,3.24852559953772,
-1.07853142926365E-15));
#260623=CARTESIAN_POINT('Ctrl Pts',(-2.04605523770132,3.32066838036946,
-8.32667268468867E-16));
#260624=CARTESIAN_POINT('Ctrl Pts',(-1.95043831892495,3.39270596065171,
-1.12437181343088E-15));
#260625=CARTESIAN_POINT('Ctrl Pts',(-1.85126778116324,3.46023588193575,
4.8784508495953E-17));
#260626=CARTESIAN_POINT('Ctrl Pts',(-1.74869447533115,3.52286199445086,
-4.9960036108132E-16));
#260627=CARTESIAN_POINT('Origin',(-1.73205080756888,-3.,-8.));
#260628=CARTESIAN_POINT('',(-1.73205080756888,-3.,-8.));
#260629=CARTESIAN_POINT('',(1.73205080756888,-3.,-8.));
#260630=CARTESIAN_POINT('',(-0.86602540378444,-3.,-8.));
#260631=CARTESIAN_POINT('',(-1.73205080756888,-3.,-4.));
#260632=CARTESIAN_POINT('',(-1.73205080756888,-3.,-8.));
#260633=CARTESIAN_POINT('',(1.73205080756888,-3.,-4.));
#260634=CARTESIAN_POINT('',(-1.73205080756888,-3.,-4.));
#260635=CARTESIAN_POINT('',(1.73205080756888,-3.,-8.));
#260636=CARTESIAN_POINT('Origin',(-3.46410161513775,4.24230095489963E-16,
-8.));
#260637=CARTESIAN_POINT('',(-3.46410161513775,4.24230095489963E-16,-8.));
#260638=CARTESIAN_POINT('',(-3.03108891324554,-0.749999999999999,-8.));
#260639=CARTESIAN_POINT('',(-3.46410161513775,5.55111512312578E-16,-4.));
#260640=CARTESIAN_POINT('',(-3.46410161513775,4.24230095489963E-16,-8.));
#260641=CARTESIAN_POINT('',(-3.46410161513775,4.24230095489963E-16,-4.));
#260642=CARTESIAN_POINT('Origin',(-1.73205080756888,3.,-8.));
#260643=CARTESIAN_POINT('',(-1.73205080756888,3.,-8.));
#260644=CARTESIAN_POINT('',(-2.1650635094611,2.25,-8.));
#260645=CARTESIAN_POINT('',(-1.73205080756888,3.,-4.));
#260646=CARTESIAN_POINT('',(-1.73205080756888,3.,-8.));
#260647=CARTESIAN_POINT('',(-1.73205080756888,3.,-4.));
#260648=CARTESIAN_POINT('Origin',(1.73205080756888,3.,-8.));
#260649=CARTESIAN_POINT('',(1.73205080756888,3.,-8.));
#260650=CARTESIAN_POINT('',(0.866025403784439,3.,-8.));
#260651=CARTESIAN_POINT('',(1.73205080756888,3.,-4.));
#260652=CARTESIAN_POINT('',(1.73205080756888,3.,-8.));
#260653=CARTESIAN_POINT('',(1.73205080756888,3.,-4.));
#260654=CARTESIAN_POINT('Origin',(3.46410161513775,0.,-8.));
#260655=CARTESIAN_POINT('',(3.46410161513775,0.,-8.));
#260656=CARTESIAN_POINT('',(3.03108891324554,0.75,-8.));
#260657=CARTESIAN_POINT('',(3.46410161513775,0.,-4.));
#260658=CARTESIAN_POINT('',(3.46410161513775,0.,-8.));
#260659=CARTESIAN_POINT('',(3.46410161513775,0.,-4.));
#260660=CARTESIAN_POINT('Origin',(1.73205080756888,-3.,-8.));
#260661=CARTESIAN_POINT('',(2.1650635094611,-2.25,-8.));
#260662=CARTESIAN_POINT('',(1.73205080756888,-3.,-4.));
#260663=CARTESIAN_POINT('Origin',(0.,5.55111512312578E-16,-4.));
#260664=CARTESIAN_POINT('Origin',(0.,0.,0.));
#260665=CARTESIAN_POINT('',(-6.5,-7.9602041944578E-16,0.));
#260666=CARTESIAN_POINT('Origin',(0.,0.,0.));
#260667=CARTESIAN_POINT('Origin',(0.,0.,-8.));
#260668=CARTESIAN_POINT('',(-6.5,-7.9602041944578E-16,-8.));
#260669=CARTESIAN_POINT('',(-6.5,-7.9602041944578E-16,-8.));
#260670=CARTESIAN_POINT('Origin',(0.,0.,-8.));
#260671=CARTESIAN_POINT('Origin',(0.,0.,-8.));
#260672=CARTESIAN_POINT('Origin',(0.,0.,20.));
#289365=UNCERTAINTY_MEASURE_WITH_UNIT(LENGTH_MEASURE(0.01),#289388,
'DISTANCE_ACCURACY_VALUE',
'Maximum model space distance between geometric entities at asserted c
onnectivities');
#289368=UNCERTAINTY_MEASURE_WITH_UNIT(LENGTH_MEASURE(0.01),#289388,
'DISTANCE_ACCURACY_VALUE',
'Maximum model space distance between geometric entities at asserted c
onnectivities');
#289384=(
GEOMETRIC_REPRESENTATION_CONTEXT(3)
GLOBAL_UNCERTAINTY_ASSIGNED_CONTEXT((#289365))
GLOBAL_UNIT_ASSIGNED_CONTEXT((#289388,#289390,#289391))
REPRESENTATION_CONTEXT('','3D')
);
#289387=(
GEOMETRIC_REPRESENTATION_CONTEXT(3)
GLOBAL_UNCERTAINTY_ASSIGNED_CONTEXT((#289368))
GLOBAL_UNIT_ASSIGNED_CONTEXT((#289388,#289390,#289391))
REPRESENTATION_CONTEXT('','3D')
);
#289388=(
LENGTH_UNIT()
NAMED_UNIT(*)
SI_UNIT(.MILLI.,.METRE.)
);
#289390=(
NAMED_UNIT(*)
PLANE_ANGLE_UNIT()
SI_UNIT($,.RADIAN.)
);
#289391=(
NAMED_UNIT(*)
SI_UNIT($,.STERADIAN.)
SOLID_ANGLE_UNIT()
);
#289407=SHAPE_DEFINITION_REPRESENTATION(#289425,#289468);
#289425=PRODUCT_DEFINITION_SHAPE('',$,#289487);
#289468=SHAPE_REPRESENTATION('',(#17747),#289384);
#289471=PRODUCT_DEFINITION_CONTEXT('part definition',#289527,'design');
#289487=PRODUCT_DEFINITION('Socket head cap screw M8x20',
'Socket head cap screw M8x20',#289505,#289471);
#289505=PRODUCT_DEFINITION_FORMATION('',$,#289544);
#289527=APPLICATION_CONTEXT(
'Core Data for Automotive Mechanical Design Process');
#289528=PRODUCT_CONTEXT('part definition',#289527,'mechanical');
#289544=PRODUCT('Socket head cap screw M8x20',
'Socket head cap screw M8x20',$,(#289528));
#289553=PRESENTATION_STYLE_ASSIGNMENT((#289560));
#289560=SURFACE_STYLE_USAGE(.BOTH.,#289567);
#289567=SURFACE_SIDE_STYLE('',(#289574));
#289574=SURFACE_STYLE_FILL_AREA(#289581);
#289581=FILL_AREA_STYLE('Opaque(64,72,82)',(#289588));
#289588=FILL_AREA_STYLE_COLOUR('Opaque(64,72,82)',#289595);
#289595=COLOUR_RGB('Opaque(64,72,82)',0.250980392156863,0.282352941176471,
0.32156862745098);
ENDSEC;
END-ISO-10303-21;
